ISO-10303-21;
HEADER;
FILE_DESCRIPTION (('STEP AP214'),
    '1' );
FILE_NAME ('Injection Molded Chain Links 12.step',
    '2026-10-08T22:59:04',
    ( '' ),
    ( '' ),
    'SwSTEP 2.0',
    'SolidWorks 2020',
    '' );
FILE_SCHEMA (( 'AUTOMOTIVE_DESIGN' ));
ENDSEC;

DATA;
#47=DIRECTION ( 'NONE',  ( -0.000000000000000000, 6.982962677686266711E-15, -1.000000000000000000 ) ) ;
#80=ORIENTED_EDGE ( 'NONE', *, *, #1653, .T. ) ;
#107=CARTESIAN_POINT ( 'NONE',  ( -23.15000000000000213, 85.60000000001221565, -146.4170766071767389 ) ) ;
#144=ORIENTED_EDGE ( 'NONE', *, *, #165937, .T. ) ;
#152=DIRECTION ( 'NONE',  ( 1.000000000000000000, 0.000000000000000000, 0.000000000000000000 ) ) ;
#162=EDGE_CURVE ( 'NONE', #138584, #10632, #99412, .T. ) ;
#250=DIRECTION ( 'NONE',  ( 2.557131231893037478E-16, 0.8660254037844420383, -0.4999999999999942824 ) ) ;
#273=DIRECTION ( 'NONE',  ( 1.000000000000000000, 0.000000000000000000, 0.000000000000000000 ) ) ;
#277=DIRECTION ( 'NONE',  ( 1.000000000000000000, 0.000000000000000000, 0.000000000000000000 ) ) ;
#289=DIRECTION ( 'NONE',  ( 0.000000000000000000, -6.982962677686266711E-15, 1.000000000000000000 ) ) ;
#328=CIRCLE ( 'NONE', #17110, 0.09999999999998898659 ) ;
#350=EDGE_CURVE ( 'NONE', #79629, #237280, #201885, .T. ) ;
#381=CARTESIAN_POINT ( 'NONE',  ( -18.59999999999999787, 77.83585931145570669, -125.0186683157258045 ) ) ;
#386=ADVANCED_FACE ( 'NONE', ( #20587 ), #193882, .T. ) ;
#392=CARTESIAN_POINT ( 'NONE',  ( -22.39999999999999858, 76.00000000001243450, -177.8138870828977360 ) ) ;
#393=EDGE_CURVE ( 'NONE', #139006, #141665, #163936, .T. ) ;
#402=EDGE_LOOP ( 'NONE', ( #242482, #239735, #248991, #84795 ) ) ;
#426=AXIS2_PLACEMENT_3D ( 'NONE', #170438, #150818, #257245 ) ;
#466=EDGE_CURVE ( 'NONE', #193723, #152968, #120794, .T. ) ;
#486=DIRECTION ( 'NONE',  ( 1.000000000000000000, -7.304098846218134667E-16, -5.100424963727256530E-30 ) ) ;
#503=AXIS2_PLACEMENT_3D ( 'NONE', #254332, #51308, #249556 ) ;
#534=LINE ( 'NONE', #56632, #244821 ) ;
#542=DIRECTION ( 'NONE',  ( 0.000000000000000000, 0.000000000000000000, 1.000000000000000000 ) ) ;
#558=ORIENTED_EDGE ( 'NONE', *, *, #48980, .F. ) ;
#580=CARTESIAN_POINT ( 'NONE',  ( 21.04999999999999716, 76.01454569058392963, -176.5201252709579194 ) ) ;
#584=CIRCLE ( 'NONE', #183777, 0.1000000000000033362 ) ;
#588=VERTEX_POINT ( 'NONE', #129920 ) ;
#599=CARTESIAN_POINT ( 'NONE',  ( 20.94999999999999929, 67.22371710471975348, -148.7731074845244166 ) ) ;
#645=CARTESIAN_POINT ( 'NONE',  ( 20.94999999999999574, 77.83534155023670564, -158.3679561919613548 ) ) ;
#671=DIRECTION ( 'NONE',  ( 0.000000000000000000, 6.982962677686266711E-15, -1.000000000000000000 ) ) ;
#673=CARTESIAN_POINT ( 'NONE',  ( 21.46681500597178882, 76.00000000001243450, -176.8806186439590249 ) ) ;
#689=CYLINDRICAL_SURFACE ( 'NONE', #44570, 11.80000000000000426 ) ;
#734=DIRECTION ( 'NONE',  ( 0.000000000000000000, -0.9998779222360097974, 0.01562500000000363945 ) ) ;
#749=VECTOR ( 'NONE', #230866, 1000.000000000000000 ) ;
#770=ORIENTED_EDGE ( 'NONE', *, *, #240435, .F. ) ;
#774=CARTESIAN_POINT ( 'NONE',  ( 20.12500000000000000, 66.25000000001223555, -148.7731074845244450 ) ) ;
#777=DIRECTION ( 'NONE',  ( 0.000000000000000000, -6.982962677686266711E-15, 1.000000000000000000 ) ) ;
#798=CARTESIAN_POINT ( 'NONE',  ( 20.94999999999999929, 67.12338541492522381, -161.6380270056797599 ) ) ;
#819=ADVANCED_FACE ( 'NONE', ( #178071 ), #102324, .T. ) ;
#822=FACE_OUTER_BOUND ( 'NONE', #16958, .T. ) ;
#824=CARTESIAN_POINT ( 'NONE',  ( 21.30000000000002558, 76.00000000001237765, -170.0231074845243597 ) ) ;
#826=AXIS2_PLACEMENT_3D ( 'NONE', #121089, #76785, #174665 ) ;
#829=FACE_OUTER_BOUND ( 'NONE', #191459, .T. ) ;
#840=FACE_OUTER_BOUND ( 'NONE', #86890, .T. ) ;
#845=AXIS2_PLACEMENT_3D ( 'NONE', #148975, #12035, #206367 ) ;
#858=ORIENTED_EDGE ( 'NONE', *, *, #21750, .T. ) ;
#866=AXIS2_PLACEMENT_3D ( 'NONE', #49325, #89726, #93591 ) ;
#871=AXIS2_PLACEMENT_3D ( 'NONE', #98806, #217487, #221333 ) ;
#898=ORIENTED_EDGE ( 'NONE', *, *, #17139, .F. ) ;
#908=CARTESIAN_POINT ( 'NONE',  ( -23.15000000000000213, 84.66355140188136374, -146.0472086025916099 ) ) ;
#915=DIRECTION ( 'NONE',  ( 2.952720810173289112E-16, 1.000000000000000000, 6.467318590049456648E-15 ) ) ;
#970=EDGE_LOOP ( 'NONE', ( #120414, #176231, #21740, #124725 ) ) ;
#994=VERTEX_POINT ( 'NONE', #31540 ) ;
#997=VERTEX_POINT ( 'NONE', #190596 ) ;
#1006=DIRECTION ( 'NONE',  ( 1.000000000000000000, 0.000000000000000000, 0.000000000000000000 ) ) ;
#1026=DIRECTION ( 'NONE',  ( -1.000000000000000000, -9.012599976027990443E-15, -6.882867235861669241E-14 ) ) ;
#1044=ORIENTED_EDGE ( 'NONE', *, *, #191598, .F. ) ;
#1065=AXIS2_PLACEMENT_3D ( 'NONE', #149817, #229347, #50668 ) ;
#1127=CARTESIAN_POINT ( 'NONE',  ( -20.94999999999999929, 76.00000000001237765, -170.0231074845243597 ) ) ;
#1146=FACE_OUTER_BOUND ( 'NONE', #164575, .T. ) ;
#1159=CIRCLE ( 'NONE', #221721, 0.09999999999998898659 ) ;
#1206=VECTOR ( 'NONE', #217210, 1000.000000000000000 ) ;
#1207=DIRECTION ( 'NONE',  ( 1.000000000000000000, 0.000000000000000000, 0.000000000000000000 ) ) ;
#1210=CARTESIAN_POINT ( 'NONE',  ( 20.99999999999997868, 76.00000000001237765, -170.0231074845243597 ) ) ;
#1260=ORIENTED_EDGE ( 'NONE', *, *, #116402, .F. ) ;
#1292=CYLINDRICAL_SURFACE ( 'NONE', #68375, 12.87499999999999822 ) ;
#1297=DIRECTION ( 'NONE',  ( 0.000000000000000000, -6.982962677686266711E-15, 1.000000000000000000 ) ) ;
#1309=CARTESIAN_POINT ( 'NONE',  ( 18.49999999999999289, 65.50857864377491069, -145.1731074845244507 ) ) ;
#1323=CARTESIAN_POINT ( 'NONE',  ( -22.42357213249529480, 75.90091303601087702, -177.6960398708842774 ) ) ;
#1331=DIRECTION ( 'NONE',  ( 0.000000000000000000, -7.086529944415886769E-15, 1.000000000000000000 ) ) ;
#1332=AXIS2_PLACEMENT_3D ( 'NONE', #140565, #62330, #242231 ) ;
#1379=AXIS2_PLACEMENT_3D ( 'NONE', #104414, #182715, #83561 ) ;
#1425=AXIS2_PLACEMENT_3D ( 'NONE', #107, #79635, #159217 ) ;
#1445=CYLINDRICAL_SURFACE ( 'NONE', #110321, 0.5000000000000004441 ) ;
#1484=DIRECTION ( 'NONE',  ( 1.000000000000000000, 0.000000000000000000, 0.000000000000000000 ) ) ;
#1504=ORIENTED_EDGE ( 'NONE', *, *, #198365, .F. ) ;
#1544=CARTESIAN_POINT ( 'NONE',  ( -23.25000000000000000, 87.75000000001237765, -170.0231074845242745 ) ) ;
#1552=DIRECTION ( 'NONE',  ( 0.000000000000000000, 0.000000000000000000, -1.000000000000000000 ) ) ;
#1567=PLANE ( 'NONE',  #132508 ) ;
#1579=ORIENTED_EDGE ( 'NONE', *, *, #24060, .T. ) ;
#1581=EDGE_CURVE ( 'NONE', #109416, #94890, #71982, .T. ) ;
#1592=DIRECTION ( 'NONE',  ( 0.000000000000000000, 0.000000000000000000, 1.000000000000000000 ) ) ;
#1593=AXIS2_PLACEMENT_3D ( 'NONE', #253971, #134029, #57037 ) ;
#1617=EDGE_CURVE ( 'NONE', #140162, #6455, #59446, .T. ) ;
#1630=CIRCLE ( 'NONE', #89135, 0.1000000000000000888 ) ;
#1635=ADVANCED_FACE ( 'NONE', ( #131258 ), #46572, .T. ) ;
#1653=EDGE_CURVE ( 'NONE', #132176, #230733, #76236, .T. ) ;
#1661=ORIENTED_EDGE ( 'NONE', *, *, #105338, .F. ) ;
#1663=ADVANCED_FACE ( 'NONE', ( #109114 ), #146954, .F. ) ;
#1679=ORIENTED_EDGE ( 'NONE', *, *, #204174, .F. ) ;
#1683=ADVANCED_FACE ( 'NONE', ( #8753 ), #89553, .F. ) ;
#1710=DIRECTION ( 'NONE',  ( 1.000000000000000000, -0.000000000000000000, 0.000000000000000000 ) ) ;
#1733=ORIENTED_EDGE ( 'NONE', *, *, #62158, .F. ) ;
#1759=DIRECTION ( 'NONE',  ( 0.000000000000000000, 0.000000000000000000, -1.000000000000000000 ) ) ;
#1798=VERTEX_POINT ( 'NONE', #64553 ) ;
#1801=CARTESIAN_POINT ( 'NONE',  ( -23.25000000000000000, 74.08971962618045382, -149.1544753397233194 ) ) ;
#1809=AXIS2_PLACEMENT_3D ( 'NONE', #153171, #240376, #125555 ) ;
#1828=CARTESIAN_POINT ( 'NONE',  ( 21.05000000000000071, 65.57661458509942065, -162.5310555606543232 ) ) ;
#1845=AXIS2_PLACEMENT_3D ( 'NONE', #174388, #171808, #248747 ) ;
#1856=ORIENTED_EDGE ( 'NONE', *, *, #244760, .T. ) ;
#1884=AXIS2_PLACEMENT_3D ( 'NONE', #26679, #106170, #245708 ) ;
#1901=VERTEX_POINT ( 'NONE', #150527 ) ;
#1925=AXIS2_PLACEMENT_3D ( 'NONE', #240575, #78902, #99751 ) ;
#1974=CARTESIAN_POINT ( 'NONE',  ( 21.53752568622141439, 75.90102553874177715, -176.8099153590729884 ) ) ;
#1981=CYLINDRICAL_SURFACE ( 'NONE', #179592, 11.75000000000001066 ) ;
#2017=ORIENTED_EDGE ( 'NONE', *, *, #164449, .T. ) ;
#2032=AXIS2_PLACEMENT_3D ( 'NONE', #32480, #72887, #152417 ) ;
#2035=CIRCLE ( 'NONE', #168706, 0.1000000000000043771 ) ;
#2066=EDGE_LOOP ( 'NONE', ( #121633, #228771, #100380, #90357 ) ) ;
#2107=LINE ( 'NONE', #102472, #215120 ) ;
#2116=AXIS2_PLACEMENT_3D ( 'NONE', #124197, #208546, #145011 ) ;
#2125=DIRECTION ( 'NONE',  ( 0.000000000000000000, 6.982962677686266711E-15, -1.000000000000000000 ) ) ;
#2135=LINE ( 'NONE', #137792, #19751 ) ;
#2171=ORIENTED_EDGE ( 'NONE', *, *, #219471, .F. ) ;
#2193=DIRECTION ( 'NONE',  ( 1.000000000000000000, 0.000000000000000000, 0.000000000000000000 ) ) ;
#2214=CARTESIAN_POINT ( 'NONE',  ( -21.55000000000000426, 68.29142135624952914, -148.8731074845244109 ) ) ;
#2220=CARTESIAN_POINT ( 'NONE',  ( -23.15000000000000213, 84.59626168225520360, -145.9732350016745954 ) ) ;
#2225=CARTESIAN_POINT ( 'NONE',  ( -21.14999999999999858, 64.25000000001232081, -163.2969768484652491 ) ) ;
#2226=ORIENTED_EDGE ( 'NONE', *, *, #96808, .F. ) ;
#2230=ORIENTED_EDGE ( 'NONE', *, *, #52736, .T. ) ;
#2246=AXIS2_PLACEMENT_3D ( 'NONE', #173608, #52297, #17068 ) ;
#2269=DIRECTION ( 'NONE',  ( 0.000000000000000000, -8.267618268485201230E-15, 1.000000000000000000 ) ) ;
#2278=DIRECTION ( 'NONE',  ( -1.000000000000000000, -0.000000000000000000, -0.000000000000000000 ) ) ;
#2282=CARTESIAN_POINT ( 'NONE',  ( -21.44999999999999929, 68.65000000001229807, -157.7731074845244166 ) ) ;
#2342=AXIS2_PLACEMENT_3D ( 'NONE', #87864, #249549, #187018 ) ;
#2347=CARTESIAN_POINT ( 'NONE',  ( 18.59999999999999076, 64.25000000001246292, -181.7731074845244450 ) ) ;
#2354=CARTESIAN_POINT ( 'NONE',  ( -20.85000000000000142, 64.25000000001220712, -143.3069731475025321 ) ) ;
#2366=CIRCLE ( 'NONE', #135647, 11.70000000000001528 ) ;
#2379=CIRCLE ( 'NONE', #148144, 11.70000000000000284 ) ;
#2383=VERTEX_POINT ( 'NONE', #205023 ) ;
#2393=ORIENTED_EDGE ( 'NONE', *, *, #26086, .F. ) ;
#2424=AXIS2_PLACEMENT_3D ( 'NONE', #164957, #146654, #103671 ) ;
#2425=AXIS2_PLACEMENT_3D ( 'NONE', #153513, #135160, #16531 ) ;
#2439=LINE ( 'NONE', #241092, #53387 ) ;
#2456=EDGE_LOOP ( 'NONE', ( #42361, #162104, #147373, #116502 ) ) ;
#2494=DIRECTION ( 'NONE',  ( 0.000000000000000000, 0.000000000000000000, 1.000000000000000000 ) ) ;
#2509=DIRECTION ( 'NONE',  ( 0.000000000000000000, 0.000000000000000000, 1.000000000000000000 ) ) ;
#2563=CARTESIAN_POINT ( 'NONE',  ( 20.95512820512820440, 67.12384868372420499, -161.4644784893834810 ) ) ;
#2577=VERTEX_POINT ( 'NONE', #79510 ) ;
#2585=DIRECTION ( 'NONE',  ( 7.304098846218134667E-16, 1.000000000000000000, 6.982962677686266711E-15 ) ) ;
#2612=ADVANCED_FACE ( 'NONE', ( #165342 ), #167937, .F. ) ;
#2626=DIRECTION ( 'NONE',  ( 1.000000000000000000, -0.000000000000000000, 0.000000000000000000 ) ) ;
#2638=AXIS2_PLACEMENT_3D ( 'NONE', #39934, #217235, #235526 ) ;
#2645=CARTESIAN_POINT ( 'NONE',  ( -23.25000000000000000, 74.00000000001223555, -149.1477294072864765 ) ) ;
#2671=ORIENTED_EDGE ( 'NONE', *, *, #59711, .T. ) ;
#2682=DIRECTION ( 'NONE',  ( 0.000000000000000000, 6.938893903907222067E-15, -1.000000000000000000 ) ) ;
#2752=EDGE_CURVE ( 'NONE', #2577, #216685, #164118, .T. ) ;
#2761=LINE ( 'NONE', #241405, #44575 ) ;
#2803=CARTESIAN_POINT ( 'NONE',  ( 20.30531438145591139, 65.90309893892226967, -162.2270896772506035 ) ) ;
#2844=DIRECTION ( 'NONE',  ( 6.938893903907222067E-15, 1.000000000000000000, 6.982962677686266711E-15 ) ) ;
#2884=DIRECTION ( 'NONE',  ( -1.040834085586054343E-13, 0.9999176327611370985, 0.01283462868040226822 ) ) ;
#2928=CARTESIAN_POINT ( 'NONE',  ( -18.50000000000000355, 85.41908450282542731, -129.6931996774989102 ) ) ;
#2938=ADVANCED_FACE ( 'NONE', ( #183308 ), #166343, .F. ) ;
#2989=CARTESIAN_POINT ( 'NONE',  ( -18.51697539158857353, 65.68434038414380893, -130.9866880726065972 ) ) ;
#3021=CARTESIAN_POINT ( 'NONE',  ( 20.95429693346638800, 65.45669512011676261, -162.4622249462115064 ) ) ;
#3047=EDGE_CURVE ( 'NONE', #223147, #5558, #55921, .T. ) ;
#3049=VERTEX_POINT ( 'NONE', #26828 ) ;
#3076=ORIENTED_EDGE ( 'NONE', *, *, #118391, .F. ) ;
#3087=DIRECTION ( 'NONE',  ( -0.000000000000000000, -6.982962677686266711E-15, 1.000000000000000000 ) ) ;
#3105=ORIENTED_EDGE ( 'NONE', *, *, #155947, .T. ) ;
#3107=CARTESIAN_POINT ( 'NONE',  ( -20.05000000000000426, 66.75000000001230660, -157.6731074845244223 ) ) ;
#3151=CARTESIAN_POINT ( 'NONE',  ( 21.04999999999999716, 76.00000000001242029, -176.5637644362255969 ) ) ;
#3182=DIRECTION ( 'NONE',  ( 0.000000000000000000, 0.9915357197604982575, -0.1298341882519033486 ) ) ;
#3197=CIRCLE ( 'NONE', #211509, 0.09999999999998712696 ) ;
#3231=ORIENTED_EDGE ( 'NONE', *, *, #111916, .F. ) ;
#3260=EDGE_CURVE ( 'NONE', #174607, #231943, #119182, .T. ) ;
#3313=ORIENTED_EDGE ( 'NONE', *, *, #74677, .F. ) ;
#3323=EDGE_CURVE ( 'NONE', #174107, #101850, #22667, .T. ) ;
#3344=CARTESIAN_POINT ( 'NONE',  ( -21.05000000000000071, 69.45934304831114048, -169.9231074845244223 ) ) ;
#3377=AXIS2_PLACEMENT_3D ( 'NONE', #211336, #250451, #93944 ) ;
#3378=CARTESIAN_POINT ( 'NONE',  ( -23.25000000000000000, 76.00000000001234923, -165.9731074845243768 ) ) ;
#3395=CIRCLE ( 'NONE', #186600, 0.2000000000000057288 ) ;
#3421=DIRECTION ( 'NONE',  ( 0.000000000000000000, 0.000000000000000000, -1.000000000000000000 ) ) ;
#3429=EDGE_CURVE ( 'NONE', #99053, #141610, #225942, .T. ) ;
#3441=B_SPLINE_CURVE_WITH_KNOTS ( 'NONE', 3,
 ( #211266, #151311, #112184, #92581, #100273, #179856, #80714, #244612 ),
 .UNSPECIFIED., .F., .F.,
 ( 4, 2, 2, 4 ),
 ( 0.000000000000000000, 0.0001094981963948473395, 0.0002189963927896946790, 0.0004379927855793893580 ),
 .UNSPECIFIED. ) ;
#3456=CARTESIAN_POINT ( 'NONE',  ( -20.94999999999999929, 74.83729825007431202, -162.1231074845243540 ) ) ;
#3474=VERTEX_POINT ( 'NONE', #8228 ) ;
#3481=ORIENTED_EDGE ( 'NONE', *, *, #98752, .T. ) ;
#3518=CARTESIAN_POINT ( 'NONE',  ( 21.06600267594171783, 67.22483393081238034, -157.8188447021496756 ) ) ;
#3559=DIRECTION ( 'NONE',  ( 0.000000000000000000, 0.000000000000000000, 1.000000000000000000 ) ) ;
#3572=DIRECTION ( 'NONE',  ( -0.000000000000000000, 1.000000000000000000, 7.525063763929033127E-15 ) ) ;
#3579=ORIENTED_EDGE ( 'NONE', *, *, #234613, .F. ) ;
#3630=EDGE_CURVE ( 'NONE', #75413, #244844, #231309, .T. ) ;
#3635=CARTESIAN_POINT ( 'NONE',  ( -23.15000000000000213, 71.75000000001229239, -157.6731074845243654 ) ) ;
#3636=ORIENTED_EDGE ( 'NONE', *, *, #249338, .T. ) ;
#3639=ORIENTED_EDGE ( 'NONE', *, *, #125512, .T. ) ;
#3675=DIRECTION ( 'NONE',  ( 0.000000000000000000, -0.2605042016806740079, 0.9654727137038698892 ) ) ;
#3684=CIRCLE ( 'NONE', #20273, 0.09999999999998898659 ) ;
#3703=EDGE_LOOP ( 'NONE', ( #146190, #206631, #770, #170790 ) ) ;
#3712=DIRECTION ( 'NONE',  ( -0.7071067811865127117, -0.7071067811865821007, 0.000000000000000000 ) ) ;
#3717=CARTESIAN_POINT ( 'NONE',  ( -21.45000000000000284, 68.29142135624952914, -148.8731074845244109 ) ) ;
#3761=DIRECTION ( 'NONE',  ( 1.000000000000000000, 0.000000000000000000, 0.000000000000000000 ) ) ;
#3775=EDGE_CURVE ( 'NONE', #58594, #93811, #73111, .T. ) ;
#3790=DIRECTION ( 'NONE',  ( 0.000000000000000000, 0.000000000000000000, 1.000000000000000000 ) ) ;
#3796=FACE_OUTER_BOUND ( 'NONE', #113310, .T. ) ;
#3800=CARTESIAN_POINT ( 'NONE',  ( 21.14999999999999858, 76.00000000001229239, -157.8731074845243540 ) ) ;
#3804=FACE_OUTER_BOUND ( 'NONE', #211597, .T. ) ;
#3819=DIRECTION ( 'NONE',  ( 1.000000000000000000, 0.000000000000000000, 0.000000000000000000 ) ) ;
#3837=ORIENTED_EDGE ( 'NONE', *, *, #83653, .F. ) ;
#3857=DIRECTION ( 'NONE',  ( 1.000000000000000000, -7.304098846218134667E-16, -5.100424963727256530E-30 ) ) ;
#3871=FACE_OUTER_BOUND ( 'NONE', #63190, .T. ) ;
#3909=FACE_OUTER_BOUND ( 'NONE', #209598, .T. ) ;
#3940=DIRECTION ( 'NONE',  ( 0.000000000000000000, 0.1455152366551700771, 0.9893560106964479628 ) ) ;
#3950=EDGE_CURVE ( 'NONE', #215500, #203407, #135413, .T. ) ;
#3964=AXIS2_PLACEMENT_3D ( 'NONE', #112383, #135770, #35439 ) ;
#3972=ORIENTED_EDGE ( 'NONE', *, *, #193163, .F. ) ;
#3978=ORIENTED_EDGE ( 'NONE', *, *, #16744, .T. ) ;
#3998=FACE_OUTER_BOUND ( 'NONE', #59322, .T. ) ;
#4005=DIRECTION ( 'NONE',  ( 0.000000000000000000, -1.000000000000000000, -6.982962677686265922E-15 ) ) ;
#4019=ORIENTED_EDGE ( 'NONE', *, *, #92586, .T. ) ;
#4020=CARTESIAN_POINT ( 'NONE',  ( 20.01093837587850288, 64.25000000001220712, -145.2687100499267672 ) ) ;
#4035=EDGE_LOOP ( 'NONE', ( #65126, #86189, #98111, #18707 ) ) ;
#4036=VERTEX_POINT ( 'NONE', #200353 ) ;
#4046=CARTESIAN_POINT ( 'NONE',  ( 23.25000000000000000, 85.00000000001232081, -160.1291383618718385 ) ) ;
#4053=EDGE_CURVE ( 'NONE', #133516, #58292, #156501, .T. ) ;
#4079=TOROIDAL_SURFACE ( 'NONE', #237322, 11.65000000000000036, 0.1000000000000000056 ) ;
#4133=CARTESIAN_POINT ( 'NONE',  ( 20.94999999999999929, 65.27628289530480288, -162.3581939154368285 ) ) ;
#4144=DIRECTION ( 'NONE',  ( 0.000000000000000000, -6.853228547068871147E-15, 1.000000000000000000 ) ) ;
#4147=ORIENTED_EDGE ( 'NONE', *, *, #135727, .F. ) ;
#4171=ORIENTED_EDGE ( 'NONE', *, *, #257302, .F. ) ;
#4180=CARTESIAN_POINT ( 'NONE',  ( -18.59999999999999787, 77.83534155023670564, -158.3679561919613548 ) ) ;
#4189=EDGE_LOOP ( 'NONE', ( #58272, #152750, #93323, #114633 ) ) ;
#4194=CARTESIAN_POINT ( 'NONE',  ( 22.50000000000000000, 76.00000000001237765, -170.0231074845243597 ) ) ;
#4256=DIRECTION ( 'NONE',  ( -1.000000000000000000, -0.000000000000000000, -0.000000000000000000 ) ) ;
#4272=CARTESIAN_POINT ( 'NONE',  ( -18.50000972452446035, 65.70673848566998743, -131.0638252334829303 ) ) ;
#4274=EDGE_CURVE ( 'NONE', #43942, #115699, #15002, .T. ) ;
#4283=EDGE_CURVE ( 'NONE', #197213, #196891, #210615, .T. ) ;
#4285=ORIENTED_EDGE ( 'NONE', *, *, #18161, .T. ) ;
#4293=EDGE_CURVE ( 'NONE', #207287, #106082, #167326, .T. ) ;
#4312=AXIS2_PLACEMENT_3D ( 'NONE', #227846, #24541, #124912 ) ;
#4338=EDGE_LOOP ( 'NONE', ( #190349, #102327, #187713, #1044 ) ) ;
#4350=EDGE_CURVE ( 'NONE', #5985, #49319, #54855, .T. ) ;
#4384=ORIENTED_EDGE ( 'NONE', *, *, #151834, .T. ) ;
#4401=LINE ( 'NONE', #225991, #106266 ) ;
#4423=AXIS2_PLACEMENT_3D ( 'NONE', #184718, #244688, #46486 ) ;
#4434=EDGE_CURVE ( 'NONE', #116513, #191184, #88152, .T. ) ;
#4479=CARTESIAN_POINT ( 'NONE',  ( 20.85000000000000142, 75.83895117929343144, -136.8072973288845731 ) ) ;
#4494=FACE_OUTER_BOUND ( 'NONE', #152266, .T. ) ;
#4520=CARTESIAN_POINT ( 'NONE',  ( 21.04999999999998650, 69.35000000001228670, -157.7731074845243882 ) ) ;
#4535=ORIENTED_EDGE ( 'NONE', *, *, #10188, .T. ) ;
#4541=CARTESIAN_POINT ( 'NONE',  ( -20.94999999999999929, 77.16270174995034381, -161.9231074845243370 ) ) ;
#4558=CARTESIAN_POINT ( 'NONE',  ( -23.15000000000000213, 74.00000000001223555, -149.2477294072864709 ) ) ;
#4572=ORIENTED_EDGE ( 'NONE', *, *, #213257, .F. ) ;
#4632=CARTESIAN_POINT ( 'NONE',  ( 20.90851465518106167, 65.67467670974440352, -130.9531731826884879 ) ) ;
#4663=VERTEX_POINT ( 'NONE', #116361 ) ;
#4677=ORIENTED_EDGE ( 'NONE', *, *, #44155, .F. ) ;
#4682=CIRCLE ( 'NONE', #150470, 0.09999999999998898659 ) ;
#4687=FACE_OUTER_BOUND ( 'NONE', #165645, .T. ) ;
#4695=CARTESIAN_POINT ( 'NONE',  ( 21.05000000000000071, 76.00000000001213607, -136.5231074845243313 ) ) ;
#4720=CARTESIAN_POINT ( 'NONE',  ( -18.50000000000000000, 64.35000000001230092, -157.8731074845244393 ) ) ;
#4753=AXIS2_PLACEMENT_3D ( 'NONE', #90814, #188641, #248618 ) ;
#4779=CARTESIAN_POINT ( 'NONE',  ( 18.44444291854882323, 85.49010118095534949, -129.8942035196332938 ) ) ;
#4785=CARTESIAN_POINT ( 'NONE',  ( 21.08832698747859169, 67.22463560659508630, -157.7943900180602554 ) ) ;
#4792=VERTEX_POINT ( 'NONE', #64074 ) ;
#4827=CARTESIAN_POINT ( 'NONE',  ( 23.14999999999999147, 80.15000000001238334, -170.0231074845243313 ) ) ;
#4829=ORIENTED_EDGE ( 'NONE', *, *, #56787, .F. ) ;
#4851=DIRECTION ( 'NONE',  ( -1.000000000000000000, -0.000000000000000000, -0.000000000000000000 ) ) ;
#4897=EDGE_CURVE ( 'NONE', #77748, #167959, #218213, .T. ) ;
#4921=DIRECTION ( 'NONE',  ( 0.000000000000000000, -6.938893903907222067E-15, 1.000000000000000000 ) ) ;
#4952=CARTESIAN_POINT ( 'NONE',  ( -20.85000000000000142, 77.36242903720540198, -128.6342262366031548 ) ) ;
#4963=VECTOR ( 'NONE', #214813, 1000.000000000000000 ) ;
#4964=EDGE_CURVE ( 'NONE', #92370, #236193, #209352, .T. ) ;
#4973=DIRECTION ( 'NONE',  ( 1.000000000000000000, 0.000000000000000000, 0.000000000000000000 ) ) ;
#4987=EDGE_CURVE ( 'NONE', #180142, #93776, #213635, .T. ) ;
#5007=DIRECTION ( 'NONE',  ( 1.000000000000000000, 0.000000000000000000, 0.000000000000000000 ) ) ;
#5022=FACE_OUTER_BOUND ( 'NONE', #214561, .T. ) ;
#5042=DIRECTION ( 'NONE',  ( 0.000000000000000000, -6.467318590049456648E-15, 1.000000000000000000 ) ) ;
#5046=CARTESIAN_POINT ( 'NONE',  ( 22.45301702632625762, 75.98478912030228116, -181.6728997087847404 ) ) ;
#5066=DIRECTION ( 'NONE',  ( -1.000000000000000000, -0.000000000000000000, -0.000000000000000000 ) ) ;
#5077=DIRECTION ( 'NONE',  ( -1.000000000000000000, 2.952720810173289112E-16, 2.061873921506763405E-30 ) ) ;
#5192=CARTESIAN_POINT ( 'NONE',  ( -20.54999999999999716, 84.66355140188147743, -160.4990063664569959 ) ) ;
#5200=DIRECTION ( 'NONE',  ( 0.000000000000000000, -1.000000000000000000, 0.000000000000000000 ) ) ;
#5233=FACE_OUTER_BOUND ( 'NONE', #141337, .T. ) ;
#5280=FACE_OUTER_BOUND ( 'NONE', #970, .T. ) ;
#5332=CARTESIAN_POINT ( 'NONE',  ( 21.00000000000000000, 66.25000000001223555, -148.8731074845244393 ) ) ;
#5353=EDGE_LOOP ( 'NONE', ( #45507, #106957, #187708, #91716 ) ) ;
#5369=CIRCLE ( 'NONE', #117819, 0.09999999999999939493 ) ;
#5402=ADVANCED_FACE ( 'NONE', ( #232812 ), #38438, .T. ) ;
#5407=FACE_OUTER_BOUND ( 'NONE', #155631, .T. ) ;
#5425=DIRECTION ( 'NONE',  ( 0.000000000000000000, 7.086529944415886769E-15, -1.000000000000000000 ) ) ;
#5438=CYLINDRICAL_SURFACE ( 'NONE', #153147, 0.09999999999999939493 ) ;
#5457=DIRECTION ( 'NONE',  ( 1.000000000000000000, 0.000000000000000000, 0.000000000000000000 ) ) ;
#5472=CARTESIAN_POINT ( 'NONE',  ( -21.11825140030083148, 69.55459243459225149, -170.0303111051570681 ) ) ;
#5474=VERTEX_POINT ( 'NONE', #78825 ) ;
#5480=CARTESIAN_POINT ( 'NONE',  ( -21.05000000000000071, 74.16465844978787914, -158.4679561919613775 ) ) ;
#5496=PRODUCT ( 'Injection Molded Chain Links 12', 'Injection Molded Chain Links 12', '', ( #57338 ) ) ;
#5503=DIRECTION ( 'NONE',  ( -1.000000000000000000, -0.000000000000000000, -0.000000000000000000 ) ) ;
#5518=VERTEX_POINT ( 'NONE', #140086 ) ;
#5558=VERTEX_POINT ( 'NONE', #65704 ) ;
#5572=EDGE_CURVE ( 'NONE', #138951, #109875, #19264, .T. ) ;
#5600=CARTESIAN_POINT ( 'NONE',  ( 20.94999999999999929, 77.83534155023671985, -158.4679561919613491 ) ) ;
#5618=FACE_OUTER_BOUND ( 'NONE', #69055, .T. ) ;
#5643=VERTEX_POINT ( 'NONE', #129545 ) ;
#5690=FACE_OUTER_BOUND ( 'NONE', #7131, .T. ) ;
#5692=AXIS2_PLACEMENT_3D ( 'NONE', #149296, #214378, #55268 ) ;
#5696=EDGE_CURVE ( 'NONE', #199802, #29646, #40145, .T. ) ;
#5699=CIRCLE ( 'NONE', #59682, 0.5000000000000004441 ) ;
#5711=ORIENTED_EDGE ( 'NONE', *, *, #65569, .F. ) ;
#5746=DIRECTION ( 'NONE',  ( -0.000000000000000000, 1.000000000000000000, 6.982962677686266711E-15 ) ) ;
#5763=CARTESIAN_POINT ( 'NONE',  ( 21.04999999999999716, 69.69554417806466518, -170.0020720079842533 ) ) ;
#5804=CARTESIAN_POINT ( 'NONE',  ( -18.59999999999999787, 74.83729825007431202, -162.0231074845243597 ) ) ;
#5830=AXIS2_PLACEMENT_3D ( 'NONE', #96527, #176117, #157857 ) ;
#5836=ORIENTED_EDGE ( 'NONE', *, *, #184423, .T. ) ;
#5846=FACE_OUTER_BOUND ( 'NONE', #240759, .T. ) ;
#5855=AXIS2_PLACEMENT_3D ( 'NONE', #225282, #144464, #10117 ) ;
#5863=VERTEX_POINT ( 'NONE', #52100 ) ;
#5905=AXIS2_PLACEMENT_3D ( 'NONE', #63005, #180402, #223358 ) ;
#5910=ORIENTED_EDGE ( 'NONE', *, *, #3429, .F. ) ;
#5939=CARTESIAN_POINT ( 'NONE',  ( 20.95512820512820440, 65.37615131630040821, -157.8229454651000481 ) ) ;
#5942=CARTESIAN_POINT ( 'NONE',  ( 18.49999999999999289, 65.75000000001223555, -148.6731074845244223 ) ) ;
#5944=TOROIDAL_SURFACE ( 'NONE', #147448, 0.6000000000000004219, 0.1000000000000000056 ) ;
#5983=EDGE_CURVE ( 'NONE', #141624, #80942, #52749, .T. ) ;
#5985=VERTEX_POINT ( 'NONE', #78085 ) ;
#5986=CYLINDRICAL_SURFACE ( 'NONE', #212989, 4.049999999999998046 ) ;
#5990=ORIENTED_EDGE ( 'NONE', *, *, #196107, .F. ) ;
#6003=FACE_OUTER_BOUND ( 'NONE', #87757, .T. ) ;
#6037=EDGE_LOOP ( 'NONE', ( #250271, #144712, #218739, #5711 ) ) ;
#6038=AXIS2_PLACEMENT_3D ( 'NONE', #69690, #202757, #107504 ) ;
#6040=DIRECTION ( 'NONE',  ( 1.000000000000000000, 0.000000000000000000, 0.000000000000000000 ) ) ;
#6083=ORIENTED_EDGE ( 'NONE', *, *, #255835, .T. ) ;
#6098=UNCERTAINTY_MEASURE_WITH_UNIT (LENGTH_MEASURE( 1.000000000000000082E-05 ), #35512, 'distance_accuracy_value', 'NONE');
#6162=CIRCLE ( 'NONE', #156044, 0.09999999999998898659 ) ;
#6166=CARTESIAN_POINT ( 'NONE',  ( -20.00857864376270001, 66.85000000001222986, -148.8731074845244393 ) ) ;
#6175=DIRECTION ( 'NONE',  ( 1.000000000000000000, 0.000000000000000000, 0.000000000000000000 ) ) ;
#6198=CARTESIAN_POINT ( 'NONE',  ( 22.59066674512271078, 64.25000000001236344, -170.0536116081545117 ) ) ;
#6265=EDGE_LOOP ( 'NONE', ( #107236, #91555, #43615, #102821 ) ) ;
#6325=CYLINDRICAL_SURFACE ( 'NONE', #67005, 0.09999999999999939493 ) ;
#6329=TOROIDAL_SURFACE ( 'NONE', #193774, 0.2000000000000000111, 0.1000000000000000056 ) ;
#6346=CARTESIAN_POINT ( 'NONE',  ( 22.42196299218230493, 75.99755832602515682, -181.6727191871738114 ) ) ;
#6353=CARTESIAN_POINT ( 'NONE',  ( -20.85000000000000142, 77.83585931145570669, -125.0186683157258045 ) ) ;
#6355=ORIENTED_EDGE ( 'NONE', *, *, #201949, .T. ) ;
#6370=EDGE_CURVE ( 'NONE', #145384, #168942, #252279, .T. ) ;
#6440=DIRECTION ( 'NONE',  ( -1.000000000000000000, 0.000000000000000000, -0.000000000000000000 ) ) ;
#6444=CARTESIAN_POINT ( 'NONE',  ( -21.05000000000000071, 74.26374286841490857, -158.4544551555068779 ) ) ;
#6455=VERTEX_POINT ( 'NONE', #243608 ) ;
#6512=AXIS2_PLACEMENT_3D ( 'NONE', #122655, #183891, #200883 ) ;
#6517=DIRECTION ( 'NONE',  ( 0.000000000000000000, 0.000000000000000000, 1.000000000000000000 ) ) ;
#6522=EDGE_LOOP ( 'NONE', ( #124280, #145993, #52232 ) ) ;
#6540=AXIS2_PLACEMENT_3D ( 'NONE', #9314, #45874, #49726 ) ;
#6546=AXIS2_PLACEMENT_3D ( 'NONE', #179968, #238647, #1297 ) ;
#6548=TOROIDAL_SURFACE ( 'NONE', #256271, 11.90000000000000391, 0.1000000000000000056 ) ;
#6558=EDGE_LOOP ( 'NONE', ( #242649, #64671, #163331, #148147 ) ) ;
#6573=DIRECTION ( 'NONE',  ( 1.000000000000000000, 0.000000000000000000, 0.000000000000000000 ) ) ;
#6586=CARTESIAN_POINT ( 'NONE',  ( 19.75857864376269291, 64.25000000001220712, -145.1731074845244223 ) ) ;
#6587=DIRECTION ( 'NONE',  ( 0.000000000000000000, 0.000000000000000000, 1.000000000000000000 ) ) ;
#6592=CARTESIAN_POINT ( 'NONE',  ( 21.14261333020286671, 65.28430735075738767, -157.7731074845242176 ) ) ;
#6594=DIRECTION ( 'NONE',  ( 0.000000000000000000, -6.982962677686266711E-15, 1.000000000000000000 ) ) ;
#6601=ORIENTED_EDGE ( 'NONE', *, *, #246686, .F. ) ;
#6603=VERTEX_POINT ( 'NONE', #79381 ) ;
#6610=CARTESIAN_POINT ( 'NONE',  ( 21.05000000000000071, 67.22371710471985295, -161.4644784893834810 ) ) ;
#6617=FACE_OUTER_BOUND ( 'NONE', #63562, .T. ) ;
#6620=ORIENTED_EDGE ( 'NONE', *, *, #195990, .F. ) ;
#6631=LINE ( 'NONE', #66619, #179762 ) ;
#6634=CARTESIAN_POINT ( 'NONE',  ( 18.49999999999999645, 77.29973367124323147, -179.9949779616549392 ) ) ;
#6636=ADVANCED_FACE ( 'NONE', ( #10138 ), #109221, .T. ) ;
#6650=CARTESIAN_POINT ( 'NONE',  ( -21.14999999999999858, 64.35000000001232934, -163.2392418215462726 ) ) ;
#6682=CARTESIAN_POINT ( 'NONE',  ( 20.94999999999999574, 87.39257802171802325, -166.9491579046923277 ) ) ;
#6686=DIRECTION ( 'NONE',  ( 1.000000000000000000, 0.000000000000000000, 0.000000000000000000 ) ) ;
#6689=EDGE_CURVE ( 'NONE', #213031, #95210, #256511, .T. ) ;
#6721=VERTEX_POINT ( 'NONE', #131360 ) ;
#6724=EDGE_LOOP ( 'NONE', ( #189383, #205714, #127359, #144892 ) ) ;
#6738=CARTESIAN_POINT ( 'NONE',  ( 20.94999999999999574, 77.83534155023670564, -158.4679561919613491 ) ) ;
#6775=CARTESIAN_POINT ( 'NONE',  ( 21.05000000000000071, 70.50000000001230660, -157.6178414656113205 ) ) ;
#6784=ORIENTED_EDGE ( 'NONE', *, *, #116312, .F. ) ;
#6795=ORIENTED_EDGE ( 'NONE', *, *, #218569, .T. ) ;
#6799=CARTESIAN_POINT ( 'NONE',  ( 19.97071067811864609, 64.27928932189355749, -145.3731074845244109 ) ) ;
#6809=EDGE_LOOP ( 'NONE', ( #51009, #6601, #240147, #222891 ) ) ;
#6819=AXIS2_PLACEMENT_3D ( 'NONE', #141345, #120528, #42255 ) ;
#6822=VECTOR ( 'NONE', #10325, 1000.000000000000000 ) ;
#6835=FACE_OUTER_BOUND ( 'NONE', #81617, .T. ) ;
#6845=AXIS2_PLACEMENT_3D ( 'NONE', #118752, #156618, #215268 ) ;
#6861=B_SPLINE_CURVE_WITH_KNOTS ( 'NONE', 3,
 ( #223261, #122906, #124193, #221958, #181600, #102010, #81174, #120363, #2928, #160768 ),
 .UNSPECIFIED., .F., .F.,
 ( 4, 2, 2, 2, 4 ),
 ( 0.000000000000000000, 4.221631689684923993E-05, 8.443263379369847987E-05, 0.0001688652675874693031, 0.0003377305351749470630 ),
 .UNSPECIFIED. ) ;
#6868=CARTESIAN_POINT ( 'NONE',  ( 18.59999999999998366, 68.97833521811203639, -132.6895420826271277 ) ) ;
#6869=ORIENTED_EDGE ( 'NONE', *, *, #131852, .T. ) ;
#6890=FACE_OUTER_BOUND ( 'NONE', #177032, .T. ) ;
#6913=ORIENTED_EDGE ( 'NONE', *, *, #36753, .F. ) ;
#6943=DIRECTION ( 'NONE',  ( -1.000000000000000000, -0.000000000000000000, -0.000000000000000000 ) ) ;
#6958=EDGE_LOOP ( 'NONE', ( #118174, #143884, #19606, #240312 ) ) ;
#6982=ORIENTED_EDGE ( 'NONE', *, *, #38828, .F. ) ;
#6984=DIRECTION ( 'NONE',  ( 0.000000000000000000, -0.008583690987135041833, 0.9999631594459055250 ) ) ;
#7022=EDGE_CURVE ( 'NONE', #241641, #30238, #19448, .T. ) ;
#7042=AXIS2_PLACEMENT_3D ( 'NONE', #89309, #162786, #21991 ) ;
#7070=DIRECTION ( 'NONE',  ( 0.000000000000000000, 0.9908441862701420355, 0.1350103645453197554 ) ) ;
#7073=DIRECTION ( 'NONE',  ( 0.000000000000000000, 0.000000000000000000, 1.000000000000000000 ) ) ;
#7131=EDGE_LOOP ( 'NONE', ( #99939, #135295, #70914, #10022 ) ) ;
#7136=DIRECTION ( 'NONE',  ( 0.000000000000000000, 0.000000000000000000, 1.000000000000000000 ) ) ;
#7172=EDGE_CURVE ( 'NONE', #5985, #39887, #248387, .T. ) ;
#7193=ORIENTED_EDGE ( 'NONE', *, *, #7172, .F. ) ;
#7198=CARTESIAN_POINT ( 'NONE',  ( 20.95000000000000284, 64.40000000001218439, -143.4513107147999449 ) ) ;
#7202=CARTESIAN_POINT ( 'NONE',  ( -21.05000000000000071, 69.58624026620211112, -169.9374944237204375 ) ) ;
#7212=ORIENTED_EDGE ( 'NONE', *, *, #239908, .F. ) ;
#7224=DIRECTION ( 'NONE',  ( 0.000000000000000000, 0.000000000000000000, 1.000000000000000000 ) ) ;
#7227=AXIS2_PLACEMENT_3D ( 'NONE', #69301, #9308, #124140 ) ;
#7241=ADVANCED_FACE ( 'NONE', ( #19794 ), #74659, .T. ) ;
#7249=EDGE_CURVE ( 'NONE', #34228, #126961, #138408, .T. ) ;
#7256=VECTOR ( 'NONE', #184514, 1000.000000000000000 ) ;
#7274=CIRCLE ( 'NONE', #186362, 6.258578643762696458 ) ;
#7299=ORIENTED_EDGE ( 'NONE', *, *, #21953, .F. ) ;
#7315=DIRECTION ( 'NONE',  ( 0.000000000000000000, -1.000000000000000000, -6.982962677686266711E-15 ) ) ;
#7321=AXIS2_PLACEMENT_3D ( 'NONE', #107219, #66819, #47231 ) ;
#7334=CARTESIAN_POINT ( 'NONE',  ( 20.94999999999999574, 77.34908441863935025, -162.0366085209788594 ) ) ;
#7339=ADVANCED_FACE ( 'NONE', ( #199722 ), #82128, .F. ) ;
#7344=EDGE_CURVE ( 'NONE', #222829, #40059, #2761, .T. ) ;
#7351=LINE ( 'NONE', #68620, #60898 ) ;
#7428=LINE ( 'NONE', #166544, #160863 ) ;
#7488=FACE_OUTER_BOUND ( 'NONE', #39131, .T. ) ;
#7506=DIRECTION ( 'NONE',  ( -0.000000000000000000, -0.1298341882519953583, -0.9915357197604862671 ) ) ;
#7514=DIRECTION ( 'NONE',  ( 1.000000000000000000, -0.000000000000000000, 0.000000000000000000 ) ) ;
#7517=ORIENTED_EDGE ( 'NONE', *, *, #87360, .F. ) ;
#7537=ADVANCED_FACE ( 'NONE', ( #147430 ), #31374, .F. ) ;
#7540=CYLINDRICAL_SURFACE ( 'NONE', #93578, 0.09999999999998898659 ) ;
#7574=CARTESIAN_POINT ( 'NONE',  ( -23.15000000000000213, 64.35000000001228670, -157.7731074845244450 ) ) ;
#7575=CARTESIAN_POINT ( 'NONE',  ( 21.05000000000000071, 71.00000000001223555, -148.9283735034374843 ) ) ;
#7591=CARTESIAN_POINT ( 'NONE',  ( -18.59999999999999787, 85.40000000001226965, -162.7258477248610120 ) ) ;
#7595=FACE_OUTER_BOUND ( 'NONE', #246010, .T. ) ;
#7639=VERTEX_POINT ( 'NONE', #192987 ) ;
#7643=CARTESIAN_POINT ( 'NONE',  ( 20.30466543256828160, 66.69576306075813932, -161.7694448331317005 ) ) ;
#7666=CARTESIAN_POINT ( 'NONE',  ( -22.47071067811865319, 68.27992525551431413, -170.1221999392270448 ) ) ;
#7681=EDGE_CURVE ( 'NONE', #61341, #249154, #15741, .T. ) ;
#7690=CIRCLE ( 'NONE', #70251, 0.6000000000000033085 ) ;
#7722=EDGE_LOOP ( 'NONE', ( #113643, #182598, #67132, #163751 ) ) ;
#7802=DIRECTION ( 'NONE',  ( -1.000000000000000000, -0.000000000000000000, -0.000000000000000000 ) ) ;
#7818=EDGE_LOOP ( 'NONE', ( #154222, #123969, #193935, #23899 ) ) ;
#7839=VECTOR ( 'NONE', #95221, 1000.000000000000000 ) ;
#7854=EDGE_CURVE ( 'NONE', #2577, #178267, #53114, .T. ) ;
#7900=CARTESIAN_POINT ( 'NONE',  ( 19.80993210785544534, 64.25000000001219291, -145.2559897356397016 ) ) ;
#7914=VERTEX_POINT ( 'NONE', #149715 ) ;
#7923=FACE_OUTER_BOUND ( 'NONE', #181610, .T. ) ;
#7933=CARTESIAN_POINT ( 'NONE',  ( 20.94999999999999574, 77.83534155023670564, -158.4679561919613491 ) ) ;
#7945=CARTESIAN_POINT ( 'NONE',  ( -20.54999999999999716, 71.75000000001229239, -157.6731074845243654 ) ) ;
#7950=DIRECTION ( 'NONE',  ( 0.000000000000000000, 0.000000000000000000, -1.000000000000000000 ) ) ;
#7984=TOROIDAL_SURFACE ( 'NONE', #153772, 2.100000000000002309, 0.1000000000000000056 ) ;
#8085=CARTESIAN_POINT ( 'NONE',  ( -21.07928932188134041, 69.67148334361368711, -170.1220026301790540 ) ) ;
#8095=ORIENTED_EDGE ( 'NONE', *, *, #190341, .F. ) ;
#8130=CARTESIAN_POINT ( 'NONE',  ( 20.84999999999999432, 77.16412189325330928, -128.6082593989527254 ) ) ;
#8161=AXIS2_PLACEMENT_3D ( 'NONE', #252720, #233202, #32446 ) ;
#8163=ADVANCED_FACE ( 'NONE', ( #124687 ), #132421, .T. ) ;
#8181=ORIENTED_EDGE ( 'NONE', *, *, #250406, .T. ) ;
#8199=CYLINDRICAL_SURFACE ( 'NONE', #28734, 0.09999999999998898659 ) ;
#8201=CARTESIAN_POINT ( 'NONE',  ( 22.45380639572713477, 75.99999985734899610, -181.7735403756410051 ) ) ;
#8228=CARTESIAN_POINT ( 'NONE',  ( 18.52928932188133970, 65.72071067813088519, -148.6731074845244223 ) ) ;
#8262=CIRCLE ( 'NONE', #99796, 0.1999999999999987899 ) ;
#8368=AXIS2_PLACEMENT_3D ( 'NONE', #245016, #182499, #65096 ) ;
#8388=CIRCLE ( 'NONE', #166629, 4.049999999999998046 ) ;
#8425=EDGE_LOOP ( 'NONE', ( #174313, #122653, #121260 ) ) ;
#8428=CIRCLE ( 'NONE', #41775, 0.09999999999998898659 ) ;
#8514=CARTESIAN_POINT ( 'NONE',  ( -18.59999999999999787, 69.01799029515568407, -132.8269553662681233 ) ) ;
#8524=FACE_OUTER_BOUND ( 'NONE', #255435, .T. ) ;
#8532=DIRECTION ( 'NONE',  ( 0.000000000000000000, -1.000000000000000000, -6.982962677686266711E-15 ) ) ;
#8566=DIRECTION ( 'NONE',  ( -1.000000000000000000, 0.000000000000000000, -0.000000000000000000 ) ) ;
#8567=CARTESIAN_POINT ( 'NONE',  ( 18.59999999999999076, 65.50857864377491069, -145.2731074845244450 ) ) ;
#8591=CARTESIAN_POINT ( 'NONE',  ( -20.94999999999999929, 74.16465844978787914, -158.4679561919613775 ) ) ;
#8599=EDGE_CURVE ( 'NONE', #19886, #141624, #174333, .T. ) ;
#8634=DIRECTION ( 'NONE',  ( 0.000000000000000000, -1.000000000000000000, -6.982962677686265922E-15 ) ) ;
#8638=CARTESIAN_POINT ( 'NONE',  ( -21.05000000000000071, 70.10000000001235776, -159.8040077198679683 ) ) ;
#8653=AXIS2_PLACEMENT_3D ( 'NONE', #196818, #160300, #140702 ) ;
#8659=EDGE_CURVE ( 'NONE', #206737, #26294, #170063, .T. ) ;
#8717=AXIS2_PLACEMENT_3D ( 'NONE', #215825, #196281, #137573 ) ;
#8753=FACE_OUTER_BOUND ( 'NONE', #211188, .T. ) ;
#8767=EDGE_CURVE ( 'NONE', #144474, #1798, #157792, .T. ) ;
#8783=EDGE_CURVE ( 'NONE', #55258, #25682, #151495, .T. ) ;
#8829=CARTESIAN_POINT ( 'NONE',  ( -21.05000000000000071, 87.65000000001215597, -139.5231074845243029 ) ) ;
#8831=VERTEX_POINT ( 'NONE', #18235 ) ;
#8861=CARTESIAN_POINT ( 'NONE',  ( -20.94999999999999929, 87.65000000001215597, -139.6231074845242688 ) ) ;
#8893=ORIENTED_EDGE ( 'NONE', *, *, #15033, .T. ) ;
#8955=AXIS2_PLACEMENT_3D ( 'NONE', #224922, #205360, #166289 ) ;
#8956=ADVANCED_FACE ( 'NONE', ( #3804 ), #205852, .T. ) ;
#8994=CARTESIAN_POINT ( 'NONE',  ( 20.84999999999998721, 64.25000000001215028, -136.5231074845244166 ) ) ;
#9032=DIRECTION ( 'NONE',  ( 1.000000000000000000, 0.000000000000000000, 0.000000000000000000 ) ) ;
#9063=ORIENTED_EDGE ( 'NONE', *, *, #136347, .T. ) ;
#9064=AXIS2_PLACEMENT_3D ( 'NONE', #204822, #167034, #48329 ) ;
#9081=ADVANCED_FACE ( 'NONE', ( #169338 ), #199820, .F. ) ;
#9083=AXIS2_PLACEMENT_3D ( 'NONE', #138737, #198747, #140040 ) ;
#9132=LINE ( 'NONE', #202195, #123687 ) ;
#9212=CARTESIAN_POINT ( 'NONE',  ( 22.60000000000000142, 76.00000000001237765, -170.0231074845243597 ) ) ;
#9218=VECTOR ( 'NONE', #142980, 1000.000000000000000 ) ;
#9220=CARTESIAN_POINT ( 'NONE',  ( 21.14999999999999858, 67.21339244341217523, -157.7731074845244166 ) ) ;
#9235=AXIS2_PLACEMENT_3D ( 'NONE', #57515, #137072, #38001 ) ;
#9274=CARTESIAN_POINT ( 'NONE',  ( 21.07928932188134397, 69.67148334361908724, -170.1220026301787982 ) ) ;
#9276=DIRECTION ( 'NONE',  ( 0.000000000000000000, 0.000000000000000000, -1.000000000000000000 ) ) ;
#9279=EDGE_CURVE ( 'NONE', #132498, #199740, #55720, .T. ) ;
#9285=AXIS2_PLACEMENT_3D ( 'NONE', #25301, #41019, #39742 ) ;
#9301=B_SPLINE_CURVE_WITH_KNOTS ( 'NONE', 3,
 ( #195955, #232520, #56404, #152996, #92975, #34322 ),
 .UNSPECIFIED., .F., .F.,
 ( 4, 2, 4 ),
 ( 0.000000000000000000, 0.0002113392456166052376, 0.0004226784912332104752 ),
 .UNSPECIFIED. ) ;
#9308=DIRECTION ( 'NONE',  ( -1.000000000000000000, -0.000000000000000000, -0.000000000000000000 ) ) ;
#9314=CARTESIAN_POINT ( 'NONE',  ( 23.14999999999999503, 69.35000000001228670, -157.8731074845244109 ) ) ;
#9323=DIRECTION ( 'NONE',  ( 0.000000000000000000, -6.982962677686266711E-15, 1.000000000000000000 ) ) ;
#9341=VERTEX_POINT ( 'NONE', #80418 ) ;
#9349=DIRECTION ( 'NONE',  ( 0.000000000000000000, 6.982962677686266711E-15, -1.000000000000000000 ) ) ;
#9424=ADVANCED_FACE ( 'NONE', ( #227663 ), #51565, .T. ) ;
#9427=SPHERICAL_SURFACE ( 'NONE', #181756, 0.1000000000000000056 ) ;
#9445=ADVANCED_FACE ( 'NONE', ( #29512 ), #28226, .F. ) ;
#9475=DIRECTION ( 'NONE',  ( -1.000000000000000000, 7.304098846218163263E-16, -4.217023435051627211E-16 ) ) ;
#9502=DIRECTION ( 'NONE',  ( 0.000000000000000000, 7.116814260417668513E-15, -1.000000000000000000 ) ) ;
#9526=DIRECTION ( 'NONE',  ( 1.734723475976817507E-14, 1.000000000000000000, 6.982962677686266711E-15 ) ) ;
#9539=LINE ( 'NONE', #129504, #93814 ) ;
#9573=CARTESIAN_POINT ( 'NONE',  ( 21.07016717456945187, 69.67905916191212157, -170.0231074845244450 ) ) ;
#9600=EDGE_CURVE ( 'NONE', #8831, #166820, #83226, .T. ) ;
#9623=CARTESIAN_POINT ( 'NONE',  ( -23.25000000000000000, 64.25000000001246292, -181.7731074845244450 ) ) ;
#9640=EDGE_LOOP ( 'NONE', ( #20436, #12534, #197916 ) ) ;
#9646=CIRCLE ( 'NONE', #38690, 0.1000000000000043771 ) ;
#9662=DIRECTION ( 'NONE',  ( 0.000000000000000000, -1.000000000000000000, -6.982962677686266711E-15 ) ) ;
#9710=VERTEX_POINT ( 'NONE', #59256 ) ;
#9737=ORIENTED_EDGE ( 'NONE', *, *, #197200, .T. ) ;
#9742=AXIS2_PLACEMENT_3D ( 'NONE', #153970, #155240, #230911 ) ;
#9765=CARTESIAN_POINT ( 'NONE',  ( 19.75857864376268935, 64.25000000001220712, -145.1731074845244507 ) ) ;
#9772=ORIENTED_EDGE ( 'NONE', *, *, #183432, .F. ) ;
#9779=CARTESIAN_POINT ( 'NONE',  ( 20.95512820512820440, 65.37615131630045084, -162.3581939154368285 ) ) ;
#9791=VERTEX_POINT ( 'NONE', #26626 ) ;
#9805=CARTESIAN_POINT ( 'NONE',  ( 21.05000000000000071, 64.25000000001219291, -143.5379132551783812 ) ) ;
#9862=CIRCLE ( 'NONE', #243090, 0.09999999999998898659 ) ;
#9871=FACE_OUTER_BOUND ( 'NONE', #123509, .T. ) ;
#9890=DIRECTION ( 'NONE',  ( 1.000000000000000000, 0.000000000000000000, 0.000000000000000000 ) ) ;
#9904=EDGE_CURVE ( 'NONE', #58764, #231343, #8428, .T. ) ;
#9916=ADVANCED_FACE ( 'NONE', ( #190850 ), #134663, .F. ) ;
#9943=CARTESIAN_POINT ( 'NONE',  ( -23.25000000000000000, 76.00000000001213607, -136.5231074845243313 ) ) ;
#9963=DIRECTION ( 'NONE',  ( 0.7071067811865487940, 4.851104656540973741E-15, -0.7071067811865463515 ) ) ;
#9973=FACE_OUTER_BOUND ( 'NONE', #244853, .T. ) ;
#9987=AXIS2_PLACEMENT_3D ( 'NONE', #80568, #58442, #137985 ) ;
#9994=AXIS2_PLACEMENT_3D ( 'NONE', #152500, #247717, #35129 ) ;
#9997=VERTEX_POINT ( 'NONE', #64045 ) ;
#9998=DIRECTION ( 'NONE',  ( -6.938893903907222067E-15, -1.000000000000000000, -7.272083257015735086E-15 ) ) ;
#10000=ORIENTED_EDGE ( 'NONE', *, *, #12869, .F. ) ;
#10022=ORIENTED_EDGE ( 'NONE', *, *, #166909, .F. ) ;
#10030=DIRECTION ( 'NONE',  ( -1.000000000000000000, 0.000000000000000000, 0.000000000000000000 ) ) ;
#10040=ORIENTED_EDGE ( 'NONE', *, *, #4897, .T. ) ;
#10044=LINE ( 'NONE', #105252, #193348 ) ;
#10066=EDGE_CURVE ( 'NONE', #128766, #216103, #104689, .T. ) ;
#10103=ORIENTED_EDGE ( 'NONE', *, *, #224122, .T. ) ;
#10117=DIRECTION ( 'NONE',  ( 0.000000000000000000, 0.000000000000000000, 1.000000000000000000 ) ) ;
#10126=CARTESIAN_POINT ( 'NONE',  ( 22.32929514600007792, 68.42135243463590655, -170.1221831626383221 ) ) ;
#10138=FACE_OUTER_BOUND ( 'NONE', #230829, .T. ) ;
#10147=ADVANCED_FACE ( 'NONE', ( #224390 ), #147435, .T. ) ;
#10188=EDGE_CURVE ( 'NONE', #168738, #243465, #6631, .T. ) ;
#10239=ADVANCED_FACE ( 'NONE', ( #168332 ), #129848, .T. ) ;
#10257=DIRECTION ( 'NONE',  ( 1.000000000000000000, 0.000000000000000000, 0.000000000000000000 ) ) ;
#10269=CIRCLE ( 'NONE', #226723, 2.000000000000001776 ) ;
#10274=DIRECTION ( 'NONE',  ( 0.000000000000000000, -6.938893903907222067E-15, 1.000000000000000000 ) ) ;
#10289=AXIS2_PLACEMENT_3D ( 'NONE', #161807, #45682, #204742 ) ;
#10290=CIRCLE ( 'NONE', #47846, 0.09999999999998898659 ) ;
#10298=DIRECTION ( 'NONE',  ( 0.000000000000000000, -0.9876197685951265681, -0.1568667991644790149 ) ) ;
#10305=CYLINDRICAL_SURFACE ( 'NONE', #1065, 0.09999999999999939493 ) ;
#10325=DIRECTION ( 'NONE',  ( -1.000000000000000000, 0.000000000000000000, -0.000000000000000000 ) ) ;
#10329=CARTESIAN_POINT ( 'NONE',  ( 19.75857864376268935, 64.35000000001220144, -145.1731074845244507 ) ) ;
#10343=TOROIDAL_SURFACE ( 'NONE', #51998, 4.149999999999999467, 0.1000000000000000056 ) ;
#10361=VERTEX_POINT ( 'NONE', #216386 ) ;
#10367=ORIENTED_EDGE ( 'NONE', *, *, #16329, .T. ) ;
#10377=LINE ( 'NONE', #44677, #118131 ) ;
#10378=CARTESIAN_POINT ( 'NONE',  ( -20.85000000000000142, 77.83585931145570669, -124.9186683157258244 ) ) ;
#10402=DIRECTION ( 'NONE',  ( -1.000000000000000000, 0.000000000000000000, 0.000000000000000000 ) ) ;
#10403=AXIS2_PLACEMENT_3D ( 'NONE', #191981, #212812, #95419 ) ;
#10406=ORIENTED_EDGE ( 'NONE', *, *, #146075, .F. ) ;
#10427=VERTEX_POINT ( 'NONE', #35226 ) ;
#10464=ORIENTED_EDGE ( 'NONE', *, *, #42281, .F. ) ;
#10510=DIRECTION ( 'NONE',  ( 1.000000000000000000, -0.000000000000000000, 0.000000000000000000 ) ) ;
#10517=EDGE_CURVE ( 'NONE', #189423, #109416, #184197, .T. ) ;
#10534=CARTESIAN_POINT ( 'NONE',  ( 21.33487959338958717, 69.27444184810119054, -170.0231074845243882 ) ) ;
#10558=EDGE_CURVE ( 'NONE', #81073, #127304, #80712, .T. ) ;
#10565=DIRECTION ( 'NONE',  ( -1.000000000000000000, 0.000000000000000000, 0.000000000000000000 ) ) ;
#10566=CARTESIAN_POINT ( 'NONE',  ( -21.11101077989000174, 75.98471473109815122, -176.4467922192504830 ) ) ;
#10630=ORIENTED_EDGE ( 'NONE', *, *, #85599, .T. ) ;
#10632=VERTEX_POINT ( 'NONE', #225361 ) ;
#10641=EDGE_CURVE ( 'NONE', #121863, #251542, #184971, .T. ) ;
#10657=CIRCLE ( 'NONE', #189708, 0.1000000000000043771 ) ;
#10666=ORIENTED_EDGE ( 'NONE', *, *, #188114, .T. ) ;
#10693=ORIENTED_EDGE ( 'NONE', *, *, #3630, .F. ) ;
#10697=CIRCLE ( 'NONE', #177326, 0.1000000000000070832 ) ;
#10714=EDGE_CURVE ( 'NONE', #22319, #203751, #192406, .T. ) ;
#10726=DIRECTION ( 'NONE',  ( -0.000000000000000000, 0.8700118002898356018, -0.4930308989875170078 ) ) ;
#10761=ADVANCED_FACE ( 'NONE', ( #14053 ), #254610, .F. ) ;
#10781=CARTESIAN_POINT ( 'NONE',  ( -23.25000000000000000, 76.00000000001213607, -136.5231074845243313 ) ) ;
#10795=CARTESIAN_POINT ( 'NONE',  ( -23.25000000000000000, 64.25000000001237765, -170.0231074845244166 ) ) ;
#10796=ORIENTED_EDGE ( 'NONE', *, *, #230927, .F. ) ;
#10807=CIRCLE ( 'NONE', #23299, 0.09999999999999489853 ) ;
#10816=DIRECTION ( 'NONE',  ( 1.000000000000000000, 0.000000000000000000, 0.000000000000000000 ) ) ;
#10841=AXIS2_PLACEMENT_3D ( 'NONE', #194095, #15453, #94962 ) ;
#10843=DIRECTION ( 'NONE',  ( 1.000000000000000000, 7.304098846218135653E-16, 5.100424963727256530E-30 ) ) ;
#10874=ORIENTED_EDGE ( 'NONE', *, *, #243078, .T. ) ;
#10875=CARTESIAN_POINT ( 'NONE',  ( 22.47071067811864609, 68.27992525551434255, -170.1221999392270448 ) ) ;
#10925=DIRECTION ( 'NONE',  ( -1.000000000000000000, -0.000000000000000000, -0.000000000000000000 ) ) ;
#10947=ORIENTED_EDGE ( 'NONE', *, *, #103447, .F. ) ;
#10949=EDGE_CURVE ( 'NONE', #241979, #58292, #26900, .T. ) ;
#10972=LINE ( 'NONE', #91792, #130675 ) ;
#10999=ORIENTED_EDGE ( 'NONE', *, *, #160129, .T. ) ;
#11019=EDGE_CURVE ( 'NONE', #173065, #76314, #100949, .T. ) ;
#11025=EDGE_LOOP ( 'NONE', ( #48008, #194421, #184946, #10947 ) ) ;
#11037=AXIS2_PLACEMENT_3D ( 'NONE', #236788, #121994, #56843 ) ;
#11040=EDGE_CURVE ( 'NONE', #40351, #146933, #63413, .T. ) ;
#11056=CARTESIAN_POINT ( 'NONE',  ( 20.04142135623730070, 64.25000000001220712, -145.3731074845244393 ) ) ;
#11104=CARTESIAN_POINT ( 'NONE',  ( -20.05000000000000426, 66.75000000001223555, -148.7731074845244166 ) ) ;
#11169=ORIENTED_EDGE ( 'NONE', *, *, #195611, .F. ) ;
#11192=EDGE_CURVE ( 'NONE', #223637, #92778, #209330, .T. ) ;
#11220=CARTESIAN_POINT ( 'NONE',  ( 22.39999999999999858, 75.90000000001242597, -177.8138870828977360 ) ) ;
#11238=CYLINDRICAL_SURFACE ( 'NONE', #43289, 0.09999999999999939493 ) ;
#11258=UNCERTAINTY_MEASURE_WITH_UNIT (LENGTH_MEASURE( 1.000000000000000082E-05 ), #33384, 'distance_accuracy_value', 'NONE');
#11259=CARTESIAN_POINT ( 'NONE',  ( -20.86777300164945004, 65.66799936921553638, -130.9299399888601272 ) ) ;
#11289=AXIS2_PLACEMENT_3D ( 'NONE', #171369, #132194, #33139 ) ;
#11329=ORIENTED_EDGE ( 'NONE', *, *, #56060, .F. ) ;
#11354=DIRECTION ( 'NONE',  ( -0.000000000000000000, 1.000000000000000000, 8.717686153663073805E-15 ) ) ;
#11381=VERTEX_POINT ( 'NONE', #26255 ) ;
#11389=EDGE_CURVE ( 'NONE', #245795, #68761, #210029, .T. ) ;
#11413=ORIENTED_EDGE ( 'NONE', *, *, #131848, .F. ) ;
#11453=CARTESIAN_POINT ( 'NONE',  ( -20.54999999999999716, 73.50000000001229239, -156.7984855617622770 ) ) ;
#11468=CARTESIAN_POINT ( 'NONE',  ( 23.14999999999999858, 76.00000000001213607, -136.5231074845243313 ) ) ;
#11505=DIRECTION ( 'NONE',  ( -7.304098846218134667E-16, -1.000000000000000000, -6.982962677686267499E-15 ) ) ;
#11513=SPHERICAL_SURFACE ( 'NONE', #98921, 0.1000000000000000056 ) ;
#11536=AXIS2_PLACEMENT_3D ( 'NONE', #106094, #44870, #185663 ) ;
#11558=DIRECTION ( 'NONE',  ( 0.000000000000000000, -6.454785026890489601E-15, 1.000000000000000000 ) ) ;
#11584=CARTESIAN_POINT ( 'NONE',  ( 20.94999999999999929, 74.16465844978787914, -158.4679561919613775 ) ) ;
#11587=CARTESIAN_POINT ( 'NONE',  ( -20.94999999999999929, 70.10000000001220144, -146.7422072491807796 ) ) ;
#11611=ORIENTED_EDGE ( 'NONE', *, *, #189723, .T. ) ;
#11616=ORIENTED_EDGE ( 'NONE', *, *, #208146, .F. ) ;
#11621=EDGE_CURVE ( 'NONE', #244761, #207287, #196856, .T. ) ;
#11624=VERTEX_POINT ( 'NONE', #19533 ) ;
#11635=DIRECTION ( 'NONE',  ( 0.000000000000000000, 1.000000000000000000, 6.688090509790097607E-15 ) ) ;
#11641=CARTESIAN_POINT ( 'NONE',  ( 20.95512820512820440, 67.12384868372420499, -161.4644784893834810 ) ) ;
#11655=AXIS2_PLACEMENT_3D ( 'NONE', #136265, #94591, #116730 ) ;
#11711=CARTESIAN_POINT ( 'NONE',  ( -21.05000000000000426, 76.02103547655254090, -176.3275633064720296 ) ) ;
#11723=EDGE_LOOP ( 'NONE', ( #233672, #80326, #174766, #217559 ) ) ;
#11772=EDGE_LOOP ( 'NONE', ( #96842, #86600, #221750, #122432 ) ) ;
#11773=ORIENTED_EDGE ( 'NONE', *, *, #119032, .T. ) ;
#11781=CARTESIAN_POINT ( 'NONE',  ( 21.14999999999999858, 64.35000000001228670, -157.7731074845244450 ) ) ;
#11790=CARTESIAN_POINT ( 'NONE',  ( -20.94999999999999929, 76.00000000001213607, -136.5231074845243313 ) ) ;
#11865=DIRECTION ( 'NONE',  ( 1.000000000000000000, 0.000000000000000000, 0.000000000000000000 ) ) ;
#11939=ADVANCED_FACE ( 'NONE', ( #94884 ), #147161, .T. ) ;
#11978=ADVANCED_FACE ( 'NONE', ( #92320 ), #131451, .F. ) ;
#12003=ADVANCED_FACE ( 'NONE', ( #71508 ), #54476, .T. ) ;
#12013=DIRECTION ( 'NONE',  ( 1.000000000000000000, 0.000000000000000000, 0.000000000000000000 ) ) ;
#12021=CARTESIAN_POINT ( 'NONE',  ( -20.94999999999999929, 77.83534155023670564, -158.4679561919613491 ) ) ;
#12033=EDGE_LOOP ( 'NONE', ( #83231, #95866, #190917, #69683 ) ) ;
#12035=DIRECTION ( 'NONE',  ( 1.000000000000000000, 0.000000000000000000, 0.000000000000000000 ) ) ;
#12053=CARTESIAN_POINT ( 'NONE',  ( -22.16821283564876666, 68.44102665923159634, -170.0231074845243882 ) ) ;
#12062=DIRECTION ( 'NONE',  ( 1.000000000000000000, 0.000000000000000000, 0.000000000000000000 ) ) ;
#12075=ORIENTED_EDGE ( 'NONE', *, *, #239776, .T. ) ;
#12084=SHAPE_REPRESENTATION_RELATIONSHIP ( 'NONE' , 'NONE' ,  #106899, #154111 ) ;
#12097=CIRCLE ( 'NONE', #199543, 11.64999999999999325 ) ;
#12104=FACE_BOUND ( 'NONE', #141237, .T. ) ;
#12108=LINE ( 'NONE', #250681, #99234 ) ;
#12115=AXIS2_PLACEMENT_3D ( 'NONE', #203398, #204657, #168161 ) ;
#12128=ORIENTED_EDGE ( 'NONE', *, *, #219778, .T. ) ;
#12144=VECTOR ( 'NONE', #205078, 1000.000000000000000 ) ;
#12155=DIRECTION ( 'NONE',  ( 0.000000000000000000, -0.9999631594459053030, -0.008583690987162452199 ) ) ;
#12180=CARTESIAN_POINT ( 'NONE',  ( -18.59999999999999787, 77.83585931145570669, -125.0186683157258045 ) ) ;
#12199=CIRCLE ( 'NONE', #157960, 0.09999999999998898659 ) ;
#12213=CARTESIAN_POINT ( 'NONE',  ( -18.33682934331526226, 85.51118559110554429, -129.6174527158510728 ) ) ;
#12227=EDGE_CURVE ( 'NONE', #140520, #228310, #64745, .T. ) ;
#12235=CIRCLE ( 'NONE', #212128, 12.87499999999999822 ) ;
#12244=DIRECTION ( 'NONE',  ( -2.812466655313719426E-14, -0.1350103645451835865, -0.9908441862701605762 ) ) ;
#12256=DIRECTION ( 'NONE',  ( 0.000000000000000000, 0.000000000000000000, -1.000000000000000000 ) ) ;
#12284=ORIENTED_EDGE ( 'NONE', *, *, #222592, .F. ) ;
#12302=EDGE_LOOP ( 'NONE', ( #167125, #159282, #1504, #216157 ) ) ;
#12329=EDGE_CURVE ( 'NONE', #161528, #15766, #155751, .T. ) ;
#12347=AXIS2_PLACEMENT_3D ( 'NONE', #381, #98174, #121650 ) ;
#12368=CARTESIAN_POINT ( 'NONE',  ( 18.59999999999999076, 69.45000000001222418, -148.8731074845244109 ) ) ;
#12371=CARTESIAN_POINT ( 'NONE',  ( -21.09096482362057046, 75.96055172123814714, -176.3866518499285121 ) ) ;
#12403=EDGE_CURVE ( 'NONE', #77802, #223637, #80691, .T. ) ;
#12422=APPLICATION_CONTEXT ( 'automotive_design' ) ;
#12426=DIRECTION ( 'NONE',  ( 0.000000000000000000, 0.9915357197604862671, -0.1298341882519953583 ) ) ;
#12474=DIRECTION ( 'NONE',  ( -1.000000000000000000, 0.000000000000000000, -0.000000000000000000 ) ) ;
#12477=EDGE_CURVE ( 'NONE', #204085, #74763, #97610, .T. ) ;
#12504=AXIS2_PLACEMENT_3D ( 'NONE', #88035, #149351, #30691 ) ;
#12534=ORIENTED_EDGE ( 'NONE', *, *, #126671, .T. ) ;
#12544=ORIENTED_EDGE ( 'NONE', *, *, #89907, .T. ) ;
#12553=FACE_OUTER_BOUND ( 'NONE', #114936, .T. ) ;
#12574=CARTESIAN_POINT ( 'NONE',  ( -20.94999999999999929, 74.25000000001229239, -158.3535959266227451 ) ) ;
#12576=ORIENTED_EDGE ( 'NONE', *, *, #210341, .F. ) ;
#12590=DIRECTION ( 'NONE',  ( 0.000000000000000000, 1.000000000000000000, 6.352154140967427193E-15 ) ) ;
#12591=TOROIDAL_SURFACE ( 'NONE', #166735, 0.4000000000000012990, 0.1000000000000000056 ) ;
#12611=DIRECTION ( 'NONE',  ( 0.000000000000000000, -2.775557561562888827E-14, 1.000000000000000000 ) ) ;
#12619=DIRECTION ( 'NONE',  ( 0.000000000000000000, 6.982962677686266711E-15, -1.000000000000000000 ) ) ;
#12623=CARTESIAN_POINT ( 'NONE',  ( -22.50000000000000000, 64.35042919246758686, -170.1231074845244393 ) ) ;
#12627=ORIENTED_EDGE ( 'NONE', *, *, #175654, .F. ) ;
#12637=CARTESIAN_POINT ( 'NONE',  ( 18.49999999999999645, 74.16465844978787914, -158.4679561919613775 ) ) ;
#12649=CARTESIAN_POINT ( 'NONE',  ( 18.39999999999999858, 85.51932773110476660, -163.0501311079649440 ) ) ;
#12656=EDGE_CURVE ( 'NONE', #8831, #199802, #14281, .T. ) ;
#12675=DIRECTION ( 'NONE',  ( -0.000000000000000000, -6.982962677686266711E-15, 1.000000000000000000 ) ) ;
#12680=AXIS2_PLACEMENT_3D ( 'NONE', #47321, #126888, #65616 ) ;
#12685=ORIENTED_EDGE ( 'NONE', *, *, #217316, .F. ) ;
#12686=EDGE_LOOP ( 'NONE', ( #188067, #235958, #244957 ) ) ;
#12716=DIRECTION ( 'NONE',  ( -1.836970198721029934E-16, -1.000000000000000000, -6.982962677686266711E-15 ) ) ;
#12735=ADVANCED_FACE ( 'NONE', ( #233807 ), #210389, .F. ) ;
#12740=VERTEX_POINT ( 'NONE', #172590 ) ;
#12759=ORIENTED_EDGE ( 'NONE', *, *, #102553, .F. ) ;
#12769=EDGE_LOOP ( 'NONE', ( #85709, #157379, #210149 ) ) ;
#12832=DIRECTION ( 'NONE',  ( 0.000000000000000000, -6.982962677686266711E-15, 1.000000000000000000 ) ) ;
#12842=VECTOR ( 'NONE', #79195, 1000.000000000000000 ) ;
#12843=ORIENTED_EDGE ( 'NONE', *, *, #26272, .T. ) ;
#12862=AXIS2_PLACEMENT_3D ( 'NONE', #107988, #68878, #150967 ) ;
#12869=EDGE_CURVE ( 'NONE', #81561, #82525, #192952, .T. ) ;
#12872=EDGE_CURVE ( 'NONE', #79646, #183531, #96814, .T. ) ;
#12878=FACE_OUTER_BOUND ( 'NONE', #157671, .T. ) ;
#12880=FACE_OUTER_BOUND ( 'NONE', #98271, .T. ) ;
#12903=ORIENTED_EDGE ( 'NONE', *, *, #79470, .T. ) ;
#12941=DIRECTION ( 'NONE',  ( -0.000000000000000000, 1.000000000000000000, 6.982962677686266711E-15 ) ) ;
#12946=ORIENTED_EDGE ( 'NONE', *, *, #198662, .T. ) ;
#12960=VECTOR ( 'NONE', #52169, 1000.000000000000000 ) ;
#12972=EDGE_LOOP ( 'NONE', ( #63437, #213151, #126932, #256855 ) ) ;
#12974=ORIENTED_EDGE ( 'NONE', *, *, #37276, .T. ) ;
#12990=EDGE_CURVE ( 'NONE', #82525, #112448, #17953, .T. ) ;
#12992=ORIENTED_EDGE ( 'NONE', *, *, #31476, .F. ) ;
#12998=ORIENTED_EDGE ( 'NONE', *, *, #59736, .T. ) ;
#13019=DIRECTION ( 'NONE',  ( -1.000000000000000000, -0.000000000000000000, -0.000000000000000000 ) ) ;
#13056=AXIS2_PLACEMENT_3D ( 'NONE', #106764, #186326, #87193 ) ;
#13081=ORIENTED_EDGE ( 'NONE', *, *, #157752, .T. ) ;
#13084=DIRECTION ( 'NONE',  ( 0.000000000000000000, -6.853228547068871147E-15, 1.000000000000000000 ) ) ;
#13088=LINE ( 'NONE', #15668, #128748 ) ;
#13125=CARTESIAN_POINT ( 'NONE',  ( -22.59999999999999787, 75.90000000001245439, -181.6726782920691505 ) ) ;
#13129=CIRCLE ( 'NONE', #33831, 0.1000000000000033362 ) ;
#13134=DIRECTION ( 'NONE',  ( 0.000000000000000000, -6.938893903907222067E-15, 1.000000000000000000 ) ) ;
#13172=AXIS2_PLACEMENT_3D ( 'NONE', #20296, #59364, #18984 ) ;
#13173=DIRECTION ( 'NONE',  ( 1.000000000000000000, 0.000000000000000000, 0.000000000000000000 ) ) ;
#13191=FACE_OUTER_BOUND ( 'NONE', #141931, .T. ) ;
#13212=DIRECTION ( 'NONE',  ( 0.000000000000000000, 0.000000000000000000, -1.000000000000000000 ) ) ;
#13261=ORIENTED_EDGE ( 'NONE', *, *, #104862, .T. ) ;
#13294=ADVANCED_FACE ( 'NONE', ( #29546 ), #11238, .T. ) ;
#13310=ORIENTED_EDGE ( 'NONE', *, *, #181262, .T. ) ;
#13319=CARTESIAN_POINT ( 'NONE',  ( 18.59999994388910238, 85.36356618708374810, -162.8419902477237144 ) ) ;
#13344=CARTESIAN_POINT ( 'NONE',  ( 21.05000000000000071, 74.63912941282028157, -161.9501095574334215 ) ) ;
#13349=( NAMED_UNIT ( * ) SI_UNIT ( $, .STERADIAN. ) SOLID_ANGLE_UNIT ( ) );
#13431=LINE ( 'NONE', #172548, #31876 ) ;
#13433=DIRECTION ( 'NONE',  ( 1.000000000000000000, 0.000000000000000000, 0.000000000000000000 ) ) ;
#13451=ORIENTED_EDGE ( 'NONE', *, *, #181874, .T. ) ;
#13480=B_SPLINE_CURVE_WITH_KNOTS ( 'NONE', 3,
 ( #130562, #14507, #92715, #93999, #91454, #113576 ),
 .UNSPECIFIED., .F., .F.,
 ( 4, 2, 4 ),
 ( 0.000000000000000000, 0.0001568709654583423218, 0.0003137419309166846436 ),
 .UNSPECIFIED. ) ;
#13484=CARTESIAN_POINT ( 'NONE',  ( -18.58744394320938298, 85.56638515456030802, -129.7002594306477761 ) ) ;
#13512=EDGE_LOOP ( 'NONE', ( #242495, #24555, #80316, #144767 ) ) ;
#13531=CARTESIAN_POINT ( 'NONE',  ( 18.49999999999999645, 77.83534155023670564, -158.4679561919613491 ) ) ;
#13545=CARTESIAN_POINT ( 'NONE',  ( -18.50000000000000000, 64.35000000001234355, -163.0083017138704236 ) ) ;
#13575=EDGE_LOOP ( 'NONE', ( #152146, #84790, #56330, #38003 ) ) ;
#13595=ORIENTED_EDGE ( 'NONE', *, *, #242690, .T. ) ;
#13605=CIRCLE ( 'NONE', #92701, 0.09999999999998898659 ) ;
#13624=LINE ( 'NONE', #235231, #136719 ) ;
#13631=AXIS2_PLACEMENT_3D ( 'NONE', #120575, #98369, #162267 ) ;
#13634=CARTESIAN_POINT ( 'NONE',  ( -21.07928932188134041, 75.90110485435803866, -176.3516241409176644 ) ) ;
#13649=LINE ( 'NONE', #172769, #104810 ) ;
#13669=CARTESIAN_POINT ( 'NONE',  ( 21.05000000000000071, 70.15000000001235492, -159.8906102602464330 ) ) ;
#13694=DIRECTION ( 'NONE',  ( 0.000000000000000000, -0.1298341882519953860, -0.9915357197604862671 ) ) ;
#13714=CIRCLE ( 'NONE', #88706, 2.000000000000001776 ) ;
#13724=DIRECTION ( 'NONE',  ( 0.000000000000000000, 6.982962677686266711E-15, -1.000000000000000000 ) ) ;
#13726=CARTESIAN_POINT ( 'NONE',  ( -22.48660254037843131, 64.25000000001236344, -170.0731074845244279 ) ) ;
#13773=ORIENTED_EDGE ( 'NONE', *, *, #162189, .F. ) ;
#13783=SURFACE_STYLE_USAGE ( .BOTH. , #208151 ) ;
#13805=CARTESIAN_POINT ( 'NONE',  ( -20.54999999999999716, 74.00000000001223555, -149.7477294072864709 ) ) ;
#13813=ADVANCED_FACE ( 'NONE', ( #234781 ), #236059, .T. ) ;
#13907=DIRECTION ( 'NONE',  ( 0.000000000000000000, -1.000000000000000000, 0.000000000000000000 ) ) ;
#13918=ORIENTED_EDGE ( 'NONE', *, *, #193548, .T. ) ;
#13925=EDGE_LOOP ( 'NONE', ( #12075, #85767, #208517, #83066 ) ) ;
#13930=DIRECTION ( 'NONE',  ( 0.000000000000000000, 0.000000000000000000, -1.000000000000000000 ) ) ;
#13940=DIRECTION ( 'NONE',  ( 0.000000000000000000, 0.000000000000000000, -1.000000000000000000 ) ) ;
#13951=EDGE_CURVE ( 'NONE', #43638, #54225, #251552, .T. ) ;
#14043=ADVANCED_FACE ( 'NONE', ( #3871 ), #45568, .T. ) ;
#14053=FACE_OUTER_BOUND ( 'NONE', #92197, .T. ) ;
#14075=DIRECTION ( 'NONE',  ( -0.000000000000000000, -1.000000000000000000, -6.982962677686266711E-15 ) ) ;
#14086=DIRECTION ( 'NONE',  ( 1.000000000000000000, 0.000000000000000000, 0.000000000000000000 ) ) ;
#14106=EDGE_CURVE ( 'NONE', #73243, #14224, #161510, .T. ) ;
#14141=CARTESIAN_POINT ( 'NONE',  ( -18.50000000000000000, 77.83534155023670564, -158.4679561919613491 ) ) ;
#14151=ORIENTED_EDGE ( 'NONE', *, *, #242061, .F. ) ;
#14171=CARTESIAN_POINT ( 'NONE',  ( -18.59999999999999787, 64.35000000001230092, -157.8731074845244393 ) ) ;
#14180=DIRECTION ( 'NONE',  ( 1.000000000000000000, 0.000000000000000000, 0.000000000000000000 ) ) ;
#14185=EDGE_CURVE ( 'NONE', #109416, #174607, #131120, .T. ) ;
#14224=VERTEX_POINT ( 'NONE', #209780 ) ;
#14249=LINE ( 'NONE', #232008, #237371 ) ;
#14260=DIRECTION ( 'NONE',  ( 0.000000000000000000, -0.01562499999999307672, 0.9998779222360100194 ) ) ;
#14263=CIRCLE ( 'NONE', #189225, 0.09999999999998898659 ) ;
#14277=LINE ( 'NONE', #54648, #184189 ) ;
#14281=CIRCLE ( 'NONE', #43477, 0.09999999999998898659 ) ;
#14288=CARTESIAN_POINT ( 'NONE',  ( -21.04999999999999716, 76.08574093704584129, -176.4369337733373584 ) ) ;
#14299=ORIENTED_EDGE ( 'NONE', *, *, #51999, .F. ) ;
#14343=ADVANCED_FACE ( 'NONE', ( #153712 ), #238312, .F. ) ;
#14405=CARTESIAN_POINT ( 'NONE',  ( 21.05000000000000071, 64.35000000001218723, -143.5379132551784096 ) ) ;
#14432=CARTESIAN_POINT ( 'NONE',  ( -20.64999999999999858, 68.85000000001228670, -157.6731074845243938 ) ) ;
#14434=CARTESIAN_POINT ( 'NONE',  ( -21.08198257630413508, 75.92735667622784490, -176.3597042185394059 ) ) ;
#14444=( BOUNDED_SURFACE ( )  B_SPLINE_SURFACE ( 3, 2, ( 
 ( #166993, #64000, #6586 ),
 ( #84809, #7900, #46981 ),
 ( #164393, #67846, #185235 ),
 ( #104381, #143528, #4020 ),
 ( #83527, #163120, #26172 ),
 ( #146095, #242626, #224352 ) ),
 .UNSPECIFIED., .F., .F., .F. ) 
 B_SPLINE_SURFACE_WITH_KNOTS ( ( 4, 2, 4 ),
 ( 3, 3 ),
 ( 4.712388980384689674, 5.497787143782137953, 6.283185307179586232 ),
 ( 0.000000000000000000, 1.000000000000000000 ),
 .UNSPECIFIED. ) 
 GEOMETRIC_REPRESENTATION_ITEM ( )  RATIONAL_B_SPLINE_SURFACE ( (
 ( 1.000000000000000000, 0.7071067811865475727, 1.000000000000000000),
 ( 1.000000000000000000, 0.7727932973488792490, 1.000000000000000000),
 ( 1.000000000000000000, 0.8282379607653241882, 1.000000000000000000),
 ( 1.000000000000000000, 0.9038128468035547813, 1.000000000000000000),
 ( 1.000000000000000000, 0.9240297172246445534, 1.000000000000000000),
 ( 1.000000000000000000, 0.9238795325112961754, 1.000000000000000000) ) ) 
 REPRESENTATION_ITEM ( '' )  SURFACE ( )  );
#14507=CARTESIAN_POINT ( 'NONE',  ( -22.45305610364635385, 76.10085836911117951, -181.7726746080137445 ) ) ;
#14512=EDGE_CURVE ( 'NONE', #111850, #235746, #109068, .T. ) ;
#14517=CIRCLE ( 'NONE', #185177, 0.09999999999998898659 ) ;
#14531=LINE ( 'NONE', #17091, #34624 ) ;
#14554=VECTOR ( 'NONE', #141441, 1000.000000000000227 ) ;
#14563=CARTESIAN_POINT ( 'NONE',  ( -18.50000000000000000, 77.36242903720540198, -128.6342262366031548 ) ) ;
#14612=VERTEX_POINT ( 'NONE', #33436 ) ;
#14625=DIRECTION ( 'NONE',  ( 0.000000000000000000, -2.775557561563196798E-13, -1.000000000000000000 ) ) ;
#14648=CARTESIAN_POINT ( 'NONE',  ( -23.15000000000000213, 87.48912529308822172, -139.6231074845242688 ) ) ;
#14681=DIRECTION ( 'NONE',  ( 1.000000000000000000, 0.000000000000000000, 0.000000000000000000 ) ) ;
#14687=ADVANCED_FACE ( 'NONE', ( #202416 ), #23816, .T. ) ;
#14706=CYLINDRICAL_SURFACE ( 'NONE', #111746, 0.09999999999999939493 ) ;
#14707=DIRECTION ( 'NONE',  ( 1.000000000000000000, 0.000000000000000000, 0.000000000000000000 ) ) ;
#14734=DIRECTION ( 'NONE',  ( 1.000000000000000000, 0.000000000000000000, 0.000000000000000000 ) ) ;
#14751=CARTESIAN_POINT ( 'NONE',  ( 23.15000000000000213, 84.59626168225530307, -160.5729799673740104 ) ) ;
#14754=EDGE_CURVE ( 'NONE', #132210, #157237, #218772, .T. ) ;
#14788=CARTESIAN_POINT ( 'NONE',  ( -18.50000000000000000, 85.40000000001209912, -129.6410656363516125 ) ) ;
#14871=ORIENTED_EDGE ( 'NONE', *, *, #41436, .F. ) ;
#14946=EDGE_CURVE ( 'NONE', #38206, #244808, #135702, .T. ) ;
#14976=ORIENTED_EDGE ( 'NONE', *, *, #94324, .F. ) ;
#14978=EDGE_CURVE ( 'NONE', #172545, #89486, #63888, .T. ) ;
#14985=TOROIDAL_SURFACE ( 'NONE', #235527, 0.4000000000000012990, 0.1000000000000000056 ) ;
#14996=DIRECTION ( 'NONE',  ( 0.000000000000000000, -1.000000000000000000, -6.982962677686265922E-15 ) ) ;
#15002=LINE ( 'NONE', #95783, #71641 ) ;
#15027=CARTESIAN_POINT ( 'NONE',  ( -22.49533356619869195, 64.34999999370828050, -170.0882300648472949 ) ) ;
#15033=EDGE_CURVE ( 'NONE', #173882, #62202, #26059, .T. ) ;
#15037=DIRECTION ( 'NONE',  ( 0.7071067811865474617, -0.7071067811865474617, -4.937700262164531476E-15 ) ) ;
#15038=VERTEX_POINT ( 'NONE', #165571 ) ;
#15069=ORIENTED_EDGE ( 'NONE', *, *, #197200, .F. ) ;
#15083=CARTESIAN_POINT ( 'NONE',  ( -18.48550754432080012, 85.46339977857178383, -162.9743177321096539 ) ) ;
#15085=DIRECTION ( 'NONE',  ( 0.000000000000000000, 1.000000000000000000, 6.853228547068871147E-15 ) ) ;
#15107=DIRECTION ( 'NONE',  ( -1.000000000000000000, 0.000000000000000000, 0.000000000000000000 ) ) ;
#15115=CARTESIAN_POINT ( 'NONE',  ( -20.94788355080264353, 65.69792220476342948, -131.0335554128461979 ) ) ;
#15119=DIRECTION ( 'NONE',  ( 0.000000000000000000, 6.982962677686267499E-15, -1.000000000000000000 ) ) ;
#15120=LINE ( 'NONE', #112932, #157071 ) ;
#15152=ORIENTED_EDGE ( 'NONE', *, *, #139163, .F. ) ;
#15185=AXIS2_PLACEMENT_3D ( 'NONE', #26269, #244007, #206182 ) ;
#15252=ORIENTED_EDGE ( 'NONE', *, *, #52736, .F. ) ;
#15267=DIRECTION ( 'NONE',  ( 0.000000000000000000, 0.1350103645451807832, 0.9908441862701610203 ) ) ;
#15295=FACE_OUTER_BOUND ( 'NONE', #73383, .T. ) ;
#15303=CIRCLE ( 'NONE', #131807, 0.1000000000000026007 ) ;
#15308=CARTESIAN_POINT ( 'NONE',  ( 21.05000000000000071, 76.00000000001234923, -165.7231074845243484 ) ) ;
#15311=CIRCLE ( 'NONE', #190081, 0.09999999999998898659 ) ;
#15343=CARTESIAN_POINT ( 'NONE',  ( 21.09551895715237180, 65.37856267284352896, -157.7859828186254845 ) ) ;
#15363=CIRCLE ( 'NONE', #161094, 0.4000000000000114575 ) ;
#15366=EDGE_CURVE ( 'NONE', #103678, #65240, #198305, .T. ) ;
#15377=CARTESIAN_POINT ( 'NONE',  ( 20.85000000000000142, 77.83585931145570669, -125.0186683157258045 ) ) ;
#15389=SPHERICAL_SURFACE ( 'NONE', #146355, 0.1000000000000000056 ) ;
#15399=CYLINDRICAL_SURFACE ( 'NONE', #233804, 0.09999999999998898659 ) ;
#15415=ORIENTED_EDGE ( 'NONE', *, *, #191678, .F. ) ;
#15419=ORIENTED_EDGE ( 'NONE', *, *, #248052, .F. ) ;
#15426=ORIENTED_EDGE ( 'NONE', *, *, #255409, .T. ) ;
#15453=DIRECTION ( 'NONE',  ( 0.000000000000000000, -1.000000000000000000, -6.860497997771532351E-15 ) ) ;
#15455=CARTESIAN_POINT ( 'NONE',  ( -22.59999999999999787, 76.00000000001237765, -170.0231074845243597 ) ) ;
#15490=ORIENTED_EDGE ( 'NONE', *, *, #75291, .T. ) ;
#15509=EDGE_CURVE ( 'NONE', #168004, #25144, #140024, .T. ) ;
#15513=CYLINDRICAL_SURFACE ( 'NONE', #157553, 0.09999999999999939493 ) ;
#15522=LINE ( 'NONE', #175873, #172620 ) ;
#15583=CARTESIAN_POINT ( 'NONE',  ( 21.05000000000000071, 76.00000000001216449, -140.6231074845243256 ) ) ;
#15592=VERTEX_POINT ( 'NONE', #226472 ) ;
#15595=CARTESIAN_POINT ( 'NONE',  ( 21.05000000000000071, 76.00000000001240608, -174.3231074845243995 ) ) ;
#15603=AXIS2_PLACEMENT_3D ( 'NONE', #199889, #121639, #22534 ) ;
#15630=AXIS2_PLACEMENT_3D ( 'NONE', #72234, #34403, #172657 ) ;
#15632=ADVANCED_FACE ( 'NONE', ( #256255 ), #98483, .F. ) ;
#15654=CARTESIAN_POINT ( 'NONE',  ( -20.85000000000000142, 77.16412189325330928, -128.6082593989527254 ) ) ;
#15659=CARTESIAN_POINT ( 'NONE',  ( -23.25000000000000000, 65.66751761918692409, -130.9282609406112670 ) ) ;
#15668=CARTESIAN_POINT ( 'NONE',  ( -23.25000000000000000, 64.35000000001245724, -181.7731074845244450 ) ) ;
#15693=DIRECTION ( 'NONE',  ( 0.000000000000000000, 1.000000000000000000, 0.000000000000000000 ) ) ;
#15727=ORIENTED_EDGE ( 'NONE', *, *, #84728, .F. ) ;
#15738=AXIS2_PLACEMENT_3D ( 'NONE', #59417, #734, #119444 ) ;
#15741=CIRCLE ( 'NONE', #44755, 0.09999999999998898659 ) ;
#15766=VERTEX_POINT ( 'NONE', #164930 ) ;
#15767=CARTESIAN_POINT ( 'NONE',  ( -18.59999999999999787, 74.16465844978787914, -158.4679561919613775 ) ) ;
#15780=DIRECTION ( 'NONE',  ( 1.000000000000000000, 0.000000000000000000, 0.000000000000000000 ) ) ;
#15791=AXIS2_PLACEMENT_3D ( 'NONE', #99963, #139085, #179556 ) ;
#15807=ORIENTED_EDGE ( 'NONE', *, *, #86463, .F. ) ;
#15819=DIRECTION ( 'NONE',  ( 1.000000000000000000, 0.000000000000000000, 0.000000000000000000 ) ) ;
#15837=ADVANCED_FACE ( 'NONE', ( #161096 ), #689, .F. ) ;
#15927=AXIS2_PLACEMENT_3D ( 'NONE', #170923, #169633, #249140 ) ;
#15929=AXIS2_PLACEMENT_3D ( 'NONE', #147328, #10402, #22589 ) ;
#15940=VERTEX_POINT ( 'NONE', #90519 ) ;
#16012=AXIS2_PLACEMENT_3D ( 'NONE', #55104, #33061, #171291 ) ;
#16057=CARTESIAN_POINT ( 'NONE',  ( 20.94999999999999929, 71.00000000001230660, -157.6178414656113205 ) ) ;
#16105=VERTEX_POINT ( 'NONE', #177801 ) ;
#16109=ORIENTED_EDGE ( 'NONE', *, *, #104843, .T. ) ;
#16136=DIRECTION ( 'NONE',  ( 0.000000000000000000, -1.077886431674909336E-14, 1.000000000000000000 ) ) ;
#16143=CIRCLE ( 'NONE', #207669, 12.87499999999999822 ) ;
#16147=EDGE_CURVE ( 'NONE', #109794, #170736, #42137, .T. ) ;
#16160=ORIENTED_EDGE ( 'NONE', *, *, #225089, .F. ) ;
#16162=ORIENTED_EDGE ( 'NONE', *, *, #240335, .F. ) ;
#16165=ORIENTED_EDGE ( 'NONE', *, *, #185330, .T. ) ;
#16221=CIRCLE ( 'NONE', #224477, 0.09999999999998898659 ) ;
#16223=DIRECTION ( 'NONE',  ( -1.000000000000000000, 0.000000000000000000, -0.000000000000000000 ) ) ;
#16229=AXIS2_PLACEMENT_3D ( 'NONE', #7575, #165373, #145786 ) ;
#16245=DIRECTION ( 'NONE',  ( 0.000000000000000000, 7.026728003956695223E-15, -1.000000000000000000 ) ) ;
#16274=DIRECTION ( 'NONE',  ( 1.000000000000000000, -0.000000000000000000, 0.000000000000000000 ) ) ;
#16275=DIRECTION ( 'NONE',  ( 1.000000000000000000, -2.952720810173289112E-16, -2.061873921506763405E-30 ) ) ;
#16294=DIRECTION ( 'NONE',  ( 0.000000000000000000, -6.982962677686266711E-15, 1.000000000000000000 ) ) ;
#16329=EDGE_CURVE ( 'NONE', #71080, #4663, #123864, .T. ) ;
#16377=CARTESIAN_POINT ( 'NONE',  ( 21.87500000000000355, 66.25000000001223555, -148.7731074845244450 ) ) ;
#16397=AXIS2_PLACEMENT_3D ( 'NONE', #225329, #205784, #187535 ) ;
#16448=EDGE_CURVE ( 'NONE', #150904, #174607, #78042, .T. ) ;
#16462=ORIENTED_EDGE ( 'NONE', *, *, #48738, .F. ) ;
#16506=DIRECTION ( 'NONE',  ( -1.000000000000000000, -0.000000000000000000, -0.000000000000000000 ) ) ;
#16514=CARTESIAN_POINT ( 'NONE',  ( -22.47120815636973745, 75.97109617810856719, -181.6730394732778393 ) ) ;
#16518=LINE ( 'NONE', #154750, #218259 ) ;
#16523=CARTESIAN_POINT ( 'NONE',  ( 18.50000000000000355, 85.41920976342157701, -162.7753380217652648 ) ) ;
#16531=DIRECTION ( 'NONE',  ( 1.000000000000000000, 0.000000000000000000, 0.000000000000000000 ) ) ;
#16534=ORIENTED_EDGE ( 'NONE', *, *, #106157, .F. ) ;
#16593=DIRECTION ( 'NONE',  ( -1.000000000000000000, 0.000000000000000000, -0.000000000000000000 ) ) ;
#16598=ADVANCED_FACE ( 'NONE', ( #7488 ), #68045, .T. ) ;
#16621=ORIENTED_EDGE ( 'NONE', *, *, #130522, .F. ) ;
#16643=EDGE_CURVE ( 'NONE', #56828, #70573, #24107, .T. ) ;
#16651=CARTESIAN_POINT ( 'NONE',  ( 18.39999999999999858, 85.60000000001210196, -129.9229180933022576 ) ) ;
#16658=EDGE_CURVE ( 'NONE', #60849, #3474, #73920, .T. ) ;
#16661=DIRECTION ( 'NONE',  ( 0.000000000000000000, 6.982962677686266711E-15, -1.000000000000000000 ) ) ;
#16666=ORIENTED_EDGE ( 'NONE', *, *, #236088, .F. ) ;
#16673=EDGE_CURVE ( 'NONE', #16833, #31671, #148290, .T. ) ;
#16674=CARTESIAN_POINT ( 'NONE',  ( -20.54999999999999716, 74.00000000001223555, -149.3477294072864652 ) ) ;
#16708=VERTEX_POINT ( 'NONE', #30943 ) ;
#16744=EDGE_CURVE ( 'NONE', #44088, #235594, #207260, .T. ) ;
#16745=ORIENTED_EDGE ( 'NONE', *, *, #215831, .T. ) ;
#16791=DIRECTION ( 'NONE',  ( -1.000000000000000000, 0.000000000000000000, -0.000000000000000000 ) ) ;
#16813=ORIENTED_EDGE ( 'NONE', *, *, #25728, .F. ) ;
#16833=VERTEX_POINT ( 'NONE', #97255 ) ;
#16851=ORIENTED_EDGE ( 'NONE', *, *, #48242, .T. ) ;
#16878=FACE_OUTER_BOUND ( 'NONE', #257581, .T. ) ;
#16917=VECTOR ( 'NONE', #3087, 1000.000000000000000 ) ;
#16949=AXIS2_PLACEMENT_3D ( 'NONE', #41342, #235651, #139090 ) ;
#16958=EDGE_LOOP ( 'NONE', ( #120618, #150177, #53891, #35754 ) ) ;
#16964=CARTESIAN_POINT ( 'NONE',  ( -21.59780538579341069, 69.15290947006911892, -170.1220861541223996 ) ) ;
#17002=ADVANCED_FACE ( 'NONE', ( #168876 ), #248369, .T. ) ;
#17004=DIRECTION ( 'NONE',  ( 1.000000000000000000, 0.000000000000000000, 0.000000000000000000 ) ) ;
#17008=ORIENTED_EDGE ( 'NONE', *, *, #96738, .T. ) ;
#17013=CARTESIAN_POINT ( 'NONE',  ( -18.50000000000000000, 74.36282728704192380, -158.4409541190523498 ) ) ;
#17017=CARTESIAN_POINT ( 'NONE',  ( -23.15000000000000213, 87.75000000001246292, -181.7731074845242745 ) ) ;
#17022=CARTESIAN_POINT ( 'NONE',  ( -18.46902351632713035, 85.50947011869320136, -163.0366535502669763 ) ) ;
#17024=DIRECTION ( 'NONE',  ( -5.603264701231743991E-32, -7.172728831056617961E-15, 1.000000000000000000 ) ) ;
#17050=CARTESIAN_POINT ( 'NONE',  ( 21.05000000000000071, 87.29603075034744109, -139.5710066441881452 ) ) ;
#17058=ORIENTED_EDGE ( 'NONE', *, *, #91718, .F. ) ;
#17068=DIRECTION ( 'NONE',  ( -7.304098846217948299E-16, -1.000000000000000000, 0.000000000000000000 ) ) ;
#17078=CARTESIAN_POINT ( 'NONE',  ( 18.49999999999996803, 68.92903212821327941, -132.7765432626560766 ) ) ;
#17091=CARTESIAN_POINT ( 'NONE',  ( -23.15000000000000213, 64.25000000001229239, -157.7731074845244450 ) ) ;
#17101=AXIS2_PLACEMENT_3D ( 'NONE', #99965, #140394, #43881 ) ;
#17110=AXIS2_PLACEMENT_3D ( 'NONE', #98023, #55051, #135875 ) ;
#17139=EDGE_CURVE ( 'NONE', #156062, #141640, #165934, .T. ) ;
#17183=CARTESIAN_POINT ( 'NONE',  ( 18.48536876927988715, 85.46352724987978888, -162.9744892194416934 ) ) ;
#17201=AXIS2_PLACEMENT_3D ( 'NONE', #151902, #174051, #16245 ) ;
#17210=EDGE_CURVE ( 'NONE', #33088, #183270, #145121, .T. ) ;
#17238=CARTESIAN_POINT ( 'NONE',  ( 20.94999999999999574, 77.16270174995034381, -161.9231074845243370 ) ) ;
#17242=CARTESIAN_POINT ( 'NONE',  ( -23.25000000000000000, 85.60000000001231513, -160.1291383618718385 ) ) ;
#17246=ORIENTED_EDGE ( 'NONE', *, *, #20975, .T. ) ;
#17276=ORIENTED_EDGE ( 'NONE', *, *, #28442, .T. ) ;
#17292=CIRCLE ( 'NONE', #29796, 0.1000000000000028644 ) ;
#17295=CIRCLE ( 'NONE', #42231, 0.09999999999999938105 ) ;
#17311=ADVANCED_FACE ( 'NONE', ( #130704 ), #108583, .T. ) ;
#17367=AXIS2_PLACEMENT_3D ( 'NONE', #60460, #160882, #196138 ) ;
#17387=ORIENTED_EDGE ( 'NONE', *, *, #37533, .F. ) ;
#17404=DIRECTION ( 'NONE',  ( -0.7071067811865475727, 0.7071067811865475727, 4.937700262164531476E-15 ) ) ;
#17422=TOROIDAL_SURFACE ( 'NONE', #88128, 0.6000000000000017542, 0.1000000000000000056 ) ;
#17439=ORIENTED_EDGE ( 'NONE', *, *, #117959, .T. ) ;
#17464=CARTESIAN_POINT ( 'NONE',  ( 20.85000000000000142, 76.00000000001213607, -136.5231074845243313 ) ) ;
#17486=ORIENTED_EDGE ( 'NONE', *, *, #116193, .T. ) ;
#17492=FACE_OUTER_BOUND ( 'NONE', #201872, .T. ) ;
#17517=ORIENTED_EDGE ( 'NONE', *, *, #187026, .F. ) ;
#17578=CARTESIAN_POINT ( 'NONE',  ( -18.59999999999999787, 68.97833521811203639, -132.6895420826271277 ) ) ;
#17584=FACE_OUTER_BOUND ( 'NONE', #170238, .T. ) ;
#17597=EDGE_LOOP ( 'NONE', ( #192319, #216289, #115148 ) ) ;
#17606=ORIENTED_EDGE ( 'NONE', *, *, #132398, .F. ) ;
#17621=ADVANCED_FACE ( 'NONE', ( #165711 ), #211322, .T. ) ;
#17622=CARTESIAN_POINT ( 'NONE',  ( 18.52928932188133970, 65.72071067813085676, -145.3731074845244109 ) ) ;
#17625=CARTESIAN_POINT ( 'NONE',  ( -18.40000000000000213, 85.51932773110476660, -163.0501311079649724 ) ) ;
#17632=AXIS2_PLACEMENT_3D ( 'NONE', #144244, #244641, #145540 ) ;
#17659=CYLINDRICAL_SURFACE ( 'NONE', #155626, 0.09999999999999939493 ) ;
#17695=CARTESIAN_POINT ( 'NONE',  ( -22.39999999999999858, 76.00000000001246292, -181.6726782920691505 ) ) ;
#17707=DIRECTION ( 'NONE',  ( 1.000000000000000000, 0.000000000000000000, 0.000000000000000000 ) ) ;
#17714=AXIS2_PLACEMENT_3D ( 'NONE', #253510, #189700, #132287 ) ;
#17715=EDGE_LOOP ( 'NONE', ( #16165, #120385 ) ) ;
#17721=CARTESIAN_POINT ( 'NONE',  ( -20.07928932188135107, 66.77928932189357170, -148.7731074845244166 ) ) ;
#17756=CARTESIAN_POINT ( 'NONE',  ( -22.44366136229477249, 75.99065843052638058, -181.6728260419982632 ) ) ;
#17762=CARTESIAN_POINT ( 'NONE',  ( -21.05000000000000071, 77.16270174995034381, -161.9231074845243370 ) ) ;
#17782=ORIENTED_EDGE ( 'NONE', *, *, #235572, .F. ) ;
#17814=VECTOR ( 'NONE', #214028, 1000.000000000000000 ) ;
#17834=ORIENTED_EDGE ( 'NONE', *, *, #140015, .F. ) ;
#17838=DIRECTION ( 'NONE',  ( 1.000000000000000000, 0.000000000000000000, 0.000000000000000000 ) ) ;
#17840=DIRECTION ( 'NONE',  ( -0.000000000000000000, 6.982962677686266711E-15, -1.000000000000000000 ) ) ;
#17852=ORIENTED_EDGE ( 'NONE', *, *, #27927, .T. ) ;
#17855=DIRECTION ( 'NONE',  ( 0.000000000000000000, -1.000000000000000000, -6.352154140967427193E-15 ) ) ;
#17925=CARTESIAN_POINT ( 'NONE',  ( 21.13422380239035192, 69.50667348520698852, -170.0231074845243882 ) ) ;
#17953=CIRCLE ( 'NONE', #163714, 0.09999999999998898659 ) ;
#18037=CARTESIAN_POINT ( 'NONE',  ( 18.40916198585728480, 85.50000000001209344, -129.9229178527008912 ) ) ;
#18051=ORIENTED_EDGE ( 'NONE', *, *, #43120, .F. ) ;
#18054=CARTESIAN_POINT ( 'NONE',  ( 18.59999999999999787, 77.83585931145570669, -125.0186683157258329 ) ) ;
#18113=VERTEX_POINT ( 'NONE', #15308 ) ;
#18119=ORIENTED_EDGE ( 'NONE', *, *, #181748, .F. ) ;
#18123=CARTESIAN_POINT ( 'NONE',  ( 20.94999999999999574, 65.52661458509942349, -162.4444530202758870 ) ) ;
#18135=EDGE_CURVE ( 'NONE', #231343, #112163, #257408, .T. ) ;
#18146=CYLINDRICAL_SURFACE ( 'NONE', #73134, 0.09999999999998898659 ) ;
#18156=AXIS2_PLACEMENT_3D ( 'NONE', #6738, #142394, #160717 ) ;
#18161=EDGE_CURVE ( 'NONE', #54460, #30238, #210921, .T. ) ;
#18201=CIRCLE ( 'NONE', #9994, 11.64999999999999325 ) ;
#18208=TOROIDAL_SURFACE ( 'NONE', #255480, 0.2000000000000000111, 0.1000000000000000056 ) ;
#18235=CARTESIAN_POINT ( 'NONE',  ( -23.15000000000000213, 76.00000000001215028, -138.5231074845243313 ) ) ;
#18249=EDGE_LOOP ( 'NONE', ( #135789, #16745, #59741, #12576 ) ) ;
#18285=CARTESIAN_POINT ( 'NONE',  ( -18.39999999999999858, 85.51932773110476660, -163.0501311079649440 ) ) ;
#18295=DIRECTION ( 'NONE',  ( -1.000000000000000000, -3.469446951953635015E-14, -2.422701857770461054E-28 ) ) ;
#18313=ORIENTED_EDGE ( 'NONE', *, *, #244569, .F. ) ;
#18378=TOROIDAL_SURFACE ( 'NONE', #122450, 11.70000000000000107, 0.1000000000000000056 ) ;
#18391=VERTEX_POINT ( 'NONE', #184623 ) ;
#18403=EDGE_CURVE ( 'NONE', #219200, #164553, #219861, .T. ) ;
#18470=VERTEX_POINT ( 'NONE', #214446 ) ;
#18485=AXIS2_PLACEMENT_3D ( 'NONE', #155917, #59319, #235412 ) ;
#18507=CYLINDRICAL_SURFACE ( 'NONE', #245893, 0.09999999999998898659 ) ;
#18587=DIRECTION ( 'NONE',  ( 0.000000000000000000, 6.982962677686266711E-15, -1.000000000000000000 ) ) ;
#18595=EDGE_CURVE ( 'NONE', #200730, #147041, #219579, .T. ) ;
#18659=DIRECTION ( 'NONE',  ( -1.000000000000000000, 0.000000000000000000, 0.000000000000000000 ) ) ;
#18663=VECTOR ( 'NONE', #55776, 1000.000000000000000 ) ;
#18707=ORIENTED_EDGE ( 'NONE', *, *, #174259, .T. ) ;
#18804=ORIENTED_EDGE ( 'NONE', *, *, #88965, .T. ) ;
#18807=DIRECTION ( 'NONE',  ( 0.000000000000000000, -0.1350103645451807555, -0.9908441862701610203 ) ) ;
#18809=VERTEX_POINT ( 'NONE', #235961 ) ;
#18841=EDGE_CURVE ( 'NONE', #201875, #49319, #141148, .T. ) ;
#18855=DIRECTION ( 'NONE',  ( 0.000000000000000000, -7.026728003956695223E-15, 1.000000000000000000 ) ) ;
#18870=CARTESIAN_POINT ( 'NONE',  ( 22.49231231312462853, 64.35001509633508476, -170.0841603721258082 ) ) ;
#18876=CARTESIAN_POINT ( 'NONE',  ( 21.13435531349836438, 76.00000000001242029, -176.5168285481167914 ) ) ;
#18899=DIRECTION ( 'NONE',  ( 1.000000000000000000, 0.000000000000000000, 0.000000000000000000 ) ) ;
#18919=CARTESIAN_POINT ( 'NONE',  ( -18.54159361262948735, 85.46313213550538990, -162.9739852682313597 ) ) ;
#18963=DIRECTION ( 'NONE',  ( 0.000000000000000000, 0.1298341882519953583, 0.9915357197604861561 ) ) ;
#18984=DIRECTION ( 'NONE',  ( 0.000000000000000000, 0.000000000000000000, -1.000000000000000000 ) ) ;
#18992=ORIENTED_EDGE ( 'NONE', *, *, #208866, .F. ) ;
#18994=TOROIDAL_SURFACE ( 'NONE', #27427, 7.791421356237335338, 0.1000000000000000056 ) ;
#19030=CARTESIAN_POINT ( 'NONE',  ( -20.64999999999999858, 68.75000000001230660, -157.7731074845244166 ) ) ;
#19049=EDGE_CURVE ( 'NONE', #117472, #119183, #228636, .T. ) ;
#19064=DIRECTION ( 'NONE',  ( 0.000000000000000000, -7.429790795770644761E-15, 1.000000000000000000 ) ) ;
#19072=CARTESIAN_POINT ( 'NONE',  ( 20.04142135623730070, 64.25000000001222134, -148.6731074845244507 ) ) ;
#19075=ORIENTED_EDGE ( 'NONE', *, *, #234321, .F. ) ;
#19085=EDGE_LOOP ( 'NONE', ( #249951, #100389, #1733, #256198 ) ) ;
#19096=CARTESIAN_POINT ( 'NONE',  ( -20.94999999999999929, 76.00000000001234923, -167.1231074845243825 ) ) ;
#19114=B_SPLINE_CURVE_WITH_KNOTS ( 'NONE', 3,
 ( #103937, #183505, #25714, #105201 ),
 .UNSPECIFIED., .F., .F.,
 ( 4, 4 ),
 ( 3.469446951953614189E-18, 0.0001058379652594852396 ),
 .UNSPECIFIED. ) ;
#19143=FACE_OUTER_BOUND ( 'NONE', #189079, .T. ) ;
#19148=CYLINDRICAL_SURFACE ( 'NONE', #189509, 0.09999999999998898659 ) ;
#19152=EDGE_CURVE ( 'NONE', #203324, #167384, #28761, .T. ) ;
#19175=VECTOR ( 'NONE', #150497, 1000.000000000000000 ) ;
#19208=CIRCLE ( 'NONE', #10841, 0.09999999999998898659 ) ;
#19214=VECTOR ( 'NONE', #181993, 1000.000000000000114 ) ;
#19240=EDGE_CURVE ( 'NONE', #91227, #125758, #83487, .T. ) ;
#19264=CIRCLE ( 'NONE', #115136, 0.09999999999999971412 ) ;
#19268=CARTESIAN_POINT ( 'NONE',  ( -18.50000000000000000, 77.16270174995034381, -161.9231074845243370 ) ) ;
#19284=CIRCLE ( 'NONE', #131897, 0.09999999999998898659 ) ;
#19293=CIRCLE ( 'NONE', #6819, 0.09999999999999939493 ) ;
#19297=AXIS2_PLACEMENT_3D ( 'NONE', #93526, #33610, #251309 ) ;
#19298=DIRECTION ( 'NONE',  ( 2.879366945564059217E-14, 0.9875055080513762684, -0.1575844902526679081 ) ) ;
#19300=DIRECTION ( 'NONE',  ( -1.000000000000000000, 1.836970198721029934E-16, 1.282749433769087757E-30 ) ) ;
#19316=EDGE_LOOP ( 'NONE', ( #51722, #39906, #82491, #87754, #243208 ) ) ;
#19351=AXIS2_PLACEMENT_3D ( 'NONE', #256096, #77497, #120536 ) ;
#19380=VECTOR ( 'NONE', #184041, 1000.000000000000000 ) ;
#19386=EDGE_LOOP ( 'NONE', ( #42840, #176497, #154445, #23566 ) ) ;
#19387=ORIENTED_EDGE ( 'NONE', *, *, #237473, .T. ) ;
#19403=VECTOR ( 'NONE', #112434, 1000.000000000000000 ) ;
#19430=DIRECTION ( 'NONE',  ( 0.000000000000000000, 0.8700118002898393765, -0.4930308989875104575 ) ) ;
#19448=CIRCLE ( 'NONE', #56807, 0.5000000000000004441 ) ;
#19482=CIRCLE ( 'NONE', #214705, 12.87499999999999822 ) ;
#19488=DIRECTION ( 'NONE',  ( -1.000000000000000000, -0.000000000000000000, -0.000000000000000000 ) ) ;
#19533=CARTESIAN_POINT ( 'NONE',  ( 23.24999999999999289, 64.35000000001222986, -148.6731074845244507 ) ) ;
#19537=DIRECTION ( 'NONE',  ( 1.000000000000000000, 0.000000000000000000, 0.000000000000000000 ) ) ;
#19543=PLANE ( 'NONE',  #68204 ) ;
#19544=TOROIDAL_SURFACE ( 'NONE', #194527, 12.97499999999999609, 0.1000000000000000056 ) ;
#19554=DIRECTION ( 'NONE',  ( -2.602085213965226419E-14, 6.982962677686266711E-15, -1.000000000000000000 ) ) ;
#19566=AXIS2_PLACEMENT_3D ( 'NONE', #154850, #233104, #55679 ) ;
#19582=EDGE_CURVE ( 'NONE', #246816, #247434, #93262, .T. ) ;
#19592=CARTESIAN_POINT ( 'NONE',  ( 18.50000324121758055, 65.70692517833235513, -131.0644653378304554 ) ) ;
#19603=AXIS2_PLACEMENT_3D ( 'NONE', #138718, #16275, #179204 ) ;
#19606=ORIENTED_EDGE ( 'NONE', *, *, #40637, .F. ) ;
#19644=FACE_OUTER_BOUND ( 'NONE', #165559, .T. ) ;
#19681=ORIENTED_EDGE ( 'NONE', *, *, #245943, .T. ) ;
#19689=ORIENTED_EDGE ( 'NONE', *, *, #18841, .F. ) ;
#19713=EDGE_CURVE ( 'NONE', #90604, #15766, #86513, .T. ) ;
#19736=VECTOR ( 'NONE', #211691, 1000.000000000000000 ) ;
#19751=VECTOR ( 'NONE', #162532, 1000.000000000000000 ) ;
#19756=DIRECTION ( 'NONE',  ( -0.000000000000000000, 0.4791956752371485107, 0.8777080977375185666 ) ) ;
#19766=ADVANCED_FACE ( 'NONE', ( #107385 ), #67131, .T. ) ;
#19769=CIRCLE ( 'NONE', #28148, 0.5000000000000004441 ) ;
#19786=EDGE_LOOP ( 'NONE', ( #89582, #249358, #173286, #204235 ) ) ;
#19794=FACE_OUTER_BOUND ( 'NONE', #70630, .T. ) ;
#19806=LINE ( 'NONE', #240129, #212263 ) ;
#19843=AXIS2_PLACEMENT_3D ( 'NONE', #234102, #195009, #134986 ) ;
#19859=CARTESIAN_POINT ( 'NONE',  ( 21.05000000000000071, 70.15000000001235492, -159.8906102602464330 ) ) ;
#19879=LINE ( 'NONE', #42013, #162310 ) ;
#19881=FACE_OUTER_BOUND ( 'NONE', #226182, .T. ) ;
#19886=VERTEX_POINT ( 'NONE', #252039 ) ;
#19901=DIRECTION ( 'NONE',  ( 0.000000000000000000, 6.577889128801576950E-15, -1.000000000000000000 ) ) ;
#19920=ORIENTED_EDGE ( 'NONE', *, *, #38761, .F. ) ;
#19949=CIRCLE ( 'NONE', #182448, 0.09999999999998898659 ) ;
#19970=AXIS2_PLACEMENT_3D ( 'NONE', #244857, #226566, #46645 ) ;
#20031=DIRECTION ( 'NONE',  ( 0.000000000000000000, 6.982962677686266711E-15, -1.000000000000000000 ) ) ;
#20032=ORIENTED_EDGE ( 'NONE', *, *, #56060, .T. ) ;
#20046=AXIS2_PLACEMENT_3D ( 'NONE', #33537, #113026, #54319 ) ;
#20050=DIRECTION ( 'NONE',  ( -1.000000000000000000, -0.000000000000000000, -0.000000000000000000 ) ) ;
#20054=CARTESIAN_POINT ( 'NONE',  ( 21.05000000000000071, 65.27628318601605883, -162.4287082486403051 ) ) ;
#20064=EDGE_CURVE ( 'NONE', #38206, #99016, #173943, .T. ) ;
#20091=ADVANCED_FACE ( 'NONE', ( #238906 ), #254580, .T. ) ;
#20114=EDGE_CURVE ( 'NONE', #111529, #143593, #48985, .T. ) ;
#20128=DIRECTION ( 'NONE',  ( 1.000000000000000000, 0.000000000000000000, 0.000000000000000000 ) ) ;
#20139=PLANE ( 'NONE',  #139584 ) ;
#20156=CARTESIAN_POINT ( 'NONE',  ( 20.85000000000000142, 77.83585931145570669, -125.0186683157258329 ) ) ;
#20187=CIRCLE ( 'NONE', #15929, 6.329289321881370611 ) ;
#20201=DIRECTION ( 'NONE',  ( 1.000000000000000000, 0.000000000000000000, 0.000000000000000000 ) ) ;
#20223=CARTESIAN_POINT ( 'NONE',  ( -18.49999999999999289, 85.32100840337362513, -162.7871692354464699 ) ) ;
#20227=VERTEX_POINT ( 'NONE', #104491 ) ;
#20273=AXIS2_PLACEMENT_3D ( 'NONE', #127500, #204452, #46656 ) ;
#20296=CARTESIAN_POINT ( 'NONE',  ( -23.15000000000000213, 87.48912529308822172, -139.6231074845242688 ) ) ;
#20320=ADVANCED_FACE ( 'NONE', ( #225277 ), #123649, .F. ) ;
#20339=ORIENTED_EDGE ( 'NONE', *, *, #52655, .F. ) ;
#20361=CARTESIAN_POINT ( 'NONE',  ( 20.94999999999999929, 87.48912529308822172, -139.4231074845242802 ) ) ;
#20377=DIRECTION ( 'NONE',  ( 1.000000000000000000, 0.000000000000000000, 0.000000000000000000 ) ) ;
#20390=ORIENTED_EDGE ( 'NONE', *, *, #75114, .F. ) ;
#20432=DIRECTION ( 'NONE',  ( 1.000000000000000000, 0.000000000000000000, 0.000000000000000000 ) ) ;
#20435=CIRCLE ( 'NONE', #174410, 7.800000000000001599 ) ;
#20436=ORIENTED_EDGE ( 'NONE', *, *, #205266, .F. ) ;
#20499=EDGE_CURVE ( 'NONE', #227362, #117472, #50488, .T. ) ;
#20505=CARTESIAN_POINT ( 'NONE',  ( -21.05000000000000071, 74.73821383144729680, -161.9366085209788935 ) ) ;
#20506=AXIS2_PLACEMENT_3D ( 'NONE', #4952, #81915, #64949 ) ;
#20525=CARTESIAN_POINT ( 'NONE',  ( -23.15000000000000213, 64.35000000001222986, -148.6731074845244507 ) ) ;
#20554=DIRECTION ( 'NONE',  ( -0.000000000000000000, -6.982962677686266711E-15, 1.000000000000000000 ) ) ;
#20561=VERTEX_POINT ( 'NONE', #96889 ) ;
#20562=TOROIDAL_SURFACE ( 'NONE', #149562, 0.2000000000000000111, 0.1000000000000000056 ) ;
#20586=FACE_OUTER_BOUND ( 'NONE', #33348, .T. ) ;
#20587=FACE_OUTER_BOUND ( 'NONE', #150803, .T. ) ;
#20601=ORIENTED_EDGE ( 'NONE', *, *, #155138, .T. ) ;
#20609=CARTESIAN_POINT ( 'NONE',  ( -20.94999999999999929, 68.97833521811203639, -132.6895420826271277 ) ) ;
#20622=ORIENTED_EDGE ( 'NONE', *, *, #94417, .F. ) ;
#20623=AXIS2_PLACEMENT_3D ( 'NONE', #65314, #41931, #238826 ) ;
#20629=CARTESIAN_POINT ( 'NONE',  ( 18.48197441911518624, 85.51795479471604722, -129.6328958423155768 ) ) ;
#20633=ORIENTED_EDGE ( 'NONE', *, *, #186865, .F. ) ;
#20644=ORIENTED_EDGE ( 'NONE', *, *, #24521, .F. ) ;
#20657=CARTESIAN_POINT ( 'NONE',  ( -18.59999999999999787, 77.16412189325330928, -128.7082593989527197 ) ) ;
#20664=ORIENTED_EDGE ( 'NONE', *, *, #160129, .F. ) ;
#20706=ORIENTED_EDGE ( 'NONE', *, *, #127167, .T. ) ;
#20714=LINE ( 'NONE', #160235, #209289 ) ;
#20745=TOROIDAL_SURFACE ( 'NONE', #220812, 0.4000000000000010214, 0.1000000000000000056 ) ;
#20755=CARTESIAN_POINT ( 'NONE',  ( -21.05000000000000071, 70.15000000001235492, -159.8906102602464330 ) ) ;
#20768=FACE_OUTER_BOUND ( 'NONE', #201104, .T. ) ;
#20788=VECTOR ( 'NONE', #5746, 1000.000000000000000 ) ;
#20803=AXIS2_PLACEMENT_3D ( 'NONE', #4720, #144230, #226328 ) ;
#20819=FACE_OUTER_BOUND ( 'NONE', #222852, .T. ) ;
#20820=CARTESIAN_POINT ( 'NONE',  ( -21.07928932188134041, 69.67148334361908724, -170.1220026301787982 ) ) ;
#20823=ADVANCED_FACE ( 'NONE', ( #37638 ), #15513, .T. ) ;
#20835=EDGE_CURVE ( 'NONE', #5474, #198025, #103975, .T. ) ;
#20856=CIRCLE ( 'NONE', #141619, 0.2000000000000057288 ) ;
#20865=CARTESIAN_POINT ( 'NONE',  ( 22.39999999999999858, 68.20922040163900135, -170.1231074845244109 ) ) ;
#20876=ORIENTED_EDGE ( 'NONE', *, *, #249074, .F. ) ;
#20881=AXIS2_PLACEMENT_3D ( 'NONE', #9212, #167041, #88725 ) ;
#20897=ORIENTED_EDGE ( 'NONE', *, *, #188315, .F. ) ;
#20902=ORIENTED_EDGE ( 'NONE', *, *, #167567, .T. ) ;
#20908=PLANE ( 'NONE',  #201567 ) ;
#20909=PLANE ( 'NONE',  #6546 ) ;
#20914=AXIS2_PLACEMENT_3D ( 'NONE', #139591, #161774, #240010 ) ;
#20938=PLANE ( 'NONE',  #228886 ) ;
#20975=EDGE_CURVE ( 'NONE', #231838, #113005, #127422, .T. ) ;
#20980=EDGE_CURVE ( 'NONE', #231838, #55547, #107603, .T. ) ;
#20982=DIRECTION ( 'NONE',  ( 0.000000000000000000, -6.982962677686266711E-15, 1.000000000000000000 ) ) ;
#21014=LINE ( 'NONE', #164359, #168731 ) ;
#21017=ORIENTED_EDGE ( 'NONE', *, *, #65889, .T. ) ;
#21039=EDGE_LOOP ( 'NONE', ( #71163, #45714, #213503, #239641 ) ) ;
#21058=PLANE ( 'NONE',  #178021 ) ;
#21064=TOROIDAL_SURFACE ( 'NONE', #54329, 0.2000000000000000111, 0.1000000000000000056 ) ;
#21132=EDGE_CURVE ( 'NONE', #221268, #231632, #78571, .T. ) ;
#21140=LINE ( 'NONE', #44538, #237641 ) ;
#21228=EDGE_LOOP ( 'NONE', ( #112489, #127366, #73414, #154019, #85088, #212505 ) ) ;
#21267=EDGE_CURVE ( 'NONE', #137060, #231838, #224907, .T. ) ;
#21303=CARTESIAN_POINT ( 'NONE',  ( -20.54999999999999716, 76.00000000001227818, -157.0481074845243938 ) ) ;
#21348=DIRECTION ( 'NONE',  ( -0.000000000000000000, -1.000000000000000000, -6.982962677686266711E-15 ) ) ;
#21350=CARTESIAN_POINT ( 'NONE',  ( 20.95512820512820085, 65.37615131630043663, -162.3581939154368285 ) ) ;
#21389=DIRECTION ( 'NONE',  ( 1.000000000000000000, 0.000000000000000000, 0.000000000000000000 ) ) ;
#21398=EDGE_CURVE ( 'NONE', #194806, #44364, #148945, .T. ) ;
#21492=CARTESIAN_POINT ( 'NONE',  ( -20.00857864376270001, 66.75000000001230660, -157.6731074845244223 ) ) ;
#21507=DIRECTION ( 'NONE',  ( 1.000000000000000000, 0.000000000000000000, 0.000000000000000000 ) ) ;
#21520=CARTESIAN_POINT ( 'NONE',  ( 18.50000000000000000, 86.35479209693758662, -142.7665665014505407 ) ) ;
#21554=DIRECTION ( 'NONE',  ( 0.000000000000000000, -6.982962677686266711E-15, 1.000000000000000000 ) ) ;
#21599=DIRECTION ( 'NONE',  ( 1.000000000000000000, 0.000000000000000000, 0.000000000000000000 ) ) ;
#21621=ORIENTED_EDGE ( 'NONE', *, *, #210676, .F. ) ;
#21658=TOROIDAL_SURFACE ( 'NONE', #200729, 12.97499999999999609, 0.1000000000000000056 ) ;
#21659=CARTESIAN_POINT ( 'NONE',  ( 20.92356734117541706, 65.68026841930924320, -130.9725740131889893 ) ) ;
#21676=FACE_OUTER_BOUND ( 'NONE', #150336, .T. ) ;
#21691=DIRECTION ( 'NONE',  ( 0.000000000000000000, -0.9908441862701610203, 0.1350103645451807555 ) ) ;
#21692=EDGE_LOOP ( 'NONE', ( #239750, #214022, #143484, #20644, #2226 ) ) ;
#21702=CARTESIAN_POINT ( 'NONE',  ( -21.00023020733502577, 76.00000000001243450, -176.4139767297927222 ) ) ;
#21722=ORIENTED_EDGE ( 'NONE', *, *, #52655, .T. ) ;
#21740=ORIENTED_EDGE ( 'NONE', *, *, #204991, .F. ) ;
#21743=EDGE_CURVE ( 'NONE', #5518, #56976, #252045, .T. ) ;
#21750=EDGE_CURVE ( 'NONE', #91227, #197213, #186542, .T. ) ;
#21795=AXIS2_PLACEMENT_3D ( 'NONE', #32647, #152585, #153890 ) ;
#21805=DIRECTION ( 'NONE',  ( -1.000000000000000000, 0.000000000000000000, -0.000000000000000000 ) ) ;
#21817=DIRECTION ( 'NONE',  ( 1.000000000000000000, 0.000000000000000000, 0.000000000000000000 ) ) ;
#21851=ORIENTED_EDGE ( 'NONE', *, *, #250783, .F. ) ;
#21897=CARTESIAN_POINT ( 'NONE',  ( 18.58725287972267637, 85.56662691070442861, -129.7006026787596511 ) ) ;
#21932=VERTEX_POINT ( 'NONE', #62685 ) ;
#21946=ORIENTED_EDGE ( 'NONE', *, *, #54722, .F. ) ;
#21950=CARTESIAN_POINT ( 'NONE',  ( -20.54999999999999716, 71.75000000001229239, -157.7731074845243882 ) ) ;
#21953=EDGE_CURVE ( 'NONE', #31671, #75757, #111363, .T. ) ;
#21956=AXIS2_PLACEMENT_3D ( 'NONE', #91104, #49414, #151086 ) ;
#21959=AXIS2_PLACEMENT_3D ( 'NONE', #167679, #82943, #67266 ) ;
#21966=ORIENTED_EDGE ( 'NONE', *, *, #156704, .F. ) ;
#21991=DIRECTION ( 'NONE',  ( 0.000000000000000000, -0.4999999999999088507, 0.8660254037844913322 ) ) ;
#21995=ORIENTED_EDGE ( 'NONE', *, *, #165108, .F. ) ;
#22084=DIRECTION ( 'NONE',  ( 0.000000000000000000, -6.982962677686266711E-15, 1.000000000000000000 ) ) ;
#22114=AXIS2_PLACEMENT_3D ( 'NONE', #179369, #81495, #59359 ) ;
#22166=DIRECTION ( 'NONE',  ( 0.000000000000000000, -0.4999999999999088507, -0.8660254037844913322 ) ) ;
#22189=CARTESIAN_POINT ( 'NONE',  ( -18.50000000000000000, 66.75000000001230660, -157.6731074845244223 ) ) ;
#22249=TOROIDAL_SURFACE ( 'NONE', #155533, 0.2000000000000000111, 0.1000000000000000056 ) ;
#22261=ORIENTED_EDGE ( 'NONE', *, *, #53151, .T. ) ;
#22283=AXIS2_PLACEMENT_3D ( 'NONE', #15377, #36229, #75362 ) ;
#22298=ORIENTED_EDGE ( 'NONE', *, *, #49432, .F. ) ;
#22312=ORIENTED_EDGE ( 'NONE', *, *, #167430, .T. ) ;
#22319=VERTEX_POINT ( 'NONE', #26274 ) ;
#22346=ORIENTED_EDGE ( 'NONE', *, *, #201218, .T. ) ;
#22361=ORIENTED_EDGE ( 'NONE', *, *, #167733, .F. ) ;
#22364=DIRECTION ( 'NONE',  ( -1.000000000000000000, 0.000000000000000000, 0.000000000000000000 ) ) ;
#22372=LINE ( 'NONE', #23668, #148761 ) ;
#22373=CARTESIAN_POINT ( 'NONE',  ( -20.94999999999999929, 74.16465844978787914, -158.4679561919613775 ) ) ;
#22376=CARTESIAN_POINT ( 'NONE',  ( 21.07928932188134397, 69.67148334361908724, -170.1220026301787982 ) ) ;
#22430=EDGE_CURVE ( 'NONE', #208786, #49789, #136816, .T. ) ;
#22431=VECTOR ( 'NONE', #252680, 1000.000000000000114 ) ;
#22452=DIRECTION ( 'NONE',  ( 1.000000000000000000, 0.000000000000000000, 0.000000000000000000 ) ) ;
#22454=LINE ( 'NONE', #101935, #234485 ) ;
#22465=DIRECTION ( 'NONE',  ( 1.000000000000000000, -3.265361837132813093E-16, -2.280189983783949500E-30 ) ) ;
#22483=DIRECTION ( 'NONE',  ( 1.000000000000000000, 0.000000000000000000, 0.000000000000000000 ) ) ;
#22495=DIRECTION ( 'NONE',  ( -0.000000000000000000, 0.1350103645451807555, 0.9908441862701610203 ) ) ;
#22510=EDGE_CURVE ( 'NONE', #206239, #141897, #40426, .T. ) ;
#22526=DIRECTION ( 'NONE',  ( -1.000000000000000000, 2.952720810173289112E-16, 2.061873921506763405E-30 ) ) ;
#22527=DIRECTION ( 'NONE',  ( 1.000000000000000000, 0.000000000000000000, 0.000000000000000000 ) ) ;
#22528=ORIENTED_EDGE ( 'NONE', *, *, #141988, .T. ) ;
#22534=DIRECTION ( 'NONE',  ( -1.000000000000000000, 0.000000000000000000, 0.000000000000000000 ) ) ;
#22541=DIRECTION ( 'NONE',  ( 1.000000000000000000, 0.000000000000000000, 0.000000000000000000 ) ) ;
#22589=DIRECTION ( 'NONE',  ( 0.000000000000000000, 6.577889128801576950E-15, -1.000000000000000000 ) ) ;
#22606=DIRECTION ( 'NONE',  ( 1.000000000000000000, 0.000000000000000000, -0.000000000000000000 ) ) ;
#22622=EDGE_CURVE ( 'NONE', #219341, #257571, #224484, .T. ) ;
#22665=DIRECTION ( 'NONE',  ( 7.304098846218134667E-16, 1.000000000000000000, 6.982962677686266711E-15 ) ) ;
#22667=LINE ( 'NONE', #220832, #52021 ) ;
#22731=DIRECTION ( 'NONE',  ( -1.000000000000000000, 0.000000000000000000, -0.000000000000000000 ) ) ;
#22740=AXIS2_PLACEMENT_3D ( 'NONE', #54611, #216245, #174627 ) ;
#22742=AXIS2_PLACEMENT_3D ( 'NONE', #70626, #150152, #69325 ) ;
#22764=CARTESIAN_POINT ( 'NONE',  ( 21.07954640115206857, 75.93399229287264518, -176.3523951805472905 ) ) ;
#22811=EDGE_LOOP ( 'NONE', ( #164033, #138133, #157167, #223721 ) ) ;
#22831=ADVANCED_FACE ( 'NONE', ( #208470 ), #29840, .F. ) ;
#22849=ORIENTED_EDGE ( 'NONE', *, *, #49668, .T. ) ;
#22868=CARTESIAN_POINT ( 'NONE',  ( 22.00411653889200991, 75.90096189422573048, -177.2765503521646622 ) ) ;
#22877=EDGE_CURVE ( 'NONE', #15592, #168233, #38804, .T. ) ;
#22901=DIRECTION ( 'NONE',  ( 1.000000000000000000, -2.952720810173289112E-16, -2.061873921506763405E-30 ) ) ;
#22920=VERTEX_POINT ( 'NONE', #98723 ) ;
#22950=VERTEX_POINT ( 'NONE', #214858 ) ;
#22994=CARTESIAN_POINT ( 'NONE',  ( 21.13461538461538325, 65.38541703798675542, -157.6731074845244223 ) ) ;
#23064=DIRECTION ( 'NONE',  ( -2.915501640297152804E-16, -1.000000000000000000, -6.997203936713167125E-15 ) ) ;
#23077=ORIENTED_EDGE ( 'NONE', *, *, #208937, .T. ) ;
#23090=CIRCLE ( 'NONE', #77222, 0.09999999999998898659 ) ;
#23094=LINE ( 'NONE', #102571, #31004 ) ;
#23163=VECTOR ( 'NONE', #76632, 1000.000000000000000 ) ;
#23208=EDGE_CURVE ( 'NONE', #74533, #144474, #169048, .T. ) ;
#23240=EDGE_CURVE ( 'NONE', #69711, #110939, #230256, .T. ) ;
#23277=EDGE_LOOP ( 'NONE', ( #80222, #82992, #107605, #4677 ) ) ;
#23282=ORIENTED_EDGE ( 'NONE', *, *, #19049, .T. ) ;
#23285=CARTESIAN_POINT ( 'NONE',  ( -20.15000000000000568, 66.70857864377492774, -148.8731074845244393 ) ) ;
#23299=AXIS2_PLACEMENT_3D ( 'NONE', #218445, #159792, #63229 ) ;
#23301=AXIS2_PLACEMENT_3D ( 'NONE', #119783, #197996, #233311 ) ;
#23345=VERTEX_POINT ( 'NONE', #172909 ) ;
#23387=CARTESIAN_POINT ( 'NONE',  ( -23.15000000000000213, 76.00000000001237765, -170.0231074845243597 ) ) ;
#23409=CARTESIAN_POINT ( 'NONE',  ( 20.94999999999999929, 85.00000000001232081, -160.1291383618718385 ) ) ;
#23454=ORIENTED_EDGE ( 'NONE', *, *, #131347, .T. ) ;
#23460=CYLINDRICAL_SURFACE ( 'NONE', #153318, 0.1000000000000028644 ) ;
#23464=LINE ( 'NONE', #102943, #180470 ) ;
#23472=ORIENTED_EDGE ( 'NONE', *, *, #27689, .F. ) ;
#23488=DIRECTION ( 'NONE',  ( 0.000000000000000000, 0.9908441862701791170, 0.1350103645450472789 ) ) ;
#23498=VERTEX_POINT ( 'NONE', #86572 ) ;
#23515=DIRECTION ( 'NONE',  ( -1.000000000000000000, 0.000000000000000000, -0.000000000000000000 ) ) ;
#23560=ORIENTED_EDGE ( 'NONE', *, *, #90255, .F. ) ;
#23566=ORIENTED_EDGE ( 'NONE', *, *, #84798, .F. ) ;
#23601=VERTEX_POINT ( 'NONE', #29244 ) ;
#23668=CARTESIAN_POINT ( 'NONE',  ( 20.94999999999999574, 74.25000000001229239, -158.3535959266227451 ) ) ;
#23674=VECTOR ( 'NONE', #52885, 1000.000000000000000 ) ;
#23705=EDGE_CURVE ( 'NONE', #159849, #79539, #248001, .T. ) ;
#23721=VERTEX_POINT ( 'NONE', #142082 ) ;
#23783=AXIS2_PLACEMENT_3D ( 'NONE', #74778, #250797, #34354 ) ;
#23813=TOROIDAL_SURFACE ( 'NONE', #94496, 0.2000000000000000111, 0.1000000000000000056 ) ;
#23816=CYLINDRICAL_SURFACE ( 'NONE', #156288, 0.09999999999998898659 ) ;
#23838=FACE_OUTER_BOUND ( 'NONE', #246311, .T. ) ;
#23842=EDGE_CURVE ( 'NONE', #238290, #167205, #52538, .T. ) ;
#23846=VERTEX_POINT ( 'NONE', #132089 ) ;
#23899=ORIENTED_EDGE ( 'NONE', *, *, #204444, .F. ) ;
#23906=DIRECTION ( 'NONE',  ( 0.000000000000000000, 0.000000000000000000, 1.000000000000000000 ) ) ;
#23912=CIRCLE ( 'NONE', #227896, 0.09999999999998898659 ) ;
#23915=CARTESIAN_POINT ( 'NONE',  ( 18.44364597020197039, 85.49048731717461180, -162.9651295948404481 ) ) ;
#23923=DIRECTION ( 'NONE',  ( 0.000000000000000000, -7.545205021724366615E-15, 1.000000000000000000 ) ) ;
#23930=CARTESIAN_POINT ( 'NONE',  ( -23.15000000000000213, 76.00000000001234923, -165.9731074845243768 ) ) ;
#23940=AXIS2_PLACEMENT_3D ( 'NONE', #191479, #29836, #50629 ) ;
#23952=EDGE_LOOP ( 'NONE', ( #30840, #169071, #169210, #3231 ) ) ;
#23967=CARTESIAN_POINT ( 'NONE',  ( -20.94999999999999929, 69.15387683765952431, -132.7853812176745407 ) ) ;
#23982=DIRECTION ( 'NONE',  ( 2.840903330521633255E-16, 0.8700118002898357128, -0.4930308989875171188 ) ) ;
#23996=DIRECTION ( 'NONE',  ( 0.000000000000000000, -1.000000000000000000, -6.982962677686266711E-15 ) ) ;
#23997=CARTESIAN_POINT ( 'NONE',  ( -22.39999999999999858, 64.35000000001238618, -169.9231074845244507 ) ) ;
#24011=ADVANCED_FACE ( 'NONE', ( #105861 ), #21064, .T. ) ;
#24048=CIRCLE ( 'NONE', #169816, 0.1000000000000028644 ) ;
#24060=EDGE_CURVE ( 'NONE', #255384, #222829, #87586, .T. ) ;
#24101=EDGE_CURVE ( 'NONE', #26294, #5985, #69347, .T. ) ;
#24107=CIRCLE ( 'NONE', #94803, 0.09999999999999939493 ) ;
#24126=LINE ( 'NONE', #243145, #127639 ) ;
#24127=ORIENTED_EDGE ( 'NONE', *, *, #17139, .T. ) ;
#24142=EDGE_CURVE ( 'NONE', #208786, #106358, #33735, .T. ) ;
#24148=CARTESIAN_POINT ( 'NONE',  ( -23.15000000000000213, 76.00000000001213607, -136.5231074845243313 ) ) ;
#24150=EDGE_LOOP ( 'NONE', ( #75488, #237638, #225570, #108314, #138746, #81317, #228112, #44932, #150568, #69400, #127830, #189165, #20633, #131309, #134520, #15252, #84051, #81321, #23282, #172223, #4019, #175651, #30293, #154807, #243769 ) ) ;
#24189=ORIENTED_EDGE ( 'NONE', *, *, #4053, .F. ) ;
#24259=CARTESIAN_POINT ( 'NONE',  ( 23.14999999999999503, 64.35000000001222986, -148.6731074845244507 ) ) ;
#24267=FACE_OUTER_BOUND ( 'NONE', #203365, .T. ) ;
#24333=CIRCLE ( 'NONE', #253254, 0.09999999999999489853 ) ;
#24335=( BOUNDED_CURVE ( )  B_SPLINE_CURVE ( 3, ( #6799, #165901, #27692, #186742 ),
 .UNSPECIFIED., .F., .F. ) 
 B_SPLINE_CURVE_WITH_KNOTS ( ( 4, 4 ),
 ( 4.937700262164173333E-15, 1.570796326794912323 ),
 .UNSPECIFIED. ) 
 CURVE ( )  GEOMETRIC_REPRESENTATION_ITEM ( )  RATIONAL_B_SPLINE_CURVE ( ( 1.000000000000000000, 0.8047378541243623840, 0.8047378541243623840, 1.000000000000000000 ) ) 
 REPRESENTATION_ITEM ( '' )  );
#24340=PLANE ( 'NONE',  #179444 ) ;
#24341=DIRECTION ( 'NONE',  ( 1.000000000000000000, -3.265361837132813093E-16, -2.280189983783949500E-30 ) ) ;
#24344=ORIENTED_EDGE ( 'NONE', *, *, #145629, .F. ) ;
#24348=AXIS2_PLACEMENT_3D ( 'NONE', #256121, #59226, #39744 ) ;
#24367=CYLINDRICAL_SURFACE ( 'NONE', #38266, 0.09999999999998898659 ) ;
#24397=CARTESIAN_POINT ( 'NONE',  ( 18.39999999999999858, 85.50000000001209344, -129.9229180933022576 ) ) ;
#24421=AXIS2_PLACEMENT_3D ( 'NONE', #84111, #125850, #140269 ) ;
#24422=CYLINDRICAL_SURFACE ( 'NONE', #112890, 0.09999999999999939493 ) ;
#24441=VECTOR ( 'NONE', #63588, 1000.000000000000114 ) ;
#24449=VECTOR ( 'NONE', #40987, 1000.000000000000000 ) ;
#24479=CYLINDRICAL_SURFACE ( 'NONE', #145183, 0.09999999999998898659 ) ;
#24495=ORIENTED_EDGE ( 'NONE', *, *, #41741, .T. ) ;
#24521=EDGE_CURVE ( 'NONE', #90604, #50990, #241815, .T. ) ;
#24541=DIRECTION ( 'NONE',  ( 1.000000000000000000, -3.265361837132813093E-16, -2.280189983783949500E-30 ) ) ;
#24555=ORIENTED_EDGE ( 'NONE', *, *, #18595, .T. ) ;
#24565=CARTESIAN_POINT ( 'NONE',  ( -22.50000000000000000, 75.90000000001245439, -181.6726782920691505 ) ) ;
#24607=EDGE_LOOP ( 'NONE', ( #135595, #171131, #188932, #200305 ) ) ;
#24625=EDGE_CURVE ( 'NONE', #56847, #208658, #36338, .T. ) ;
#24650=DIRECTION ( 'NONE',  ( -1.000000000000000000, 0.000000000000000000, 0.000000000000000000 ) ) ;
#24657=AXIS2_PLACEMENT_3D ( 'NONE', #65623, #46061, #9502 ) ;
#24667=CYLINDRICAL_SURFACE ( 'NONE', #229933, 0.09999999999998898659 ) ;
#24684=FACE_OUTER_BOUND ( 'NONE', #50029, .T. ) ;
#24691=EDGE_CURVE ( 'NONE', #227218, #18809, #76283, .T. ) ;
#24696=LINE ( 'NONE', #125062, #225639 ) ;
#24704=AXIS2_PLACEMENT_3D ( 'NONE', #221266, #137877, #197864 ) ;
#24706=CARTESIAN_POINT ( 'NONE',  ( -21.05000000000000071, 77.83534155023671985, -158.4679561919613491 ) ) ;
#24740=EDGE_CURVE ( 'NONE', #244509, #135741, #213673, .T. ) ;
#24750=EDGE_LOOP ( 'NONE', ( #171132, #198588, #190561, #249444 ) ) ;
#24810=DIRECTION ( 'NONE',  ( 1.000000000000000000, -3.265361837132813093E-16, -2.280189983783949500E-30 ) ) ;
#24819=CARTESIAN_POINT ( 'NONE',  ( 18.49999999999999645, 76.00000000001213607, -136.5231074845243313 ) ) ;
#24875=VERTEX_POINT ( 'NONE', #145667 ) ;
#24901=CARTESIAN_POINT ( 'NONE',  ( 23.15000000000000213, 85.00000000001222134, -146.4170766071767389 ) ) ;
#24905=DIRECTION ( 'NONE',  ( -0.7071067811865474617, 0.7071067811865474617, 4.937700262164531476E-15 ) ) ;
#24933=ORIENTED_EDGE ( 'NONE', *, *, #124110, .T. ) ;
#24935=DIRECTION ( 'NONE',  ( -1.000000000000000000, -0.000000000000000000, -0.000000000000000000 ) ) ;
#24950=CARTESIAN_POINT ( 'NONE',  ( 21.13461538461538325, 67.11458296203782936, -157.6731074845244223 ) ) ;
#24956=VECTOR ( 'NONE', #91103, 1000.000000000000000 ) ;
#24999=VECTOR ( 'NONE', #118418, 1000.000000000000000 ) ;
#25000=LINE ( 'NONE', #1544, #19380 ) ;
#25007=DIRECTION ( 'NONE',  ( 2.952720810173289112E-16, 1.000000000000000000, 6.938893903907229955E-15 ) ) ;
#25026=DIRECTION ( 'NONE',  ( 1.000000000000000000, 0.000000000000000000, 0.000000000000000000 ) ) ;
#25032=FACE_OUTER_BOUND ( 'NONE', #140293, .T. ) ;
#25095=DIRECTION ( 'NONE',  ( 0.000000000000000000, 0.000000000000000000, -1.000000000000000000 ) ) ;
#25097=CARTESIAN_POINT ( 'NONE',  ( -21.05000000000000071, 69.50298221358124806, -170.0085617939582505 ) ) ;
#25106=DIRECTION ( 'NONE',  ( 0.000000000000000000, -6.982962677686266711E-15, 1.000000000000000000 ) ) ;
#25110=CARTESIAN_POINT ( 'NONE',  ( 21.05000005001280172, 67.12872030824209446, -157.8451598962784317 ) ) ;
#25138=LINE ( 'NONE', #143763, #52741 ) ;
#25144=VERTEX_POINT ( 'NONE', #4558 ) ;
#25159=EDGE_LOOP ( 'NONE', ( #84881, #227115, #173546, #234364 ) ) ;
#25267=CARTESIAN_POINT ( 'NONE',  ( 23.14999999999999503, 64.25000000001244871, -181.7731074845244450 ) ) ;
#25274=CARTESIAN_POINT ( 'NONE',  ( -21.05000000000000071, 88.41227409416184457, -139.4231074845242802 ) ) ;
#25284=DIRECTION ( 'NONE',  ( 0.000000000000000000, -0.9887567792719351711, 0.1495327102803594987 ) ) ;
#25301=CARTESIAN_POINT ( 'NONE',  ( 18.59999999999999076, 65.79142135624951493, -145.3731074845244109 ) ) ;
#25322=ORIENTED_EDGE ( 'NONE', *, *, #184216, .T. ) ;
#25340=CIRCLE ( 'NONE', #87831, 0.09999999999999939493 ) ;
#25355=ORIENTED_EDGE ( 'NONE', *, *, #130906, .F. ) ;
#25378=CARTESIAN_POINT ( 'NONE',  ( 21.05000000000000426, 69.58617371119942163, -169.9373665474910240 ) ) ;
#25383=CARTESIAN_POINT ( 'NONE',  ( 22.60000000000000142, 75.89914163091376054, -181.7726746080137445 ) ) ;
#25403=DIRECTION ( 'NONE',  ( -1.000000000000000000, -0.000000000000000000, -0.000000000000000000 ) ) ;
#25409=ORIENTED_EDGE ( 'NONE', *, *, #85021, .T. ) ;
#25417=AXIS2_PLACEMENT_3D ( 'NONE', #54742, #235944, #71769 ) ;
#25454=CYLINDRICAL_SURFACE ( 'NONE', #246115, 0.09999999999998898659 ) ;
#25504=EDGE_CURVE ( 'NONE', #113635, #59420, #1630, .T. ) ;
#25513=ADVANCED_FACE ( 'NONE', ( #186054 ), #76652, .T. ) ;
#25539=CARTESIAN_POINT ( 'NONE',  ( 21.05000000000000071, 69.65000000001231228, -160.1792853948412869 ) ) ;
#25541=EDGE_CURVE ( 'NONE', #36614, #250601, #33439, .T. ) ;
#25554=ORIENTED_EDGE ( 'NONE', *, *, #106627, .F. ) ;
#25571=CARTESIAN_POINT ( 'NONE',  ( 18.49999999999999645, 77.63717271298267519, -158.4409541190523214 ) ) ;
#25589=ORIENTED_EDGE ( 'NONE', *, *, #167222, .F. ) ;
#25599=AXIS2_PLACEMENT_3D ( 'NONE', #224900, #168847, #87947 ) ;
#25616=VERTEX_POINT ( 'NONE', #174233 ) ;
#25626=CARTESIAN_POINT ( 'NONE',  ( -23.25000000000000000, 76.00000000001207923, -128.6231074845243540 ) ) ;
#25639=CIRCLE ( 'NONE', #233757, 7.720710678118692272 ) ;
#25641=CARTESIAN_POINT ( 'NONE',  ( -21.05000000000000071, 70.10000000001220144, -146.7422072491807796 ) ) ;
#25670=CARTESIAN_POINT ( 'NONE',  ( 21.04999999999908411, 67.22371710472162931, -157.8651984818719143 ) ) ;
#25682=VERTEX_POINT ( 'NONE', #203902 ) ;
#25693=ORIENTED_EDGE ( 'NONE', *, *, #96158, .F. ) ;
#25714=CARTESIAN_POINT ( 'NONE',  ( 22.59999999999999432, 64.25012875563587045, -170.0885370755381132 ) ) ;
#25717=AXIS2_PLACEMENT_3D ( 'NONE', #108363, #187904, #235994 ) ;
#25728=EDGE_CURVE ( 'NONE', #177863, #49440, #9646, .T. ) ;
#25729=DIRECTION ( 'NONE',  ( -0.000000000000000000, 0.8660254037844377084, 0.5000000000000016653 ) ) ;
#25747=( BOUNDED_CURVE ( )  B_SPLINE_CURVE ( 3, ( #87730, #228560, #90303, #69496 ),
 .UNSPECIFIED., .F., .F. ) 
 B_SPLINE_CURVE_WITH_KNOTS ( ( 4, 4 ),
 ( 1.570796326794895448, 3.141592653589791784 ),
 .UNSPECIFIED. ) 
 CURVE ( )  GEOMETRIC_REPRESENTATION_ITEM ( )  RATIONAL_B_SPLINE_CURVE ( ( 1.000000000000000000, 0.8047378541243650485, 0.8047378541243650485, 1.000000000000000000 ) ) 
 REPRESENTATION_ITEM ( '' )  );
#25759=EDGE_CURVE ( 'NONE', #223637, #46965, #80342, .T. ) ;
#25770=CARTESIAN_POINT ( 'NONE',  ( -18.59999999999999787, 65.66751761918692409, -130.9282609406112670 ) ) ;
#25860=DIRECTION ( 'NONE',  ( 0.7071359030027593029, 0.7070776581709197206, 0.000000000000000000 ) ) ;
#25925=DIRECTION ( 'NONE',  ( 1.000000000000000000, 0.000000000000000000, 0.000000000000000000 ) ) ;
#25938=EDGE_LOOP ( 'NONE', ( #12544, #149152, #84362, #95821 ) ) ;
#26000=CARTESIAN_POINT ( 'NONE',  ( -18.60000000000001563, 85.36424052760324344, -162.8428589026835311 ) ) ;
#26022=CARTESIAN_POINT ( 'NONE',  ( -18.50000000000000000, 70.05000000001236060, -159.7174051794895320 ) ) ;
#26031=CARTESIAN_POINT ( 'NONE',  ( 21.05000000000000071, 87.65000000001235492, -167.1231074845242688 ) ) ;
#26059=LINE ( 'NONE', #101692, #193852 ) ;
#26086=EDGE_CURVE ( 'NONE', #113219, #256686, #5699, .T. ) ;
#26122=DIRECTION ( 'NONE',  ( 0.000000000000000000, 6.982962677686266711E-15, -1.000000000000000000 ) ) ;
#26129=DIRECTION ( 'NONE',  ( 0.000000000000000000, 0.000000000000000000, -1.000000000000000000 ) ) ;
#26172=CARTESIAN_POINT ( 'NONE',  ( 20.04142135391667168, 64.25000000001220712, -145.3206006188949004 ) ) ;
#26193=EDGE_CURVE ( 'NONE', #91448, #209114, #101346, .T. ) ;
#26197=CARTESIAN_POINT ( 'NONE',  ( -21.45000000000000284, 68.29142135624952914, -148.8731074845244109 ) ) ;
#26208=ORIENTED_EDGE ( 'NONE', *, *, #117136, .T. ) ;
#26255=CARTESIAN_POINT ( 'NONE',  ( -18.59999999999999787, 64.35000000001230092, -157.7731074845244450 ) ) ;
#26257=CARTESIAN_POINT ( 'NONE',  ( -23.25000000000000000, 74.00000000001223555, -149.7477294072864709 ) ) ;
#26268=FACE_OUTER_BOUND ( 'NONE', #233151, .T. ) ;
#26269=CARTESIAN_POINT ( 'NONE',  ( -21.05000000000000071, 87.41227409416205774, -167.0231074845242745 ) ) ;
#26272=EDGE_CURVE ( 'NONE', #58764, #76100, #118154, .T. ) ;
#26274=CARTESIAN_POINT ( 'NONE',  ( -20.54999999999999716, 76.00000000001215028, -138.4231074845243654 ) ) ;
#26287=VERTEX_POINT ( 'NONE', #137846 ) ;
#26294=VERTEX_POINT ( 'NONE', #60884 ) ;
#26306=DIRECTION ( 'NONE',  ( 0.000000000000000000, 0.000000000000000000, -1.000000000000000000 ) ) ;
#26331=CARTESIAN_POINT ( 'NONE',  ( -18.39999999999999858, 85.60000000001210196, -129.8229180933022633 ) ) ;
#26377=CARTESIAN_POINT ( 'NONE',  ( 20.95512820512820440, 67.12384868372417657, -157.8731074845244109 ) ) ;
#26413=DIRECTION ( 'NONE',  ( -0.000000000000000000, 0.1298341882519953583, 0.9915357197604862671 ) ) ;
#26437=EDGE_CURVE ( 'NONE', #158699, #44711, #204247, .T. ) ;
#26442=CARTESIAN_POINT ( 'NONE',  ( 18.49999999999999645, 77.86671491006960366, -158.2704322382423356 ) ) ;
#26453=ORIENTED_EDGE ( 'NONE', *, *, #98787, .F. ) ;
#26460=ORIENTED_EDGE ( 'NONE', *, *, #148111, .F. ) ;
#26526=CARTESIAN_POINT ( 'NONE',  ( -21.00250684356850073, 64.25000000001233502, -163.0083017157664358 ) ) ;
#26541=VECTOR ( 'NONE', #97995, 1000.000000000000000 ) ;
#26545=CYLINDRICAL_SURFACE ( 'NONE', #104357, 0.1000000000000118433 ) ;
#26626=CARTESIAN_POINT ( 'NONE',  ( 20.94999999999999929, 76.00000000001227818, -157.0481074845243938 ) ) ;
#26629=VERTEX_POINT ( 'NONE', #179283 ) ;
#26665=DIRECTION ( 'NONE',  ( 0.000000000000000000, 0.1350103645451946055, -0.9908441862701591329 ) ) ;
#26670=ORIENTED_EDGE ( 'NONE', *, *, #141181, .F. ) ;
#26679=CARTESIAN_POINT ( 'NONE',  ( 21.05000000000000071, 87.65000000001215597, -139.4231074845242802 ) ) ;
#26705=DIRECTION ( 'NONE',  ( 0.000000000000000000, -8.905812670947865054E-15, 1.000000000000000000 ) ) ;
#26710=CIRCLE ( 'NONE', #93314, 0.09999999999998898659 ) ;
#26729=ORIENTED_EDGE ( 'NONE', *, *, #86968, .F. ) ;
#26739=ORIENTED_EDGE ( 'NONE', *, *, #182785, .F. ) ;
#26760=CYLINDRICAL_SURFACE ( 'NONE', #2424, 0.1000000000000028644 ) ;
#26816=CARTESIAN_POINT ( 'NONE',  ( 20.91682497891423154, 65.67736539654967487, -130.9625116876572406 ) ) ;
#26828=CARTESIAN_POINT ( 'NONE',  ( 20.94999999999999929, 77.36242903720540198, -128.6342262366031548 ) ) ;
#26836=CARTESIAN_POINT ( 'NONE',  ( -18.59999999999999787, 85.32100840337361092, -162.7871692354464130 ) ) ;
#26844=DIRECTION ( 'NONE',  ( -1.000000000000000000, 0.000000000000000000, 0.000000000000000000 ) ) ;
#26859=AXIS2_PLACEMENT_3D ( 'NONE', #62896, #142430, #185418 ) ;
#26861=CIRCLE ( 'NONE', #114127, 0.09999999999998898659 ) ;
#26867=CARTESIAN_POINT ( 'NONE',  ( -22.39999999999999858, 76.10000000001245724, -181.6726782920691505 ) ) ;
#26893=ORIENTED_EDGE ( 'NONE', *, *, #21132, .T. ) ;
#26897=DIRECTION ( 'NONE',  ( 0.000000000000000000, -0.1575844902526687130, -0.9875055080513762684 ) ) ;
#26900=LINE ( 'NONE', #208095, #34400 ) ;
#26902=AXIS2_PLACEMENT_3D ( 'NONE', #187400, #227788, #105233 ) ;
#26903=VECTOR ( 'NONE', #222923, 1000.000000000000000 ) ;
#26932=CIRCLE ( 'NONE', #243375, 0.4000000000000114575 ) ;
#26935=AXIS2_PLACEMENT_3D ( 'NONE', #169251, #192633, #208360 ) ;
#26975=ORIENTED_EDGE ( 'NONE', *, *, #137943, .T. ) ;
#26980=DIRECTION ( 'NONE',  ( 6.938893903907224433E-15, 1.000000000000000000, 7.272083257015735086E-15 ) ) ;
#26985=CIRCLE ( 'NONE', #151889, 0.09999999999998898659 ) ;
#26987=LINE ( 'NONE', #68662, #183447 ) ;
#26989=CYLINDRICAL_SURFACE ( 'NONE', #254025, 11.80000000000000426 ) ;
#27006=DIRECTION ( 'NONE',  ( 0.000000000000000000, -0.9274965247785323941, -0.3738317757009769760 ) ) ;
#27009=ORIENTED_EDGE ( 'NONE', *, *, #133785, .T. ) ;
#27056=CIRCLE ( 'NONE', #10289, 0.2000000000000057288 ) ;
#27057=ORIENTED_EDGE ( 'NONE', *, *, #174087, .T. ) ;
#27059=DIRECTION ( 'NONE',  ( 0.000000000000000000, -0.9908441862701420355, -0.1350103645453197554 ) ) ;
#27077=CARTESIAN_POINT ( 'NONE',  ( -22.45354308602760796, 75.99999978012890267, -181.7735403749906595 ) ) ;
#27114=CARTESIAN_POINT ( 'NONE',  ( 23.15000000000000213, 87.48912529308822172, -139.6231074845242688 ) ) ;
#27169=SPHERICAL_SURFACE ( 'NONE', #230745, 0.1000000000000000056 ) ;
#27197=CARTESIAN_POINT ( 'NONE',  ( 21.14999999999999503, 76.10000000001245724, -181.6726782920691505 ) ) ;
#27203=DIRECTION ( 'NONE',  ( 1.000000000000000000, 0.000000000000000000, 0.000000000000000000 ) ) ;
#27205=CARTESIAN_POINT ( 'NONE',  ( 21.05000000000000071, 76.00000000001229239, -157.1481074845243882 ) ) ;
#27244=CARTESIAN_POINT ( 'NONE',  ( -21.13614978966382196, 69.50089529817859102, -170.0231074845243882 ) ) ;
#27255=CARTESIAN_POINT ( 'NONE',  ( -21.00023020733438628, 69.60913075474465472, -170.0231074845244166 ) ) ;
#27257=EDGE_LOOP ( 'NONE', ( #24127, #31391, #38612, #170986 ) ) ;
#27272=FACE_OUTER_BOUND ( 'NONE', #79804, .T. ) ;
#27294=CARTESIAN_POINT ( 'NONE',  ( -20.64999999999999858, 68.85000000001222986, -148.8731074845244109 ) ) ;
#27342=AXIS2_PLACEMENT_3D ( 'NONE', #214995, #14260, #75519 ) ;
#27355=ORIENTED_EDGE ( 'NONE', *, *, #194644, .F. ) ;
#27396=DIRECTION ( 'NONE',  ( -1.000000000000000000, 3.265361837132813093E-16, 2.280189983783949500E-30 ) ) ;
#27427=AXIS2_PLACEMENT_3D ( 'NONE', #157282, #80244, #141534 ) ;
#27474=ORIENTED_EDGE ( 'NONE', *, *, #12227, .T. ) ;
#27519=EDGE_LOOP ( 'NONE', ( #181750, #62776, #45661, #204647 ) ) ;
#27527=DIRECTION ( 'NONE',  ( 0.000000000000000000, 0.000000000000000000, -1.000000000000000000 ) ) ;
#27534=CARTESIAN_POINT ( 'NONE',  ( 23.24999999999999289, 64.25000000001227818, -157.8731074845244393 ) ) ;
#27543=CIRCLE ( 'NONE', #173292, 0.1000000000000000888 ) ;
#27607=EDGE_LOOP ( 'NONE', ( #216799, #158695, #100994, #182952, #132149, #101807 ) ) ;
#27643=VECTOR ( 'NONE', #49043, 1000.000000000000000 ) ;
#27646=EDGE_LOOP ( 'NONE', ( #200927, #230556, #131223, #121887 ) ) ;
#27649=ADVANCED_FACE ( 'NONE', ( #257474 ), #99983, .T. ) ;
#27689=EDGE_CURVE ( 'NONE', #49789, #9341, #184415, .T. ) ;
#27691=CARTESIAN_POINT ( 'NONE',  ( -18.59999999999999787, 68.92903212821327941, -132.7765432626560766 ) ) ;
#27692=CARTESIAN_POINT ( 'NONE',  ( 19.88284271247461987, 64.30857864377489364, -145.2731074845244450 ) ) ;
#27704=CYLINDRICAL_SURFACE ( 'NONE', #193235, 11.75000000000001066 ) ;
#27726=EDGE_LOOP ( 'NONE', ( #69366, #121983, #66609, #178975 ) ) ;
#27735=CIRCLE ( 'NONE', #6845, 0.09999999999998898659 ) ;
#27741=DIRECTION ( 'NONE',  ( 0.000000000000000000, 1.000000000000000000, 0.000000000000000000 ) ) ;
#27751=CIRCLE ( 'NONE', #173522, 0.5000000000000004441 ) ;
#27754=ORIENTED_EDGE ( 'NONE', *, *, #22877, .F. ) ;
#27758=ORIENTED_EDGE ( 'NONE', *, *, #247855, .F. ) ;
#27770=CYLINDRICAL_SURFACE ( 'NONE', #43122, 0.09999999999998898659 ) ;
#27773=CARTESIAN_POINT ( 'NONE',  ( -22.39999999999999858, 68.20922040163897293, -170.0231074845243882 ) ) ;
#27782=DIRECTION ( 'NONE',  ( -1.000000000000000000, 1.836970198721029934E-16, 1.282749433769087582E-30 ) ) ;
#27784=CARTESIAN_POINT ( 'NONE',  ( 22.50927854361892955, 76.10085807354020915, -181.7726746105512348 ) ) ;
#27806=LINE ( 'NONE', #105995, #236927 ) ;
#27824=CARTESIAN_POINT ( 'NONE',  ( 20.95512820512820440, 65.37615131630045084, -162.3581939154368285 ) ) ;
#27829=DIRECTION ( 'NONE',  ( 0.000000000000000000, 0.000000000000000000, -1.000000000000000000 ) ) ;
#27922=DIRECTION ( 'NONE',  ( 0.000000000000000000, 0.000000000000000000, -1.000000000000000000 ) ) ;
#27927=EDGE_CURVE ( 'NONE', #186771, #10427, #114798, .T. ) ;
#27960=CARTESIAN_POINT ( 'NONE',  ( 21.05000000000000071, 69.74218538953624602, -170.1208977758331855 ) ) ;
#27966=ADVANCED_FACE ( 'NONE', ( #69629 ), #229972, .F. ) ;
#27972=CIRCLE ( 'NONE', #231971, 0.4000000000000114575 ) ;
#27977=AXIS2_PLACEMENT_3D ( 'NONE', #180087, #256988, #237485 ) ;
#28004=VECTOR ( 'NONE', #241659, 1000.000000000000000 ) ;
#28009=EDGE_LOOP ( 'NONE', ( #2671, #94756, #243071, #173360 ) ) ;
#28032=DIRECTION ( 'NONE',  ( -1.000000000000000000, -0.000000000000000000, -0.000000000000000000 ) ) ;
#28034=DIRECTION ( 'NONE',  ( 1.000000000000000000, 0.000000000000000000, 0.000000000000000000 ) ) ;
#28043=DIRECTION ( 'NONE',  ( -0.000000000000000000, -6.982962677686266711E-15, 1.000000000000000000 ) ) ;
#28044=DIRECTION ( 'NONE',  ( 0.000000000000000000, 0.8700118002898393765, -0.4930308989875104575 ) ) ;
#28068=AXIS2_PLACEMENT_3D ( 'NONE', #106706, #147126, #109275 ) ;
#28073=ADVANCED_FACE ( 'NONE', ( #257179 ), #73314, .T. ) ;
#28076=VERTEX_POINT ( 'NONE', #255898 ) ;
#28077=DIRECTION ( 'NONE',  ( 1.000000000000000000, 0.000000000000000000, 0.000000000000000000 ) ) ;
#28093=ADVANCED_FACE ( 'NONE', ( #158185 ), #94300, .F. ) ;
#28095=CARTESIAN_POINT ( 'NONE',  ( -20.94999999999999929, 64.35000000001220144, -143.3069731475025321 ) ) ;
#28100=ORIENTED_EDGE ( 'NONE', *, *, #109601, .T. ) ;
#28108=ORIENTED_EDGE ( 'NONE', *, *, #253820, .F. ) ;
#28148=AXIS2_PLACEMENT_3D ( 'NONE', #93800, #212491, #114657 ) ;
#28178=CIRCLE ( 'NONE', #65739, 11.75000000000001066 ) ;
#28207=DIRECTION ( 'NONE',  ( 1.000000000000000000, -1.875376730785737719E-16, -1.309568571767809260E-30 ) ) ;
#28217=EDGE_CURVE ( 'NONE', #59337, #138337, #27543, .T. ) ;
#28226=CYLINDRICAL_SURFACE ( 'NONE', #91635, 0.09999999999998898659 ) ;
#28256=DIRECTION ( 'NONE',  ( -0.000000000000000000, -1.000000000000000000, -6.982962677686266711E-15 ) ) ;
#28271=DIRECTION ( 'NONE',  ( 0.000000000000000000, 0.9908441862701791170, -0.1350103645450472789 ) ) ;
#28314=LINE ( 'NONE', #30878, #177243 ) ;
#28318=CARTESIAN_POINT ( 'NONE',  ( 20.12500000000000000, 66.25000000001232081, -161.9113362024101548 ) ) ;
#28365=CARTESIAN_POINT ( 'NONE',  ( 23.14999999999999858, 76.00000000001237765, -170.0231074845243597 ) ) ;
#28379=CARTESIAN_POINT ( 'NONE',  ( 18.46921299892756352, 85.50937817783609773, -163.0365287751538972 ) ) ;
#28401=DIRECTION ( 'NONE',  ( 0.000000000000000000, 6.982962677686266711E-15, -1.000000000000000000 ) ) ;
#28411=EDGE_CURVE ( 'NONE', #48521, #223292, #123357, .T. ) ;
#28422=DIRECTION ( 'NONE',  ( 0.000000000000000000, 7.056502275159890832E-15, -1.000000000000000000 ) ) ;
#28442=EDGE_CURVE ( 'NONE', #36614, #216103, #206734, .T. ) ;
#28490=ORIENTED_EDGE ( 'NONE', *, *, #10066, .F. ) ;
#28492=CARTESIAN_POINT ( 'NONE',  ( 23.14999999999999858, 71.00000000001223555, -148.9283735034374843 ) ) ;
#28494=EDGE_CURVE ( 'NONE', #151867, #127058, #41755, .T. ) ;
#28511=CARTESIAN_POINT ( 'NONE',  ( 20.94999999999999574, 77.16270174995034381, -161.9231074845243370 ) ) ;
#28520=CIRCLE ( 'NONE', #149103, 7.899999999999990585 ) ;
#28522=AXIS2_PLACEMENT_3D ( 'NONE', #32975, #112479, #257058 ) ;
#28534=CARTESIAN_POINT ( 'NONE',  ( 20.52683494730046476, 67.01946918171096002, -161.5178547619902076 ) ) ;
#28541=VECTOR ( 'NONE', #81121, 1000.000000000000000 ) ;
#28548=ORIENTED_EDGE ( 'NONE', *, *, #221459, .F. ) ;
#28549=DIRECTION ( 'NONE',  ( 1.000000000000000000, 0.000000000000000000, 0.000000000000000000 ) ) ;
#28632=DIRECTION ( 'NONE',  ( 0.000000000000000000, 1.000000000000000000, 0.000000000000000000 ) ) ;
#28637=EDGE_CURVE ( 'NONE', #43638, #36614, #46842, .T. ) ;
#28645=EDGE_LOOP ( 'NONE', ( #181661, #238771, #168754, #249399, #256649 ) ) ;
#28688=CARTESIAN_POINT ( 'NONE',  ( 21.05000000000000071, 85.00000000001222134, -146.4170766071767389 ) ) ;
#28696=VERTEX_POINT ( 'NONE', #188947 ) ;
#28734=AXIS2_PLACEMENT_3D ( 'NONE', #166007, #206390, #188109 ) ;
#28761=CIRCLE ( 'NONE', #236996, 0.09999999999998898659 ) ;
#28783=CARTESIAN_POINT ( 'NONE',  ( -21.05000000000000071, 87.75000000001216449, -139.6231074845242688 ) ) ;
#28819=DIRECTION ( 'NONE',  ( 0.000000000000000000, 0.000000000000000000, 1.000000000000000000 ) ) ;
#28831=CARTESIAN_POINT ( 'NONE',  ( -18.59999999999999787, 64.25000000001223555, -148.6731074845244507 ) ) ;
#28854=FACE_OUTER_BOUND ( 'NONE', #28645, .T. ) ;
#28868=CYLINDRICAL_SURFACE ( 'NONE', #25717, 0.09999999999999939493 ) ;
#28892=CARTESIAN_POINT ( 'NONE',  ( 21.08621493067296271, 69.65070570884071799, -170.0793023240005084 ) ) ;
#28895=CARTESIAN_POINT ( 'NONE',  ( -20.94999999999999929, 76.00000000001216449, -140.6231074845243256 ) ) ;
#28942=EDGE_CURVE ( 'NONE', #18391, #120146, #24126, .T. ) ;
#28952=DIRECTION ( 'NONE',  ( -3.469446951953515108E-14, -1.000000000000000000, 0.000000000000000000 ) ) ;
#28987=CARTESIAN_POINT ( 'NONE',  ( -20.94999999999999929, 64.30000000001219007, -143.2781056340430439 ) ) ;
#28989=EDGE_LOOP ( 'NONE', ( #216052, #212467 ) ) ;
#28991=DIRECTION ( 'NONE',  ( 0.000000000000000000, -7.026728003956695223E-15, 1.000000000000000000 ) ) ;
#28997=ORIENTED_EDGE ( 'NONE', *, *, #95303, .T. ) ;
#29047=DIRECTION ( 'NONE',  ( -3.265361837132813093E-16, -1.000000000000000000, 7.445645354460596589E-46 ) ) ;
#29072=ADVANCED_FACE ( 'NONE', ( #130903 ), #144555, .T. ) ;
#29161=DIRECTION ( 'NONE',  ( 0.000000000000000000, -6.352154140967427193E-15, 1.000000000000000000 ) ) ;
#29166=AXIS2_PLACEMENT_3D ( 'NONE', #184748, #246024, #183483 ) ;
#29188=CARTESIAN_POINT ( 'NONE',  ( 18.60000000000000497, 76.00000000001237765, -170.0231074845243597 ) ) ;
#29195=LINE ( 'NONE', #151699, #128123 ) ;
#29231=ORIENTED_EDGE ( 'NONE', *, *, #122087, .F. ) ;
#29244=CARTESIAN_POINT ( 'NONE',  ( -20.94999999999999929, 70.15000000001221281, -146.6556047088023149 ) ) ;
#29277=ADVANCED_FACE ( 'NONE', ( #83731 ), #110381, .F. ) ;
#29290=DIRECTION ( 'NONE',  ( 0.000000000000000000, 6.982962677686266711E-15, -1.000000000000000000 ) ) ;
#29301=EDGE_CURVE ( 'NONE', #75757, #41308, #44621, .T. ) ;
#29315=EDGE_LOOP ( 'NONE', ( #186817, #82819, #218529, #56246 ) ) ;
#29356=EDGE_CURVE ( 'NONE', #1798, #86120, #240426, .T. ) ;
#29390=CARTESIAN_POINT ( 'NONE',  ( 20.95575313997065336, 65.38544669673750320, -162.4018167825796297 ) ) ;
#29412=CARTESIAN_POINT ( 'NONE',  ( 20.85000000106584750, 64.25000000001219291, -143.3676028280509627 ) ) ;
#29433=AXIS2_PLACEMENT_3D ( 'NONE', #139745, #116372, #78497 ) ;
#29441=ORIENTED_EDGE ( 'NONE', *, *, #14185, .T. ) ;
#29474=DIRECTION ( 'NONE',  ( -1.000000000000000000, 2.952720810173289112E-16, 2.061873921506763405E-30 ) ) ;
#29478=CARTESIAN_POINT ( 'NONE',  ( -22.59066674512275696, 64.25000000001236344, -170.0536116081549380 ) ) ;
#29490=CARTESIAN_POINT ( 'NONE',  ( -22.39999999999999858, 68.20922040163897293, -170.1231074845244109 ) ) ;
#29512=FACE_OUTER_BOUND ( 'NONE', #102977, .T. ) ;
#29515=CARTESIAN_POINT ( 'NONE',  ( 21.14999999999999858, 64.35000000001228670, -157.8731074845244393 ) ) ;
#29529=ORIENTED_EDGE ( 'NONE', *, *, #134283, .F. ) ;
#29537=AXIS2_PLACEMENT_3D ( 'NONE', #233742, #173815, #115067 ) ;
#29546=FACE_OUTER_BOUND ( 'NONE', #231658, .T. ) ;
#29547=EDGE_CURVE ( 'NONE', #30528, #138157, #159991, .T. ) ;
#29553=LINE ( 'NONE', #167775, #76687 ) ;
#29577=DIRECTION ( 'NONE',  ( 0.000000000000000000, 6.982962677686266711E-15, -1.000000000000000000 ) ) ;
#29619=VECTOR ( 'NONE', #52310, 1000.000000000000000 ) ;
#29626=CARTESIAN_POINT ( 'NONE',  ( -21.05000000000000071, 76.00000000001237765, -170.0231074845243597 ) ) ;
#29640=DIRECTION ( 'NONE',  ( 0.000000000000000000, 7.116814260417676401E-15, -1.000000000000000000 ) ) ;
#29646=VERTEX_POINT ( 'NONE', #161748 ) ;
#29655=CARTESIAN_POINT ( 'NONE',  ( 18.58685178364169488, 85.40673308381654749, -162.8986870154365363 ) ) ;
#29719=CIRCLE ( 'NONE', #204637, 0.09999999999999939493 ) ;
#29755=DIRECTION ( 'NONE',  ( 0.000000000000000000, 6.982962677686266711E-15, -1.000000000000000000 ) ) ;
#29796=AXIS2_PLACEMENT_3D ( 'NONE', #48134, #202089, #83385 ) ;
#29808=CARTESIAN_POINT ( 'NONE',  ( 20.58091095332318332, 66.98152984665858867, -161.6044573023666260 ) ) ;
#29809=ORIENTED_EDGE ( 'NONE', *, *, #151432, .F. ) ;
#29815=VECTOR ( 'NONE', #96269, 1000.000000000000000 ) ;
#29836=DIRECTION ( 'NONE',  ( -1.000000000000000000, -0.000000000000000000, -0.000000000000000000 ) ) ;
#29840=CYLINDRICAL_SURFACE ( 'NONE', #141282, 0.09999999999998898659 ) ;
#29856=ORIENTED_EDGE ( 'NONE', *, *, #164913, .T. ) ;
#29867=ADVANCED_FACE ( 'NONE', ( #148588 ), #54599, .T. ) ;
#29869=VERTEX_POINT ( 'NONE', #214960 ) ;
#29879=FACE_OUTER_BOUND ( 'NONE', #145956, .T. ) ;
#29893=CARTESIAN_POINT ( 'NONE',  ( -20.64999999999999858, 76.00000000001213607, -136.5231074845243313 ) ) ;
#29903=DIRECTION ( 'NONE',  ( -1.000000000000000000, -0.000000000000000000, -0.000000000000000000 ) ) ;
#29925=CARTESIAN_POINT ( 'NONE',  ( 20.95083306685154056, 67.08315735812212210, -161.5457826312660643 ) ) ;
#29975=DIRECTION ( 'NONE',  ( 1.000000000000000000, 0.000000000000000000, 0.000000000000000000 ) ) ;
#29979=EDGE_CURVE ( 'NONE', #70573, #168873, #53325, .T. ) ;
#30043=DIRECTION ( 'NONE',  ( -1.000000000000000000, 0.000000000000000000, 0.000000000000000000 ) ) ;
#30082=DIRECTION ( 'NONE',  ( 1.000000000000000000, 0.000000000000000000, 0.000000000000000000 ) ) ;
#30087=CIRCLE ( 'NONE', #238328, 11.80000000000000426 ) ;
#30094=DIRECTION ( 'NONE',  ( 1.000000000000000000, 0.000000000000000000, 0.000000000000000000 ) ) ;
#30109=CARTESIAN_POINT ( 'NONE',  ( 21.70464131381650219, 68.90464198104452009, -170.0231074845243882 ) ) ;
#30134=FACE_OUTER_BOUND ( 'NONE', #22811, .T. ) ;
#30145=VERTEX_POINT ( 'NONE', #88256 ) ;
#30146=CARTESIAN_POINT ( 'NONE',  ( 21.08376601933332495, 69.65805272873672038, -170.0868834954544297 ) ) ;
#30148=CARTESIAN_POINT ( 'NONE',  ( -20.64999999999999858, 73.50000000001223555, -149.7477294072864709 ) ) ;
#30174=ADVANCED_FACE ( 'NONE', ( #226487 ), #247628, .T. ) ;
#30209=CARTESIAN_POINT ( 'NONE',  ( 20.94999999999999574, 76.00000000001237765, -170.0231074845243597 ) ) ;
#30238=VERTEX_POINT ( 'NONE', #72596 ) ;
#30271=ORIENTED_EDGE ( 'NONE', *, *, #43120, .T. ) ;
#30293=ORIENTED_EDGE ( 'NONE', *, *, #131848, .T. ) ;
#30314=AXIS2_PLACEMENT_3D ( 'NONE', #189659, #28044, #150538 ) ;
#30329=CARTESIAN_POINT ( 'NONE',  ( 23.25000000000000000, 85.60000000001231513, -160.1291383618718385 ) ) ;
#30333=DIRECTION ( 'NONE',  ( 0.000000000000000000, -1.000000000000000000, -6.352154140967427193E-15 ) ) ;
#30346=( BOUNDED_CURVE ( )  B_SPLINE_CURVE ( 3, ( #147694, #69458, #70751, #189389 ),
 .UNSPECIFIED., .F., .T. ) 
 B_SPLINE_CURVE_WITH_KNOTS ( ( 4, 4 ),
 ( 4.712388980384689674, 6.283185307179586232 ),
 .UNSPECIFIED. ) 
 CURVE ( )  GEOMETRIC_REPRESENTATION_ITEM ( )  RATIONAL_B_SPLINE_CURVE ( ( 1.000000000000000000, 0.8047378541243649375, 0.8047378541243649375, 1.000000000000000000 ) ) 
 REPRESENTATION_ITEM ( '' )  );
#30347=DIRECTION ( 'NONE',  ( 0.000000000000000000, 1.000000000000000000, 6.982962677686266711E-15 ) ) ;
#30348=DIRECTION ( 'NONE',  ( 1.000000000000000000, 0.000000000000000000, 0.000000000000000000 ) ) ;
#30364=CARTESIAN_POINT ( 'NONE',  ( -20.85000000000000142, 68.97833521811203639, -132.6895420826271277 ) ) ;
#30438=CARTESIAN_POINT ( 'NONE',  ( -21.05000000000000071, 77.16270174995034381, -162.0231074845243313 ) ) ;
#30456=FACE_OUTER_BOUND ( 'NONE', #237170, .T. ) ;
#30477=VECTOR ( 'NONE', #80752, 1000.000000000000114 ) ;
#30491=ORIENTED_EDGE ( 'NONE', *, *, #122796, .F. ) ;
#30502=DIRECTION ( 'NONE',  ( 1.000000000000000000, 0.000000000000000000, 0.000000000000000000 ) ) ;
#30528=VERTEX_POINT ( 'NONE', #32869 ) ;
#30568=DIRECTION ( 'NONE',  ( 0.000000000000000000, 0.000000000000000000, -1.000000000000000000 ) ) ;
#30591=ORIENTED_EDGE ( 'NONE', *, *, #197103, .T. ) ;
#30621=DIRECTION ( 'NONE',  ( 1.000000000000000000, 7.304098846218134667E-16, 5.100424963727256530E-30 ) ) ;
#30627=ORIENTED_EDGE ( 'NONE', *, *, #240057, .F. ) ;
#30649=CARTESIAN_POINT ( 'NONE',  ( -21.05000000000000426, 75.98514436511895553, -176.3674665265674832 ) ) ;
#30686=CARTESIAN_POINT ( 'NONE',  ( 20.94999999999999929, 64.35000000001218723, -143.3069731475025037 ) ) ;
#30688=EDGE_CURVE ( 'NONE', #149398, #26287, #114931, .T. ) ;
#30691=DIRECTION ( 'NONE',  ( 0.000000000000000000, 0.4999999999999088507, 0.8660254037844913322 ) ) ;
#30743=VECTOR ( 'NONE', #9323, 1000.000000000000000 ) ;
#30780=ORIENTED_EDGE ( 'NONE', *, *, #18135, .T. ) ;
#30788=AXIS2_PLACEMENT_3D ( 'NONE', #798, #178215, #39994 ) ;
#30840=ORIENTED_EDGE ( 'NONE', *, *, #60059, .F. ) ;
#30871=EDGE_CURVE ( 'NONE', #18809, #134102, #179610, .T. ) ;
#30878=CARTESIAN_POINT ( 'NONE',  ( -21.55000000000000426, 68.25000000001230660, -157.6731074845243938 ) ) ;
#30915=DIRECTION ( 'NONE',  ( -1.000000000000000000, 1.836970198721029934E-16, 1.282749433769087582E-30 ) ) ;
#30943=CARTESIAN_POINT ( 'NONE',  ( -20.94999999999999929, 70.10000000001235776, -159.8040077198679683 ) ) ;
#30968=ORIENTED_EDGE ( 'NONE', *, *, #211222, .T. ) ;
#30979=VERTEX_POINT ( 'NONE', #243407 ) ;
#30980=TOROIDAL_SURFACE ( 'NONE', #222459, 0.2000000000000000111, 0.1000000000000000056 ) ;
#31004=VECTOR ( 'NONE', #105126, 1000.000000000000000 ) ;
#31030=CIRCLE ( 'NONE', #93337, 0.09999999999998898659 ) ;
#31054=AXIS2_PLACEMENT_3D ( 'NONE', #108893, #106307, #47619 ) ;
#31059=FACE_OUTER_BOUND ( 'NONE', #217899, .T. ) ;
#31074=LINE ( 'NONE', #110566, #162507 ) ;
#31087=FACE_OUTER_BOUND ( 'NONE', #117822, .T. ) ;
#31092=CARTESIAN_POINT ( 'NONE',  ( 20.51284917709620359, 65.68911337716701837, -162.3506342989327038 ) ) ;
#31098=LINE ( 'NONE', #110588, #252187 ) ;
#31104=DIRECTION ( 'NONE',  ( 0.000000000000000000, -1.000000000000000000, -6.982962677686265922E-15 ) ) ;
#31110=EDGE_CURVE ( 'NONE', #121929, #243465, #101280, .T. ) ;
#31168=LINE ( 'NONE', #71562, #149492 ) ;
#31214=DIRECTION ( 'NONE',  ( -1.000000000000000000, 0.000000000000000000, 0.000000000000000000 ) ) ;
#31218=CARTESIAN_POINT ( 'NONE',  ( 20.94999999999999929, 64.35000000001214460, -136.5231074845244166 ) ) ;
#31221=DIRECTION ( 'NONE',  ( -0.7070776581709311559, 4.937903618720164857E-15, -0.7071359030027479786 ) ) ;
#31238=ORIENTED_EDGE ( 'NONE', *, *, #227726, .F. ) ;
#31249=DIRECTION ( 'NONE',  ( -0.4999999999999799050, -6.047423072554995242E-15, 0.8660254037844502539 ) ) ;
#31298=AXIS2_PLACEMENT_3D ( 'NONE', #232616, #210468, #16136 ) ;
#31373=CYLINDRICAL_SURFACE ( 'NONE', #172972, 2.000000000000001776 ) ;
#31374=PLANE ( 'NONE',  #52924 ) ;
#31381=DIRECTION ( 'NONE',  ( 0.000000000000000000, -1.000000000000000000, -6.982962677686265922E-15 ) ) ;
#31391=ORIENTED_EDGE ( 'NONE', *, *, #181548, .T. ) ;
#31406=ORIENTED_EDGE ( 'NONE', *, *, #235106, .T. ) ;
#31413=AXIS2_PLACEMENT_3D ( 'NONE', #146385, #241654, #63009 ) ;
#31433=DIRECTION ( 'NONE',  ( 0.000000000000000000, -0.008583690987162452199, -0.9999631594459053030 ) ) ;
#31445=VECTOR ( 'NONE', #121897, 1000.000000000000000 ) ;
#31446=CARTESIAN_POINT ( 'NONE',  ( 21.08035267497491105, 69.66829316022936780, -170.1057961093005417 ) ) ;
#31454=EDGE_CURVE ( 'NONE', #79646, #68928, #60712, .T. ) ;
#31476=EDGE_CURVE ( 'NONE', #156062, #91225, #187634, .T. ) ;
#31480=ORIENTED_EDGE ( 'NONE', *, *, #222878, .F. ) ;
#31517=ORIENTED_EDGE ( 'NONE', *, *, #73263, .T. ) ;
#31540=CARTESIAN_POINT ( 'NONE',  ( 22.39999999999999503, 76.10085836911117951, -181.7726746080137445 ) ) ;
#31545=ORIENTED_EDGE ( 'NONE', *, *, #205034, .T. ) ;
#31575=AXIS2_PLACEMENT_3D ( 'NONE', #131925, #211464, #210193 ) ;
#31586=DIRECTION ( 'NONE',  ( -1.000000000000000000, 0.000000000000000000, -0.000000000000000000 ) ) ;
#31616=DIRECTION ( 'NONE',  ( 0.000000000000000000, -0.7397360091702647189, -0.6728971962616949742 ) ) ;
#31634=CARTESIAN_POINT ( 'NONE',  ( 20.94999999999999929, 76.00000000001213607, -136.5231074845243313 ) ) ;
#31671=VERTEX_POINT ( 'NONE', #154935 ) ;
#31687=VECTOR ( 'NONE', #7506, 999.9999999999998863 ) ;
#31697=CARTESIAN_POINT ( 'NONE',  ( -20.94999999999999929, 76.00000000001232081, -162.1231074845243540 ) ) ;
#31714=ORIENTED_EDGE ( 'NONE', *, *, #184789, .T. ) ;
#31716=AXIS2_PLACEMENT_3D ( 'NONE', #208206, #187358, #247303 ) ;
#31718=DIRECTION ( 'NONE',  ( -7.304098846218134667E-16, 1.000000000000000000, 6.982962677686267499E-15 ) ) ;
#31744=DIRECTION ( 'NONE',  ( 1.000000000000000000, 0.000000000000000000, 0.000000000000000000 ) ) ;
#31771=DIRECTION ( 'NONE',  ( 0.000000000000000000, 0.000000000000000000, 1.000000000000000000 ) ) ;
#31809=AXIS2_PLACEMENT_3D ( 'NONE', #17050, #194412, #174878 ) ;
#31816=EDGE_CURVE ( 'NONE', #11624, #33291, #101835, .T. ) ;
#31818=CARTESIAN_POINT ( 'NONE',  ( -20.94999999999999929, 77.83534155023670564, -158.4679561919613491 ) ) ;
#31834=FACE_OUTER_BOUND ( 'NONE', #69869, .T. ) ;
#31839=EDGE_CURVE ( 'NONE', #240428, #33310, #185258, .T. ) ;
#31842=EDGE_CURVE ( 'NONE', #224923, #15592, #72854, .T. ) ;
#31847=ADVANCED_FACE ( 'NONE', ( #47452 ), #190873, .T. ) ;
#31864=CARTESIAN_POINT ( 'NONE',  ( 18.60000000000000142, 85.48068669529106955, -129.5819923157664562 ) ) ;
#31866=CARTESIAN_POINT ( 'NONE',  ( 23.14999999999999503, 69.35000000001228670, -157.7731074845243882 ) ) ;
#31876=VECTOR ( 'NONE', #190808, 1000.000000000000000 ) ;
#31878=CIRCLE ( 'NONE', #244212, 0.09999999999998898659 ) ;
#31899=CARTESIAN_POINT ( 'NONE',  ( -20.94999999999999929, 76.00000000001210765, -132.4231074845243370 ) ) ;
#31922=VERTEX_POINT ( 'NONE', #171332 ) ;
#31927=AXIS2_PLACEMENT_3D ( 'NONE', #180671, #103665, #222324 ) ;
#32004=DIRECTION ( 'NONE',  ( -1.000000000000000000, 0.000000000000000000, -0.000000000000000000 ) ) ;
#32011=EDGE_LOOP ( 'NONE', ( #179614, #108765, #81943, #150978 ) ) ;
#32024=ORIENTED_EDGE ( 'NONE', *, *, #83321, .T. ) ;
#32031=CARTESIAN_POINT ( 'NONE',  ( 23.15000000000000213, 84.66355140188147743, -160.4990063664569959 ) ) ;
#32049=CIRCLE ( 'NONE', #48771, 0.2000000000000057288 ) ;
#32091=ADVANCED_FACE ( 'NONE', ( #64172 ), #182858, .F. ) ;
#32115=EDGE_CURVE ( 'NONE', #218493, #108252, #135341, .T. ) ;
#32126=CARTESIAN_POINT ( 'NONE',  ( -20.93302460841142931, 65.68434038414380893, -130.9866880726065972 ) ) ;
#32140=ORIENTED_EDGE ( 'NONE', *, *, #126671, .F. ) ;
#32141=EDGE_CURVE ( 'NONE', #80942, #237795, #206289, .T. ) ;
#32158=EDGE_LOOP ( 'NONE', ( #87706, #182677, #245665, #59628 ) ) ;
#32180=EDGE_LOOP ( 'NONE', ( #189978, #55874, #171321, #197014 ) ) ;
#32188=DIRECTION ( 'NONE',  ( 0.000000000000000000, 6.982962677686266711E-15, -1.000000000000000000 ) ) ;
#32203=DIRECTION ( 'NONE',  ( 1.000000000000000000, 0.000000000000000000, 0.000000000000000000 ) ) ;
#32286=CARTESIAN_POINT ( 'NONE',  ( -23.15000000000000213, 74.07476635515241981, -149.2533510176504876 ) ) ;
#32291=AXIS2_PLACEMENT_3D ( 'NONE', #107890, #85721, #226529 ) ;
#32321=ORIENTED_EDGE ( 'NONE', *, *, #148904, .F. ) ;
#32337=ADVANCED_FACE ( 'NONE', ( #13191 ), #235486, .F. ) ;
#32351=DIRECTION ( 'NONE',  ( 0.000000000000000000, -1.000000000000000000, -6.982962677686266711E-15 ) ) ;
#32355=ADVANCED_FACE ( 'NONE', ( #34066 ), #216509, .F. ) ;
#32377=CARTESIAN_POINT ( 'NONE',  ( -20.94999999999999929, 77.36087058720436005, -161.9501095574333931 ) ) ;
#32388=CARTESIAN_POINT ( 'NONE',  ( -21.07016717456945898, 69.67905916191212157, -170.0231074845244450 ) ) ;
#32393=DIRECTION ( 'NONE',  ( 1.000000000000000000, 0.000000000000000000, 0.000000000000000000 ) ) ;
#32395=DIRECTION ( 'NONE',  ( 2.694716079187273439E-16, 1.000000000000000000, 6.467318590049456648E-15 ) ) ;
#32446=DIRECTION ( 'NONE',  ( 0.000000000000000000, 1.000000000000000000, 7.116814260417668513E-15 ) ) ;
#32480=CARTESIAN_POINT ( 'NONE',  ( -21.05000000000000071, 74.75000000001232081, -162.0231074845243597 ) ) ;
#32525=DIRECTION ( 'NONE',  ( -1.000000000000000000, 0.000000000000000000, 0.000000000000000000 ) ) ;
#32548=ADVANCED_FACE ( 'NONE', ( #241229, #159136 ), #20909, .T. ) ;
#32567=ORIENTED_EDGE ( 'NONE', *, *, #209381, .T. ) ;
#32585=ORIENTED_EDGE ( 'NONE', *, *, #224730, .F. ) ;
#32603=ORIENTED_EDGE ( 'NONE', *, *, #153041, .T. ) ;
#32618=APPLICATION_CONTEXT ( 'automotive_design' ) ;
#32619=ORIENTED_EDGE ( 'NONE', *, *, #200063, .F. ) ;
#32647=CARTESIAN_POINT ( 'NONE',  ( -20.64999999999999858, 76.00000000001215028, -138.4231074845243654 ) ) ;
#32702=DIRECTION ( 'NONE',  ( 0.000000000000000000, 0.000000000000000000, 1.000000000000000000 ) ) ;
#32736=CARTESIAN_POINT ( 'NONE',  ( 21.13498764882293557, 69.50438185653851519, -170.0247638792557439 ) ) ;
#32739=( BOUNDED_SURFACE ( )  B_SPLINE_SURFACE ( 3, 2, ( 
 ( #10875, #171278, #167399 ),
 ( #152985, #249492, #89115 ),
 ( #129537, #111256, #250753 ),
 ( #151698, #9573, #209068 ) ),
 .UNSPECIFIED., .F., .F., .F. ) 
 B_SPLINE_SURFACE_WITH_KNOTS ( ( 4, 4 ),
 ( 3, 3 ),
 ( 0.04058434257139476031, 0.04256401539001599538 ),
 ( 0.000000000000000000, 1.000000000000000000 ),
 .UNSPECIFIED. ) 
 GEOMETRIC_REPRESENTATION_ITEM ( )  RATIONAL_B_SPLINE_SURFACE ( (
 ( 1.000000000000000000, 0.7103081912007810361, 1.000000000000000000),
 ( 1.000000000000000000, 0.7104998333556836743, 1.000000000000000000),
 ( 1.000000000000000000, 0.7107238315753999780, 1.000000000000000000),
 ( 1.000000000000000000, 0.7110073749539779220, 1.000000000000000000) ) ) 
 REPRESENTATION_ITEM ( '' )  SURFACE ( )  );
#32741=FACE_OUTER_BOUND ( 'NONE', #48059, .T. ) ;
#32742=FACE_OUTER_BOUND ( 'NONE', #52029, .T. ) ;
#32797=EDGE_CURVE ( 'NONE', #72750, #215500, #157556, .T. ) ;
#32800=ADVANCED_FACE ( 'NONE', ( #177105 ), #154973, .F. ) ;
#32811=ORIENTED_EDGE ( 'NONE', *, *, #234867, .F. ) ;
#32813=DIRECTION ( 'NONE',  ( 0.000000000000000000, 0.000000000000000000, 1.000000000000000000 ) ) ;
#32819=AXIS2_PLACEMENT_3D ( 'NONE', #3717, #203204, #162820 ) ;
#32835=VECTOR ( 'NONE', #28043, 1000.000000000000000 ) ;
#32869=CARTESIAN_POINT ( 'NONE',  ( 21.05000000000000071, 87.65000000001236913, -170.0231074845242745 ) ) ;
#32872=EDGE_CURVE ( 'NONE', #206239, #114885, #19208, .T. ) ;
#32922=CARTESIAN_POINT ( 'NONE',  ( 18.49351773456780634, 85.44302569515740231, -162.8377819584964925 ) ) ;
#32960=ADVANCED_FACE ( 'NONE', ( #20586 ), #83062, .F. ) ;
#32975=CARTESIAN_POINT ( 'NONE',  ( -18.59999999999999787, 64.35000000001234355, -163.0083017138704236 ) ) ;
#32977=DIRECTION ( 'NONE',  ( 1.000000000000000000, 0.000000000000000000, 0.000000000000000000 ) ) ;
#32996=EDGE_LOOP ( 'NONE', ( #90338, #98333, #248315, #124029, #150007 ) ) ;
#33000=EDGE_CURVE ( 'NONE', #148346, #102268, #235676, .T. ) ;
#33045=EDGE_LOOP ( 'NONE', ( #39842, #12903, #251442 ) ) ;
#33061=DIRECTION ( 'NONE',  ( -0.000000000000000000, 0.1298341882519735979, 0.9915357197604890427 ) ) ;
#33085=CARTESIAN_POINT ( 'NONE',  ( -21.05000000000000071, 64.35000000001238618, -169.9231074845244507 ) ) ;
#33088=VERTEX_POINT ( 'NONE', #226440 ) ;
#33110=VECTOR ( 'NONE', #58903, 1000.000000000000000 ) ;
#33131=DIRECTION ( 'NONE',  ( 0.000000000000000000, 6.982962677686266711E-15, -1.000000000000000000 ) ) ;
#33139=DIRECTION ( 'NONE',  ( 2.952720810173289112E-16, 1.000000000000000000, -6.088138035986627436E-46 ) ) ;
#33200=AXIS2_PLACEMENT_3D ( 'NONE', #164396, #65285, #30043 ) ;
#33207=PLANE ( 'NONE',  #228233 ) ;
#33214=ORIENTED_EDGE ( 'NONE', *, *, #179433, .F. ) ;
#33235=CARTESIAN_POINT ( 'NONE',  ( -21.04999999999999716, 75.90156250001244587, -176.3223383946112222 ) ) ;
#33237=ORIENTED_EDGE ( 'NONE', *, *, #208854, .F. ) ;
#33270=AXIS2_PLACEMENT_3D ( 'NONE', #256163, #20201, #42322 ) ;
#33284=ORIENTED_EDGE ( 'NONE', *, *, #130906, .T. ) ;
#33291=VERTEX_POINT ( 'NONE', #161066 ) ;
#33310=VERTEX_POINT ( 'NONE', #99766 ) ;
#33344=CARTESIAN_POINT ( 'NONE',  ( 20.94999999999999929, 84.73084112150763758, -160.4250327655399531 ) ) ;
#33346=DIRECTION ( 'NONE',  ( 1.000000000000000000, 0.000000000000000000, 0.000000000000000000 ) ) ;
#33348=EDGE_LOOP ( 'NONE', ( #168859, #212454, #151844, #71290 ) ) ;
#33349=DIRECTION ( 'NONE',  ( 0.000000000000000000, -1.000000000000000000, 0.000000000000000000 ) ) ;
#33384=( LENGTH_UNIT ( ) NAMED_UNIT ( * ) SI_UNIT ( .MILLI., .METRE. ) );
#33387=CIRCLE ( 'NONE', #241638, 0.09999999999999938105 ) ;
#33393=DIRECTION ( 'NONE',  ( 1.000000000000000000, 0.000000000000000000, 0.000000000000000000 ) ) ;
#33395=CARTESIAN_POINT ( 'NONE',  ( 23.14999999999998437, 76.00000000001237765, -170.0231074845243597 ) ) ;
#33396=VECTOR ( 'NONE', #69213, 1000.000000000000000 ) ;
#33436=CARTESIAN_POINT ( 'NONE',  ( -18.50000000000000000, 64.35000000001222986, -148.6731074845244507 ) ) ;
#33439=LINE ( 'NONE', #12574, #72584 ) ;
#33450=EDGE_CURVE ( 'NONE', #200975, #206663, #252790, .T. ) ;
#33537=CARTESIAN_POINT ( 'NONE',  ( 23.14999999999998437, 76.00000000001237765, -170.0231074845243597 ) ) ;
#33604=EDGE_LOOP ( 'NONE', ( #140236, #28100, #56123, #139503 ) ) ;
#33610=DIRECTION ( 'NONE',  ( 1.000000000000000000, 0.000000000000000000, 0.000000000000000000 ) ) ;
#33618=DIRECTION ( 'NONE',  ( 0.7070776581709139474, 0.7071359030027652981, 2.946958787807621248E-14 ) ) ;
#33633=LINE ( 'NONE', #150966, #114295 ) ;
#33635=ADVANCED_FACE ( 'NONE', ( #242532 ), #160465, .F. ) ;
#33687=CIRCLE ( 'NONE', #37756, 0.09999999999998802902 ) ;
#33689=DIRECTION ( 'NONE',  ( -3.265361837132813093E-16, -1.000000000000000000, 7.445645354460596589E-46 ) ) ;
#33692=ORIENTED_EDGE ( 'NONE', *, *, #90601, .F. ) ;
#33735=CIRCLE ( 'NONE', #212762, 0.09999999999998898659 ) ;
#33830=AXIS2_PLACEMENT_3D ( 'NONE', #34377, #70938, #112605 ) ;
#33831=AXIS2_PLACEMENT_3D ( 'NONE', #248559, #84290, #28271 ) ;
#33883=AXIS2_PLACEMENT_3D ( 'NONE', #216412, #37806, #117320 ) ;
#33913=ORIENTED_EDGE ( 'NONE', *, *, #143408, .F. ) ;
#33953=DIRECTION ( 'NONE',  ( 0.000000000000000000, -7.056502275159890832E-15, 1.000000000000000000 ) ) ;
#33968=ORIENTED_EDGE ( 'NONE', *, *, #225089, .T. ) ;
#33981=AXIS2_PLACEMENT_3D ( 'NONE', #116094, #75691, #56081 ) ;
#34009=CARTESIAN_POINT ( 'NONE',  ( 21.14999999999999858, 64.35000000001228670, -157.8731074845244393 ) ) ;
#34027=EDGE_CURVE ( 'NONE', #81561, #184336, #139244, .T. ) ;
#34028=ORIENTED_EDGE ( 'NONE', *, *, #85426, .F. ) ;
#34048=AXIS2_PLACEMENT_3D ( 'NONE', #185333, #6686, #86198 ) ;
#34066=FACE_OUTER_BOUND ( 'NONE', #142176, .T. ) ;
#34074=VERTEX_POINT ( 'NONE', #182262 ) ;
#34122=CARTESIAN_POINT ( 'NONE',  ( -18.39999999999999858, 85.40000000001246860, -181.7731074845243029 ) ) ;
#34123=ORIENTED_EDGE ( 'NONE', *, *, #189256, .F. ) ;
#34128=EDGE_CURVE ( 'NONE', #240571, #78383, #7274, .T. ) ;
#34139=DIRECTION ( 'NONE',  ( 1.836970198721029934E-16, 1.000000000000000000, 6.982962677686266711E-15 ) ) ;
#34153=AXIS2_PLACEMENT_3D ( 'NONE', #115150, #95578, #175171 ) ;
#34175=ORIENTED_EDGE ( 'NONE', *, *, #138454, .T. ) ;
#34190=DIRECTION ( 'NONE',  ( -1.000000000000000000, 0.000000000000000000, -0.000000000000000000 ) ) ;
#34191=ORIENTED_EDGE ( 'NONE', *, *, #33000, .T. ) ;
#34194=CARTESIAN_POINT ( 'NONE',  ( 18.49713797159848738, 85.44648232759141138, -162.9516493629143952 ) ) ;
#34201=DIRECTION ( 'NONE',  ( -0.7071067811865475727, 0.7071067811865475727, 4.937700262164531476E-15 ) ) ;
#34206=CARTESIAN_POINT ( 'NONE',  ( -20.15000000000000568, 66.70857864377492774, -148.7731074845244166 ) ) ;
#34224=CIRCLE ( 'NONE', #130022, 4.299999999999970512 ) ;
#34228=VERTEX_POINT ( 'NONE', #49152 ) ;
#34243=PLANE ( 'NONE',  #123497 ) ;
#34250=DIRECTION ( 'NONE',  ( 0.000000000000000000, 0.000000000000000000, 1.000000000000000000 ) ) ;
#34263=ADVANCED_FACE ( 'NONE', ( #66152, #193806 ), #196358, .T. ) ;
#34290=CIRCLE ( 'NONE', #21795, 0.09999999999998898659 ) ;
#34314=DIRECTION ( 'NONE',  ( -1.000000000000000000, 1.875376730785737719E-16, 1.309568571767809260E-30 ) ) ;
#34322=CARTESIAN_POINT ( 'NONE',  ( 21.05000000000000071, 65.27628289530480288, -162.3581939154368285 ) ) ;
#34344=AXIS2_PLACEMENT_3D ( 'NONE', #191323, #12675, #92178 ) ;
#34349=CARTESIAN_POINT ( 'NONE',  ( -18.41809261886928439, 85.68240331476874871, -129.8662639344331637 ) ) ;
#34351=LINE ( 'NONE', #77286, #218918 ) ;
#34354=DIRECTION ( 'NONE',  ( 0.000000000000000000, 0.000000000000000000, -1.000000000000000000 ) ) ;
#34370=CARTESIAN_POINT ( 'NONE',  ( -21.55000000000000071, 68.75000000001230660, -157.6731074845243938 ) ) ;
#34377=CARTESIAN_POINT ( 'NONE',  ( -20.54999999999999716, 76.00000000001237765, -170.0231074845243597 ) ) ;
#34400=VECTOR ( 'NONE', #107682, 1000.000000000000000 ) ;
#34403=DIRECTION ( 'NONE',  ( -1.000000000000000000, -0.000000000000000000, -0.000000000000000000 ) ) ;
#34416=DIRECTION ( 'NONE',  ( -1.000000000000000000, 3.265361837132813093E-16, 2.280189983783949500E-30 ) ) ;
#34450=CARTESIAN_POINT ( 'NONE',  ( -20.64999999999999858, 85.50000000001222134, -146.4170766071767389 ) ) ;
#34464=EDGE_CURVE ( 'NONE', #161528, #92616, #9301, .T. ) ;
#34467=FACE_OUTER_BOUND ( 'NONE', #166365, .T. ) ;
#34474=LINE ( 'NONE', #91847, #217860 ) ;
#34490=CARTESIAN_POINT ( 'NONE',  ( 21.00000000000000000, 66.25000000001229239, -157.7731074845244166 ) ) ;
#34503=EDGE_CURVE ( 'NONE', #128659, #64025, #113824, .T. ) ;
#34504=CYLINDRICAL_SURFACE ( 'NONE', #17714, 0.09999999999998898659 ) ;
#34506=VERTEX_POINT ( 'NONE', #173858 ) ;
#34557=ORIENTED_EDGE ( 'NONE', *, *, #117332, .T. ) ;
#34564=DIRECTION ( 'NONE',  ( 0.000000000000000000, 0.9908441862701420355, 0.1350103645453197554 ) ) ;
#34589=DIRECTION ( 'NONE',  ( -0.000000000000000000, 0.9876197685951241256, 0.1568667991644932258 ) ) ;
#34595=CARTESIAN_POINT ( 'NONE',  ( -22.50000000000000000, 64.35042919246758686, -170.1231074845244393 ) ) ;
#34616=ADVANCED_FACE ( 'NONE', ( #242747 ), #144925, .F. ) ;
#34624=VECTOR ( 'NONE', #213993, 1000.000000000000000 ) ;
#34647=ORIENTED_EDGE ( 'NONE', *, *, #99840, .T. ) ;
#34661=CARTESIAN_POINT ( 'NONE',  ( -18.41799967126743454, 85.50000000001233502, -162.9910376712692539 ) ) ;
#34679=ORIENTED_EDGE ( 'NONE', *, *, #53523, .T. ) ;
#34704=ORIENTED_EDGE ( 'NONE', *, *, #231874, .T. ) ;
#34712=ADVANCED_FACE ( 'NONE', ( #181998 ), #145419, .T. ) ;
#34774=EDGE_LOOP ( 'NONE', ( #103044, #177176, #191614, #76452, #139880, #41186 ) ) ;
#34781=ORIENTED_EDGE ( 'NONE', *, *, #138256, .F. ) ;
#34800=EDGE_CURVE ( 'NONE', #198367, #149398, #51432, .T. ) ;
#34808=PLANE ( 'NONE',  #186208 ) ;
#34820=ORIENTED_EDGE ( 'NONE', *, *, #29979, .T. ) ;
#34864=ORIENTED_EDGE ( 'NONE', *, *, #157193, .T. ) ;
#34909=EDGE_CURVE ( 'NONE', #59389, #5863, #135013, .T. ) ;
#34919=CARTESIAN_POINT ( 'NONE',  ( -23.25000000000000000, 87.75000000001216449, -139.6231074845242688 ) ) ;
#34932=DIRECTION ( 'NONE',  ( 0.000000000000000000, 1.000000000000000000, 6.982962677686266711E-15 ) ) ;
#34952=VECTOR ( 'NONE', #90149, 1000.000000000000000 ) ;
#34961=CARTESIAN_POINT ( 'NONE',  ( -23.25000000000000000, 76.00000000001237765, -170.0231074845243597 ) ) ;
#34964=ORIENTED_EDGE ( 'NONE', *, *, #109336, .T. ) ;
#34982=CARTESIAN_POINT ( 'NONE',  ( 21.05000000000000071, 76.00000000001213607, -136.5231074845243313 ) ) ;
#35006=ORIENTED_EDGE ( 'NONE', *, *, #198245, .F. ) ;
#35018=PRODUCT_DEFINITION_CONTEXT ( 'detailed design', #32618, 'design' ) ;
#35057=EDGE_CURVE ( 'NONE', #64025, #138313, #38336, .T. ) ;
#35075=ORIENTED_EDGE ( 'NONE', *, *, #65539, .F. ) ;
#35089=ADVANCED_FACE ( 'NONE', ( #202531 ), #182984, .F. ) ;
#35105=AXIS2_PLACEMENT_3D ( 'NONE', #97861, #172349, #251830 ) ;
#35115=DIRECTION ( 'NONE',  ( -1.000000000000000000, -0.000000000000000000, -0.000000000000000000 ) ) ;
#35129=DIRECTION ( 'NONE',  ( 0.000000000000000000, 7.147358527629766941E-15, -1.000000000000000000 ) ) ;
#35138=DIRECTION ( 'NONE',  ( 0.000000000000000000, 1.000000000000000000, 0.000000000000000000 ) ) ;
#35189=FACE_OUTER_BOUND ( 'NONE', #110256, .T. ) ;
#35201=EDGE_CURVE ( 'NONE', #52101, #5474, #147700, .T. ) ;
#35219=EDGE_CURVE ( 'NONE', #56292, #16105, #90267, .T. ) ;
#35222=DIRECTION ( 'NONE',  ( -1.000000000000000000, 0.000000000000000000, -0.000000000000000000 ) ) ;
#35226=CARTESIAN_POINT ( 'NONE',  ( 20.94999999999999929, 76.00000000001215028, -138.4231074845243654 ) ) ;
#35243=FACE_OUTER_BOUND ( 'NONE', #27646, .T. ) ;
#35278=LINE ( 'NONE', #233463, #233547 ) ;
#35281=EDGE_CURVE ( 'NONE', #25616, #75851, #168595, .T. ) ;
#35292=ADVANCED_FACE ( 'NONE', ( #210253 ), #86402, .T. ) ;
#35296=LINE ( 'NONE', #236013, #131010 ) ;
#35297=ADVANCED_FACE ( 'NONE', ( #91576 ), #8199, .T. ) ;
#35312=ADVANCED_FACE ( 'NONE', ( #97964 ), #211527, .T. ) ;
#35313=VERTEX_POINT ( 'NONE', #232393 ) ;
#35328=CARTESIAN_POINT ( 'NONE',  ( 23.15000000000000213, 85.60000000001220144, -146.4170766071767389 ) ) ;
#35339=ORIENTED_EDGE ( 'NONE', *, *, #136519, .F. ) ;
#35350=DIRECTION ( 'NONE',  ( -7.304098846218134667E-16, 1.000000000000000000, 6.982962677686266711E-15 ) ) ;
#35356=EDGE_LOOP ( 'NONE', ( #5990, #210522, #148025, #184212 ) ) ;
#35360=AXIS2_PLACEMENT_3D ( 'NONE', #257963, #241030, #179779 ) ;
#35392=ORIENTED_EDGE ( 'NONE', *, *, #253422, .T. ) ;
#35408=ORIENTED_EDGE ( 'NONE', *, *, #177498, .T. ) ;
#35415=AXIS2_PLACEMENT_3D ( 'NONE', #10329, #29903, #151115 ) ;
#35417=ORIENTED_EDGE ( 'NONE', *, *, #108225, .T. ) ;
#35439=DIRECTION ( 'NONE',  ( -1.000000000000000000, 0.000000000000000000, 0.000000000000000000 ) ) ;
#35441=CARTESIAN_POINT ( 'NONE',  ( -20.64999999999999858, 76.00000000001227818, -157.1481074845243882 ) ) ;
#35444=ORIENTED_EDGE ( 'NONE', *, *, #89907, .F. ) ;
#35450=CARTESIAN_POINT ( 'NONE',  ( -20.85000000000000142, 64.25000000001220712, -143.3069731475025321 ) ) ;
#35465=ORIENTED_EDGE ( 'NONE', *, *, #179990, .F. ) ;
#35470=ORIENTED_EDGE ( 'NONE', *, *, #70609, .F. ) ;
#35485=CARTESIAN_POINT ( 'NONE',  ( 21.05000000000000071, 76.00000000001212186, -134.5231074845243313 ) ) ;
#35491=EDGE_CURVE ( 'NONE', #47348, #74533, #99561, .T. ) ;
#35503=EDGE_CURVE ( 'NONE', #248708, #211242, #139663, .T. ) ;
#35512=( LENGTH_UNIT ( ) NAMED_UNIT ( * ) SI_UNIT ( .MILLI., .METRE. ) );
#35519=AXIS2_PLACEMENT_3D ( 'NONE', #15455, #144332, #2269 ) ;
#35540=DIRECTION ( 'NONE',  ( 0.000000000000000000, 0.8700118002898393765, -0.4930308989875104575 ) ) ;
#35551=DIRECTION ( 'NONE',  ( 1.000000000000000000, 0.000000000000000000, 0.000000000000000000 ) ) ;
#35577=VERTEX_POINT ( 'NONE', #178856 ) ;
#35621=ORIENTED_EDGE ( 'NONE', *, *, #253435, .F. ) ;
#35636=LINE ( 'NONE', #96819, #45047 ) ;
#35637=CARTESIAN_POINT ( 'NONE',  ( 21.30000000000002558, 76.00000000001234923, -165.9731074845243768 ) ) ;
#35642=ORIENTED_EDGE ( 'NONE', *, *, #109336, .F. ) ;
#35659=ORIENTED_EDGE ( 'NONE', *, *, #123115, .T. ) ;
#35679=CARTESIAN_POINT ( 'NONE',  ( 18.59999999999999432, 77.63717271298267519, -158.4409541190523214 ) ) ;
#35692=CARTESIAN_POINT ( 'NONE',  ( -20.54999999999999716, 68.85000000001228670, -157.6731074845243938 ) ) ;
#35705=EDGE_CURVE ( 'NONE', #99016, #180036, #137192, .T. ) ;
#35708=AXIS2_PLACEMENT_3D ( 'NONE', #106965, #147390, #207380 ) ;
#35715=EDGE_LOOP ( 'NONE', ( #94497, #48979, #236396, #180970 ) ) ;
#35730=DIRECTION ( 'NONE',  ( 0.000000000000000000, 0.1350103645451974088, -0.9908441862701587999 ) ) ;
#35750=ORIENTED_EDGE ( 'NONE', *, *, #199789, .T. ) ;
#35754=ORIENTED_EDGE ( 'NONE', *, *, #105723, .F. ) ;
#35763=AXIS2_PLACEMENT_3D ( 'NONE', #251573, #211170, #247725 ) ;
#35789=ORIENTED_EDGE ( 'NONE', *, *, #3260, .T. ) ;
#35820=CARTESIAN_POINT ( 'NONE',  ( -21.14999999893415250, 64.25000000001233502, -163.1786121409978136 ) ) ;
#35821=CARTESIAN_POINT ( 'NONE',  ( 21.05000000000000071, 76.00000000001216449, -140.5231074845243597 ) ) ;
#35857=DIRECTION ( 'NONE',  ( 0.000000000000000000, -0.9998779222360104635, -0.01562499999996343723 ) ) ;
#35864=CARTESIAN_POINT ( 'NONE',  ( -18.59999999999999787, 74.16465844978787914, -158.4679561919613775 ) ) ;
#35878=DIRECTION ( 'NONE',  ( 1.000000000000000000, 0.000000000000000000, 0.000000000000000000 ) ) ;
#35926=DIRECTION ( 'NONE',  ( -1.000000000000000000, 0.000000000000000000, -0.000000000000000000 ) ) ;
#35927=VERTEX_POINT ( 'NONE', #182039 ) ;
#35937=CARTESIAN_POINT ( 'NONE',  ( -21.37071067811865532, 67.92928932189357738, -148.7731074845244166 ) ) ;
#35938=FACE_OUTER_BOUND ( 'NONE', #177327, .T. ) ;
#35941=CIRCLE ( 'NONE', #139951, 0.09999999999998898659 ) ;
#35962=DIRECTION ( 'NONE',  ( -1.000000000000000000, 0.000000000000000000, -0.000000000000000000 ) ) ;
#35972=DIRECTION ( 'NONE',  ( 1.000000000000000000, 0.000000000000000000, 0.000000000000000000 ) ) ;
#35976=VERTEX_POINT ( 'NONE', #25539 ) ;
#36015=CONICAL_SURFACE ( 'NONE', #86034, 4.299999999999970512, 0.7853981633974466137 ) ;
#36020=DIRECTION ( 'NONE',  ( 0.000000000000000000, -0.4999999999999088507, 0.8660254037844913322 ) ) ;
#36022=VECTOR ( 'NONE', #10726, 1000.000000000000114 ) ;
#36027=ADVANCED_FACE ( 'NONE', ( #69808 ), #188447, .F. ) ;
#36067=ORIENTED_EDGE ( 'NONE', *, *, #167222, .T. ) ;
#36080=DIRECTION ( 'NONE',  ( 0.000000000000000000, 6.608470384673536035E-15, -1.000000000000000000 ) ) ;
#36083=CARTESIAN_POINT ( 'NONE',  ( 18.50000000000000000, 85.40000000001232650, -162.7258477248609836 ) ) ;
#36115=TOROIDAL_SURFACE ( 'NONE', #181853, 11.89999999999999858, 0.1000000000000000056 ) ;
#36141=FACE_OUTER_BOUND ( 'NONE', #150933, .T. ) ;
#36142=EDGE_LOOP ( 'NONE', ( #134491, #32585, #68253, #21995 ) ) ;
#36197=ADVANCED_FACE ( 'NONE', ( #179190 ), #187464, .T. ) ;
#36205=VECTOR ( 'NONE', #4256, 1000.000000000000000 ) ;
#36212=VECTOR ( 'NONE', #253887, 1000.000000000000114 ) ;
#36229=DIRECTION ( 'NONE',  ( 0.000000000000000000, -1.000000000000000000, -6.982962677686265922E-15 ) ) ;
#36236=CYLINDRICAL_SURFACE ( 'NONE', #225491, 0.09999999999999939493 ) ;
#36244=FACE_OUTER_BOUND ( 'NONE', #185453, .T. ) ;
#36289=ORIENTED_EDGE ( 'NONE', *, *, #215764, .F. ) ;
#36294=ORIENTED_EDGE ( 'NONE', *, *, #253435, .T. ) ;
#36307=ORIENTED_EDGE ( 'NONE', *, *, #15509, .F. ) ;
#36336=ORIENTED_EDGE ( 'NONE', *, *, #153925, .T. ) ;
#36338=LINE ( 'NONE', #174606, #29815 ) ;
#36372=DIRECTION ( 'NONE',  ( 1.000000000000000000, -0.000000000000000000, 0.000000000000000000 ) ) ;
#36376=VECTOR ( 'NONE', #6594, 1000.000000000000000 ) ;
#36382=CIRCLE ( 'NONE', #82120, 0.09999999999998898659 ) ;
#36395=CARTESIAN_POINT ( 'NONE',  ( -18.59999999999999787, 76.00000000001213607, -136.5231074845243313 ) ) ;
#36433=CARTESIAN_POINT ( 'NONE',  ( -18.50000000000000000, 85.50000000001246292, -181.7731074845243029 ) ) ;
#36434=CARTESIAN_POINT ( 'NONE',  ( 20.95017935633852346, 65.52451072038701341, -162.4456676871339482 ) ) ;
#36443=ORIENTED_EDGE ( 'NONE', *, *, #156858, .F. ) ;
#36458=DIRECTION ( 'NONE',  ( 0.000000000000000000, 1.000000000000000000, 7.116814260417668513E-15 ) ) ;
#36459=ORIENTED_EDGE ( 'NONE', *, *, #216556, .F. ) ;
#36502=CARTESIAN_POINT ( 'NONE',  ( -18.50000000000000000, 66.85000000001245724, -181.7731074845244166 ) ) ;
#36530=CARTESIAN_POINT ( 'NONE',  ( -22.47071067811865319, 76.00000000001237765, -170.0231074845243597 ) ) ;
#36536=CARTESIAN_POINT ( 'NONE',  ( -23.15000000000000213, 76.00000000001212186, -134.4231074845243370 ) ) ;
#36539=AXIS2_PLACEMENT_3D ( 'NONE', #130967, #90541, #72290 ) ;
#36542=CIRCLE ( 'NONE', #78184, 0.09999999999998898659 ) ;
#36609=AXIS2_PLACEMENT_3D ( 'NONE', #75071, #76304, #98404 ) ;
#36614=VERTEX_POINT ( 'NONE', #38085 ) ;
#36616=DIRECTION ( 'NONE',  ( 0.000000000000000000, 0.000000000000000000, -1.000000000000000000 ) ) ;
#36642=VERTEX_POINT ( 'NONE', #234992 ) ;
#36643=CARTESIAN_POINT ( 'NONE',  ( 21.05000000000000071, 75.96513199699931818, -176.2931933482134923 ) ) ;
#36647=EDGE_CURVE ( 'NONE', #248809, #216685, #136990, .T. ) ;
#36674=ORIENTED_EDGE ( 'NONE', *, *, #96406, .T. ) ;
#36689=EDGE_LOOP ( 'NONE', ( #23560, #50621, #253483 ) ) ;
#36693=VECTOR ( 'NONE', #8532, 1000.000000000000000 ) ;
#36712=TOROIDAL_SURFACE ( 'NONE', #140731, 0.2000000000000000111, 0.1000000000000000056 ) ;
#36734=CARTESIAN_POINT ( 'NONE',  ( -23.25000000000000000, 64.25000000001215028, -136.5231074845244166 ) ) ;
#36741=ORIENTED_EDGE ( 'NONE', *, *, #131347, .F. ) ;
#36753=EDGE_CURVE ( 'NONE', #238847, #221268, #141029, .T. ) ;
#36766=DIRECTION ( 'NONE',  ( 0.000000000000000000, 1.000000000000000000, 6.982962677686266711E-15 ) ) ;
#36799=DIRECTION ( 'NONE',  ( -1.000000000000000000, -0.000000000000000000, -0.000000000000000000 ) ) ;
#36832=EDGE_CURVE ( 'NONE', #147377, #230733, #48333, .T. ) ;
#36843=CARTESIAN_POINT ( 'NONE',  ( 23.14999999999999503, 64.35000000001228670, -157.8731074845244393 ) ) ;
#36860=EDGE_CURVE ( 'NONE', #166025, #49789, #66622, .T. ) ;
#36875=CARTESIAN_POINT ( 'NONE',  ( 18.59999999999999076, 65.75000000001222134, -145.2731074845244450 ) ) ;
#36916=AXIS2_PLACEMENT_3D ( 'NONE', #138362, #39311, #215347 ) ;
#36928=AXIS2_PLACEMENT_3D ( 'NONE', #216741, #194653, #219310 ) ;
#36966=ORIENTED_EDGE ( 'NONE', *, *, #96761, .T. ) ;
#36979=ORIENTED_EDGE ( 'NONE', *, *, #87933, .F. ) ;
#37058=AXIS2_PLACEMENT_3D ( 'NONE', #219010, #134328, #178644 ) ;
#37061=DIRECTION ( 'NONE',  ( -1.000000000000000000, -0.000000000000000000, -0.000000000000000000 ) ) ;
#37096=DIRECTION ( 'NONE',  ( -0.000000000000000000, 0.1350103645451945777, -0.9908441862701590219 ) ) ;
#37132=SPHERICAL_SURFACE ( 'NONE', #205244, 0.1000000000000000056 ) ;
#37148=FACE_OUTER_BOUND ( 'NONE', #83811, .T. ) ;
#37149=ADVANCED_FACE ( 'NONE', ( #5022 ), #203249, .T. ) ;
#37155=DIRECTION ( 'NONE',  ( -1.000000000000000000, -0.000000000000000000, -0.000000000000000000 ) ) ;
#37169=AXIS2_PLACEMENT_3D ( 'NONE', #154238, #233738, #55060 ) ;
#37198=( BOUNDED_SURFACE ( )  B_SPLINE_SURFACE ( 3, 2, ( 
 ( #163305, #242822, #64200 ),
 ( #143722, #25097, #223252 ),
 ( #5472, #85009, #51013 ),
 ( #105860, #65470, #188001 ),
 ( #168483, #91468, #146289 ),
 ( #8085, #185427, #45914 ) ),
 .UNSPECIFIED., .F., .F., .F. ) 
 B_SPLINE_SURFACE_WITH_KNOTS ( ( 4, 2, 4 ),
 ( 3, 3 ),
 ( 0.0001300404313046710908, 0.0003183318589266651835, 0.0005066232865486592490 ),
 ( 0.000000000000000000, 1.000000000000000000 ),
 .UNSPECIFIED. ) 
 GEOMETRIC_REPRESENTATION_ITEM ( )  RATIONAL_B_SPLINE_SURFACE ( (
 ( 1.000000000000000000, 0.7071067811865475727, 1.000000000000000000),
 ( 1.000000000000000000, 0.7625113560553226089, 1.000000000000000000),
 ( 1.000000000000000000, 0.8126073484671799685, 1.000000000000000000),
 ( 1.000000000000000000, 0.8923049332749427576, 1.000000000000000000),
 ( 1.000000000000000000, 0.9231914937756658945, 1.000000000000000000),
 ( 1.000000000000000000, 0.9238795325112945100, 1.000000000000000000) ) ) 
 REPRESENTATION_ITEM ( '' )  SURFACE ( )  );
#37206=LINE ( 'NONE', #217081, #23674 ) ;
#37217=DIRECTION ( 'NONE',  ( -1.000000000000000000, 0.000000000000000000, -0.000000000000000000 ) ) ;
#37220=CARTESIAN_POINT ( 'NONE',  ( 18.49999999999999289, 65.62657994473259748, -145.2573193598993839 ) ) ;
#37238=EDGE_CURVE ( 'NONE', #77194, #55547, #133266, .T. ) ;
#37251=CARTESIAN_POINT ( 'NONE',  ( -20.54999999999999716, 68.85000000001222986, -148.8731074845244109 ) ) ;
#37276=EDGE_CURVE ( 'NONE', #9997, #228810, #31074, .T. ) ;
#37289=CARTESIAN_POINT ( 'NONE',  ( -23.15000000000000213, 76.00000000001213607, -136.5231074845243313 ) ) ;
#37309=EDGE_LOOP ( 'NONE', ( #54924, #70869, #74214, #81340 ) ) ;
#37341=AXIS2_PLACEMENT_3D ( 'NONE', #85280, #125716, #106136 ) ;
#37370=ORIENTED_EDGE ( 'NONE', *, *, #180054, .F. ) ;
#37390=CARTESIAN_POINT ( 'NONE',  ( 18.49999999999999645, 74.27191306321800823, -183.1386724793566145 ) ) ;
#37397=ORIENTED_EDGE ( 'NONE', *, *, #111600, .F. ) ;
#37409=CIRCLE ( 'NONE', #91558, 4.150000000000001243 ) ;
#37423=CARTESIAN_POINT ( 'NONE',  ( -21.46681500598105430, 76.00000000001243450, -176.8806186439499299 ) ) ;
#37471=TOROIDAL_SURFACE ( 'NONE', #66679, 0.2000000000000000111, 0.1000000000000000056 ) ;
#37483=DIRECTION ( 'NONE',  ( -1.000000000000000000, -0.000000000000000000, -0.000000000000000000 ) ) ;
#37504=DIRECTION ( 'NONE',  ( 1.000000000000000000, 0.000000000000000000, 0.000000000000000000 ) ) ;
#37515=DIRECTION ( 'NONE',  ( 0.000000000000000000, -1.000000000000000000, -6.982962677686266711E-15 ) ) ;
#37517=CARTESIAN_POINT ( 'NONE',  ( -20.85000000000000142, 87.75000000001216449, -139.4231074845242802 ) ) ;
#37524=DIRECTION ( 'NONE',  ( 1.000000000000000000, 0.000000000000000000, 0.000000000000000000 ) ) ;
#37529=CIRCLE ( 'NONE', #183264, 2.000000000000001776 ) ;
#37533=EDGE_CURVE ( 'NONE', #111529, #157651, #45776, .T. ) ;
#37544=CARTESIAN_POINT ( 'NONE',  ( -20.94999999999999929, 74.73821383144729680, -161.9366085209788935 ) ) ;
#37581=AXIS2_PLACEMENT_3D ( 'NONE', #42885, #5007, #183685 ) ;
#37604=CARTESIAN_POINT ( 'NONE',  ( 21.14999999999999858, 69.35000000001228670, -157.8731074845244109 ) ) ;
#37638=FACE_OUTER_BOUND ( 'NONE', #154613, .T. ) ;
#37647=CARTESIAN_POINT ( 'NONE',  ( -21.44999999999999929, 68.75000000001230660, -157.6731074845243938 ) ) ;
#37657=CARTESIAN_POINT ( 'NONE',  ( 23.24999999999999289, 64.35000000001228670, -157.8731074845244393 ) ) ;
#37675=CARTESIAN_POINT ( 'NONE',  ( -18.59999999999999787, 64.40000000001234071, -163.0949042542488883 ) ) ;
#37684=ORIENTED_EDGE ( 'NONE', *, *, #243685, .F. ) ;
#37702=DIRECTION ( 'NONE',  ( 1.000000000000000000, 0.000000000000000000, 0.000000000000000000 ) ) ;
#37711=DIRECTION ( 'NONE',  ( 0.000000000000000000, 0.000000000000000000, -1.000000000000000000 ) ) ;
#37722=DIRECTION ( 'NONE',  ( 0.000000000000000000, 0.000000000000000000, 1.000000000000000000 ) ) ;
#37747=ADVANCED_FACE ( 'NONE', ( #215452 ), #66811, .T. ) ;
#37756=AXIS2_PLACEMENT_3D ( 'NONE', #177975, #121851, #198799 ) ;
#37806=DIRECTION ( 'NONE',  ( -1.000000000000000000, 0.000000000000000000, -0.000000000000000000 ) ) ;
#37830=ADVANCED_FACE ( 'NONE', ( #134612 ), #133452, .T. ) ;
#37848=DIRECTION ( 'NONE',  ( -1.000000000000000000, 0.000000000000000000, 0.000000000000000000 ) ) ;
#37866=CARTESIAN_POINT ( 'NONE',  ( -23.15000000000000213, 71.65000000001222702, -148.8731074845244109 ) ) ;
#37876=CARTESIAN_POINT ( 'NONE',  ( -18.52139480978223318, 85.48135884507924231, -162.9985509174052538 ) ) ;
#37884=CARTESIAN_POINT ( 'NONE',  ( 18.50211644919734866, 65.69792220476341527, -131.0335554128461695 ) ) ;
#37924=CARTESIAN_POINT ( 'NONE',  ( -23.15000000000000213, 87.48912529308822172, -139.6231074845242688 ) ) ;
#37948=VECTOR ( 'NONE', #223474, 1000.000000000000000 ) ;
#37955=ORIENTED_EDGE ( 'NONE', *, *, #249904, .F. ) ;
#37964=EDGE_CURVE ( 'NONE', #226867, #111850, #79447, .T. ) ;
#37987=ORIENTED_EDGE ( 'NONE', *, *, #21267, .T. ) ;
#38001=DIRECTION ( 'NONE',  ( 0.000000000000000000, 0.000000000000000000, -1.000000000000000000 ) ) ;
#38003=ORIENTED_EDGE ( 'NONE', *, *, #45296, .F. ) ;
#38005=ORIENTED_EDGE ( 'NONE', *, *, #117332, .F. ) ;
#38049=CARTESIAN_POINT ( 'NONE',  ( 21.05000000000000071, 65.27628289530476025, -157.8731074845244393 ) ) ;
#38055=CIRCLE ( 'NONE', #175430, 0.09999999999998898659 ) ;
#38071=VERTEX_POINT ( 'NONE', #203141 ) ;
#38085=CARTESIAN_POINT ( 'NONE',  ( -20.94999999999999929, 74.26374286841490857, -158.4544551555068779 ) ) ;
#38087=DIRECTION ( 'NONE',  ( 0.7071067811865487940, -4.937700262164522799E-15, 0.7071067811865463515 ) ) ;
#38098=VECTOR ( 'NONE', #152339, 1000.000000000000000 ) ;
#38121=CARTESIAN_POINT ( 'NONE',  ( 18.59999999999999787, 76.00000000001237765, -170.0231074845243597 ) ) ;
#38156=ORIENTED_EDGE ( 'NONE', *, *, #30871, .T. ) ;
#38163=DIRECTION ( 'NONE',  ( 1.000000000000000000, -1.836970198721029934E-16, -1.601412966608202925E-30 ) ) ;
#38176=CIRCLE ( 'NONE', #59529, 0.09999999999999939493 ) ;
#38206=VERTEX_POINT ( 'NONE', #109160 ) ;
#38231=ORIENTED_EDGE ( 'NONE', *, *, #39474, .F. ) ;
#38242=CARTESIAN_POINT ( 'NONE',  ( 18.59999999999999787, 77.73670573947964613, -125.0056848969006182 ) ) ;
#38259=EDGE_LOOP ( 'NONE', ( #61457, #228634, #558, #119293 ) ) ;
#38266=AXIS2_PLACEMENT_3D ( 'NONE', #47738, #183427, #204251 ) ;
#38275=DIRECTION ( 'NONE',  ( -1.000000000000000000, 0.000000000000000000, 0.000000000000000000 ) ) ;
#38291=ORIENTED_EDGE ( 'NONE', *, *, #136408, .T. ) ;
#38301=ORIENTED_EDGE ( 'NONE', *, *, #239591, .T. ) ;
#38331=DIRECTION ( 'NONE',  ( -1.000000000000000000, 0.000000000000000000, -0.000000000000000000 ) ) ;
#38334=EDGE_CURVE ( 'NONE', #105518, #164553, #119915, .T. ) ;
#38336=LINE ( 'NONE', #77423, #74525 ) ;
#38350=CARTESIAN_POINT ( 'NONE',  ( -21.05000000000000071, 77.36087058720436005, -161.9501095574333931 ) ) ;
#38438=SPHERICAL_SURFACE ( 'NONE', #106741, 0.1000000000000000056 ) ;
#38470=CIRCLE ( 'NONE', #225876, 12.87499999999999822 ) ;
#38477=CARTESIAN_POINT ( 'NONE',  ( 18.49999999999999645, 77.13501884592227498, -128.8061306010920362 ) ) ;
#38484=FACE_OUTER_BOUND ( 'NONE', #73972, .T. ) ;
#38488=AXIS2_PLACEMENT_3D ( 'NONE', #217313, #17838, #253886 ) ;
#38516=ORIENTED_EDGE ( 'NONE', *, *, #181576, .T. ) ;
#38531=ORIENTED_EDGE ( 'NONE', *, *, #240435, .T. ) ;
#38555=CARTESIAN_POINT ( 'NONE',  ( 18.59999999999999076, 69.55000000001223270, -148.8731074845244109 ) ) ;
#38594=DIRECTION ( 'NONE',  ( -0.000000000000000000, -6.982962677686266711E-15, 1.000000000000000000 ) ) ;
#38612=ORIENTED_EDGE ( 'NONE', *, *, #186865, .T. ) ;
#38619=VERTEX_POINT ( 'NONE', #119267 ) ;
#38659=CARTESIAN_POINT ( 'NONE',  ( -18.50000000000000000, 68.97833521811203639, -132.6895420826271277 ) ) ;
#38674=ORIENTED_EDGE ( 'NONE', *, *, #174750, .T. ) ;
#38690=AXIS2_PLACEMENT_3D ( 'NONE', #206477, #6984, #12155 ) ;
#38693=ORIENTED_EDGE ( 'NONE', *, *, #131888, .T. ) ;
#38696=CARTESIAN_POINT ( 'NONE',  ( -22.00411653889225505, 75.90096189422567363, -177.2765503521648895 ) ) ;
#38761=EDGE_CURVE ( 'NONE', #123398, #93811, #107407, .T. ) ;
#38804=LINE ( 'NONE', #157494, #74865 ) ;
#38828=EDGE_CURVE ( 'NONE', #168421, #138590, #221926, .T. ) ;
#38833=DIRECTION ( 'NONE',  ( -1.000000000000000000, 0.000000000000000000, -0.000000000000000000 ) ) ;
#38848=AXIS2_PLACEMENT_3D ( 'NONE', #238449, #62385, #141907 ) ;
#38877=DIRECTION ( 'NONE',  ( -1.836970198721029934E-16, -1.000000000000000000, -6.982962677686266711E-15 ) ) ;
#38883=DIRECTION ( 'NONE',  ( 0.000000000000000000, -6.982962677686266711E-15, 1.000000000000000000 ) ) ;
#38894=DIRECTION ( 'NONE',  ( -0.000000000000000000, 1.000000000000000000, 6.982962677686266711E-15 ) ) ;
#38898=CARTESIAN_POINT ( 'NONE',  ( -20.64999999999999858, 74.05981308412442843, -157.1939882734710352 ) ) ;
#38944=EDGE_LOOP ( 'NONE', ( #125206, #228912, #18051, #187040 ) ) ;
#38987=FACE_OUTER_BOUND ( 'NONE', #24150, .T. ) ;
#38988=CARTESIAN_POINT ( 'NONE',  ( 20.95325940946048249, 65.47660992931604085, -162.4586453552843466 ) ) ;
#38997=DIRECTION ( 'NONE',  ( -1.000000000000000000, 0.000000000000000000, 0.000000000000000000 ) ) ;
#39009=ORIENTED_EDGE ( 'NONE', *, *, #248590, .T. ) ;
#39010=DIRECTION ( 'NONE',  ( 0.000000000000000000, -8.326672684688666480E-14, 1.000000000000000000 ) ) ;
#39095=SPHERICAL_SURFACE ( 'NONE', #98727, 0.1000000000000000056 ) ;
#39102=DIRECTION ( 'NONE',  ( 0.000000000000000000, 6.982962677686266711E-15, -1.000000000000000000 ) ) ;
#39120=DIRECTION ( 'NONE',  ( -1.000000000000000000, 2.952720810173289112E-16, 2.061873921506763405E-30 ) ) ;
#39131=EDGE_LOOP ( 'NONE', ( #99596, #85693, #2171, #91464 ) ) ;
#39148=AXIS2_PLACEMENT_3D ( 'NONE', #31818, #12244, #229982 ) ;
#39164=CIRCLE ( 'NONE', #68369, 0.09999999999999939493 ) ;
#39173=CARTESIAN_POINT ( 'NONE',  ( 20.85000000000000142, 64.35000000001214460, -136.5231074845244166 ) ) ;
#39192=B_SPLINE_CURVE_WITH_KNOTS ( 'NONE', 3,
 ( #196223, #56682, #237920, #236628, #18870, #136224, #215774 ),
 .UNSPECIFIED., .F., .F.,
 ( 4, 3, 4 ),
 ( 0.000000000000000000, 3.357501770816500864E-05, 5.199112466352410285E-05 ),
 .UNSPECIFIED. ) ;
#39194=VECTOR ( 'NONE', #106428, 999.9999999999998863 ) ;
#39215=CARTESIAN_POINT ( 'NONE',  ( -21.07928932188134041, 75.90110485435802445, -176.3516241409176644 ) ) ;
#39218=DIRECTION ( 'NONE',  ( 0.000000000000000000, 0.000000000000000000, 1.000000000000000000 ) ) ;
#39221=ORIENTED_EDGE ( 'NONE', *, *, #206222, .T. ) ;
#39225=CYLINDRICAL_SURFACE ( 'NONE', #102671, 0.09999999999999939493 ) ;
#39242=DIRECTION ( 'NONE',  ( -0.000000000000000000, 6.982962677686266711E-15, -1.000000000000000000 ) ) ;
#39253=AXIS2_PLACEMENT_3D ( 'NONE', #39942, #118169, #75215 ) ;
#39276=AXIS2_PLACEMENT_3D ( 'NONE', #86921, #127363, #166518 ) ;
#39293=DIRECTION ( 'NONE',  ( 1.000000000000000000, 0.000000000000000000, 0.000000000000000000 ) ) ;
#39311=DIRECTION ( 'NONE',  ( -0.000000000000000000, 1.000000000000000000, 6.982962677686266711E-15 ) ) ;
#39324=FACE_OUTER_BOUND ( 'NONE', #174555, .T. ) ;
#39358=DIRECTION ( 'NONE',  ( 0.000000000000000000, -6.853228547068871147E-15, 1.000000000000000000 ) ) ;
#39375=EDGE_CURVE ( 'NONE', #23846, #132498, #213949, .T. ) ;
#39426=VERTEX_POINT ( 'NONE', #181205 ) ;
#39433=ORIENTED_EDGE ( 'NONE', *, *, #48980, .T. ) ;
#39450=ADVANCED_FACE ( 'NONE', ( #217721 ), #239885, .T. ) ;
#39474=EDGE_CURVE ( 'NONE', #133516, #236311, #176366, .T. ) ;
#39572=EDGE_LOOP ( 'NONE', ( #237391, #221442, #136934, #59098 ) ) ;
#39600=FACE_OUTER_BOUND ( 'NONE', #2456, .T. ) ;
#39637=CARTESIAN_POINT ( 'NONE',  ( 21.05000000000000071, 65.52661458509942349, -162.4444530202758870 ) ) ;
#39671=ORIENTED_EDGE ( 'NONE', *, *, #181576, .F. ) ;
#39709=DIRECTION ( 'NONE',  ( 0.000000000000000000, 0.1350103645451945777, -0.9908441862701591329 ) ) ;
#39727=FACE_OUTER_BOUND ( 'NONE', #202680, .T. ) ;
#39740=LINE ( 'NONE', #236610, #190070 ) ;
#39742=DIRECTION ( 'NONE',  ( -1.000000000000000000, 1.387778780781454006E-13, 0.000000000000000000 ) ) ;
#39744=DIRECTION ( 'NONE',  ( 0.000000000000000000, -7.056502275159890832E-15, -1.000000000000000000 ) ) ;
#39745=CARTESIAN_POINT ( 'NONE',  ( -18.47653818581421348, 85.46528038777530867, -162.8971466683844653 ) ) ;
#39791=VECTOR ( 'NONE', #119683, 1000.000000000000000 ) ;
#39797=CARTESIAN_POINT ( 'NONE',  ( -23.25000000000000000, 76.00000000001237765, -170.0231074845243597 ) ) ;
#39808=CARTESIAN_POINT ( 'NONE',  ( -18.51555513499511463, 85.35265705451770657, -162.8279375888266998 ) ) ;
#39827=CARTESIAN_POINT ( 'NONE',  ( -21.64999999999999858, 68.65000000001222702, -148.7731074845244166 ) ) ;
#39842=ORIENTED_EDGE ( 'NONE', *, *, #224744, .F. ) ;
#39871=ORIENTED_EDGE ( 'NONE', *, *, #36647, .T. ) ;
#39880=TOROIDAL_SURFACE ( 'NONE', #185602, 0.2000000000000000111, 0.1000000000000000056 ) ;
#39887=VERTEX_POINT ( 'NONE', #115766 ) ;
#39906=ORIENTED_EDGE ( 'NONE', *, *, #185296, .F. ) ;
#39931=ORIENTED_EDGE ( 'NONE', *, *, #466, .T. ) ;
#39934=CARTESIAN_POINT ( 'NONE',  ( -23.15000000000000213, 74.00000000001223555, -149.7477294072864709 ) ) ;
#39942=CARTESIAN_POINT ( 'NONE',  ( 20.85000000000000142, 77.36242903720540198, -128.6342262366031548 ) ) ;
#39974=CARTESIAN_POINT ( 'NONE',  ( -20.64999999999999858, 85.00000000001232081, -160.1291383618718385 ) ) ;
#39994=DIRECTION ( 'NONE',  ( 0.000000000000000000, 0.4999999999999088507, -0.8660254037844913322 ) ) ;
#40041=CARTESIAN_POINT ( 'NONE',  ( -18.59999999999999787, 77.16412189325330928, -128.6082593989527254 ) ) ;
#40059=VERTEX_POINT ( 'NONE', #33085 ) ;
#40086=TOROIDAL_SURFACE ( 'NONE', #144071, 11.70000000000000107, 0.1000000000000000056 ) ;
#40092=ADVANCED_FACE ( 'NONE', ( #235097 ), #80657, .T. ) ;
#40107=CARTESIAN_POINT ( 'NONE',  ( 21.05000000000000071, 67.12338541492522381, -161.6380270056797599 ) ) ;
#40122=LINE ( 'NONE', #199164, #12842 ) ;
#40145=CIRCLE ( 'NONE', #160939, 2.099999999999990763 ) ;
#40151=ORIENTED_EDGE ( 'NONE', *, *, #218569, .F. ) ;
#40164=CARTESIAN_POINT ( 'NONE',  ( -20.94999999999999929, 87.48912529308822172, -139.6231074845242688 ) ) ;
#40192=AXIS2_PLACEMENT_3D ( 'NONE', #70500, #30082, #109573 ) ;
#40203=CARTESIAN_POINT ( 'NONE',  ( 18.54271179734072561, 85.62408429011051680, -129.7821426318235183 ) ) ;
#40216=CARTESIAN_POINT ( 'NONE',  ( -18.50000000000000000, 66.65000000001222702, -148.6731074845244223 ) ) ;
#40258=ADVANCED_FACE ( 'NONE', ( #62867 ), #120319, .F. ) ;
#40266=ORIENTED_EDGE ( 'NONE', *, *, #133347, .F. ) ;
#40280=ORIENTED_EDGE ( 'NONE', *, *, #93623, .T. ) ;
#40289=FACE_OUTER_BOUND ( 'NONE', #102401, .T. ) ;
#40351=VERTEX_POINT ( 'NONE', #147542 ) ;
#40367=CARTESIAN_POINT ( 'NONE',  ( 20.94999999999999929, 71.18691588786271041, -148.4646252410481964 ) ) ;
#40374=AXIS2_PLACEMENT_3D ( 'NONE', #36843, #14707, #115062 ) ;
#40395=DIRECTION ( 'NONE',  ( 0.000000000000000000, -0.4999999999999088507, -0.8660254037844913322 ) ) ;
#40402=CARTESIAN_POINT ( 'NONE',  ( 18.59999999999999076, 69.45000000001222418, -148.7731074845244166 ) ) ;
#40426=LINE ( 'NONE', #234735, #7839 ) ;
#40428=CARTESIAN_POINT ( 'NONE',  ( 23.15000000000000213, 87.65000000001215597, -139.6231074845242688 ) ) ;
#40446=ORIENTED_EDGE ( 'NONE', *, *, #34027, .T. ) ;
#40454=VECTOR ( 'NONE', #175055, 1000.000000000000000 ) ;
#40459=ORIENTED_EDGE ( 'NONE', *, *, #99840, .F. ) ;
#40484=DIRECTION ( 'NONE',  ( 0.000000000000000000, 0.000000000000000000, 1.000000000000000000 ) ) ;
#40491=ORIENTED_EDGE ( 'NONE', *, *, #21743, .T. ) ;
#40500=CARTESIAN_POINT ( 'NONE',  ( 22.50000000000000000, 76.00000000001237765, -170.0231074845243597 ) ) ;
#40513=ORIENTED_EDGE ( 'NONE', *, *, #202771, .T. ) ;
#40514=DIRECTION ( 'NONE',  ( 0.000000000000000000, 0.8700118002898356018, -0.4930308989875170078 ) ) ;
#40522=DIRECTION ( 'NONE',  ( 1.000000000000000000, 0.000000000000000000, 0.000000000000000000 ) ) ;
#40528=EDGE_CURVE ( 'NONE', #47348, #219843, #149245, .T. ) ;
#40551=DIRECTION ( 'NONE',  ( 0.000000000000000000, -6.454785026890489601E-15, 1.000000000000000000 ) ) ;
#40567=ORIENTED_EDGE ( 'NONE', *, *, #114790, .F. ) ;
#40593=EDGE_CURVE ( 'NONE', #171646, #253610, #57629, .T. ) ;
#40596=ORIENTED_EDGE ( 'NONE', *, *, #235228, .T. ) ;
#40634=DIRECTION ( 'NONE',  ( -0.000000000000000000, 6.982962677686266711E-15, -1.000000000000000000 ) ) ;
#40637=EDGE_CURVE ( 'NONE', #240241, #91489, #107518, .T. ) ;
#40653=CARTESIAN_POINT ( 'NONE',  ( 18.59999999999999076, 77.16412189325330928, -128.6082593989527254 ) ) ;
#40658=CARTESIAN_POINT ( 'NONE',  ( 18.49999999999999289, 69.35000000001222986, -148.8731074845244109 ) ) ;
#40675=DIRECTION ( 'NONE',  ( 1.441126678808781001E-14, -0.9876197685951241256, -0.1568667991644932258 ) ) ;
#40690=FACE_OUTER_BOUND ( 'NONE', #54805, .T. ) ;
#40715=DIRECTION ( 'NONE',  ( 1.000000000000000000, -0.000000000000000000, 0.000000000000000000 ) ) ;
#40734=AXIS2_PLACEMENT_3D ( 'NONE', #150994, #55692, #230535 ) ;
#40744=ORIENTED_EDGE ( 'NONE', *, *, #48738, .T. ) ;
#40762=CIRCLE ( 'NONE', #132671, 0.1000000000000028644 ) ;
#40785=LINE ( 'NONE', #120335, #147236 ) ;
#40809=ORIENTED_EDGE ( 'NONE', *, *, #118889, .T. ) ;
#40827=CARTESIAN_POINT ( 'NONE',  ( 21.13461538461538680, 67.11458296203782936, -157.6731074845244223 ) ) ;
#40839=EDGE_CURVE ( 'NONE', #10632, #138584, #170308, .T. ) ;
#40880=CARTESIAN_POINT ( 'NONE',  ( -18.50000324121759121, 65.70692517833255408, -131.0644653378303985 ) ) ;
#40898=ADVANCED_FACE ( 'NONE', ( #153711 ), #253626, .T. ) ;
#40928=SPHERICAL_SURFACE ( 'NONE', #192722, 0.1000000000000000056 ) ;
#40931=VERTEX_POINT ( 'NONE', #96231 ) ;
#40954=CIRCLE ( 'NONE', #78332, 0.1000000000000070832 ) ;
#40963=CARTESIAN_POINT ( 'NONE',  ( -18.50000000000000000, 76.00000000001237765, -170.0231074845243597 ) ) ;
#40978=VECTOR ( 'NONE', #232186, 1000.000000000000000 ) ;
#40987=DIRECTION ( 'NONE',  ( -0.000000000000000000, 7.172728831056617961E-15, -1.000000000000000000 ) ) ;
#41001=AXIS2_PLACEMENT_3D ( 'NONE', #43286, #25026, #4144 ) ;
#41009=VECTOR ( 'NONE', #6175, 1000.000000000000000 ) ;
#41019=DIRECTION ( 'NONE',  ( -0.000000000000000000, 6.982962677686266711E-15, -1.000000000000000000 ) ) ;
#41057=DIRECTION ( 'NONE',  ( -1.000000000000000000, 3.265361837132813093E-16, 2.280189983783949500E-30 ) ) ;
#41073=CARTESIAN_POINT ( 'NONE',  ( 21.14999999999999858, 76.00000000001242029, -176.5637644362255969 ) ) ;
#41093=ADVANCED_FACE ( 'NONE', ( #247292 ), #128751, .T. ) ;
#41143=DIRECTION ( 'NONE',  ( -1.000000000000000000, 0.000000000000000000, 0.000000000000000000 ) ) ;
#41186=ORIENTED_EDGE ( 'NONE', *, *, #105338, .T. ) ;
#41203=ORIENTED_EDGE ( 'NONE', *, *, #40593, .T. ) ;
#41204=DIRECTION ( 'NONE',  ( 0.000000000000000000, 1.000000000000000000, 0.000000000000000000 ) ) ;
#41205=DIRECTION ( 'NONE',  ( 0.000000000000000000, -1.000000000000000000, -6.982962677686265922E-15 ) ) ;
#41236=ORIENTED_EDGE ( 'NONE', *, *, #165081, .F. ) ;
#41244=CARTESIAN_POINT ( 'NONE',  ( 20.94999999999999929, 65.70729864261026876, -131.0657455973724836 ) ) ;
#41249=ORIENTED_EDGE ( 'NONE', *, *, #162743, .F. ) ;
#41267=DIRECTION ( 'NONE',  ( 0.000000000000000000, 0.000000000000000000, -1.000000000000000000 ) ) ;
#41289=CARTESIAN_POINT ( 'NONE',  ( -21.53699400384945051, 76.00000000001243450, -176.8108192777617660 ) ) ;
#41291=AXIS2_PLACEMENT_3D ( 'NONE', #113449, #95171, #173485 ) ;
#41308=VERTEX_POINT ( 'NONE', #197592 ) ;
#41320=EDGE_LOOP ( 'NONE', ( #83838, #109552, #68029, #164983 ) ) ;
#41340=LINE ( 'NONE', #42595, #105730 ) ;
#41342=CARTESIAN_POINT ( 'NONE',  ( -18.59999999999999787, 66.65000000001222702, -148.8731074845244393 ) ) ;
#41379=CARTESIAN_POINT ( 'NONE',  ( 21.05000000000000071, 69.58602111852397343, -169.9373083682504273 ) ) ;
#41388=CARTESIAN_POINT ( 'NONE',  ( 21.05000000000000071, 65.27628289530476025, -157.8731074845244393 ) ) ;
#41394=CYLINDRICAL_SURFACE ( 'NONE', #181166, 12.87499999999999822 ) ;
#41399=CARTESIAN_POINT ( 'NONE',  ( -21.05000000000000071, 76.00000000001237765, -170.0231074845243597 ) ) ;
#41436=EDGE_CURVE ( 'NONE', #133183, #46365, #183112, .T. ) ;
#41458=DIRECTION ( 'NONE',  ( 0.000000000000000000, -7.272083257015735086E-15, 1.000000000000000000 ) ) ;
#41464=CARTESIAN_POINT ( 'NONE',  ( -20.64999999999999858, 73.50000000001223555, -149.7477294072864709 ) ) ;
#41491=CARTESIAN_POINT ( 'NONE',  ( -20.94999999999999929, 76.25610579210459150, -170.0580039261966192 ) ) ;
#41504=DIRECTION ( 'NONE',  ( 0.000000000000000000, 0.000000000000000000, 1.000000000000000000 ) ) ;
#41509=ORIENTED_EDGE ( 'NONE', *, *, #93372, .F. ) ;
#41511=ORIENTED_EDGE ( 'NONE', *, *, #76058, .T. ) ;
#41513=DIRECTION ( 'NONE',  ( 0.000000000000000000, 0.000000000000000000, 1.000000000000000000 ) ) ;
#41519=VECTOR ( 'NONE', #207430, 1000.000000000000114 ) ;
#41524=DIRECTION ( 'NONE',  ( -1.000000000000000000, 0.000000000000000000, 0.000000000000000000 ) ) ;
#41554=ORIENTED_EDGE ( 'NONE', *, *, #19049, .F. ) ;
#41560=CARTESIAN_POINT ( 'NONE',  ( -23.25000000000000000, 76.00000000001237765, -170.0231074845243597 ) ) ;
#41561=DIRECTION ( 'NONE',  ( -0.7071067811865475727, 0.7071067811865475727, 4.937700262164531476E-15 ) ) ;
#41564=CARTESIAN_POINT ( 'NONE',  ( 20.95539060131842746, 65.37613784235668390, -162.3693736708682422 ) ) ;
#41596=DIRECTION ( 'NONE',  ( -7.304098846218134667E-16, 1.000000000000000000, 6.982962677686267499E-15 ) ) ;
#41620=CARTESIAN_POINT ( 'NONE',  ( -18.50000000000000000, 68.97833521811203639, -132.6895420826271277 ) ) ;
#41632=DIRECTION ( 'NONE',  ( -1.000000000000000000, -0.000000000000000000, 0.000000000000000000 ) ) ;
#41651=ADVANCED_FACE ( 'NONE', ( #61322 ), #20938, .F. ) ;
#41656=AXIS2_PLACEMENT_3D ( 'NONE', #222270, #124498, #47500 ) ;
#41699=CARTESIAN_POINT ( 'NONE',  ( -21.44999999999999929, 68.65000000001229807, -157.6731074845243938 ) ) ;
#41713=DIRECTION ( 'NONE',  ( 0.000000000000000000, -6.982962677686266711E-15, 1.000000000000000000 ) ) ;
#41714=TOROIDAL_SURFACE ( 'NONE', #20881, 11.65000000000000036, 0.1000000000000000056 ) ;
#41731=CARTESIAN_POINT ( 'NONE',  ( 18.57399277249656322, 65.66887361445355964, -130.9329845918269370 ) ) ;
#41741=EDGE_CURVE ( 'NONE', #95684, #258015, #102661, .T. ) ;
#41755=LINE ( 'NONE', #104247, #144171 ) ;
#41769=DIRECTION ( 'NONE',  ( 1.000000000000000000, 0.000000000000000000, 0.000000000000000000 ) ) ;
#41775=AXIS2_PLACEMENT_3D ( 'NONE', #254612, #232535, #94270 ) ;
#41814=CARTESIAN_POINT ( 'NONE',  ( 21.05000000000000071, 64.25000000001219291, -143.5379132551784096 ) ) ;
#41815=ORIENTED_EDGE ( 'NONE', *, *, #115717, .T. ) ;
#41889=ORIENTED_EDGE ( 'NONE', *, *, #249074, .T. ) ;
#41902=DIRECTION ( 'NONE',  ( 0.000000000000000000, -6.982962677686266711E-15, 1.000000000000000000 ) ) ;
#41920=CARTESIAN_POINT ( 'NONE',  ( 20.94999999999999929, 67.07338541492521244, -161.5514244653012952 ) ) ;
#41931=DIRECTION ( 'NONE',  ( 0.000000000000000000, -0.9999631594459057471, 0.008583690987121077309 ) ) ;
#41971=DIRECTION ( 'NONE',  ( 1.000000000000000000, 0.000000000000000000, 0.000000000000000000 ) ) ;
#41976=CARTESIAN_POINT ( 'NONE',  ( 23.14999999999999503, 61.90000000001218439, -142.1234050956638271 ) ) ;
#42013=CARTESIAN_POINT ( 'NONE',  ( 20.94999999999999929, 71.00000000001223555, -148.4283735034374843 ) ) ;
#42032=ADVANCED_FACE ( 'NONE', ( #96051 ), #193900, .T. ) ;
#42071=CARTESIAN_POINT ( 'NONE',  ( -20.94999999999999929, 77.13501884592227498, -128.8061306010920362 ) ) ;
#42078=CARTESIAN_POINT ( 'NONE',  ( 20.85000000000000142, 64.25000000001219291, -143.3069731475025321 ) ) ;
#42089=FACE_OUTER_BOUND ( 'NONE', #112702, .T. ) ;
#42105=CARTESIAN_POINT ( 'NONE',  ( 21.05000000000000071, 67.22371710471982453, -157.8731074845244109 ) ) ;
#42114=VECTOR ( 'NONE', #36372, 1000.000000000000000 ) ;
#42137=LINE ( 'NONE', #99493, #36205 ) ;
#42152=EDGE_LOOP ( 'NONE', ( #124855, #237150, #253469, #106676, #135474 ) ) ;
#42182=CARTESIAN_POINT ( 'NONE',  ( 21.05000000000000071, 65.39167043205833352, -162.4314224712280748 ) ) ;
#42228=AXIS2_PLACEMENT_3D ( 'NONE', #164255, #45578, #65129 ) ;
#42231=AXIS2_PLACEMENT_3D ( 'NONE', #165566, #63882, #45607 ) ;
#42255=DIRECTION ( 'NONE',  ( -1.000000000000000000, 0.000000000000000000, 0.000000000000000000 ) ) ;
#42267=ADVANCED_FACE ( 'NONE', ( #8524 ), #88025, .F. ) ;
#42281=EDGE_CURVE ( 'NONE', #38619, #89486, #12235, .T. ) ;
#42322=DIRECTION ( 'NONE',  ( 0.000000000000000000, -6.308085367188367561E-15, 1.000000000000000000 ) ) ;
#42339=DIRECTION ( 'NONE',  ( 0.000000000000000000, 0.8700118002898357128, -0.4930308989875170633 ) ) ;
#42345=AXIS2_PLACEMENT_3D ( 'NONE', #225792, #202404, #147568 ) ;
#42361=ORIENTED_EDGE ( 'NONE', *, *, #9904, .F. ) ;
#42435=VERTEX_POINT ( 'NONE', #67868 ) ;
#42472=CIRCLE ( 'NONE', #154944, 0.4000000000000114575 ) ;
#42481=ADVANCED_FACE ( 'NONE', ( #87424 ), #70811, .F. ) ;
#42486=CARTESIAN_POINT ( 'NONE',  ( -21.05000000000000071, 69.74218538953626023, -170.1208977758331855 ) ) ;
#42492=EDGE_LOOP ( 'NONE', ( #208957, #53599, #94322, #217022 ) ) ;
#42493=DIRECTION ( 'NONE',  ( -1.000000000000000000, -0.000000000000000000, -0.000000000000000000 ) ) ;
#42496=ORIENTED_EDGE ( 'NONE', *, *, #26086, .T. ) ;
#42521=VERTEX_POINT ( 'NONE', #86119 ) ;
#42556=VECTOR ( 'NONE', #123722, 1000.000000000000000 ) ;
#42558=DIRECTION ( 'NONE',  ( 0.000000000000000000, -7.086529944415886769E-15, 1.000000000000000000 ) ) ;
#42565=CARTESIAN_POINT ( 'NONE',  ( 21.00000000000000000, 66.25000000001223555, -148.8731074845244393 ) ) ;
#42595=CARTESIAN_POINT ( 'NONE',  ( -18.39999999999999858, 85.50000000001233502, -163.0238218066854472 ) ) ;
#42631=CARTESIAN_POINT ( 'NONE',  ( 21.04999999999999716, 69.55891531154070151, -170.0053880512155615 ) ) ;
#42644=DIRECTION ( 'NONE',  ( 1.000000000000000000, -0.000000000000000000, 0.000000000000000000 ) ) ;
#42718=DIRECTION ( 'NONE',  ( 0.000000000000000000, 1.000000000000000000, 6.982962677686266711E-15 ) ) ;
#42736=AXIS2_PLACEMENT_3D ( 'NONE', #188396, #89288, #47588 ) ;
#42743=AXIS2_PLACEMENT_3D ( 'NONE', #6166, #85675, #1006 ) ;
#42771=CARTESIAN_POINT ( 'NONE',  ( 22.59999985501178799, 64.25013020700939137, -170.0887061543242567 ) ) ;
#42783=EDGE_LOOP ( 'NONE', ( #193405, #115087, #143187, #186313 ) ) ;
#42809=EDGE_CURVE ( 'NONE', #109875, #138313, #191489, .T. ) ;
#42811=CARTESIAN_POINT ( 'NONE',  ( -21.05000000000000071, 74.73821383144729680, -161.9366085209788935 ) ) ;
#42821=CIRCLE ( 'NONE', #150975, 0.09999999999999939493 ) ;
#42834=DIRECTION ( 'NONE',  ( 5.603264701231745086E-32, 7.172728831056619538E-15, -1.000000000000000000 ) ) ;
#42840=ORIENTED_EDGE ( 'NONE', *, *, #217316, .T. ) ;
#42846=CARTESIAN_POINT ( 'NONE',  ( -20.85000000000000142, 64.35000000001214460, -136.5231074845244166 ) ) ;
#42867=DIRECTION ( 'NONE',  ( 1.000000000000000000, 0.000000000000000000, 0.000000000000000000 ) ) ;
#42885=CARTESIAN_POINT ( 'NONE',  ( -23.15000000000000213, 71.65000000001228386, -157.6731074845243938 ) ) ;
#42893=ORIENTED_EDGE ( 'NONE', *, *, #66187, .T. ) ;
#42916=DIRECTION ( 'NONE',  ( 1.000000000000000000, -0.000000000000000000, 0.000000000000000000 ) ) ;
#42919=DIRECTION ( 'NONE',  ( 0.000000000000000000, -1.000000000000000000, -6.982962677686266711E-15 ) ) ;
#42931=DIRECTION ( 'NONE',  ( 0.000000000000000000, 0.000000000000000000, -1.000000000000000000 ) ) ;
#42970=CARTESIAN_POINT ( 'NONE',  ( -21.14999999999999858, 64.35000000001238618, -169.9231074845244507 ) ) ;
#42977=DIRECTION ( 'NONE',  ( 1.000000000000000000, -0.000000000000000000, 0.000000000000000000 ) ) ;
#43013=ORIENTED_EDGE ( 'NONE', *, *, #91019, .T. ) ;
#43039=CARTESIAN_POINT ( 'NONE',  ( 18.49999999999999645, 74.83729825007431202, -161.9231074845243654 ) ) ;
#43043=DIRECTION ( 'NONE',  ( 1.000000000000000000, 0.000000000000000000, 0.000000000000000000 ) ) ;
#43045=CARTESIAN_POINT ( 'NONE',  ( -18.59999999999999787, 66.85000000001222986, -148.8731074845244393 ) ) ;
#43078=CARTESIAN_POINT ( 'NONE',  ( 20.85000000000000142, 64.25000000001219291, -143.3069731475025321 ) ) ;
#43096=ADVANCED_FACE ( 'NONE', ( #19143 ), #253893, .F. ) ;
#43102=EDGE_LOOP ( 'NONE', ( #33214, #176477, #201205 ) ) ;
#43116=DIRECTION ( 'NONE',  ( 1.000000000000000000, 0.000000000000000000, 0.000000000000000000 ) ) ;
#43120=EDGE_CURVE ( 'NONE', #43685, #127337, #174944, .T. ) ;
#43122=AXIS2_PLACEMENT_3D ( 'NONE', #86389, #107264, #68147 ) ;
#43177=EDGE_CURVE ( 'NONE', #229354, #72750, #37529, .T. ) ;
#43212=CARTESIAN_POINT ( 'NONE',  ( -23.15000000000000213, 76.00000000001213607, -136.5231074845243313 ) ) ;
#43245=FACE_OUTER_BOUND ( 'NONE', #152835, .T. ) ;
#43286=CARTESIAN_POINT ( 'NONE',  ( -23.25000000000000000, 76.00000000001237765, -170.0231074845243597 ) ) ;
#43289=AXIS2_PLACEMENT_3D ( 'NONE', #109035, #88167, #86891 ) ;
#43338=CARTESIAN_POINT ( 'NONE',  ( -18.59999999999999787, 64.35000000001234355, -163.0083017138704236 ) ) ;
#43341=AXIS2_PLACEMENT_3D ( 'NONE', #8130, #107214, #135758 ) ;
#43343=FACE_OUTER_BOUND ( 'NONE', #162496, .T. ) ;
#43359=DIRECTION ( 'NONE',  ( 0.000000000000000000, 0.000000000000000000, -1.000000000000000000 ) ) ;
#43364=ORIENTED_EDGE ( 'NONE', *, *, #66429, .T. ) ;
#43370=DIRECTION ( 'NONE',  ( 0.000000000000000000, 7.109473446599835262E-15, -1.000000000000000000 ) ) ;
#43371=CARTESIAN_POINT ( 'NONE',  ( 21.12400222705963415, 67.22148809293508975, -157.7731074845244166 ) ) ;
#43389=EDGE_LOOP ( 'NONE', ( #171308, #148804 ) ) ;
#43402=CIRCLE ( 'NONE', #26859, 0.09999999999998898659 ) ;
#43407=AXIS2_PLACEMENT_3D ( 'NONE', #38555, #59357, #214609 ) ;
#43418=CARTESIAN_POINT ( 'NONE',  ( -18.50211644919735932, 65.69792220476342948, -131.0335554128461979 ) ) ;
#43452=CARTESIAN_POINT ( 'NONE',  ( 21.14999999999999858, 87.75000000001229239, -157.7731074845242745 ) ) ;
#43454=CARTESIAN_POINT ( 'NONE',  ( 21.05000000000000071, 65.51540711881798984, -162.5663939139407432 ) ) ;
#43455=DIRECTION ( 'NONE',  ( 1.000000000000000000, 0.000000000000000000, 0.000000000000000000 ) ) ;
#43460=DIRECTION ( 'NONE',  ( 0.000000000000000000, 0.000000000000000000, 1.000000000000000000 ) ) ;
#43463=AXIS2_PLACEMENT_3D ( 'NONE', #217806, #40522, #1331 ) ;
#43477=AXIS2_PLACEMENT_3D ( 'NONE', #205220, #206525, #27922 ) ;
#43490=CARTESIAN_POINT ( 'NONE',  ( 20.85000000000000142, 69.06610602788578035, -132.7374616501508342 ) ) ;
#43570=EDGE_CURVE ( 'NONE', #36642, #108264, #58523, .T. ) ;
#43615=ORIENTED_EDGE ( 'NONE', *, *, #245377, .F. ) ;
#43638=VERTEX_POINT ( 'NONE', #162227 ) ;
#43685=VERTEX_POINT ( 'NONE', #205156 ) ;
#43689=CARTESIAN_POINT ( 'NONE',  ( 21.07016717457009847, 76.00000000001243450, -176.3440483226252411 ) ) ;
#43695=ORIENTED_EDGE ( 'NONE', *, *, #182156, .T. ) ;
#43760=EDGE_CURVE ( 'NONE', #217847, #211242, #137819, .T. ) ;
#43782=CARTESIAN_POINT ( 'NONE',  ( -21.05000000000000071, 69.74168394268035343, -170.0888090948464537 ) ) ;
#43799=ORIENTED_EDGE ( 'NONE', *, *, #190341, .T. ) ;
#43848=CARTESIAN_POINT ( 'NONE',  ( 23.15000000000000213, 87.65000000001215597, -139.6231074845242688 ) ) ;
#43852=CARTESIAN_POINT ( 'NONE',  ( -22.39999999999999858, 64.25000000001237765, -170.0231074845244166 ) ) ;
#43860=CIRCLE ( 'NONE', #73115, 0.09999999999999820144 ) ;
#43874=DIRECTION ( 'NONE',  ( 0.000000000000000000, -1.176083712526648525E-14, 1.000000000000000000 ) ) ;
#43881=DIRECTION ( 'NONE',  ( 0.000000000000000000, 0.1568667991644355497, 0.9876197685951332295 ) ) ;
#43886=CARTESIAN_POINT ( 'NONE',  ( 20.94999999999999929, 76.00000000001213607, -136.5231074845243313 ) ) ;
#43897=FACE_OUTER_BOUND ( 'NONE', #41320, .T. ) ;
#43911=CIRCLE ( 'NONE', #206240, 11.80000000000000426 ) ;
#43942=VERTEX_POINT ( 'NONE', #201027 ) ;
#43943=DIRECTION ( 'NONE',  ( 0.000000000000000000, 0.9908441862701420355, 0.1350103645453197554 ) ) ;
#43949=EDGE_LOOP ( 'NONE', ( #237412, #235517, #217630, #51560 ) ) ;
#43990=ORIENTED_EDGE ( 'NONE', *, *, #18403, .F. ) ;
#44012=CARTESIAN_POINT ( 'NONE',  ( -18.59999999999999787, 85.50000000001233502, -161.9231074845242802 ) ) ;
#44020=CARTESIAN_POINT ( 'NONE',  ( -20.94999999999999929, 61.95000000001218154, -142.0368025552853624 ) ) ;
#44056=CIRCLE ( 'NONE', #139888, 4.049999999999998046 ) ;
#44086=ORIENTED_EDGE ( 'NONE', *, *, #393, .F. ) ;
#44088=VERTEX_POINT ( 'NONE', #105741 ) ;
#44100=ORIENTED_EDGE ( 'NONE', *, *, #194811, .F. ) ;
#44102=DIRECTION ( 'NONE',  ( -3.787827842127534447E-15, -0.7397360091702729346, -0.6728971962616859814 ) ) ;
#44118=CARTESIAN_POINT ( 'NONE',  ( 23.25000000000000000, 85.60000000001247145, -181.7731074845243029 ) ) ;
#44155=EDGE_CURVE ( 'NONE', #65207, #182460, #195283, .T. ) ;
#44190=CIRCLE ( 'NONE', #131470, 2.000000000000001776 ) ;
#44193=LINE ( 'NONE', #104128, #237702 ) ;
#44276=LINE ( 'NONE', #183779, #92305 ) ;
#44311=ADVANCED_FACE ( 'NONE', ( #86837 ), #161280, .F. ) ;
#44322=CARTESIAN_POINT ( 'NONE',  ( -23.25000000000000000, 73.40000000001228386, -156.7984855617622770 ) ) ;
#44358=EDGE_CURVE ( 'NONE', #92778, #212831, #108786, .T. ) ;
#44364=VERTEX_POINT ( 'NONE', #162568 ) ;
#44413=ORIENTED_EDGE ( 'NONE', *, *, #167454, .T. ) ;
#44416=ADVANCED_FACE ( 'NONE', ( #167711 ), #89416, .T. ) ;
#44443=ADVANCED_FACE ( 'NONE', ( #111564 ), #129827, .F. ) ;
#44459=LINE ( 'NONE', #82248, #36376 ) ;
#44467=ORIENTED_EDGE ( 'NONE', *, *, #148301, .T. ) ;
#44530=AXIS2_PLACEMENT_3D ( 'NONE', #5600, #108584, #124304 ) ;
#44538=CARTESIAN_POINT ( 'NONE',  ( -18.50000000000000000, 64.25000000001229239, -157.8731074845244393 ) ) ;
#44547=DIRECTION ( 'NONE',  ( 1.000000000000000000, -7.304098846218134667E-16, -5.100424963727256530E-30 ) ) ;
#44551=EDGE_CURVE ( 'NONE', #177863, #144130, #39192, .T. ) ;
#44570=AXIS2_PLACEMENT_3D ( 'NONE', #240617, #141511, #183221 ) ;
#44575=VECTOR ( 'NONE', #220549, 1000.000000000000000 ) ;
#44580=ORIENTED_EDGE ( 'NONE', *, *, #148183, .T. ) ;
#44589=CARTESIAN_POINT ( 'NONE',  ( -21.37071067811865532, 67.92928932189363422, -157.7731074845244166 ) ) ;
#44615=ADVANCED_FACE ( 'NONE', ( #93272 ), #88277, .T. ) ;
#44621=CIRCLE ( 'NONE', #15603, 0.09999999999999939493 ) ;
#44636=CARTESIAN_POINT ( 'NONE',  ( -20.64999999999999858, 76.00000000001237765, -170.0231074845243597 ) ) ;
#44647=ORIENTED_EDGE ( 'NONE', *, *, #215653, .T. ) ;
#44653=CARTESIAN_POINT ( 'NONE',  ( 21.05000000000000071, 67.22371711014456253, -157.8468923434562612 ) ) ;
#44660=VERTEX_POINT ( 'NONE', #124410 ) ;
#44677=CARTESIAN_POINT ( 'NONE',  ( 18.59999999999999076, 74.75000000001230660, -162.0231074845243597 ) ) ;
#44705=CIRCLE ( 'NONE', #61263, 0.09999999999999939493 ) ;
#44711=VERTEX_POINT ( 'NONE', #102224 ) ;
#44713=CARTESIAN_POINT ( 'NONE',  ( 20.94999999999999929, 67.22371710471985295, -161.4644784893834810 ) ) ;
#44721=AXIS2_PLACEMENT_3D ( 'NONE', #116288, #34201, #236212 ) ;
#44727=ORIENTED_EDGE ( 'NONE', *, *, #88965, .F. ) ;
#44755=AXIS2_PLACEMENT_3D ( 'NONE', #15654, #35222, #153903 ) ;
#44761=VERTEX_POINT ( 'NONE', #89123 ) ;
#44805=ADVANCED_FACE ( 'NONE', ( #30456 ), #138179, .T. ) ;
#44830=CARTESIAN_POINT ( 'NONE',  ( -20.64999999999999858, 74.05981308412438580, -149.3522266955776843 ) ) ;
#44833=ORIENTED_EDGE ( 'NONE', *, *, #87933, .T. ) ;
#44870=DIRECTION ( 'NONE',  ( 0.000000000000000000, -7.272083257015735086E-15, 1.000000000000000000 ) ) ;
#44907=CARTESIAN_POINT ( 'NONE',  ( 18.59999999999997655, 76.00000000001213607, -136.5231074845243313 ) ) ;
#44917=DIRECTION ( 'NONE',  ( 1.000000000000000000, 0.000000000000000000, 0.000000000000000000 ) ) ;
#44932=ORIENTED_EDGE ( 'NONE', *, *, #250721, .F. ) ;
#44935=TOROIDAL_SURFACE ( 'NONE', #190713, 0.6000000000000004219, 0.1000000000000000056 ) ;
#44970=AXIS2_PLACEMENT_3D ( 'NONE', #7334, #124720, #123435 ) ;
#44973=EDGE_CURVE ( 'NONE', #35927, #105518, #105011, .T. ) ;
#44993=ORIENTED_EDGE ( 'NONE', *, *, #86112, .T. ) ;
#45013=CIRCLE ( 'NONE', #211621, 0.2000000000000057288 ) ;
#45022=ORIENTED_EDGE ( 'NONE', *, *, #115614, .F. ) ;
#45047=VECTOR ( 'NONE', #177709, 1000.000000000000000 ) ;
#45053=AXIS2_PLACEMENT_3D ( 'NONE', #14648, #115005, #253221 ) ;
#45087=ORIENTED_EDGE ( 'NONE', *, *, #16744, .F. ) ;
#45186=FACE_OUTER_BOUND ( 'NONE', #93586, .T. ) ;
#45194=EDGE_LOOP ( 'NONE', ( #228492, #39871, #75794, #65321 ) ) ;
#45222=CARTESIAN_POINT ( 'NONE',  ( 21.05000000000000071, 67.22371710471982453, -157.8731074845244109 ) ) ;
#45236=ADVANCED_FACE ( 'NONE', ( #138056, #173406, #174689 ), #97635, .F. ) ;
#45274=CIRCLE ( 'NONE', #95172, 0.1999999999999987899 ) ;
#45296=EDGE_CURVE ( 'NONE', #42435, #250411, #20714, .T. ) ;
#45342=ORIENTED_EDGE ( 'NONE', *, *, #250739, .F. ) ;
#45382=CARTESIAN_POINT ( 'NONE',  ( -18.50000000000000000, 65.70729864261028297, -131.0657455973724836 ) ) ;
#45418=AXIS2_PLACEMENT_3D ( 'NONE', #97480, #118374, #157534 ) ;
#45476=CARTESIAN_POINT ( 'NONE',  ( -23.15000000000000213, 64.35000000001228670, -157.8731074845244393 ) ) ;
#45507=ORIENTED_EDGE ( 'NONE', *, *, #122087, .T. ) ;
#45555=CARTESIAN_POINT ( 'NONE',  ( -18.54118089899631983, 85.46353763186043295, -162.9745298866561711 ) ) ;
#45560=DIRECTION ( 'NONE',  ( 1.000000000000000000, -0.000000000000000000, 0.000000000000000000 ) ) ;
#45568=CYLINDRICAL_SURFACE ( 'NONE', #105970, 0.1000000000000046685 ) ;
#45573=VERTEX_POINT ( 'NONE', #33344 ) ;
#45574=DIRECTION ( 'NONE',  ( 1.000000000000000000, -2.952720810173289112E-16, -2.061873921506763405E-30 ) ) ;
#45578=DIRECTION ( 'NONE',  ( -1.000000000000000000, 0.000000000000000000, -0.000000000000000000 ) ) ;
#45607=DIRECTION ( 'NONE',  ( 0.000000000000000000, -0.1568667991644355497, 0.9876197685951332295 ) ) ;
#45642=ORIENTED_EDGE ( 'NONE', *, *, #76267, .T. ) ;
#45645=EDGE_CURVE ( 'NONE', #77194, #71592, #155534, .T. ) ;
#45661=ORIENTED_EDGE ( 'NONE', *, *, #174087, .F. ) ;
#45666=CYLINDRICAL_SURFACE ( 'NONE', #6512, 0.1000000000000028644 ) ;
#45678=DIRECTION ( 'NONE',  ( 1.000000000000000000, -0.000000000000000000, 0.000000000000000000 ) ) ;
#45682=DIRECTION ( 'NONE',  ( 1.000000000000000000, -0.000000000000000000, 0.000000000000000000 ) ) ;
#45703=VECTOR ( 'NONE', #66905, 1000.000000000000000 ) ;
#45714=ORIENTED_EDGE ( 'NONE', *, *, #76267, .F. ) ;
#45766=CARTESIAN_POINT ( 'NONE',  ( 21.05000000000000071, 77.25000000001232081, -162.1231074845243540 ) ) ;
#45776=CIRCLE ( 'NONE', #79070, 0.09999999999999080458 ) ;
#45780=CARTESIAN_POINT ( 'NONE',  ( -18.59999999999999787, 77.16270174995034381, -161.9231074845243370 ) ) ;
#45865=DIRECTION ( 'NONE',  ( 1.301042606982683734E-14, 0.8660254037844367092, -0.5000000000000037748 ) ) ;
#45874=DIRECTION ( 'NONE',  ( 0.000000000000000000, 1.000000000000000000, 6.982962677686266711E-15 ) ) ;
#45883=CARTESIAN_POINT ( 'NONE',  ( 20.94999999999999929, 88.41227409416185878, -139.5231074845242745 ) ) ;
#45892=FACE_OUTER_BOUND ( 'NONE', #223986, .T. ) ;
#45907=CIRCLE ( 'NONE', #249910, 11.80000000000000426 ) ;
#45911=CARTESIAN_POINT ( 'NONE',  ( 23.14999999999999858, 76.00000000001213607, -136.5231074845243313 ) ) ;
#45914=CARTESIAN_POINT ( 'NONE',  ( -21.05000000000000071, 69.74218538953086011, -170.1208977758336118 ) ) ;
#45918=CARTESIAN_POINT ( 'NONE',  ( 23.24999999999999645, 76.00000000001213607, -136.5231074845243313 ) ) ;
#45926=CARTESIAN_POINT ( 'NONE',  ( 23.15000000000000213, 85.50000000001222134, -146.4170766071767389 ) ) ;
#45928=CARTESIAN_POINT ( 'NONE',  ( 21.06086055315980232, 67.22529248505607313, -157.8207853293704090 ) ) ;
#45976=ORIENTED_EDGE ( 'NONE', *, *, #32115, .T. ) ;
#46003=CIRCLE ( 'NONE', #79310, 0.1000000000000021289 ) ;
#46012=CARTESIAN_POINT ( 'NONE',  ( -20.64999999999999858, 74.00000000001229239, -156.7984855617622770 ) ) ;
#46013=SPHERICAL_SURFACE ( 'NONE', #210942, 0.1000000000000000056 ) ;
#46029=ADVANCED_FACE ( 'NONE', ( #190828 ), #228656, .T. ) ;
#46058=DIRECTION ( 'NONE',  ( 1.000000000000000000, 0.000000000000000000, 0.000000000000000000 ) ) ;
#46061=DIRECTION ( 'NONE',  ( -1.000000000000000000, 0.000000000000000000, -0.000000000000000000 ) ) ;
#46071=VERTEX_POINT ( 'NONE', #179906 ) ;
#46076=ORIENTED_EDGE ( 'NONE', *, *, #183453, .T. ) ;
#46078=FACE_OUTER_BOUND ( 'NONE', #103282, .T. ) ;
#46080=ADVANCED_FACE ( 'NONE', ( #59915 ), #19543, .T. ) ;
#46146=ORIENTED_EDGE ( 'NONE', *, *, #233872, .F. ) ;
#46170=EDGE_LOOP ( 'NONE', ( #102710, #197618, #223764, #158452 ) ) ;
#46196=EDGE_LOOP ( 'NONE', ( #214481, #80583, #36741, #223273 ) ) ;
#46229=CARTESIAN_POINT ( 'NONE',  ( 23.14999999999998792, 64.35000000001238618, -170.0231074845244166 ) ) ;
#46274=CARTESIAN_POINT ( 'NONE',  ( -20.64999999999999858, 85.00000000001222134, -146.4170766071767389 ) ) ;
#46298=CIRCLE ( 'NONE', #250325, 0.09999999999998898659 ) ;
#46308=EDGE_CURVE ( 'NONE', #212831, #35577, #233162, .T. ) ;
#46328=CARTESIAN_POINT ( 'NONE',  ( -21.04386569057572132, 64.25000000001220712, -143.3802701327438740 ) ) ;
#46331=DIRECTION ( 'NONE',  ( 0.000000000000000000, 1.000000000000000000, 6.982962677686266711E-15 ) ) ;
#46344=CARTESIAN_POINT ( 'NONE',  ( -23.25000000000000000, 76.00000000001213607, -136.5231074845243313 ) ) ;
#46365=VERTEX_POINT ( 'NONE', #194031 ) ;
#46375=ORIENTED_EDGE ( 'NONE', *, *, #22510, .T. ) ;
#46383=ADVANCED_FACE ( 'NONE', ( #68949 ), #93317, .T. ) ;
#46481=LINE ( 'NONE', #245992, #54014 ) ;
#46486=DIRECTION ( 'NONE',  ( 0.000000000000000000, -8.232585987686539041E-15, 1.000000000000000000 ) ) ;
#46487=EDGE_CURVE ( 'NONE', #195708, #34506, #180823, .T. ) ;
#46507=DIRECTION ( 'NONE',  ( 0.000000000000000000, -7.056502275159890832E-15, 1.000000000000000000 ) ) ;
#46515=CARTESIAN_POINT ( 'NONE',  ( -22.50000000000000000, 75.90000000001242597, -177.8138870828977360 ) ) ;
#46532=EDGE_CURVE ( 'NONE', #210220, #26629, #122181, .T. ) ;
#46542=EDGE_CURVE ( 'NONE', #212171, #117495, #23094, .T. ) ;
#46572=CYLINDRICAL_SURFACE ( 'NONE', #205224, 0.8750000000000007772 ) ;
#46582=CARTESIAN_POINT ( 'NONE',  ( -22.59999999999999787, 64.25043287652299284, -170.1239658536231616 ) ) ;
#46584=DIRECTION ( 'NONE',  ( 0.000000000000000000, -6.454785026890406770E-15, 1.000000000000000000 ) ) ;
#46596=CARTESIAN_POINT ( 'NONE',  ( 22.49544290803777358, 64.25012976215509752, -170.0884194437818735 ) ) ;
#46618=DIRECTION ( 'NONE',  ( 5.421010862427554711E-16, 1.000000000000000000, 1.023556919514279895E-14 ) ) ;
#46623=ORIENTED_EDGE ( 'NONE', *, *, #37238, .T. ) ;
#46636=VECTOR ( 'NONE', #172416, 999.9999999999998863 ) ;
#46645=DIRECTION ( 'NONE',  ( 0.000000000000000000, 0.000000000000000000, 1.000000000000000000 ) ) ;
#46656=DIRECTION ( 'NONE',  ( 0.000000000000000000, 0.000000000000000000, 1.000000000000000000 ) ) ;
#46670=ORIENTED_EDGE ( 'NONE', *, *, #24521, .T. ) ;
#46683=EDGE_CURVE ( 'NONE', #66247, #221268, #97386, .T. ) ;
#46756=CARTESIAN_POINT ( 'NONE',  ( -21.12230431290519306, 69.54243334671936339, -170.0283173362134335 ) ) ;
#46759=ORIENTED_EDGE ( 'NONE', *, *, #257302, .T. ) ;
#46768=SPHERICAL_SURFACE ( 'NONE', #167533, 0.1000000000000000056 ) ;
#46787=EDGE_CURVE ( 'NONE', #30145, #114885, #242774, .T. ) ;
#46842=LINE ( 'NONE', #6444, #6822 ) ;
#46851=CARTESIAN_POINT ( 'NONE',  ( 18.59999999999999076, 77.85161776048096272, -124.9199177649206689 ) ) ;
#46856=ADVANCED_FACE ( 'NONE', ( #118011 ), #235382, .T. ) ;
#46863=ORIENTED_EDGE ( 'NONE', *, *, #103165, .F. ) ;
#46865=LINE ( 'NONE', #108149, #142175 ) ;
#46939=ORIENTED_EDGE ( 'NONE', *, *, #84627, .T. ) ;
#46958=EDGE_CURVE ( 'NONE', #219844, #127337, #59586, .T. ) ;
#46959=DIRECTION ( 'NONE',  ( 0.000000000000000000, 0.000000000000000000, 1.000000000000000000 ) ) ;
#46965=VERTEX_POINT ( 'NONE', #244371 ) ;
#46981=CARTESIAN_POINT ( 'NONE',  ( 19.83283456528359423, 64.25000000001220712, -145.1731074851066410 ) ) ;
#46982=CARTESIAN_POINT ( 'NONE',  ( 20.94999999999999929, 87.48912529308822172, -139.6231074845242688 ) ) ;
#46987=CARTESIAN_POINT ( 'NONE',  ( -18.59999999999999787, 77.16270174995034381, -161.9231074845243370 ) ) ;
#47022=CARTESIAN_POINT ( 'NONE',  ( 22.39999999999999503, 64.35000000001237197, -169.9231074845244507 ) ) ;
#47039=EDGE_CURVE ( 'NONE', #216685, #25616, #130855, .T. ) ;
#47093=ORIENTED_EDGE ( 'NONE', *, *, #216367, .T. ) ;
#47123=CARTESIAN_POINT ( 'NONE',  ( -23.25000000000000000, 77.16412189325330928, -128.6082593989527254 ) ) ;
#47155=DIRECTION ( 'NONE',  ( 0.000000000000000000, 0.000000000000000000, 1.000000000000000000 ) ) ;
#47211=VECTOR ( 'NONE', #16506, 1000.000000000000000 ) ;
#47212=AXIS2_PLACEMENT_3D ( 'NONE', #34982, #94899, #253969 ) ;
#47220=CARTESIAN_POINT ( 'NONE',  ( 20.85000000000000142, 77.75000000001206502, -124.9041574459021007 ) ) ;
#47231=DIRECTION ( 'NONE',  ( 0.000000000000000000, -1.000000000000000000, 0.000000000000000000 ) ) ;
#47258=FACE_OUTER_BOUND ( 'NONE', #38944, .T. ) ;
#47267=VERTEX_POINT ( 'NONE', #119015 ) ;
#47282=DIRECTION ( 'NONE',  ( 0.000000000000000000, -1.000000000000000000, 0.000000000000000000 ) ) ;
#47290=ORIENTED_EDGE ( 'NONE', *, *, #235713, .T. ) ;
#47294=ORIENTED_EDGE ( 'NONE', *, *, #160418, .T. ) ;
#47308=CARTESIAN_POINT ( 'NONE',  ( 21.05000000000000071, 64.25000000001219291, -143.5379132551784096 ) ) ;
#47316=DIRECTION ( 'NONE',  ( 0.000000000000000000, -0.4999999999999608646, 0.8660254037844612451 ) ) ;
#47321=CARTESIAN_POINT ( 'NONE',  ( -21.14999999999999858, 64.25000000001237765, -169.9231074845244507 ) ) ;
#47348=VERTEX_POINT ( 'NONE', #180265 ) ;
#47408=DIRECTION ( 'NONE',  ( 1.000000000000000000, 0.000000000000000000, 0.000000000000000000 ) ) ;
#47444=CARTESIAN_POINT ( 'NONE',  ( -20.64999999999999858, 73.60000000001224407, -149.7477294072864709 ) ) ;
#47452=FACE_OUTER_BOUND ( 'NONE', #254820, .T. ) ;
#47463=AXIS2_PLACEMENT_3D ( 'NONE', #254202, #192975, #75612 ) ;
#47487=CARTESIAN_POINT ( 'NONE',  ( -20.64999999999999858, 68.75000000001223555, -148.7731074845244166 ) ) ;
#47500=DIRECTION ( 'NONE',  ( -1.000000000000000000, 0.000000000000000000, 0.000000000000000000 ) ) ;
#47503=AXIS2_PLACEMENT_3D ( 'NONE', #151786, #192189, #189615 ) ;
#47562=EDGE_LOOP ( 'NONE', ( #167055, #49821, #93077, #37955, #21966 ) ) ;
#47580=ORIENTED_EDGE ( 'NONE', *, *, #34027, .F. ) ;
#47588=DIRECTION ( 'NONE',  ( 0.000000000000000000, -6.688090509790120484E-15, 1.000000000000000000 ) ) ;
#47600=CIRCLE ( 'NONE', #1809, 0.8750000000000007772 ) ;
#47602=ORIENTED_EDGE ( 'NONE', *, *, #242572, .F. ) ;
#47608=CARTESIAN_POINT ( 'NONE',  ( 20.94999999999999574, 87.75000000001234923, -167.1231074845242688 ) ) ;
#47619=DIRECTION ( 'NONE',  ( 0.000000000000000000, 0.000000000000000000, -1.000000000000000000 ) ) ;
#47683=ADVANCED_FACE ( 'NONE', ( #120010 ), #1292, .T. ) ;
#47712=CARTESIAN_POINT ( 'NONE',  ( -18.39999999999999858, 85.60000000001232934, -162.9910380878246201 ) ) ;
#47722=DIRECTION ( 'NONE',  ( 0.000000000000000000, 1.000000000000000000, 6.982962677686266711E-15 ) ) ;
#47724=CIRCLE ( 'NONE', #193499, 0.1000000000000072220 ) ;
#47734=CARTESIAN_POINT ( 'NONE',  ( -21.05000000000000071, 74.16465844978787914, -158.4679561919613775 ) ) ;
#47738=CARTESIAN_POINT ( 'NONE',  ( -23.24999999999999645, 85.60000000001210196, -129.9229180933022576 ) ) ;
#47764=EDGE_LOOP ( 'NONE', ( #178811, #159523, #163775, #175480 ) ) ;
#47768=CARTESIAN_POINT ( 'NONE',  ( 21.09706851349341861, 67.22415748653889978, -157.7875412681247838 ) ) ;
#47846=AXIS2_PLACEMENT_3D ( 'NONE', #20865, #119969, #142057 ) ;
#47860=DIRECTION ( 'NONE',  ( 0.000000000000000000, -1.000000000000000000, 0.000000000000000000 ) ) ;
#47862=CARTESIAN_POINT ( 'NONE',  ( -21.05000000000000071, 74.16465844978787914, -158.4679561919613775 ) ) ;
#47868=ADVANCED_FACE ( 'NONE', ( #12553 ), #30980, .T. ) ;
#47878=VECTOR ( 'NONE', #216592, 1000.000000000000000 ) ;
#47885=CARTESIAN_POINT ( 'NONE',  ( 18.52130828395273099, 85.48139550263810804, -162.9986007606406702 ) ) ;
#47890=VERTEX_POINT ( 'NONE', #39827 ) ;
#47944=EDGE_LOOP ( 'NONE', ( #239636, #167197, #54004, #49061 ) ) ;
#47966=EDGE_CURVE ( 'NONE', #167063, #43942, #143371, .T. ) ;
#48001=EDGE_CURVE ( 'NONE', #35976, #109724, #180984, .T. ) ;
#48007=ORIENTED_EDGE ( 'NONE', *, *, #23705, .F. ) ;
#48008=ORIENTED_EDGE ( 'NONE', *, *, #15366, .T. ) ;
#48039=FACE_OUTER_BOUND ( 'NONE', #21692, .T. ) ;
#48040=B_SPLINE_CURVE_WITH_KNOTS ( 'NONE', 3,
 ( #140441, #236997, #57034, #40107 ),
 .UNSPECIFIED., .F., .F.,
 ( 4, 4 ),
 ( 0.000000000000000000, 0.0002118541922231925311 ),
 .UNSPECIFIED. ) ;
#48047=CARTESIAN_POINT ( 'NONE',  ( -21.08479644141222664, 69.65496134228050096, -170.0816619270885610 ) ) ;
#48052=VERTEX_POINT ( 'NONE', #224845 ) ;
#48058=CARTESIAN_POINT ( 'NONE',  ( -22.47007471830799474, 68.27928934808589645, -170.0231074845244450 ) ) ;
#48059=EDGE_LOOP ( 'NONE', ( #248540, #156082, #246450, #214660 ) ) ;
#48063=VECTOR ( 'NONE', #176451, 1000.000000000000000 ) ;
#48075=CYLINDRICAL_SURFACE ( 'NONE', #228376, 0.09999999999998898659 ) ;
#48079=CARTESIAN_POINT ( 'NONE',  ( -20.54999999999999716, 71.65000000001222702, -148.8731074845244109 ) ) ;
#48112=EDGE_CURVE ( 'NONE', #242376, #255891, #164239, .T. ) ;
#48134=CARTESIAN_POINT ( 'NONE',  ( 20.85000000000000142, 77.83585931145570669, -125.0186683157258045 ) ) ;
#48157=EDGE_LOOP ( 'NONE', ( #13081, #74460, #11329, #19681 ) ) ;
#48235=DIRECTION ( 'NONE',  ( 1.000000000000000000, 0.000000000000000000, 0.000000000000000000 ) ) ;
#48238=CIRCLE ( 'NONE', #6540, 0.09999999999998898659 ) ;
#48242=EDGE_CURVE ( 'NONE', #75851, #255897, #76918, .T. ) ;
#48329=DIRECTION ( 'NONE',  ( 0.000000000000000000, 7.026728003956695223E-15, -1.000000000000000000 ) ) ;
#48333=LINE ( 'NONE', #6634, #41519 ) ;
#48412=EDGE_LOOP ( 'NONE', ( #61327, #204588, #119800, #67886 ) ) ;
#48450=ORIENTED_EDGE ( 'NONE', *, *, #257819, .T. ) ;
#48470=LINE ( 'NONE', #133155, #226413 ) ;
#48488=DIRECTION ( 'NONE',  ( 1.000000000000000000, 0.000000000000000000, 0.000000000000000000 ) ) ;
#48491=DIRECTION ( 'NONE',  ( 0.000000000000000000, -2.775557561563196798E-13, -1.000000000000000000 ) ) ;
#48506=CARTESIAN_POINT ( 'NONE',  ( 18.59999999999999432, 77.86671491006960366, -158.2704322382423356 ) ) ;
#48521=VERTEX_POINT ( 'NONE', #51018 ) ;
#48527=ADVANCED_FACE ( 'NONE', ( #92737 ), #112329, .T. ) ;
#48565=AXIS2_PLACEMENT_3D ( 'NONE', #48664, #64391, #203887 ) ;
#48606=ORIENTED_EDGE ( 'NONE', *, *, #137167, .T. ) ;
#48617=DIRECTION ( 'NONE',  ( -1.000000000000000000, 0.000000000000000000, -0.000000000000000000 ) ) ;
#48618=DIRECTION ( 'NONE',  ( 0.000000000000000000, -6.982962677686266711E-15, 1.000000000000000000 ) ) ;
#48664=CARTESIAN_POINT ( 'NONE',  ( -20.54999999999999716, 85.00000000001232081, -160.1291383618718385 ) ) ;
#48676=CARTESIAN_POINT ( 'NONE',  ( 23.24999999999999645, 76.00000000001213607, -136.5231074845243313 ) ) ;
#48679=ORIENTED_EDGE ( 'NONE', *, *, #43570, .F. ) ;
#48713=AXIS2_PLACEMENT_3D ( 'NONE', #178940, #257101, #160654 ) ;
#48728=CARTESIAN_POINT ( 'NONE',  ( -21.05000000000000071, 74.83729825007431202, -162.0231074845243597 ) ) ;
#48729=EDGE_CURVE ( 'NONE', #183270, #91489, #252528, .T. ) ;
#48738=EDGE_CURVE ( 'NONE', #133183, #16105, #27735, .T. ) ;
#48761=EDGE_LOOP ( 'NONE', ( #203010, #167751, #46863, #4171 ) ) ;
#48771=AXIS2_PLACEMENT_3D ( 'NONE', #214791, #133965, #213504 ) ;
#48802=ADVANCED_FACE ( 'NONE', ( #19644 ), #39225, .T. ) ;
#48814=DIRECTION ( 'NONE',  ( 0.000000000000000000, -3.469446951953515108E-14, 1.000000000000000000 ) ) ;
#48865=DIRECTION ( 'NONE',  ( 0.000000000000000000, 1.000000000000000000, 0.000000000000000000 ) ) ;
#48892=CARTESIAN_POINT ( 'NONE',  ( 20.04142135623731136, 64.25000000001220712, -145.2559501969990663 ) ) ;
#48894=DIRECTION ( 'NONE',  ( -1.000000000000000000, -7.304098846218163263E-16, 4.217023435051627211E-16 ) ) ;
#48930=CARTESIAN_POINT ( 'NONE',  ( 21.05000000000000071, 85.00000000001222134, -146.0170766071767332 ) ) ;
#48949=FACE_OUTER_BOUND ( 'NONE', #122079, .T. ) ;
#48954=AXIS2_PLACEMENT_3D ( 'NONE', #218490, #97241, #158571 ) ;
#48979=ORIENTED_EDGE ( 'NONE', *, *, #199205, .F. ) ;
#48980=EDGE_CURVE ( 'NONE', #231838, #71592, #236159, .T. ) ;
#48985=CIRCLE ( 'NONE', #165535, 12.97499999999999964 ) ;
#48986=AXIS2_PLACEMENT_3D ( 'NONE', #8591, #185939, #148104 ) ;
#49023=VECTOR ( 'NONE', #188596, 999.9999999999998863 ) ;
#49037=EDGE_CURVE ( 'NONE', #47890, #162856, #61198, .T. ) ;
#49043=DIRECTION ( 'NONE',  ( 0.000000000000000000, 6.982962677686266711E-15, -1.000000000000000000 ) ) ;
#49061=ORIENTED_EDGE ( 'NONE', *, *, #242474, .T. ) ;
#49077=LINE ( 'NONE', #249857, #48063 ) ;
#49078=EDGE_LOOP ( 'NONE', ( #175442, #57809, #139929, #131918, #55916 ) ) ;
#49080=CARTESIAN_POINT ( 'NONE',  ( 21.14999999999999503, 87.65000000001245439, -181.7731074845242745 ) ) ;
#49088=CARTESIAN_POINT ( 'NONE',  ( 23.24999999999999645, 72.10000000001214460, -136.5231074845243597 ) ) ;
#49148=ORIENTED_EDGE ( 'NONE', *, *, #204444, .T. ) ;
#49152=CARTESIAN_POINT ( 'NONE',  ( -20.54999999999999716, 85.40000000001221281, -146.4170766071767389 ) ) ;
#49176=VECTOR ( 'NONE', #16593, 1000.000000000000000 ) ;
#49184=DIRECTION ( 'NONE',  ( -1.000000000000000000, 0.000000000000000000, 0.000000000000000000 ) ) ;
#49185=ORIENTED_EDGE ( 'NONE', *, *, #129223, .T. ) ;
#49190=AXIS2_PLACEMENT_3D ( 'NONE', #187135, #226197, #69747 ) ;
#49192=ORIENTED_EDGE ( 'NONE', *, *, #81195, .T. ) ;
#49208=ORIENTED_EDGE ( 'NONE', *, *, #219471, .T. ) ;
#49232=DIRECTION ( 'NONE',  ( 0.000000000000000000, 0.000000000000000000, 1.000000000000000000 ) ) ;
#49283=EDGE_CURVE ( 'NONE', #240428, #246816, #173833, .T. ) ;
#49291=ADVANCED_FACE ( 'NONE', ( #195933 ), #23813, .F. ) ;
#49319=VERTEX_POINT ( 'NONE', #252026 ) ;
#49325=CARTESIAN_POINT ( 'NONE',  ( 18.59999999999999432, 74.83729825007431202, -161.9231074845243654 ) ) ;
#49330=CARTESIAN_POINT ( 'NONE',  ( 23.24999999999999645, 71.00000000001223555, -148.9283735034374843 ) ) ;
#49342=DIRECTION ( 'NONE',  ( 0.000000000000000000, -1.000000000000000000, -6.982962677686265922E-15 ) ) ;
#49373=DIRECTION ( 'NONE',  ( 1.000000000000000000, 0.000000000000000000, 0.000000000000000000 ) ) ;
#49392=CARTESIAN_POINT ( 'NONE',  ( -20.54999999999999716, 85.00000000001222134, -146.4170766071767389 ) ) ;
#49414=DIRECTION ( 'NONE',  ( -1.000000000000000000, 2.952720810173289112E-16, 2.061873921506763405E-30 ) ) ;
#49430=DIRECTION ( 'NONE',  ( -1.000000000000000000, 0.000000000000000000, -0.000000000000000000 ) ) ;
#49432=EDGE_CURVE ( 'NONE', #206936, #44660, #236744, .T. ) ;
#49440=VERTEX_POINT ( 'NONE', #124093 ) ;
#49443=CARTESIAN_POINT ( 'NONE',  ( -20.94999999999999929, 87.48912529308822172, -139.5231074845243029 ) ) ;
#49451=CARTESIAN_POINT ( 'NONE',  ( 23.15000000000000213, 88.41227409416184457, -139.5231074845242745 ) ) ;
#49459=DIRECTION ( 'NONE',  ( -1.000000000000000000, 2.952720810173289112E-16, 2.061873921506763405E-30 ) ) ;
#49521=CARTESIAN_POINT ( 'NONE',  ( -20.54999999999999716, 84.73084112150753811, -146.1211822035086243 ) ) ;
#49532=FACE_OUTER_BOUND ( 'NONE', #156248, .T. ) ;
#49587=VERTEX_POINT ( 'NONE', #107071 ) ;
#49590=ORIENTED_EDGE ( 'NONE', *, *, #234927, .T. ) ;
#49591=ORIENTED_EDGE ( 'NONE', *, *, #130400, .T. ) ;
#49628=CARTESIAN_POINT ( 'NONE',  ( -20.94999999999999929, 76.00000000001222134, -148.2231074845243199 ) ) ;
#49656=DIRECTION ( 'NONE',  ( 0.000000000000000000, -0.9915357197604982575, 0.1298341882519033486 ) ) ;
#49668=EDGE_CURVE ( 'NONE', #123863, #167063, #136911, .T. ) ;
#49691=EDGE_LOOP ( 'NONE', ( #53695, #153234, #242903, #132535 ) ) ;
#49697=VERTEX_POINT ( 'NONE', #54795 ) ;
#49706=ORIENTED_EDGE ( 'NONE', *, *, #73019, .T. ) ;
#49726=DIRECTION ( 'NONE',  ( 0.000000000000000000, 0.000000000000000000, 1.000000000000000000 ) ) ;
#49737=VECTOR ( 'NONE', #132851, 1000.000000000000000 ) ;
#49756=CIRCLE ( 'NONE', #3964, 0.09999999999999939493 ) ;
#49766=ADVANCED_FACE ( 'NONE', ( #181199 ), #116167, .F. ) ;
#49789=VERTEX_POINT ( 'NONE', #58638 ) ;
#49794=AXIS2_PLACEMENT_3D ( 'NONE', #92538, #96380, #93830 ) ;
#49821=ORIENTED_EDGE ( 'NONE', *, *, #44551, .T. ) ;
#49840=ORIENTED_EDGE ( 'NONE', *, *, #153041, .F. ) ;
#49850=CARTESIAN_POINT ( 'NONE',  ( -23.25000000000000000, 76.00000000001213607, -136.5231074845243313 ) ) ;
#49857=TOROIDAL_SURFACE ( 'NONE', #195642, 0.2000000000000000111, 0.1000000000000000056 ) ;
#49902=CARTESIAN_POINT ( 'NONE',  ( 20.94999999999999574, 62.00000000001233502, -164.5960149541419071 ) ) ;
#49916=SPHERICAL_SURFACE ( 'NONE', #203857, 0.1000000000000000056 ) ;
#49954=ADVANCED_FACE ( 'NONE', ( #228007 ), #65076, .F. ) ;
#49984=DIRECTION ( 'NONE',  ( -2.940209281316621016E-16, -1.000000000000000000, -7.056502275159890832E-15 ) ) ;
#50029=EDGE_LOOP ( 'NONE', ( #157967, #132686, #189311, #27754 ) ) ;
#50032=EDGE_LOOP ( 'NONE', ( #107967, #257405, #41509, #125930 ) ) ;
#50051=CARTESIAN_POINT ( 'NONE',  ( -21.14999999999999858, 87.75000000001237765, -170.0231074845242745 ) ) ;
#50170=LINE ( 'NONE', #170182, #111187 ) ;
#50230=AXIS2_PLACEMENT_3D ( 'NONE', #76858, #159007, #217635 ) ;
#50236=ADVANCED_FACE ( 'NONE', ( #201710 ), #178329, .F. ) ;
#50250=AXIS2_PLACEMENT_3D ( 'NONE', #69112, #45678, #26129 ) ;
#50309=ORIENTED_EDGE ( 'NONE', *, *, #234533, .T. ) ;
#50367=CARTESIAN_POINT ( 'NONE',  ( -20.64999999999999858, 68.85000000001222986, -148.7731074845244166 ) ) ;
#50390=ORIENTED_EDGE ( 'NONE', *, *, #69148, .T. ) ;
#50409=ORIENTED_EDGE ( 'NONE', *, *, #257819, .F. ) ;
#50413=DIRECTION ( 'NONE',  ( 1.000000000000000000, 0.000000000000000000, 0.000000000000000000 ) ) ;
#50426=ORIENTED_EDGE ( 'NONE', *, *, #46787, .T. ) ;
#50488=LINE ( 'NONE', #153521, #153263 ) ;
#50505=AXIS2_PLACEMENT_3D ( 'NONE', #188526, #88109, #108978 ) ;
#50511=CARTESIAN_POINT ( 'NONE',  ( -20.64999999999999858, 73.60000000001224407, -149.7477294072864709 ) ) ;
#50560=ADVANCED_FACE ( 'NONE', ( #104522 ), #208118, .T. ) ;
#50568=CARTESIAN_POINT ( 'NONE',  ( 20.95512820512820440, 65.37615131630040821, -157.8731074845244393 ) ) ;
#50578=AXIS2_PLACEMENT_3D ( 'NONE', #233223, #89818, #72876 ) ;
#50593=CARTESIAN_POINT ( 'NONE',  ( 20.86036036209897304, 65.37895722344136118, -162.3567590660221924 ) ) ;
#50603=CARTESIAN_POINT ( 'NONE',  ( 20.94999999999999929, 74.16465844978787914, -158.4679561919613775 ) ) ;
#50611=CARTESIAN_POINT ( 'NONE',  ( -22.00411653962159875, 68.74655713164217730, -170.1221455902930302 ) ) ;
#50621=ORIENTED_EDGE ( 'NONE', *, *, #186473, .F. ) ;
#50629=DIRECTION ( 'NONE',  ( 0.000000000000000000, -5.956132106358139644E-15, 1.000000000000000000 ) ) ;
#50634=ADVANCED_FACE ( 'NONE', ( #225765 ), #126689, .F. ) ;
#50651=DIRECTION ( 'NONE',  ( 1.000000000000000000, 0.000000000000000000, 0.000000000000000000 ) ) ;
#50658=ORIENTED_EDGE ( 'NONE', *, *, #96906, .T. ) ;
#50666=DIRECTION ( 'NONE',  ( 1.000000000000000000, 0.000000000000000000, 0.000000000000000000 ) ) ;
#50668=DIRECTION ( 'NONE',  ( 1.000000000000000000, 0.000000000000000000, 0.000000000000000000 ) ) ;
#50685=CIRCLE ( 'NONE', #225659, 0.5999999999999894307 ) ;
#50699=DIRECTION ( 'NONE',  ( 0.000000000000000000, -6.982962677686266711E-15, 1.000000000000000000 ) ) ;
#50708=ORIENTED_EDGE ( 'NONE', *, *, #257599, .T. ) ;
#50714=CARTESIAN_POINT ( 'NONE',  ( 20.95443524775735256, 67.12144573613950627, -161.4893852089242898 ) ) ;
#50715=ORIENTED_EDGE ( 'NONE', *, *, #121240, .F. ) ;
#50771=CIRCLE ( 'NONE', #63257, 4.000000000000003553 ) ;
#50817=DIRECTION ( 'NONE',  ( 0.000000000000000000, 0.000000000000000000, 1.000000000000000000 ) ) ;
#50819=ORIENTED_EDGE ( 'NONE', *, *, #181748, .T. ) ;
#50867=DIRECTION ( 'NONE',  ( 0.000000000000000000, -6.240597636138643358E-14, -1.000000000000000000 ) ) ;
#50907=AXIS2_PLACEMENT_3D ( 'NONE', #217649, #41632, #97697 ) ;
#50936=CARTESIAN_POINT ( 'NONE',  ( -21.12757541349819590, 75.99483878420269889, -176.4964880557759273 ) ) ;
#50939=VERTEX_POINT ( 'NONE', #58677 ) ;
#50968=DIRECTION ( 'NONE',  ( 0.000000000000000000, 6.982962677686266711E-15, -1.000000000000000000 ) ) ;
#50990=VERTEX_POINT ( 'NONE', #2563 ) ;
#50998=DIRECTION ( 'NONE',  ( 0.000000000000000000, 0.01283462868040404978, 0.9999176327611370985 ) ) ;
#51009=ORIENTED_EDGE ( 'NONE', *, *, #199001, .F. ) ;
#51013=CARTESIAN_POINT ( 'NONE',  ( -21.05000000000000071, 69.58633726514275963, -169.9375146211616254 ) ) ;
#51018=CARTESIAN_POINT ( 'NONE',  ( 20.94999999999999929, 87.29603075034744109, -139.5710066441881452 ) ) ;
#51073=CARTESIAN_POINT ( 'NONE',  ( -20.94999999999999929, 77.16412189325330928, -128.6082593989527254 ) ) ;
#51125=CARTESIAN_POINT ( 'NONE',  ( -21.93642651522410247, 68.67283376068657219, -170.0231074845243882 ) ) ;
#51137=AXIS2_PLACEMENT_3D ( 'NONE', #252787, #12941, #132872 ) ;
#51160=FACE_OUTER_BOUND ( 'NONE', #234069, .T. ) ;
#51200=AXIS2_PLACEMENT_3D ( 'NONE', #125924, #235004, #132041 ) ;
#51238=DIRECTION ( 'NONE',  ( 0.000000000000000000, -6.417474130781257643E-15, 1.000000000000000000 ) ) ;
#51258=EDGE_LOOP ( 'NONE', ( #160491, #95687, #85758, #240370 ) ) ;
#51260=AXIS2_PLACEMENT_3D ( 'NONE', #218055, #219352, #60277 ) ;
#51289=CARTESIAN_POINT ( 'NONE',  ( -21.05000000000000071, 77.26178616857734482, -161.9366085209788650 ) ) ;
#51295=CARTESIAN_POINT ( 'NONE',  ( -20.94999999999999929, 76.00000000001213607, -136.5231074845243313 ) ) ;
#51308=DIRECTION ( 'NONE',  ( 1.000000000000000000, 0.000000000000000000, 0.000000000000000000 ) ) ;
#51370=VERTEX_POINT ( 'NONE', #145612 ) ;
#51427=DIRECTION ( 'NONE',  ( 1.000000000000000000, 0.000000000000000000, 0.000000000000000000 ) ) ;
#51432=LINE ( 'NONE', #71053, #257384 ) ;
#51546=EDGE_CURVE ( 'NONE', #15592, #198025, #248769, .T. ) ;
#51560=ORIENTED_EDGE ( 'NONE', *, *, #130522, .T. ) ;
#51561=VERTEX_POINT ( 'NONE', #101008 ) ;
#51565=SPHERICAL_SURFACE ( 'NONE', #187323, 0.1000000000000000056 ) ;
#51584=DIRECTION ( 'NONE',  ( 0.000000000000000000, 0.01283462868040404978, 0.9999176327611370985 ) ) ;
#51617=EDGE_LOOP ( 'NONE', ( #250262, #106505, #129477, #32321 ) ) ;
#51626=AXIS2_PLACEMENT_3D ( 'NONE', #174169, #92011, #72471 ) ;
#51628=CARTESIAN_POINT ( 'NONE',  ( -20.94999999999999929, 65.70711192142388768, -131.0651054685122574 ) ) ;
#51641=CIRCLE ( 'NONE', #239116, 0.5000000000000004441 ) ;
#51643=ORIENTED_EDGE ( 'NONE', *, *, #7681, .T. ) ;
#51666=AXIS2_PLACEMENT_3D ( 'NONE', #206054, #105639, #229477 ) ;
#51687=AXIS2_PLACEMENT_3D ( 'NONE', #216646, #73325, #214085 ) ;
#51722=ORIENTED_EDGE ( 'NONE', *, *, #160460, .T. ) ;
#51769=AXIS2_PLACEMENT_3D ( 'NONE', #125477, #204982, #184150 ) ;
#51791=VECTOR ( 'NONE', #10925, 1000.000000000000000 ) ;
#51795=CARTESIAN_POINT ( 'NONE',  ( 18.49999999999999289, 65.70729864261026876, -131.0657455973724836 ) ) ;
#51863=CIRCLE ( 'NONE', #143457, 2.000000000000001776 ) ;
#51907=PLANE ( 'NONE',  #148832 ) ;
#51909=CARTESIAN_POINT ( 'NONE',  ( 21.05000000000000071, 76.00000000001237765, -170.0231074845243597 ) ) ;
#51912=DIRECTION ( 'NONE',  ( 0.000000000000000000, 1.000000000000000000, 6.982962677686266711E-15 ) ) ;
#51936=CARTESIAN_POINT ( 'NONE',  ( -20.54999999999999716, 68.85000000001222986, -148.8731074845244109 ) ) ;
#51983=FACE_OUTER_BOUND ( 'NONE', #119339, .T. ) ;
#51989=CARTESIAN_POINT ( 'NONE',  ( -20.94999999999999929, 64.35000000001232934, -163.0083017138704236 ) ) ;
#51993=FACE_BOUND ( 'NONE', #28989, .T. ) ;
#51998=AXIS2_PLACEMENT_3D ( 'NONE', #53320, #132869, #149869 ) ;
#51999=EDGE_CURVE ( 'NONE', #62499, #52922, #79625, .T. ) ;
#52021=VECTOR ( 'NONE', #197417, 1000.000000000000000 ) ;
#52029=EDGE_LOOP ( 'NONE', ( #80743, #3313, #100783, #229744 ) ) ;
#52054=CARTESIAN_POINT ( 'NONE',  ( -21.14999999999999858, 69.45934304831114048, -170.0231074845243882 ) ) ;
#52067=ORIENTED_EDGE ( 'NONE', *, *, #168727, .F. ) ;
#52086=ORIENTED_EDGE ( 'NONE', *, *, #94992, .T. ) ;
#52100=CARTESIAN_POINT ( 'NONE',  ( 19.75857864376268935, 64.25000000001220712, -145.1731074845244507 ) ) ;
#52101=VERTEX_POINT ( 'NONE', #27691 ) ;
#52132=DIRECTION ( 'NONE',  ( 0.000000000000000000, 0.000000000000000000, 1.000000000000000000 ) ) ;
#52137=ORIENTED_EDGE ( 'NONE', *, *, #104862, .F. ) ;
#52169=DIRECTION ( 'NONE',  ( -1.000000000000000000, -0.000000000000000000, -0.000000000000000000 ) ) ;
#52176=DIRECTION ( 'NONE',  ( 0.000000000000000000, -3.513364001978347611E-15, -1.000000000000000000 ) ) ;
#52182=EDGE_CURVE ( 'NONE', #172545, #143593, #79811, .T. ) ;
#52188=DIRECTION ( 'NONE',  ( -1.000000000000000000, -0.000000000000000000, -0.000000000000000000 ) ) ;
#52198=ORIENTED_EDGE ( 'NONE', *, *, #122153, .F. ) ;
#52200=DIRECTION ( 'NONE',  ( 1.000000000000000000, -2.952720810173289112E-16, -2.061873921506763405E-30 ) ) ;
#52232=ORIENTED_EDGE ( 'NONE', *, *, #83321, .F. ) ;
#52259=CARTESIAN_POINT ( 'NONE',  ( -23.25000000000000000, 85.00000000001222134, -146.4170766071767389 ) ) ;
#52297=DIRECTION ( 'NONE',  ( 1.000000000000000000, -7.304098846218134667E-16, -5.100424963727255829E-30 ) ) ;
#52309=CARTESIAN_POINT ( 'NONE',  ( -20.99142135623731065, 64.40000000001219860, -143.4513107147999449 ) ) ;
#52310=DIRECTION ( 'NONE',  ( -2.557131231893037478E-16, -0.8660254037844420383, 0.4999999999999941713 ) ) ;
#52335=DIRECTION ( 'NONE',  ( 0.000000000000000000, 8.326672684689590899E-13, -1.000000000000000000 ) ) ;
#52344=CARTESIAN_POINT ( 'NONE',  ( 18.59999999999999432, 77.73625713160970463, -158.4544551555068495 ) ) ;
#52355=PLANE ( 'NONE',  #92190 ) ;
#52364=AXIS2_PLACEMENT_3D ( 'NONE', #199928, #194801, #235189 ) ;
#52371=ADVANCED_FACE ( 'NONE', ( #238348 ), #59690, .F. ) ;
#52376=EDGE_CURVE ( 'NONE', #248304, #190389, #125787, .T. ) ;
#52400=EDGE_LOOP ( 'NONE', ( #232922, #53902, #38231 ) ) ;
#52417=VERTEX_POINT ( 'NONE', #41464 ) ;
#52423=DIRECTION ( 'NONE',  ( 0.000000000000000000, 7.116814260417676401E-15, -1.000000000000000000 ) ) ;
#52456=DIRECTION ( 'NONE',  ( 0.000000000000000000, 0.000000000000000000, -1.000000000000000000 ) ) ;
#52486=ORIENTED_EDGE ( 'NONE', *, *, #36753, .T. ) ;
#52487=CARTESIAN_POINT ( 'NONE',  ( 18.39999999999999858, 85.60000000001210196, -129.9229180933022576 ) ) ;
#52490=ORIENTED_EDGE ( 'NONE', *, *, #14978, .F. ) ;
#52510=AXIS2_PLACEMENT_3D ( 'NONE', #195380, #132829, #212372 ) ;
#52524=EDGE_CURVE ( 'NONE', #225850, #56768, #175896, .T. ) ;
#52538=LINE ( 'NONE', #30438, #166813 ) ;
#52547=DIRECTION ( 'NONE',  ( 0.000000000000000000, -0.7397360091702823714, 0.6728971962616756564 ) ) ;
#52602=VERTEX_POINT ( 'NONE', #222168 ) ;
#52611=ORIENTED_EDGE ( 'NONE', *, *, #99967, .T. ) ;
#52617=EDGE_CURVE ( 'NONE', #60849, #228310, #238220, .T. ) ;
#52624=CARTESIAN_POINT ( 'NONE',  ( 18.59999999999999787, 70.10000000001235776, -159.8040077198679683 ) ) ;
#52632=FACE_OUTER_BOUND ( 'NONE', #116535, .T. ) ;
#52655=EDGE_CURVE ( 'NONE', #59337, #9791, #200826, .T. ) ;
#52677=ORIENTED_EDGE ( 'NONE', *, *, #23208, .T. ) ;
#52692=CIRCLE ( 'NONE', #131814, 0.09999999999998898659 ) ;
#52703=CARTESIAN_POINT ( 'NONE',  ( -20.94999999999999929, 64.35000000001220144, -143.3069731475025321 ) ) ;
#52712=CARTESIAN_POINT ( 'NONE',  ( -21.05000000000000071, 74.75000000001232081, -162.0231074845243597 ) ) ;
#52719=EDGE_CURVE ( 'NONE', #255897, #6721, #137734, .T. ) ;
#52736=EDGE_CURVE ( 'NONE', #209114, #257571, #117439, .T. ) ;
#52741=VECTOR ( 'NONE', #124230, 1000.000000000000000 ) ;
#52749=CIRCLE ( 'NONE', #198517, 0.09999999999998898659 ) ;
#52754=DIRECTION ( 'NONE',  ( -1.000000000000000000, -0.000000000000000000, -0.000000000000000000 ) ) ;
#52806=CARTESIAN_POINT ( 'NONE',  ( -20.94999999999999929, 77.83534155023671985, -158.4679561919613491 ) ) ;
#52810=DIRECTION ( 'NONE',  ( 0.000000000000000000, -0.8660254037844377084, -0.5000000000000016653 ) ) ;
#52852=DIRECTION ( 'NONE',  ( -0.000000000000000000, 1.000000000000000000, 6.352154140967427193E-15 ) ) ;
#52855=FACE_OUTER_BOUND ( 'NONE', #229564, .T. ) ;
#52873=DIRECTION ( 'NONE',  ( 0.000000000000000000, -6.938893903907222067E-15, 1.000000000000000000 ) ) ;
#52880=EDGE_CURVE ( 'NONE', #128947, #171646, #159333, .T. ) ;
#52885=DIRECTION ( 'NONE',  ( 1.000000000000000000, 0.000000000000000000, 0.000000000000000000 ) ) ;
#52922=VERTEX_POINT ( 'NONE', #231429 ) ;
#52924=AXIS2_PLACEMENT_3D ( 'NONE', #186573, #230842, #110870 ) ;
#52939=SPHERICAL_SURFACE ( 'NONE', #243369, 0.1000000000000000056 ) ;
#52989=B_SPLINE_CURVE_WITH_KNOTS ( 'NONE', 3,
 ( #41073, #196260, #141424, #235381, #217087, #161003, #76300, #155884 ),
 .UNSPECIFIED., .F., .F.,
 ( 4, 2, 2, 4 ),
 ( 0.000000000000000000, 0.0001306511400390773054, 0.0001959767100586598141, 0.0002613022800782423228 ),
 .UNSPECIFIED. ) ;
#53040=EDGE_CURVE ( 'NONE', #51561, #204905, #89316, .T. ) ;
#53048=CARTESIAN_POINT ( 'NONE',  ( -20.85000000000000142, 77.25000000001209344, -128.7226267301092548 ) ) ;
#53053=CARTESIAN_POINT ( 'NONE',  ( -21.05000000000000071, 76.00000000001213607, -136.5231074845243313 ) ) ;
#53071=EDGE_LOOP ( 'NONE', ( #181400, #215004, #105499, #179135, #196429 ) ) ;
#53081=CARTESIAN_POINT ( 'NONE',  ( 23.14999999999998437, 80.05000000001237481, -170.0231074845243313 ) ) ;
#53114=CIRCLE ( 'NONE', #94804, 0.2000000000000057288 ) ;
#53125=CARTESIAN_POINT ( 'NONE',  ( 21.00000000000000000, 66.25000000001229239, -157.6731074845244223 ) ) ;
#53151=EDGE_CURVE ( 'NONE', #22950, #138951, #146423, .T. ) ;
#53154=SPHERICAL_SURFACE ( 'NONE', #202833, 0.1000000000000000056 ) ;
#53168=CIRCLE ( 'NONE', #128185, 0.2000000000000057288 ) ;
#53172=ORIENTED_EDGE ( 'NONE', *, *, #3323, .T. ) ;
#53221=DIRECTION ( 'NONE',  ( 0.000000000000000000, -7.429790795770644761E-15, 1.000000000000000000 ) ) ;
#53239=PLANE ( 'NONE',  #179073 ) ;
#53270=CARTESIAN_POINT ( 'NONE',  ( 21.05000000000000071, 85.50000000001222134, -146.4170766071767389 ) ) ;
#53283=CARTESIAN_POINT ( 'NONE',  ( -21.44999999999999929, 68.75000000001223555, -148.8731074845244109 ) ) ;
#53320=CARTESIAN_POINT ( 'NONE',  ( 23.14999999999999147, 76.00000000001237765, -170.0231074845243597 ) ) ;
#53325=LINE ( 'NONE', #132876, #210046 ) ;
#53377=EDGE_LOOP ( 'NONE', ( #58870, #190647, #111395, #185049 ) ) ;
#53387=VECTOR ( 'NONE', #141958, 1000.000000000000000 ) ;
#53434=EDGE_CURVE ( 'NONE', #35976, #178841, #200433, .T. ) ;
#53439=CIRCLE ( 'NONE', #140925, 0.09999999999998898659 ) ;
#53477=CARTESIAN_POINT ( 'NONE',  ( -20.85000000000000142, 76.00000000001213607, -136.5231074845243313 ) ) ;
#53523=EDGE_CURVE ( 'NONE', #176760, #92784, #185563, .T. ) ;
#53585=VERTEX_POINT ( 'NONE', #193280 ) ;
#53599=ORIENTED_EDGE ( 'NONE', *, *, #84627, .F. ) ;
#53610=CARTESIAN_POINT ( 'NONE',  ( -23.25000000000000000, 71.65000000001228386, -157.7731074845243882 ) ) ;
#53629=TOROIDAL_SURFACE ( 'NONE', #161983, 2.100000000000002309, 0.1000000000000000056 ) ;
#53633=CARTESIAN_POINT ( 'NONE',  ( 23.24999999999999289, 69.55000000001246008, -181.7731074845244166 ) ) ;
#53646=DIRECTION ( 'NONE',  ( 1.000000000000000000, 0.000000000000000000, 0.000000000000000000 ) ) ;
#53661=EDGE_CURVE ( 'NONE', #52417, #168004, #233694, .T. ) ;
#53677=DIRECTION ( 'NONE',  ( 1.000000000000000000, 0.000000000000000000, 0.000000000000000000 ) ) ;
#53695=ORIENTED_EDGE ( 'NONE', *, *, #87822, .F. ) ;
#53703=DIRECTION ( 'NONE',  ( 0.000000000000000000, -7.116814260417693756E-15, 1.000000000000000000 ) ) ;
#53707=CIRCLE ( 'NONE', #216188, 0.09999999999998712696 ) ;
#53718=CARTESIAN_POINT ( 'NONE',  ( 18.50000000000000355, 85.42145614550645405, -162.7811254005061414 ) ) ;
#53721=CYLINDRICAL_SURFACE ( 'NONE', #10403, 12.87499999999999822 ) ;
#53790=AXIS2_PLACEMENT_3D ( 'NONE', #222861, #220315, #80768 ) ;
#53833=CARTESIAN_POINT ( 'NONE',  ( -20.94999999999999929, 61.95000000001234497, -164.5094124137634708 ) ) ;
#53837=CIRCLE ( 'NONE', #199610, 0.2000000000000057288 ) ;
#53861=CARTESIAN_POINT ( 'NONE',  ( -21.05000000000000071, 87.65000000001235492, -167.0231074845242460 ) ) ;
#53887=CARTESIAN_POINT ( 'NONE',  ( -18.43459694179558639, 85.49421012501012740, -129.9061022818631841 ) ) ;
#53891=ORIENTED_EDGE ( 'NONE', *, *, #43177, .F. ) ;
#53902=ORIENTED_EDGE ( 'NONE', *, *, #109131, .T. ) ;
#53904=CARTESIAN_POINT ( 'NONE',  ( -20.54999999999999716, 74.00000000001229239, -156.7984855617622770 ) ) ;
#53951=TOROIDAL_SURFACE ( 'NONE', #249777, 7.800000000000000711, 0.1000000000000000056 ) ;
#53995=ORIENTED_EDGE ( 'NONE', *, *, #70372, .T. ) ;
#54001=ADVANCED_FACE ( 'NONE', ( #822 ), #254897, .F. ) ;
#54004=ORIENTED_EDGE ( 'NONE', *, *, #141783, .F. ) ;
#54010=CARTESIAN_POINT ( 'NONE',  ( 21.14999999999999503, 87.75000000001246292, -181.7731074845242745 ) ) ;
#54014=VECTOR ( 'NONE', #28256, 1000.000000000000000 ) ;
#54021=DIRECTION ( 'NONE',  ( 0.000000000000000000, -0.9875055080513754913, 0.1575844902526733482 ) ) ;
#54045=EDGE_CURVE ( 'NONE', #112163, #120222, #184222, .T. ) ;
#54082=DIRECTION ( 'NONE',  ( 1.000000000000000000, 0.000000000000000000, 0.000000000000000000 ) ) ;
#54124=CARTESIAN_POINT ( 'NONE',  ( -22.50000000000000000, 64.35012909624819599, -170.1056273753973471 ) ) ;
#54149=FACE_OUTER_BOUND ( 'NONE', #6037, .T. ) ;
#54158=ORIENTED_EDGE ( 'NONE', *, *, #81499, .T. ) ;
#54187=CYLINDRICAL_SURFACE ( 'NONE', #204914, 0.8750000000000007772 ) ;
#54189=CARTESIAN_POINT ( 'NONE',  ( -18.46093223321789978, 85.48068296828677148, -162.9385569705971193 ) ) ;
#54209=AXIS2_PLACEMENT_3D ( 'NONE', #56304, #217940, #39358 ) ;
#54215=ORIENTED_EDGE ( 'NONE', *, *, #199205, .T. ) ;
#54225=VERTEX_POINT ( 'NONE', #131067 ) ;
#54230=DIRECTION ( 'NONE',  ( -0.000000000000000000, 0.1350103645451945777, -0.9908441862701590219 ) ) ;
#54260=CARTESIAN_POINT ( 'NONE',  ( -21.64999999999999858, 68.75000000001224976, -148.7731074845244166 ) ) ;
#54296=DIRECTION ( 'NONE',  ( 0.000000000000000000, 0.000000000000000000, 1.000000000000000000 ) ) ;
#54319=DIRECTION ( 'NONE',  ( 0.000000000000000000, 1.000000000000000000, 6.853228547068871147E-15 ) ) ;
#54329=AXIS2_PLACEMENT_3D ( 'NONE', #163306, #221950, #43359 ) ;
#54373=ORIENTED_EDGE ( 'NONE', *, *, #139478, .F. ) ;
#54376=ADVANCED_FACE ( 'NONE', ( #78777 ), #37132, .T. ) ;
#54408=DIRECTION ( 'NONE',  ( 0.7071359030027593029, -0.7070776581709197206, 0.000000000000000000 ) ) ;
#54417=DIRECTION ( 'NONE',  ( -0.000000000000000000, 0.4791956752371484551, 0.8777080977375184556 ) ) ;
#54418=ORIENTED_EDGE ( 'NONE', *, *, #181548, .F. ) ;
#54447=ORIENTED_EDGE ( 'NONE', *, *, #157061, .F. ) ;
#54460=VERTEX_POINT ( 'NONE', #201313 ) ;
#54476=SPHERICAL_SURFACE ( 'NONE', #22283, 0.1000000000000000056 ) ;
#54490=CARTESIAN_POINT ( 'NONE',  ( 20.85000000000000142, 77.83585931145570669, -125.0186683157258045 ) ) ;
#54510=EDGE_CURVE ( 'NONE', #76314, #166025, #203877, .T. ) ;
#54532=EDGE_CURVE ( 'NONE', #74763, #248708, #120526, .T. ) ;
#54565=DIRECTION ( 'NONE',  ( 3.469446951953801622E-14, -0.1575844902526687130, -0.9875055080513762684 ) ) ;
#54599=SPHERICAL_SURFACE ( 'NONE', #218196, 0.1000000000000000056 ) ;
#54611=CARTESIAN_POINT ( 'NONE',  ( -23.25000000000000000, 85.00000000001222134, -146.4170766071767389 ) ) ;
#54648=CARTESIAN_POINT ( 'NONE',  ( -21.55000000000000071, 68.65000000001229807, -157.7731074845244166 ) ) ;
#54699=DIRECTION ( 'NONE',  ( -0.000000000000000000, -6.982962677686266711E-15, 1.000000000000000000 ) ) ;
#54716=ORIENTED_EDGE ( 'NONE', *, *, #35219, .T. ) ;
#54722=EDGE_CURVE ( 'NONE', #47267, #33310, #188683, .T. ) ;
#54737=ORIENTED_EDGE ( 'NONE', *, *, #149311, .T. ) ;
#54742=CARTESIAN_POINT ( 'NONE',  ( 22.47071067811865319, 76.00000000001237765, -170.0231074845243597 ) ) ;
#54767=CARTESIAN_POINT ( 'NONE',  ( -20.94999999999999929, 74.16465844978787914, -158.3679561919613832 ) ) ;
#54795=CARTESIAN_POINT ( 'NONE',  ( 22.60000000000000142, 75.89914163091376054, -181.7726746080137445 ) ) ;
#54805=EDGE_LOOP ( 'NONE', ( #110338, #163108, #24189, #92750 ) ) ;
#54855=CIRCLE ( 'NONE', #184042, 0.09999999999999939493 ) ;
#54861=AXIS2_PLACEMENT_3D ( 'NONE', #182244, #180958, #106520 ) ;
#54903=CIRCLE ( 'NONE', #229711, 0.2000000000000057288 ) ;
#54907=DIRECTION ( 'NONE',  ( 1.000000000000000000, 0.000000000000000000, -0.000000000000000000 ) ) ;
#54924=ORIENTED_EDGE ( 'NONE', *, *, #43760, .T. ) ;
#54948=AXIS2_PLACEMENT_3D ( 'NONE', #17762, #20377, #236820 ) ;
#54974=DIRECTION ( 'NONE',  ( -0.7071067811865127117, -0.7071067811865821007, 0.000000000000000000 ) ) ;
#55003=DIRECTION ( 'NONE',  ( 1.000000000000000000, 0.000000000000000000, 0.000000000000000000 ) ) ;
#55014=AXIS2_PLACEMENT_3D ( 'NONE', #201219, #22606, #105948 ) ;
#55025=DIRECTION ( 'NONE',  ( -0.000000000000000000, 7.109473446599835262E-15, -1.000000000000000000 ) ) ;
#55044=DIRECTION ( 'NONE',  ( -0.000000000000000000, 1.000000000000000000, 6.352154140967427193E-15 ) ) ;
#55051=DIRECTION ( 'NONE',  ( 0.000000000000000000, 1.000000000000000000, 6.982962677686267499E-15 ) ) ;
#55060=DIRECTION ( 'NONE',  ( -1.000000000000000000, 0.000000000000000000, 0.000000000000000000 ) ) ;
#55084=DIRECTION ( 'NONE',  ( 1.000000000000000000, 0.000000000000000000, 0.000000000000000000 ) ) ;
#55086=DIRECTION ( 'NONE',  ( 2.715809747126117987E-16, 1.000000000000000000, 6.517943393102682774E-15 ) ) ;
#55104=CARTESIAN_POINT ( 'NONE',  ( -20.85000000000000142, 77.83585931145570669, -125.0186683157258045 ) ) ;
#55116=CIRCLE ( 'NONE', #71911, 0.1000000000000028783 ) ;
#55131=CARTESIAN_POINT ( 'NONE',  ( -18.46919391072061956, 85.67072438828979841, -129.8493039527246822 ) ) ;
#55132=VERTEX_POINT ( 'NONE', #54767 ) ;
#55182=FACE_OUTER_BOUND ( 'NONE', #94621, .T. ) ;
#55206=CARTESIAN_POINT ( 'NONE',  ( 20.94999999999999574, 87.48912529308842068, -167.0231074845242745 ) ) ;
#55256=ADVANCED_FACE ( 'NONE', ( #3796 ), #102866, .T. ) ;
#55258=VERTEX_POINT ( 'NONE', #101572 ) ;
#55268=DIRECTION ( 'NONE',  ( 0.000000000000000000, 0.8068669527897506244, 0.5907332058516622242 ) ) ;
#55269=ADVANCED_FACE ( 'NONE', ( #123750 ), #181161, .T. ) ;
#55271=DIRECTION ( 'NONE',  ( 0.000000000000000000, -1.086323898850447076E-14, 1.000000000000000000 ) ) ;
#55284=SPHERICAL_SURFACE ( 'NONE', #188418, 0.1000000000000000056 ) ;
#55304=CIRCLE ( 'NONE', #213558, 0.1000000000000021289 ) ;
#55368=ORIENTED_EDGE ( 'NONE', *, *, #116312, .T. ) ;
#55376=LINE ( 'NONE', #131102, #87828 ) ;
#55442=EDGE_CURVE ( 'NONE', #55258, #168942, #56933, .T. ) ;
#55444=CARTESIAN_POINT ( 'NONE',  ( 18.49999999999998934, 65.71984138295503897, -145.2985354133222415 ) ) ;
#55471=CARTESIAN_POINT ( 'NONE',  ( -20.85882249326303040, 65.66751761918692409, -130.9282609406112670 ) ) ;
#55476=FACE_OUTER_BOUND ( 'NONE', #208851, .T. ) ;
#55547=VERTEX_POINT ( 'NONE', #159676 ) ;
#55601=ORIENTED_EDGE ( 'NONE', *, *, #22877, .T. ) ;
#55656=LINE ( 'NONE', #94818, #36212 ) ;
#55679=DIRECTION ( 'NONE',  ( 0.000000000000000000, -0.9908441862701420355, -0.1350103645453197554 ) ) ;
#55685=CARTESIAN_POINT ( 'NONE',  ( 20.97468175916167255, 65.37473483564126298, -157.7683460491116421 ) ) ;
#55687=AXIS2_PLACEMENT_3D ( 'NONE', #40428, #177368, #176080 ) ;
#55692=DIRECTION ( 'NONE',  ( -1.000000000000000000, 0.000000000000000000, -0.000000000000000000 ) ) ;
#55707=DIRECTION ( 'NONE',  ( 0.000000000000000000, -0.9908441862701791170, 0.1350103645450472789 ) ) ;
#55711=DIRECTION ( 'NONE',  ( 1.000000000000000000, 0.000000000000000000, 0.000000000000000000 ) ) ;
#55720=LINE ( 'NONE', #234390, #174714 ) ;
#55722=ORIENTED_EDGE ( 'NONE', *, *, #176870, .F. ) ;
#55741=DIRECTION ( 'NONE',  ( 0.000000000000000000, -1.000000000000000000, -6.982962677686265922E-15 ) ) ;
#55773=ADVANCED_FACE ( 'NONE', ( #130809 ), #32739, .F. ) ;
#55776=DIRECTION ( 'NONE',  ( 1.000000000000000000, 0.000000000000000000, 0.000000000000000000 ) ) ;
#55874=ORIENTED_EDGE ( 'NONE', *, *, #256033, .T. ) ;
#55916=ORIENTED_EDGE ( 'NONE', *, *, #202249, .F. ) ;
#55921=CIRCLE ( 'NONE', #80880, 3.899999999999987033 ) ;
#55966=EDGE_CURVE ( 'NONE', #141897, #588, #89451, .T. ) ;
#56019=EDGE_CURVE ( 'NONE', #160550, #92616, #106003, .T. ) ;
#56032=CIRCLE ( 'NONE', #43407, 0.09999999999999939493 ) ;
#56038=CARTESIAN_POINT ( 'NONE',  ( -21.52071067811865746, 68.22071067813087097, -148.7731074845244166 ) ) ;
#56060=EDGE_CURVE ( 'NONE', #77748, #160821, #166013, .T. ) ;
#56081=DIRECTION ( 'NONE',  ( -2.978066053179069723E-16, -1.000000000000000000, -7.147358527629766941E-15 ) ) ;
#56123=ORIENTED_EDGE ( 'NONE', *, *, #24060, .F. ) ;
#56141=ORIENTED_EDGE ( 'NONE', *, *, #181821, .F. ) ;
#56157=FACE_OUTER_BOUND ( 'NONE', #146706, .T. ) ;
#56189=ORIENTED_EDGE ( 'NONE', *, *, #95679, .T. ) ;
#56201=CIRCLE ( 'NONE', #185223, 0.1000000000000009492 ) ;
#56202=CIRCLE ( 'NONE', #197865, 0.4000000000000114575 ) ;
#56223=DIRECTION ( 'NONE',  ( 0.7071067811865474617, -0.7071067811865474617, -4.937700262164531476E-15 ) ) ;
#56246=ORIENTED_EDGE ( 'NONE', *, *, #137943, .F. ) ;
#56292=VERTEX_POINT ( 'NONE', #8829 ) ;
#56300=DIRECTION ( 'NONE',  ( 1.000000000000000000, -3.265361837132813093E-16, -2.280189983783949500E-30 ) ) ;
#56304=CARTESIAN_POINT ( 'NONE',  ( 21.30000000000002558, 76.00000000001237765, -170.0231074845243597 ) ) ;
#56308=ORIENTED_EDGE ( 'NONE', *, *, #162986, .F. ) ;
#56316=DIRECTION ( 'NONE',  ( 0.000000000000000000, -1.000000000000000000, -6.982962677686265922E-15 ) ) ;
#56330=ORIENTED_EDGE ( 'NONE', *, *, #208937, .F. ) ;
#56347=CARTESIAN_POINT ( 'NONE',  ( -20.64999999999999858, 68.75000000001223555, -148.8731074845244109 ) ) ;
#56348=DIRECTION ( 'NONE',  ( 0.000000000000000000, 6.982962677686266711E-15, -1.000000000000000000 ) ) ;
#56371=CARTESIAN_POINT ( 'NONE',  ( 18.39999999999999858, 85.51932773110476660, -163.0501311079649440 ) ) ;
#56404=CARTESIAN_POINT ( 'NONE',  ( 21.05000000000000426, 65.43724016256129516, -162.5662935266058184 ) ) ;
#56456=ORIENTED_EDGE ( 'NONE', *, *, #247698, .T. ) ;
#56549=AXIS2_PLACEMENT_3D ( 'NONE', #121404, #84761, #2682 ) ;
#56556=DIRECTION ( 'NONE',  ( 0.000000000000000000, 6.982962677686266711E-15, -1.000000000000000000 ) ) ;
#56570=AXIS2_PLACEMENT_3D ( 'NONE', #132565, #93419, #114276 ) ;
#56588=PLANE ( 'NONE',  #17367 ) ;
#56593=ORIENTED_EDGE ( 'NONE', *, *, #6370, .F. ) ;
#56626=ORIENTED_EDGE ( 'NONE', *, *, #166909, .T. ) ;
#56628=AXIS2_PLACEMENT_3D ( 'NONE', #83133, #181009, #41504 ) ;
#56629=CARTESIAN_POINT ( 'NONE',  ( 20.94999999999999929, 77.34915357198813979, -128.7356101489344837 ) ) ;
#56632=CARTESIAN_POINT ( 'NONE',  ( 23.14999999999999503, 69.45000000001222418, -148.7731074845244166 ) ) ;
#56682=CARTESIAN_POINT ( 'NONE',  ( 22.49999999999999645, 64.35023708198045256, -170.1119174609113713 ) ) ;
#56719=FACE_OUTER_BOUND ( 'NONE', #85103, .T. ) ;
#56735=ORIENTED_EDGE ( 'NONE', *, *, #23842, .F. ) ;
#56768=VERTEX_POINT ( 'NONE', #255354 ) ;
#56787=EDGE_CURVE ( 'NONE', #174960, #160821, #139701, .T. ) ;
#56795=DIRECTION ( 'NONE',  ( 1.000000000000000000, 0.000000000000000000, 0.000000000000000000 ) ) ;
#56807=AXIS2_PLACEMENT_3D ( 'NONE', #228564, #90306, #68195 ) ;
#56813=EDGE_CURVE ( 'NONE', #134685, #213031, #110683, .T. ) ;
#56826=DIRECTION ( 'NONE',  ( -1.000000000000000000, 0.000000000000000000, 0.000000000000000000 ) ) ;
#56828=VERTEX_POINT ( 'NONE', #155064 ) ;
#56843=DIRECTION ( 'NONE',  ( 0.000000000000000000, 0.000000000000000000, 1.000000000000000000 ) ) ;
#56847=VERTEX_POINT ( 'NONE', #37675 ) ;
#56853=CIRCLE ( 'NONE', #190186, 11.75000000000001066 ) ;
#56867=CARTESIAN_POINT ( 'NONE',  ( -22.42253884134832020, 75.99806764887715360, -181.6727131818727798 ) ) ;
#56868=DIRECTION ( 'NONE',  ( 1.000000000000000000, 0.000000000000000000, 0.000000000000000000 ) ) ;
#56878=CARTESIAN_POINT ( 'NONE',  ( 18.41356215285960829, 85.50000000001232081, -162.9910380878246485 ) ) ;
#56898=ORIENTED_EDGE ( 'NONE', *, *, #235289, .T. ) ;
#56899=CARTESIAN_POINT ( 'NONE',  ( 23.15000000000000213, 87.65000000001238334, -170.0231074845242745 ) ) ;
#56913=ORIENTED_EDGE ( 'NONE', *, *, #160261, .F. ) ;
#56929=CARTESIAN_POINT ( 'NONE',  ( -22.47007471830799830, 76.00000000001244871, -177.7438181364508694 ) ) ;
#56933=B_SPLINE_CURVE_WITH_KNOTS ( 'NONE', 3,
 ( #133680, #85863, #48047, #66341, #145857, #46756, #27244, #99659 ),
 .UNSPECIFIED., .F., .F.,
 ( 4, 2, 2, 4 ),
 ( 0.000000000000000000, 6.534141206311790389E-05, 0.0001306828241262358078, 0.0002613656482524339937 ),
 .UNSPECIFIED. ) ;
#56939=VECTOR ( 'NONE', #255008, 1000.000000000000000 ) ;
#56976=VERTEX_POINT ( 'NONE', #2354 ) ;
#56978=DIRECTION ( 'NONE',  ( 1.000000000000000000, 0.000000000000000000, 0.000000000000000000 ) ) ;
#57012=CARTESIAN_POINT ( 'NONE',  ( -20.64999999999999858, 71.65000000001228386, -157.6731074845243938 ) ) ;
#57022=CARTESIAN_POINT ( 'NONE',  ( 23.14999999999999858, 76.00000000001237765, -170.0231074845243597 ) ) ;
#57034=CARTESIAN_POINT ( 'NONE',  ( 21.05000000000000071, 67.18454772081477699, -161.6027149319101568 ) ) ;
#57037=DIRECTION ( 'NONE',  ( 0.000000000000000000, 1.000000000000000000, 0.000000000000000000 ) ) ;
#57076=CARTESIAN_POINT ( 'NONE',  ( 18.59999999999999076, 64.35000000001220144, -145.2731074845244450 ) ) ;
#57089=DIRECTION ( 'NONE',  ( -1.000000000000000000, 0.000000000000000000, -0.000000000000000000 ) ) ;
#57118=AXIS2_PLACEMENT_3D ( 'NONE', #65990, #67272, #26897 ) ;
#57194=ORIENTED_EDGE ( 'NONE', *, *, #82121, .T. ) ;
#57280=EDGE_CURVE ( 'NONE', #223147, #216520, #90179, .T. ) ;
#57309=EDGE_CURVE ( 'NONE', #67356, #85130, #19284, .T. ) ;
#57332=CYLINDRICAL_SURFACE ( 'NONE', #167498, 0.09999999999998898659 ) ;
#57338=PRODUCT_CONTEXT ( 'NONE', #12422, 'mechanical' ) ;
#57353=CARTESIAN_POINT ( 'NONE',  ( 18.39999999999999858, 85.50000000001209344, -129.6084491415546154 ) ) ;
#57356=CARTESIAN_POINT ( 'NONE',  ( -23.25000000000000000, 77.83585931145570669, -124.9186683157258244 ) ) ;
#57376=DIRECTION ( 'NONE',  ( 0.000000000000000000, 0.000000000000000000, 1.000000000000000000 ) ) ;
#57382=TOROIDAL_SURFACE ( 'NONE', #203137, 7.800000000000000711, 0.1000000000000000056 ) ;
#57493=LINE ( 'NONE', #134460, #17814 ) ;
#57514=VERTEX_POINT ( 'NONE', #245818 ) ;
#57515=CARTESIAN_POINT ( 'NONE',  ( -20.64999999999999858, 71.65000000001222702, -148.8731074845244109 ) ) ;
#57516=CARTESIAN_POINT ( 'NONE',  ( -23.15000000000000213, 76.00000000001237765, -170.0231074845243597 ) ) ;
#57528=ORIENTED_EDGE ( 'NONE', *, *, #221459, .T. ) ;
#57536=DIRECTION ( 'NONE',  ( -1.000000000000000000, 0.000000000000000000, -0.000000000000000000 ) ) ;
#57550=CARTESIAN_POINT ( 'NONE',  ( -21.59142135623730852, 68.15000000001228386, -157.6731074845243938 ) ) ;
#57576=ORIENTED_EDGE ( 'NONE', *, *, #37276, .F. ) ;
#57584=FACE_OUTER_BOUND ( 'NONE', #87149, .T. ) ;
#57594=ADVANCED_FACE ( 'NONE', ( #94433 ), #227556, .T. ) ;
#57605=CARTESIAN_POINT ( 'NONE',  ( -23.25000000000000000, 64.25000000001237765, -170.0231074845244166 ) ) ;
#57628=AXIS2_PLACEMENT_3D ( 'NONE', #245622, #168702, #205188 ) ;
#57629=CIRCLE ( 'NONE', #211777, 0.9750000000000036415 ) ;
#57635=CARTESIAN_POINT ( 'NONE',  ( -22.59999999999999787, 75.89914163091376054, -181.7726746080137445 ) ) ;
#57707=ORIENTED_EDGE ( 'NONE', *, *, #78535, .F. ) ;
#57776=CARTESIAN_POINT ( 'NONE',  ( 18.59999999999999076, 68.92903212821327941, -132.7765432626560766 ) ) ;
#57809=ORIENTED_EDGE ( 'NONE', *, *, #223630, .F. ) ;
#57810=CARTESIAN_POINT ( 'NONE',  ( -18.59999999999999787, 74.83729825007431202, -161.9231074845243654 ) ) ;
#57838=ORIENTED_EDGE ( 'NONE', *, *, #165335, .F. ) ;
#57878=EDGE_CURVE ( 'NONE', #214666, #21932, #19482, .T. ) ;
#57895=EDGE_CURVE ( 'NONE', #59389, #152420, #185498, .T. ) ;
#57897=ORIENTED_EDGE ( 'NONE', *, *, #10066, .T. ) ;
#57914=AXIS2_PLACEMENT_3D ( 'NONE', #11104, #211886, #213145 ) ;
#57942=EDGE_CURVE ( 'NONE', #176041, #110939, #160585, .T. ) ;
#57943=CARTESIAN_POINT ( 'NONE',  ( 21.05000000000000071, 64.35000000001237197, -169.9231074845244507 ) ) ;
#57975=DIRECTION ( 'NONE',  ( 1.000000000000000000, 0.000000000000000000, 0.000000000000000000 ) ) ;
#57988=CIRCLE ( 'NONE', #107884, 0.5000000000000004441 ) ;
#58023=CARTESIAN_POINT ( 'NONE',  ( 18.49999999999999289, 65.76093837589073132, -145.2687100499267387 ) ) ;
#58036=ORIENTED_EDGE ( 'NONE', *, *, #48729, .T. ) ;
#58044=EDGE_CURVE ( 'NONE', #125708, #117495, #133271, .T. ) ;
#58062=CARTESIAN_POINT ( 'NONE',  ( -20.64999999999999858, 85.00000000001222134, -146.4170766071767389 ) ) ;
#58088=CARTESIAN_POINT ( 'NONE',  ( 21.53699400383916185, 76.00000000001243450, -176.8108192777720831 ) ) ;
#58090=CYLINDRICAL_SURFACE ( 'NONE', #22114, 0.09999999999999939493 ) ;
#58091=VERTEX_POINT ( 'NONE', #207682 ) ;
#58105=CARTESIAN_POINT ( 'NONE',  ( -20.64999999999999858, 76.00000000001213607, -136.5231074845243313 ) ) ;
#58119=ORIENTED_EDGE ( 'NONE', *, *, #222955, .F. ) ;
#58123=DIRECTION ( 'NONE',  ( 0.000000000000000000, -6.982962677686266711E-15, 1.000000000000000000 ) ) ;
#58150=ORIENTED_EDGE ( 'NONE', *, *, #145802, .T. ) ;
#58185=VERTEX_POINT ( 'NONE', #175015 ) ;
#58253=DIRECTION ( 'NONE',  ( 1.000000000000000000, 0.000000000000000000, 0.000000000000000000 ) ) ;
#58259=EDGE_CURVE ( 'NONE', #152420, #60849, #146102, .T. ) ;
#58263=DIRECTION ( 'NONE',  ( 0.000000000000000000, -0.008583690987135041833, 0.9999631594459055250 ) ) ;
#58271=PLANE ( 'NONE',  #173682 ) ;
#58272=ORIENTED_EDGE ( 'NONE', *, *, #75114, .T. ) ;
#58292=VERTEX_POINT ( 'NONE', #143532 ) ;
#58319=DIRECTION ( 'NONE',  ( 1.000000000000000000, 0.000000000000000000, 0.000000000000000000 ) ) ;
#58365=ORIENTED_EDGE ( 'NONE', *, *, #44155, .T. ) ;
#58409=ORIENTED_EDGE ( 'NONE', *, *, #64092, .F. ) ;
#58424=CARTESIAN_POINT ( 'NONE',  ( 18.48413544395640074, 85.66430403364005031, -129.8400024914862456 ) ) ;
#58442=DIRECTION ( 'NONE',  ( 1.000000000000000000, 0.000000000000000000, 0.000000000000000000 ) ) ;
#58466=CIRCLE ( 'NONE', #4312, 11.90000000000000746 ) ;
#58485=ORIENTED_EDGE ( 'NONE', *, *, #142432, .T. ) ;
#58488=CARTESIAN_POINT ( 'NONE',  ( 20.94999999999999574, 87.65000000001235492, -167.0231074845242460 ) ) ;
#58496=CARTESIAN_POINT ( 'NONE',  ( -20.54999999999999716, 76.00000000001237765, -170.0231074845243597 ) ) ;
#58517=DIRECTION ( 'NONE',  ( 1.836970198721029934E-16, 1.000000000000000000, 6.982962677686266711E-15 ) ) ;
#58522=ADVANCED_FACE ( 'NONE', ( #158646 ), #180753, .F. ) ;
#58523=CIRCLE ( 'NONE', #100207, 0.09999999999998898659 ) ;
#58591=DIRECTION ( 'NONE',  ( 1.000000000000000000, -3.265361837132813093E-16, -2.280189983783949500E-30 ) ) ;
#58594=VERTEX_POINT ( 'NONE', #26836 ) ;
#58614=CIRCLE ( 'NONE', #91937, 0.2000000000000057288 ) ;
#58638=CARTESIAN_POINT ( 'NONE',  ( 21.14999999999999858, 64.25000000001227818, -157.8731074845244393 ) ) ;
#58674=FACE_OUTER_BOUND ( 'NONE', #109755, .T. ) ;
#58677=CARTESIAN_POINT ( 'NONE',  ( 20.94999999999999574, 87.75000000001234923, -166.9231074845242802 ) ) ;
#58683=ORIENTED_EDGE ( 'NONE', *, *, #52524, .T. ) ;
#58703=CIRCLE ( 'NONE', #92034, 0.09999999999999939493 ) ;
#58712=PLANE ( 'NONE',  #252235 ) ;
#58720=CARTESIAN_POINT ( 'NONE',  ( -21.30740335185486245, 75.90106547423657446, -176.5797654065523545 ) ) ;
#58748=TOROIDAL_SURFACE ( 'NONE', #183688, 0.4000000000000009104, 0.1000000000000000056 ) ;
#58750=FACE_OUTER_BOUND ( 'NONE', #66508, .T. ) ;
#58764=VERTEX_POINT ( 'NONE', #134862 ) ;
#58818=CARTESIAN_POINT ( 'NONE',  ( -18.59999999999999787, 76.00000000001237765, -170.0231074845243597 ) ) ;
#58834=CARTESIAN_POINT ( 'NONE',  ( 18.58719872626880942, 85.56664439761073027, -129.7006292881272884 ) ) ;
#58853=ORIENTED_EDGE ( 'NONE', *, *, #215764, .T. ) ;
#58870=ORIENTED_EDGE ( 'NONE', *, *, #159592, .F. ) ;
#58903=DIRECTION ( 'NONE',  ( 1.000000000000000000, 7.304098846218105085E-16, 4.217023435051677501E-16 ) ) ;
#58908=AXIS2_PLACEMENT_3D ( 'NONE', #233619, #95380, #254424 ) ;
#59005=ORIENTED_EDGE ( 'NONE', *, *, #241713, .T. ) ;
#59032=FACE_OUTER_BOUND ( 'NONE', #28009, .T. ) ;
#59054=ADVANCED_FACE ( 'NONE', ( #112478, #12104 ), #34243, .F. ) ;
#59062=CARTESIAN_POINT ( 'NONE',  ( -21.56666275994539816, 76.00000000001242029, -176.9804758914176830 ) ) ;
#59098=ORIENTED_EDGE ( 'NONE', *, *, #5983, .F. ) ;
#59126=CARTESIAN_POINT ( 'NONE',  ( 21.05000000000000071, 65.45624872451672616, -162.4667196758603893 ) ) ;
#59217=SPHERICAL_SURFACE ( 'NONE', #157350, 0.1000000000000000056 ) ;
#59226=DIRECTION ( 'NONE',  ( 1.000000000000000000, -0.000000000000000000, 0.000000000000000000 ) ) ;
#59227=CARTESIAN_POINT ( 'NONE',  ( -18.50000000000000000, 85.40000000001232650, -162.7258477248610120 ) ) ;
#59241=AXIS2_PLACEMENT_3D ( 'NONE', #245657, #82689, #181832 ) ;
#59256=CARTESIAN_POINT ( 'NONE',  ( -20.85000000000000142, 77.73670573947964613, -125.0056848969006182 ) ) ;
#59257=ADVANCED_FACE ( 'NONE', ( #138416 ), #18507, .F. ) ;
#59258=AXIS2_PLACEMENT_3D ( 'NONE', #232681, #54021, #133561 ) ;
#59272=CIRCLE ( 'NONE', #67703, 0.09999999999998898659 ) ;
#59282=FACE_OUTER_BOUND ( 'NONE', #184899, .T. ) ;
#59296=CIRCLE ( 'NONE', #221634, 12.77499999999999503 ) ;
#59304=VERTEX_POINT ( 'NONE', #160610 ) ;
#59312=AXIS2_PLACEMENT_3D ( 'NONE', #63457, #185983, #125999 ) ;
#59314=CIRCLE ( 'NONE', #21959, 0.09999999999999939493 ) ;
#59319=DIRECTION ( 'NONE',  ( -4.336808689941751890E-15, -0.8660254037844445918, -0.4999999999999897304 ) ) ;
#59322=EDGE_LOOP ( 'NONE', ( #159822, #181528, #186984, #240541, #153190 ) ) ;
#59337=VERTEX_POINT ( 'NONE', #242674 ) ;
#59339=VECTOR ( 'NONE', #90623, 1000.000000000000000 ) ;
#59357=DIRECTION ( 'NONE',  ( -0.000000000000000000, 6.982962677686266711E-15, -1.000000000000000000 ) ) ;
#59358=CARTESIAN_POINT ( 'NONE',  ( 22.47007471830799474, 76.00000000001243450, -177.7438181364508694 ) ) ;
#59359=DIRECTION ( 'NONE',  ( -1.000000000000000000, 0.000000000000000000, 0.000000000000000000 ) ) ;
#59364=DIRECTION ( 'NONE',  ( 1.000000000000000000, 0.000000000000000000, -0.000000000000000000 ) ) ;
#59389=VERTEX_POINT ( 'NONE', #110878 ) ;
#59408=VECTOR ( 'NONE', #246049, 1000.000000000000000 ) ;
#59414=CARTESIAN_POINT ( 'NONE',  ( 23.24999999999999645, 71.00000000001230660, -157.6178414656113205 ) ) ;
#59416=VERTEX_POINT ( 'NONE', #252940 ) ;
#59417=CARTESIAN_POINT ( 'NONE',  ( 21.14999999999999858, 75.90220970870363715, -176.2809220950004772 ) ) ;
#59420=VERTEX_POINT ( 'NONE', #93876 ) ;
#59422=EDGE_CURVE ( 'NONE', #86183, #206239, #8388, .T. ) ;
#59430=CARTESIAN_POINT ( 'NONE',  ( -22.49756042579671700, 75.92195366299527848, -181.6729724456266979 ) ) ;
#59444=VECTOR ( 'NONE', #227003, 1000.000000000000000 ) ;
#59446=CIRCLE ( 'NONE', #42743, 0.09999999999999939493 ) ;
#59450=ORIENTED_EDGE ( 'NONE', *, *, #71140, .F. ) ;
#59463=ORIENTED_EDGE ( 'NONE', *, *, #199789, .F. ) ;
#59483=PLANE ( 'NONE',  #159358 ) ;
#59489=ORIENTED_EDGE ( 'NONE', *, *, #234867, .T. ) ;
#59526=CARTESIAN_POINT ( 'NONE',  ( -22.59999999999999787, 64.35042919246758686, -170.1231074845244393 ) ) ;
#59529=AXIS2_PLACEMENT_3D ( 'NONE', #142281, #62754, #22364 ) ;
#59556=CARTESIAN_POINT ( 'NONE',  ( 20.94999999999999574, 77.73625713160970463, -158.4544551555068495 ) ) ;
#59586=CIRCLE ( 'NONE', #205344, 7.900000000000003908 ) ;
#59597=CARTESIAN_POINT ( 'NONE',  ( 21.05000000000000071, 69.45934304831114048, -170.0231074845243882 ) ) ;
#59603=AXIS2_PLACEMENT_3D ( 'NONE', #147602, #671, #41143 ) ;
#59605=TOROIDAL_SURFACE ( 'NONE', #84539, 0.9750000000000019762, 0.1000000000000000056 ) ;
#59618=ORIENTED_EDGE ( 'NONE', *, *, #162, .F. ) ;
#59628=ORIENTED_EDGE ( 'NONE', *, *, #77197, .T. ) ;
#59643=AXIS2_PLACEMENT_3D ( 'NONE', #213093, #37061, #55271 ) ;
#59648=ORIENTED_EDGE ( 'NONE', *, *, #246900, .F. ) ;
#59680=AXIS2_PLACEMENT_3D ( 'NONE', #153664, #228341, #147512 ) ;
#59682=AXIS2_PLACEMENT_3D ( 'NONE', #163203, #238883, #240174 ) ;
#59685=EDGE_CURVE ( 'NONE', #86120, #77802, #44193, .T. ) ;
#59689=DIRECTION ( 'NONE',  ( 0.000000000000000000, -0.1350103645451945777, 0.9908441862701591329 ) ) ;
#59690=CYLINDRICAL_SURFACE ( 'NONE', #79976, 0.09999999999998898659 ) ;
#59709=CARTESIAN_POINT ( 'NONE',  ( 18.31325810956293410, 85.53638847601938267, -129.6546672782193923 ) ) ;
#59711=EDGE_CURVE ( 'NONE', #112125, #117495, #25340, .T. ) ;
#59724=CIRCLE ( 'NONE', #176481, 0.1000000000000028644 ) ;
#59732=DIRECTION ( 'NONE',  ( 1.000000000000000000, 0.000000000000000000, 0.000000000000000000 ) ) ;
#59736=EDGE_CURVE ( 'NONE', #77760, #164498, #171109, .T. ) ;
#59737=AXIS2_PLACEMENT_3D ( 'NONE', #37866, #97782, #176097 ) ;
#59740=FACE_OUTER_BOUND ( 'NONE', #236715, .T. ) ;
#59741=ORIENTED_EDGE ( 'NONE', *, *, #64092, .T. ) ;
#59757=CARTESIAN_POINT ( 'NONE',  ( -21.05000000000000071, 87.75000000001216449, -139.5231074845243029 ) ) ;
#59762=CARTESIAN_POINT ( 'NONE',  ( 18.59999999999999432, 77.16270174995034381, -161.9231074845243370 ) ) ;
#59786=DIRECTION ( 'NONE',  ( 0.000000000000000000, 6.982962677686266711E-15, -1.000000000000000000 ) ) ;
#59787=CARTESIAN_POINT ( 'NONE',  ( 20.95462737510932882, 65.44321804836857837, -162.4531574279621395 ) ) ;
#59788=CARTESIAN_POINT ( 'NONE',  ( 23.14999999999999503, 64.35000000001218723, -143.4379132551783869 ) ) ;
#59800=ORIENTED_EDGE ( 'NONE', *, *, #130400, .F. ) ;
#59864=DIRECTION ( 'NONE',  ( 1.000000000000000000, 0.000000000000000000, 0.000000000000000000 ) ) ;
#59876=EDGE_CURVE ( 'NONE', #84708, #14612, #175207, .T. ) ;
#59883=CYLINDRICAL_SURFACE ( 'NONE', #177220, 0.09999999999999939493 ) ;
#59885=AXIS2_PLACEMENT_3D ( 'NONE', #191923, #34139, #113636 ) ;
#59896=CARTESIAN_POINT ( 'NONE',  ( -20.85000000000000142, 64.35000000001220144, -143.3069731475025321 ) ) ;
#59915=FACE_OUTER_BOUND ( 'NONE', #62613, .T. ) ;
#59935=DIRECTION ( 'NONE',  ( 0.000000000000000000, -1.000000000000000000, 0.000000000000000000 ) ) ;
#59945=CARTESIAN_POINT ( 'NONE',  ( 21.05000000000000071, 67.22371710471982453, -157.8731074845244109 ) ) ;
#60008=AXIS2_PLACEMENT_3D ( 'NONE', #215862, #244431, #162353 ) ;
#60009=SPHERICAL_SURFACE ( 'NONE', #108676, 0.1000000000000000056 ) ;
#60016=DIRECTION ( 'NONE',  ( -1.000000000000000000, 0.000000000000000000, -0.000000000000000000 ) ) ;
#60031=DIRECTION ( 'NONE',  ( 0.000000000000000000, 0.000000000000000000, -1.000000000000000000 ) ) ;
#60057=VERTEX_POINT ( 'NONE', #151053 ) ;
#60058=DIRECTION ( 'NONE',  ( 1.000000000000000000, 0.000000000000000000, 0.000000000000000000 ) ) ;
#60059=EDGE_CURVE ( 'NONE', #44660, #249154, #233612, .T. ) ;
#60064=CIRCLE ( 'NONE', #43341, 0.09999999999998898659 ) ;
#60068=ORIENTED_EDGE ( 'NONE', *, *, #85021, .F. ) ;
#60154=CYLINDRICAL_SURFACE ( 'NONE', #174046, 0.1000000000000028644 ) ;
#60179=ORIENTED_EDGE ( 'NONE', *, *, #229230, .T. ) ;
#60191=ORIENTED_EDGE ( 'NONE', *, *, #203595, .F. ) ;
#60193=EDGE_CURVE ( 'NONE', #244844, #86021, #208684, .T. ) ;
#60235=EDGE_LOOP ( 'NONE', ( #113938, #90047, #35417, #238150 ) ) ;
#60277=DIRECTION ( 'NONE',  ( 0.000000000000000000, 0.000000000000000000, -1.000000000000000000 ) ) ;
#60281=DIRECTION ( 'NONE',  ( -0.000000000000000000, -6.982962677686266711E-15, 1.000000000000000000 ) ) ;
#60285=ADVANCED_FACE ( 'NONE', ( #217411 ), #15399, .F. ) ;
#60295=DIRECTION ( 'NONE',  ( 1.000000000000000000, -2.952720810173289112E-16, -2.061873921506763405E-30 ) ) ;
#60302=DIRECTION ( 'NONE',  ( 0.000000000000000000, 0.1495327102803283015, 0.9887567792719397231 ) ) ;
#60305=ORIENTED_EDGE ( 'NONE', *, *, #250739, .T. ) ;
#60335=DIRECTION ( 'NONE',  ( 0.000000000000000000, 0.000000000000000000, 1.000000000000000000 ) ) ;
#60353=VERTEX_POINT ( 'NONE', #41388 ) ;
#60371=ORIENTED_EDGE ( 'NONE', *, *, #147953, .T. ) ;
#60376=DIRECTION ( 'NONE',  ( -0.000000000000000000, 1.000000000000000000, 6.982962677686266711E-15 ) ) ;
#60390=AXIS2_PLACEMENT_3D ( 'NONE', #150624, #191060, #177602 ) ;
#60448=ORIENTED_EDGE ( 'NONE', *, *, #195659, .F. ) ;
#60460=CARTESIAN_POINT ( 'NONE',  ( -21.05000000000000071, 61.95000000001234497, -164.5094124137634708 ) ) ;
#60464=CARTESIAN_POINT ( 'NONE',  ( 23.24999999999999289, 64.25000000001244871, -181.7731074845244450 ) ) ;
#60551=DIRECTION ( 'NONE',  ( 0.000000000000000000, 0.000000000000000000, 1.000000000000000000 ) ) ;
#60560=DIRECTION ( 'NONE',  ( -1.000000000000000000, 1.836970198721029934E-16, 1.282749433769087582E-30 ) ) ;
#60565=DIRECTION ( 'NONE',  ( -1.000000000000000000, 7.304098846218134667E-16, 5.100424963727255829E-30 ) ) ;
#60615=CARTESIAN_POINT ( 'NONE',  ( 22.45305468355010703, 76.10085836911217427, -181.7726746080141140 ) ) ;
#60624=DIRECTION ( 'NONE',  ( -0.000000000000000000, 1.000000000000000000, 6.982962677686266711E-15 ) ) ;
#60635=ADVANCED_FACE ( 'NONE', ( #35938 ), #245936, .T. ) ;
#60650=EDGE_CURVE ( 'NONE', #128947, #231343, #154616, .T. ) ;
#60672=ADVANCED_FACE ( 'NONE', ( #251094 ), #54187, .T. ) ;
#60712=CIRCLE ( 'NONE', #185639, 0.09999999999998898659 ) ;
#60762=EDGE_LOOP ( 'NONE', ( #38674, #30627, #106624, #222702 ) ) ;
#60803=ORIENTED_EDGE ( 'NONE', *, *, #238619, .T. ) ;
#60821=DIRECTION ( 'NONE',  ( 2.710505431213777355E-16, 1.000000000000000000, 6.982962677686266711E-15 ) ) ;
#60842=ORIENTED_EDGE ( 'NONE', *, *, #137452, .F. ) ;
#60849=VERTEX_POINT ( 'NONE', #150452 ) ;
#60877=AXIS2_PLACEMENT_3D ( 'NONE', #99648, #35878, #18855 ) ;
#60879=TOROIDAL_SURFACE ( 'NONE', #73396, 4.099999999999999645, 0.1000000000000000056 ) ;
#60884=CARTESIAN_POINT ( 'NONE',  ( 23.24999999999999289, 70.05000000001221849, -146.8288097895591875 ) ) ;
#60898=VECTOR ( 'NONE', #90727, 1000.000000000000000 ) ;
#60919=FACE_OUTER_BOUND ( 'NONE', #95560, .T. ) ;
#60930=ORIENTED_EDGE ( 'NONE', *, *, #222592, .T. ) ;
#60967=CARTESIAN_POINT ( 'NONE',  ( 20.94999999999999574, 87.41227409416205774, -167.1231074845242688 ) ) ;
#60972=DIRECTION ( 'NONE',  ( 0.000000000000000000, -6.982962677686267499E-15, 1.000000000000000000 ) ) ;
#61008=CARTESIAN_POINT ( 'NONE',  ( 18.59999996954842771, 85.52320413787039399, -129.6400657726071017 ) ) ;
#61059=DIRECTION ( 'NONE',  ( 1.000000000000000000, 7.304098846218163263E-16, -4.217023435051627211E-16 ) ) ;
#61061=DIRECTION ( 'NONE',  ( 0.000000000000000000, 1.000000000000000000, 6.982962677686266711E-15 ) ) ;
#61090=ORIENTED_EDGE ( 'NONE', *, *, #81531, .F. ) ;
#61091=FACE_OUTER_BOUND ( 'NONE', #64835, .T. ) ;
#61120=CARTESIAN_POINT ( 'NONE',  ( 20.94999999999999929, 87.48912529308822172, -139.5231074845243029 ) ) ;
#61198=CIRCLE ( 'NONE', #140272, 0.1999999999999987899 ) ;
#61215=CYLINDRICAL_SURFACE ( 'NONE', #150581, 0.1000000000000118433 ) ;
#61217=CYLINDRICAL_SURFACE ( 'NONE', #79566, 0.5000000000000004441 ) ;
#61219=CIRCLE ( 'NONE', #231928, 0.09999999999998898659 ) ;
#61230=CARTESIAN_POINT ( 'NONE',  ( 21.05000000000000071, 87.75000000001216449, -139.6231074845242688 ) ) ;
#61259=AXIS2_PLACEMENT_3D ( 'NONE', #180212, #81075, #160664 ) ;
#61263=AXIS2_PLACEMENT_3D ( 'NONE', #228729, #67069, #72220 ) ;
#61275=CARTESIAN_POINT ( 'NONE',  ( 18.53317502108576775, 65.67736539654967487, -130.9625116876572406 ) ) ;
#61294=ORIENTED_EDGE ( 'NONE', *, *, #130194, .F. ) ;
#61296=ADVANCED_FACE ( 'NONE', ( #12880 ), #192644, .T. ) ;
#61299=VERTEX_POINT ( 'NONE', #111970 ) ;
#61303=DIRECTION ( 'NONE',  ( 2.940209281316621016E-16, 1.000000000000000000, 7.056502275159890832E-15 ) ) ;
#61322=FACE_OUTER_BOUND ( 'NONE', #19786, .T. ) ;
#61327=ORIENTED_EDGE ( 'NONE', *, *, #253149, .F. ) ;
#61341=VERTEX_POINT ( 'NONE', #191521 ) ;
#61343=ORIENTED_EDGE ( 'NONE', *, *, #138796, .T. ) ;
#61371=ADVANCED_FACE ( 'NONE', ( #29879 ), #10305, .T. ) ;
#61384=VERTEX_POINT ( 'NONE', #216171 ) ;
#61416=DIRECTION ( 'NONE',  ( 1.000000000000000000, -0.000000000000000000, 0.000000000000000000 ) ) ;
#61418=ORIENTED_EDGE ( 'NONE', *, *, #120333, .T. ) ;
#61430=VERTEX_POINT ( 'NONE', #19268 ) ;
#61431=CARTESIAN_POINT ( 'NONE',  ( -23.15000000000000213, 64.35000000001218723, -143.5379132551784096 ) ) ;
#61435=CARTESIAN_POINT ( 'NONE',  ( 18.39999999999999858, 85.68240343348850274, -129.8662641071115047 ) ) ;
#61457=ORIENTED_EDGE ( 'NONE', *, *, #37238, .F. ) ;
#61488=CARTESIAN_POINT ( 'NONE',  ( 21.14999999999999503, 76.00000000001242029, -176.2731074845243597 ) ) ;
#61493=ORIENTED_EDGE ( 'NONE', *, *, #213032, .F. ) ;
#61508=ORIENTED_EDGE ( 'NONE', *, *, #96906, .F. ) ;
#61521=ORIENTED_EDGE ( 'NONE', *, *, #255682, .T. ) ;
#61523=AXIS2_PLACEMENT_3D ( 'NONE', #4479, #42339, #103566 ) ;
#61534=CYLINDRICAL_SURFACE ( 'NONE', #70237, 7.899999999999990585 ) ;
#61558=EDGE_LOOP ( 'NONE', ( #115863, #168709, #34781 ) ) ;
#61576=DIRECTION ( 'NONE',  ( 0.000000000000000000, 6.982962677686266711E-15, -1.000000000000000000 ) ) ;
#61592=ORIENTED_EDGE ( 'NONE', *, *, #193360, .T. ) ;
#61603=DIRECTION ( 'NONE',  ( 0.000000000000000000, -0.9274965247785504907, -0.3738317757009320674 ) ) ;
#61608=VECTOR ( 'NONE', #46058, 1000.000000000000000 ) ;
#61642=CARTESIAN_POINT ( 'NONE',  ( 21.13461538461538325, 67.11458296203782936, -157.7731074845244166 ) ) ;
#61654=EDGE_CURVE ( 'NONE', #148976, #219200, #225143, .T. ) ;
#61694=ORIENTED_EDGE ( 'NONE', *, *, #220705, .F. ) ;
#61696=VERTEX_POINT ( 'NONE', #49088 ) ;
#61741=ADVANCED_FACE ( 'NONE', ( #9973 ), #131195, .T. ) ;
#61744=DIRECTION ( 'NONE',  ( 1.000000000000000000, -0.000000000000000000, 0.000000000000000000 ) ) ;
#61770=ORIENTED_EDGE ( 'NONE', *, *, #170355, .T. ) ;
#61788=ORIENTED_EDGE ( 'NONE', *, *, #3260, .F. ) ;
#61813=VECTOR ( 'NONE', #148698, 1000.000000000000000 ) ;
#61831=ADVANCED_FACE ( 'NONE', ( #55476 ), #17659, .T. ) ;
#61883=CARTESIAN_POINT ( 'NONE',  ( -21.05000000000000071, 76.00000000001237765, -170.0231074845243597 ) ) ;
#61886=CIRCLE ( 'NONE', #186799, 0.09999999999999938105 ) ;
#61926=CIRCLE ( 'NONE', #174403, 0.09999999999999939493 ) ;
#61927=AXIS2_PLACEMENT_3D ( 'NONE', #157728, #155149, #218919 ) ;
#61950=ORIENTED_EDGE ( 'NONE', *, *, #130681, .F. ) ;
#61952=EDGE_CURVE ( 'NONE', #92370, #129641, #181894, .T. ) ;
#61993=CARTESIAN_POINT ( 'NONE',  ( 18.59999999999999076, 70.05000000001236060, -159.7174051794895320 ) ) ;
#62002=CARTESIAN_POINT ( 'NONE',  ( 23.24999999999999289, 64.35000000001237197, -169.9231074845244507 ) ) ;
#62006=DIRECTION ( 'NONE',  ( 0.000000000000000000, -1.000000000000000000, -6.982962677686265922E-15 ) ) ;
#62033=CIRCLE ( 'NONE', #107806, 11.80000000000000426 ) ;
#62038=TOROIDAL_SURFACE ( 'NONE', #207802, 12.77500000000000036, 0.1000000000000000056 ) ;
#62106=VERTEX_POINT ( 'NONE', #170082 ) ;
#62111=CIRCLE ( 'NONE', #82914, 0.09999999999999939493 ) ;
#62158=EDGE_CURVE ( 'NONE', #248221, #253904, #114056, .T. ) ;
#62162=ORIENTED_EDGE ( 'NONE', *, *, #210439, .F. ) ;
#62181=DIRECTION ( 'NONE',  ( 0.000000000000000000, 1.000000000000000000, 1.387778780781444413E-14 ) ) ;
#62188=CIRCLE ( 'NONE', #20506, 0.1000000000000046685 ) ;
#62202=VERTEX_POINT ( 'NONE', #194759 ) ;
#62209=DIRECTION ( 'NONE',  ( 0.000000000000000000, -6.982962677686266711E-15, 1.000000000000000000 ) ) ;
#62223=DIRECTION ( 'NONE',  ( -0.000000000000000000, -6.982962677686266711E-15, 1.000000000000000000 ) ) ;
#62261=DIRECTION ( 'NONE',  ( 0.000000000000000000, 0.000000000000000000, 1.000000000000000000 ) ) ;
#62269=VECTOR ( 'NONE', #140656, 1000.000000000000000 ) ;
#62291=EDGE_LOOP ( 'NONE', ( #20664, #85539, #231077, #146394 ) ) ;
#62302=ADVANCED_FACE ( 'NONE', ( #151780 ), #155793, .T. ) ;
#62330=DIRECTION ( 'NONE',  ( -1.000000000000000000, -0.000000000000000000, -0.000000000000000000 ) ) ;
#62344=CARTESIAN_POINT ( 'NONE',  ( -21.05000000000000071, 74.83729825007431202, -161.9231074845243654 ) ) ;
#62369=DIRECTION ( 'NONE',  ( 1.000000000000000000, -0.000000000000000000, 0.000000000000000000 ) ) ;
#62385=DIRECTION ( 'NONE',  ( 0.000000000000000000, 1.000000000000000000, 6.982962677686266711E-15 ) ) ;
#62389=CARTESIAN_POINT ( 'NONE',  ( 20.95568717954149562, 65.39800594612050588, -162.4205991162557723 ) ) ;
#62399=ADVANCED_FACE ( 'NONE', ( #59032 ), #160773, .T. ) ;
#62400=AXIS2_PLACEMENT_3D ( 'NONE', #147313, #105592, #6517 ) ;
#62473=DIRECTION ( 'NONE',  ( -0.000000000000000000, 6.982962677686266711E-15, -1.000000000000000000 ) ) ;
#62499=VERTEX_POINT ( 'NONE', #45926 ) ;
#62501=ADVANCED_FACE ( 'NONE', ( #107175 ), #227120, .T. ) ;
#62508=DIRECTION ( 'NONE',  ( 1.000000000000000000, 0.000000000000000000, 0.000000000000000000 ) ) ;
#62514=ORIENTED_EDGE ( 'NONE', *, *, #214449, .F. ) ;
#62531=CARTESIAN_POINT ( 'NONE',  ( -22.47071067811865319, 75.90090754530983475, -177.7431822290224090 ) ) ;
#62543=EDGE_CURVE ( 'NONE', #152420, #247434, #24335, .T. ) ;
#62596=LINE ( 'NONE', #49443, #113617 ) ;
#62613=EDGE_LOOP ( 'NONE', ( #212349, #117313, #221771, #212177, #85660, #35659, #121503, #204609, #38301, #135165, #257172, #230106 ) ) ;
#62617=AXIS2_PLACEMENT_3D ( 'NONE', #1127, #255424, #80667 ) ;
#62631=ORIENTED_EDGE ( 'NONE', *, *, #165140, .T. ) ;
#62637=DIRECTION ( 'NONE',  ( 0.000000000000000000, -5.551115123125777653E-14, 1.000000000000000000 ) ) ;
#62685=CARTESIAN_POINT ( 'NONE',  ( -20.64999999999999858, 84.66355140188147743, -160.4990063664569959 ) ) ;
#62714=ORIENTED_EDGE ( 'NONE', *, *, #196070, .F. ) ;
#62754=DIRECTION ( 'NONE',  ( -1.836970198721029934E-16, -1.000000000000000000, -6.982962677686266711E-15 ) ) ;
#62769=LINE ( 'NONE', #45766, #120683 ) ;
#62776=ORIENTED_EDGE ( 'NONE', *, *, #236360, .F. ) ;
#62798=CARTESIAN_POINT ( 'NONE',  ( 20.21567752745066215, 65.80188589878034122, -162.1404871368697798 ) ) ;
#62830=AXIS2_PLACEMENT_3D ( 'NONE', #226027, #47408, #147823 ) ;
#62831=DIRECTION ( 'NONE',  ( 1.000000000000000000, 0.000000000000000000, 0.000000000000000000 ) ) ;
#62863=B_SPLINE_CURVE_WITH_KNOTS ( 'NONE', 3,
 ( #100745, #59062, #255961, #392 ),
 .UNSPECIFIED., .F., .F.,
 ( 4, 4 ),
 ( 0.000000000000000000, 0.001767853679387123601 ),
 .UNSPECIFIED. ) ;
#62867=FACE_OUTER_BOUND ( 'NONE', #162841, .T. ) ;
#62885=DIRECTION ( 'NONE',  ( 0.000000000000000000, 0.000000000000000000, 1.000000000000000000 ) ) ;
#62896=CARTESIAN_POINT ( 'NONE',  ( -21.05000000000000071, 87.48912529308822172, -139.4231074845242802 ) ) ;
#62909=DIRECTION ( 'NONE',  ( 0.000000000000000000, -7.429790795770644761E-15, 1.000000000000000000 ) ) ;
#62924=CARTESIAN_POINT ( 'NONE',  ( -23.15000000000000213, 85.60000000001245724, -181.7731074845243029 ) ) ;
#62967=CIRCLE ( 'NONE', #17201, 7.899999999999990585 ) ;
#63001=CARTESIAN_POINT ( 'NONE',  ( 23.14999999999999503, 64.25000000001227818, -157.8731074845244393 ) ) ;
#63005=CARTESIAN_POINT ( 'NONE',  ( -18.59999999999999787, 66.65000000001229807, -157.6731074845244223 ) ) ;
#63008=LINE ( 'NONE', #222055, #19403 ) ;
#63009=DIRECTION ( 'NONE',  ( -1.000000000000000000, 2.775557561562908012E-13, 0.000000000000000000 ) ) ;
#63016=FACE_OUTER_BOUND ( 'NONE', #101185, .T. ) ;
#63032=DIRECTION ( 'NONE',  ( 1.000000000000000000, 0.000000000000000000, 0.000000000000000000 ) ) ;
#63054=CARTESIAN_POINT ( 'NONE',  ( -20.94999999999999929, 64.25000000001233502, -163.1815067946273246 ) ) ;
#63168=FACE_OUTER_BOUND ( 'NONE', #11723, .T. ) ;
#63182=CARTESIAN_POINT ( 'NONE',  ( -18.59999999999999787, 77.68707439010402993, -182.8376804510660065 ) ) ;
#63190=EDGE_LOOP ( 'NONE', ( #211976, #190068, #76481, #91727 ) ) ;
#63194=CIRCLE ( 'NONE', #58908, 0.09999999999999939493 ) ;
#63205=DIRECTION ( 'NONE',  ( 0.000000000000000000, -0.1350103645451807555, -0.9908441862701610203 ) ) ;
#63229=DIRECTION ( 'NONE',  ( 0.000000000000000000, -0.3738317757008748909, -0.9274965247785733613 ) ) ;
#63252=ORIENTED_EDGE ( 'NONE', *, *, #21743, .F. ) ;
#63257=AXIS2_PLACEMENT_3D ( 'NONE', #251400, #136571, #98703 ) ;
#63264=DIRECTION ( 'NONE',  ( 1.000000000000000000, -7.304098846218133681E-16, -4.639676173203992654E-30 ) ) ;
#63317=AXIS2_PLACEMENT_3D ( 'NONE', #163569, #85277, #3182 ) ;
#63326=CARTESIAN_POINT ( 'NONE',  ( 20.93975676684922504, 65.68895814178263493, -131.0026557862138645 ) ) ;
#63332=DIRECTION ( 'NONE',  ( 0.000000000000000000, 0.000000000000000000, 1.000000000000000000 ) ) ;
#63335=EDGE_LOOP ( 'NONE', ( #54737, #78935, #119106, #20390 ) ) ;
#63369=ORIENTED_EDGE ( 'NONE', *, *, #152737, .F. ) ;
#63406=AXIS2_PLACEMENT_3D ( 'NONE', #144577, #244975, #145864 ) ;
#63413=LINE ( 'NONE', #205493, #67684 ) ;
#63425=ORIENTED_EDGE ( 'NONE', *, *, #96709, .F. ) ;
#63432=VECTOR ( 'NONE', #153522, 1000.000000000000114 ) ;
#63437=ORIENTED_EDGE ( 'NONE', *, *, #28411, .T. ) ;
#63447=TOROIDAL_SURFACE ( 'NONE', #92678, 11.65000000000000036, 0.1000000000000000056 ) ;
#63457=CARTESIAN_POINT ( 'NONE',  ( 18.59999999999999432, 74.83729825007431202, -161.9231074845243654 ) ) ;
#63470=DIRECTION ( 'NONE',  ( 0.000000000000000000, -1.565658005757035267E-14, 1.000000000000000000 ) ) ;
#63490=CARTESIAN_POINT ( 'NONE',  ( 21.12802099929860944, 67.21944740979007804, -157.7749174995927888 ) ) ;
#63562=EDGE_LOOP ( 'NONE', ( #129321, #160226, #214364, #116988 ) ) ;
#63583=ORIENTED_EDGE ( 'NONE', *, *, #177329, .T. ) ;
#63588=DIRECTION ( 'NONE',  ( -0.000000000000000000, -0.8700118002898356018, 0.4930308989875170078 ) ) ;
#63652=ORIENTED_EDGE ( 'NONE', *, *, #113924, .T. ) ;
#63676=ORIENTED_EDGE ( 'NONE', *, *, #52376, .T. ) ;
#63684=CARTESIAN_POINT ( 'NONE',  ( 20.85000000000000142, 76.00000000001213607, -136.5231074845243313 ) ) ;
#63686=ADVANCED_FACE ( 'NONE', ( #186776 ), #225848, .T. ) ;
#63745=DIRECTION ( 'NONE',  ( 0.000000000000000000, -6.982962677686266711E-15, 1.000000000000000000 ) ) ;
#63780=EDGE_CURVE ( 'NONE', #171719, #88042, #60064, .T. ) ;
#63790=ADVANCED_FACE ( 'NONE', ( #95363 ), #18378, .F. ) ;
#63836=( BOUNDED_CURVE ( )  B_SPLINE_CURVE ( 3, ( #92729, #52309, #114875, #194437 ),
 .UNSPECIFIED., .F., .F. ) 
 B_SPLINE_CURVE_WITH_KNOTS ( ( 4, 4 ),
 ( 3.141592653589793116, 4.712388980384689674 ),
 .UNSPECIFIED. ) 
 CURVE ( )  GEOMETRIC_REPRESENTATION_ITEM ( )  RATIONAL_B_SPLINE_CURVE ( ( 1.000000000000000000, 0.8047378541243649375, 0.8047378541243649375, 1.000000000000000000 ) ) 
 REPRESENTATION_ITEM ( '' )  );
#63848=CARTESIAN_POINT ( 'NONE',  ( -20.85000000000000142, 76.32388570108247450, -136.5655178952103768 ) ) ;
#63873=CARTESIAN_POINT ( 'NONE',  ( -21.05000000000000071, 70.15000000001221281, -146.6556047088023149 ) ) ;
#63882=DIRECTION ( 'NONE',  ( 0.000000000000000000, 0.9876197685951241256, 0.1568667991644932258 ) ) ;
#63887=CARTESIAN_POINT ( 'NONE',  ( -22.37643362114956602, 75.90091862633104824, -177.6488974784827519 ) ) ;
#63888=LINE ( 'NONE', #163008, #127214 ) ;
#63902=CARTESIAN_POINT ( 'NONE',  ( 18.49999999999999289, 64.25000000001246292, -181.7731074845244450 ) ) ;
#63971=ORIENTED_EDGE ( 'NONE', *, *, #94419, .F. ) ;
#63981=AXIS2_PLACEMENT_3D ( 'NONE', #203274, #139427, #100297 ) ;
#64000=CARTESIAN_POINT ( 'NONE',  ( 19.75857864376268935, 64.25000000001220712, -145.2731074845243882 ) ) ;
#64019=EDGE_CURVE ( 'NONE', #219844, #64653, #119796, .T. ) ;
#64025=VERTEX_POINT ( 'NONE', #58488 ) ;
#64045=CARTESIAN_POINT ( 'NONE',  ( 20.94999999999999929, 85.40000000001231228, -160.1291383618718385 ) ) ;
#64058=AXIS2_PLACEMENT_3D ( 'NONE', #24259, #82885, #7224 ) ;
#64074=CARTESIAN_POINT ( 'NONE',  ( 21.05000000000000071, 70.10000000001220144, -146.7422072491807796 ) ) ;
#64092=EDGE_CURVE ( 'NONE', #166820, #8831, #51863, .T. ) ;
#64094=TOROIDAL_SURFACE ( 'NONE', #176542, 0.4000000000000015210, 0.1000000000000000056 ) ;
#64096=DIRECTION ( 'NONE',  ( 1.000000000000000000, 0.000000000000000000, 0.000000000000000000 ) ) ;
#64116=CARTESIAN_POINT ( 'NONE',  ( -22.48660254037843487, 64.35000000001238618, -170.0731074845244279 ) ) ;
#64128=CARTESIAN_POINT ( 'NONE',  ( 23.14999999999999503, 64.35000000001218723, -143.5379132551783812 ) ) ;
#64130=ORIENTED_EDGE ( 'NONE', *, *, #60193, .T. ) ;
#64154=TOROIDAL_SURFACE ( 'NONE', #218235, 12.97499999999999787, 0.1000000000000000056 ) ;
#64165=DIRECTION ( 'NONE',  ( -1.000000000000000000, 0.000000000000000000, 0.000000000000000000 ) ) ;
#64172=FACE_OUTER_BOUND ( 'NONE', #99683, .T. ) ;
#64173=ORIENTED_EDGE ( 'NONE', *, *, #195629, .T. ) ;
#64200=CARTESIAN_POINT ( 'NONE',  ( -21.05000000000000071, 69.45934304831114048, -169.9231074845244223 ) ) ;
#64208=DIRECTION ( 'NONE',  ( 4.377807931758639578E-15, -0.2605042016806606298, -0.9654727137038736640 ) ) ;
#64210=CARTESIAN_POINT ( 'NONE',  ( -18.59999999999999787, 68.97833521811203639, -132.7895420826271220 ) ) ;
#64213=ORIENTED_EDGE ( 'NONE', *, *, #194811, .T. ) ;
#64255=CIRCLE ( 'NONE', #214284, 0.09999999999998898659 ) ;
#64259=CARTESIAN_POINT ( 'NONE',  ( -18.59999999999999787, 102.4393534156131977, -151.8815988770167280 ) ) ;
#64268=AXIS2_PLACEMENT_3D ( 'NONE', #65631, #6943, #126901 ) ;
#64276=CIRCLE ( 'NONE', #93301, 0.09999999999998712696 ) ;
#64301=CARTESIAN_POINT ( 'NONE',  ( 21.05000000000000071, 65.37127968600796635, -162.3581939154368285 ) ) ;
#64346=LINE ( 'NONE', #201273, #118923 ) ;
#64365=CARTESIAN_POINT ( 'NONE',  ( -20.64999999999999858, 85.00000000001232081, -160.1291383618718385 ) ) ;
#64391=DIRECTION ( 'NONE',  ( -1.000000000000000000, 0.000000000000000000, -0.000000000000000000 ) ) ;
#64417=TOROIDAL_SURFACE ( 'NONE', #22742, 7.800000000000000711, 0.1000000000000000056 ) ;
#64453=ORIENTED_EDGE ( 'NONE', *, *, #182785, .T. ) ;
#64479=AXIS2_PLACEMENT_3D ( 'NONE', #4827, #60972, #84338 ) ;
#64502=ORIENTED_EDGE ( 'NONE', *, *, #138757, .F. ) ;
#64553=CARTESIAN_POINT ( 'NONE',  ( 18.59999999999999076, 69.45000000001230944, -160.0060803140843859 ) ) ;
#64563=DIRECTION ( 'NONE',  ( 0.000000000000000000, 0.000000000000000000, -1.000000000000000000 ) ) ;
#64567=TOROIDAL_SURFACE ( 'NONE', #77045, 0.2000000000000000111, 0.1000000000000000056 ) ;
#64604=ORIENTED_EDGE ( 'NONE', *, *, #247855, .T. ) ;
#64613=CARTESIAN_POINT ( 'NONE',  ( -20.85000000000000142, 64.25000000001220712, -143.3069731475025321 ) ) ;
#64618=ORIENTED_EDGE ( 'NONE', *, *, #130199, .T. ) ;
#64619=CARTESIAN_POINT ( 'NONE',  ( 20.93302460841142931, 65.68434038414380893, -130.9866880726065972 ) ) ;
#64653=VERTEX_POINT ( 'NONE', #241368 ) ;
#64656=DIRECTION ( 'NONE',  ( -3.265361837132813093E-16, -1.000000000000000000, -7.026728003956683390E-15 ) ) ;
#64671=ORIENTED_EDGE ( 'NONE', *, *, #179163, .T. ) ;
#64674=AXIS2_PLACEMENT_3D ( 'NONE', #190432, #170902, #33953 ) ;
#64690=AXIS2_PLACEMENT_3D ( 'NONE', #7591, #87113, #89677 ) ;
#64711=ADVANCED_FACE ( 'NONE', ( #180111 ), #1445, .F. ) ;
#64713=DIRECTION ( 'NONE',  ( 0.000000000000000000, 6.982962677686266711E-15, -1.000000000000000000 ) ) ;
#64735=DIRECTION ( 'NONE',  ( 1.000000000000000000, 0.000000000000000000, 0.000000000000000000 ) ) ;
#64737=ORIENTED_EDGE ( 'NONE', *, *, #132833, .T. ) ;
#64741=EDGE_CURVE ( 'NONE', #87344, #157707, #160620, .T. ) ;
#64745=LINE ( 'NONE', #103854, #205790 ) ;
#64747=ADVANCED_FACE ( 'NONE', ( #116286 ), #14444, .T. ) ;
#64767=CARTESIAN_POINT ( 'NONE',  ( 20.94999999999999929, 87.65000000001214175, -136.5231074845242745 ) ) ;
#64779=ORIENTED_EDGE ( 'NONE', *, *, #146392, .T. ) ;
#64786=ADVANCED_FACE ( 'NONE', ( #182682 ), #177182, .F. ) ;
#64835=EDGE_LOOP ( 'NONE', ( #198029, #32603, #181917, #101093 ) ) ;
#64868=ORIENTED_EDGE ( 'NONE', *, *, #179542, .F. ) ;
#64870=CARTESIAN_POINT ( 'NONE',  ( 21.05000000000000071, 70.60000000001222986, -148.9283735034374843 ) ) ;
#64880=ORIENTED_EDGE ( 'NONE', *, *, #93268, .T. ) ;
#64893=VERTEX_POINT ( 'NONE', #192944 ) ;
#64931=ORIENTED_EDGE ( 'NONE', *, *, #186226, .T. ) ;
#64949=DIRECTION ( 'NONE',  ( 0.000000000000000000, 0.9915357197604982575, -0.1298341882519033486 ) ) ;
#64954=CIRCLE ( 'NONE', #256431, 0.6000000000000033085 ) ;
#64961=CARTESIAN_POINT ( 'NONE',  ( 22.39999999999999503, 68.20922040163900135, -170.1231074845244109 ) ) ;
#64963=ADVANCED_FACE ( 'NONE', ( #35189 ), #18146, .T. ) ;
#65016=DIRECTION ( 'NONE',  ( -1.000000000000000000, -0.000000000000000000, -0.000000000000000000 ) ) ;
#65062=CARTESIAN_POINT ( 'NONE',  ( -20.85000000000000142, 75.83895117929343144, -136.8072973288845731 ) ) ;
#65076=CYLINDRICAL_SURFACE ( 'NONE', #216092, 0.09999999999998898659 ) ;
#65096=DIRECTION ( 'NONE',  ( 0.000000000000000000, 0.000000000000000000, 1.000000000000000000 ) ) ;
#65103=EDGE_LOOP ( 'NONE', ( #50390, #189706, #72720, #214630 ) ) ;
#65111=CARTESIAN_POINT ( 'NONE',  ( -21.44999999999999929, 68.85000000001222986, -148.7731074845244166 ) ) ;
#65122=CARTESIAN_POINT ( 'NONE',  ( 22.39999999999999503, 76.00000000001243450, -177.8138870828977360 ) ) ;
#65126=ORIENTED_EDGE ( 'NONE', *, *, #26437, .F. ) ;
#65129=DIRECTION ( 'NONE',  ( 0.000000000000000000, 0.000000000000000000, -1.000000000000000000 ) ) ;
#65207=VERTEX_POINT ( 'NONE', #201925 ) ;
#65215=ORIENTED_EDGE ( 'NONE', *, *, #123909, .T. ) ;
#65240=VERTEX_POINT ( 'NONE', #105345 ) ;
#65247=VERTEX_POINT ( 'NONE', #131364 ) ;
#65285=DIRECTION ( 'NONE',  ( 0.000000000000000000, -6.982962677686266711E-15, 1.000000000000000000 ) ) ;
#65303=CARTESIAN_POINT ( 'NONE',  ( 21.05000000000000071, 67.18479819544532461, -161.6025699878404396 ) ) ;
#65314=CARTESIAN_POINT ( 'NONE',  ( 22.59999999999999432, 75.90000000001245439, -181.6726782920691505 ) ) ;
#65321=ORIENTED_EDGE ( 'NONE', *, *, #7854, .T. ) ;
#65362=ORIENTED_EDGE ( 'NONE', *, *, #31816, .T. ) ;
#65396=DIRECTION ( 'NONE',  ( -3.265361837132813093E-16, -1.000000000000000000, -6.982962677686266711E-15 ) ) ;
#65426=DIRECTION ( 'NONE',  ( 1.000000000000000000, 0.000000000000000000, 0.000000000000000000 ) ) ;
#65445=DIRECTION ( 'NONE',  ( 0.000000000000000000, 0.3738317757009942399, -0.9274965247785252886 ) ) ;
#65446=ADVANCED_FACE ( 'NONE', ( #15295 ), #123354, .F. ) ;
#65447=DIRECTION ( 'NONE',  ( 0.000000000000000000, -7.086529944415886769E-15, 1.000000000000000000 ) ) ;
#65470=CARTESIAN_POINT ( 'NONE',  ( -21.05000000000041993, 69.65527659592207499, -170.0378253410491709 ) ) ;
#65480=CARTESIAN_POINT ( 'NONE',  ( -20.85000000000000142, 65.66751761918692409, -130.9282609406112670 ) ) ;
#65504=EDGE_LOOP ( 'NONE', ( #96502, #161885, #248017, #159014, #157693, #26975, #246026, #54215, #132257, #39009, #121406, #105321 ) ) ;
#65506=AXIS2_PLACEMENT_3D ( 'NONE', #182340, #3675, #117221 ) ;
#65539=EDGE_CURVE ( 'NONE', #123398, #132009, #2107, .T. ) ;
#65549=AXIS2_PLACEMENT_3D ( 'NONE', #196775, #174711, #3712 ) ;
#65563=ORIENTED_EDGE ( 'NONE', *, *, #22622, .F. ) ;
#65569=EDGE_CURVE ( 'NONE', #237787, #224923, #142892, .T. ) ;
#65570=EDGE_LOOP ( 'NONE', ( #135508, #47602, #214715, #238689 ) ) ;
#65584=CARTESIAN_POINT ( 'NONE',  ( -20.64999999999999858, 76.00000000001237765, -170.0231074845243597 ) ) ;
#65616=DIRECTION ( 'NONE',  ( 0.000000000000000000, 0.000000000000000000, 1.000000000000000000 ) ) ;
#65621=CARTESIAN_POINT ( 'NONE',  ( -23.25000000000000000, 64.25000000001215028, -136.5231074845244166 ) ) ;
#65623=CARTESIAN_POINT ( 'NONE',  ( -20.94999999999999929, 76.00000000001213607, -136.5231074845243313 ) ) ;
#65625=CARTESIAN_POINT ( 'NONE',  ( -23.25000000000000000, 73.40000000001222702, -149.7477294072864709 ) ) ;
#65631=CARTESIAN_POINT ( 'NONE',  ( -23.25000000000000000, 71.65000000001222702, -148.8731074845244109 ) ) ;
#65704=CARTESIAN_POINT ( 'NONE',  ( -23.25000000000000000, 76.00000000001216449, -140.4231074845243370 ) ) ;
#65739=AXIS2_PLACEMENT_3D ( 'NONE', #137496, #37155, #219607 ) ;
#65750=CYLINDRICAL_SURFACE ( 'NONE', #190724, 0.1000000000000028644 ) ;
#65786=DIRECTION ( 'NONE',  ( 0.000000000000000000, -1.000000000000000000, -6.982962677686266711E-15 ) ) ;
#65790=CARTESIAN_POINT ( 'NONE',  ( -20.94999999999999929, 87.75000000001216449, -139.6231074845242688 ) ) ;
#65799=AXIS2_PLACEMENT_3D ( 'NONE', #185081, #45574, #28632 ) ;
#65839=EDGE_CURVE ( 'NONE', #198025, #127762, #56853, .T. ) ;
#65889=EDGE_CURVE ( 'NONE', #222470, #230504, #73684, .T. ) ;
#65910=CARTESIAN_POINT ( 'NONE',  ( -20.94999999999999929, 64.25000000001219291, -143.3069731475025321 ) ) ;
#65940=CARTESIAN_POINT ( 'NONE',  ( -21.05000000000000071, 69.45934304831114048, -169.9231074845244223 ) ) ;
#65942=CARTESIAN_POINT ( 'NONE',  ( 21.03670563405601968, 65.37517631068404000, -157.6975605983152775 ) ) ;
#65979=VECTOR ( 'NONE', #89801, 1000.000000000000000 ) ;
#65990=CARTESIAN_POINT ( 'NONE',  ( -20.85000000000000142, 77.83585931145570669, -125.0186683157258329 ) ) ;
#65996=CARTESIAN_POINT ( 'NONE',  ( -20.94999999999999929, 76.00000000001213607, -136.5231074845243313 ) ) ;
#66013=DIRECTION ( 'NONE',  ( 1.000000000000000000, 0.000000000000000000, 0.000000000000000000 ) ) ;
#66067=AXIS2_PLACEMENT_3D ( 'NONE', #83623, #241463, #218017 ) ;
#66075=AXIS2_PLACEMENT_3D ( 'NONE', #167013, #127859, #207403 ) ;
#66077=CIRCLE ( 'NONE', #16229, 0.5000000000000004441 ) ;
#66078=AXIS2_PLACEMENT_3D ( 'NONE', #255405, #175953, #215050 ) ;
#66126=CARTESIAN_POINT ( 'NONE',  ( 23.14999999999999858, 76.00000000001213607, -136.5231074845243313 ) ) ;
#66134=CIRCLE ( 'NONE', #136873, 0.09999999999998898659 ) ;
#66152=FACE_BOUND ( 'NONE', #138497, .T. ) ;
#66185=CARTESIAN_POINT ( 'NONE',  ( 22.49533356619862801, 64.34999999370828050, -170.0882300648472096 ) ) ;
#66187=EDGE_CURVE ( 'NONE', #40059, #145384, #112492, .T. ) ;
#66205=CARTESIAN_POINT ( 'NONE',  ( -21.29999999999995808, 76.00000000001237765, -170.0231074845243597 ) ) ;
#66247=VERTEX_POINT ( 'NONE', #251982 ) ;
#66273=VERTEX_POINT ( 'NONE', #123719 ) ;
#66287=VECTOR ( 'NONE', #120168, 1000.000000000000000 ) ;
#66306=ORIENTED_EDGE ( 'NONE', *, *, #78548, .F. ) ;
#66341=CARTESIAN_POINT ( 'NONE',  ( -21.09610168723073187, 69.62104428478760099, -170.0566969914158904 ) ) ;
#66349=CARTESIAN_POINT ( 'NONE',  ( -23.25000000000000000, 76.00000000001213607, -136.5231074845243313 ) ) ;
#66402=ADVANCED_FACE ( 'NONE', ( #147110 ), #165428, .F. ) ;
#66405=DIRECTION ( 'NONE',  ( -1.000000000000000000, -0.000000000000000000, -0.000000000000000000 ) ) ;
#66429=EDGE_CURVE ( 'NONE', #243885, #62106, #90562, .T. ) ;
#66437=AXIS2_PLACEMENT_3D ( 'NONE', #118976, #220635, #135938 ) ;
#66458=EDGE_LOOP ( 'NONE', ( #106137, #50715, #26739, #166809, #214607 ) ) ;
#66459=AXIS2_PLACEMENT_3D ( 'NONE', #76223, #39709, #34564 ) ;
#66465=DIRECTION ( 'NONE',  ( 0.000000000000000000, 6.982962677686267499E-15, -1.000000000000000000 ) ) ;
#66468=LINE ( 'NONE', #247671, #234503 ) ;
#66508=EDGE_LOOP ( 'NONE', ( #243594, #145788, #29809, #175748 ) ) ;
#66525=ORIENTED_EDGE ( 'NONE', *, *, #28942, .T. ) ;
#66541=CARTESIAN_POINT ( 'NONE',  ( 21.05000000000000071, 61.95000000001218154, -142.0368025552853624 ) ) ;
#66580=DIRECTION ( 'NONE',  ( 0.000000000000000000, 1.000000000000000000, 0.000000000000000000 ) ) ;
#66609=ORIENTED_EDGE ( 'NONE', *, *, #81531, .T. ) ;
#66619=CARTESIAN_POINT ( 'NONE',  ( -23.25000000000000000, 87.75000000001237765, -170.0231074845242745 ) ) ;
#66622=LINE ( 'NONE', #27534, #108145 ) ;
#66672=CARTESIAN_POINT ( 'NONE',  ( 23.25000000000000000, 64.25000000001222134, -148.6731074845244507 ) ) ;
#66679=AXIS2_PLACEMENT_3D ( 'NONE', #217843, #104316, #202162 ) ;
#66704=DIRECTION ( 'NONE',  ( -1.000000000000000000, 0.000000000000000000, 0.000000000000000000 ) ) ;
#66707=AXIS2_PLACEMENT_3D ( 'NONE', #91598, #190727, #151600 ) ;
#66754=AXIS2_PLACEMENT_3D ( 'NONE', #117019, #231851, #77875 ) ;
#66776=DIRECTION ( 'NONE',  ( 1.000000000000000000, 0.000000000000000000, 0.000000000000000000 ) ) ;
#66811=TOROIDAL_SURFACE ( 'NONE', #29433, 12.77499999999999858, 0.1000000000000000056 ) ;
#66815=DIRECTION ( 'NONE',  ( -3.265361837132813093E-16, -1.000000000000000000, -6.982962677686266711E-15 ) ) ;
#66819=DIRECTION ( 'NONE',  ( 0.000000000000000000, -7.272083257015735086E-15, 1.000000000000000000 ) ) ;
#66855=CIRCLE ( 'NONE', #104427, 0.1000000000000028644 ) ;
#66905=DIRECTION ( 'NONE',  ( 1.000000000000000000, 0.000000000000000000, 0.000000000000000000 ) ) ;
#66933=ORIENTED_EDGE ( 'NONE', *, *, #71758, .T. ) ;
#66940=DIRECTION ( 'NONE',  ( 0.7070776581708965169, 4.937903618720407826E-15, -0.7071359030027827286 ) ) ;
#67005=AXIS2_PLACEMENT_3D ( 'NONE', #85839, #225367, #126276 ) ;
#67009=EDGE_CURVE ( 'NONE', #195092, #105820, #53168, .T. ) ;
#67057=VECTOR ( 'NONE', #227596, 999.9999999999998863 ) ;
#67069=DIRECTION ( 'NONE',  ( 0.000000000000000000, -6.982962677686266711E-15, 1.000000000000000000 ) ) ;
#67074=ORIENTED_EDGE ( 'NONE', *, *, #12872, .T. ) ;
#67131=TOROIDAL_SURFACE ( 'NONE', #137853, 2.100000000000002309, 0.1000000000000000056 ) ;
#67132=ORIENTED_EDGE ( 'NONE', *, *, #229230, .F. ) ;
#67144=EDGE_LOOP ( 'NONE', ( #196834, #248573, #118900, #163346 ) ) ;
#67226=VECTOR ( 'NONE', #136167, 999.9999999999998863 ) ;
#67266=DIRECTION ( 'NONE',  ( 1.000000000000000000, 0.000000000000000000, 0.000000000000000000 ) ) ;
#67272=DIRECTION ( 'NONE',  ( 2.259780016855445309E-14, -0.9875055080513764905, 0.1575844902526679359 ) ) ;
#67276=DIRECTION ( 'NONE',  ( 2.952720810173289605E-16, 1.000000000000000000, 7.086529944415894657E-15 ) ) ;
#67281=DIRECTION ( 'NONE',  ( 0.000000000000000000, 6.769652589177795712E-15, -1.000000000000000000 ) ) ;
#67317=AXIS2_PLACEMENT_3D ( 'NONE', #229551, #31381, #110877 ) ;
#67322=AXIS2_PLACEMENT_3D ( 'NONE', #167067, #69237, #227000 ) ;
#67337=ORIENTED_EDGE ( 'NONE', *, *, #20835, .T. ) ;
#67356=VERTEX_POINT ( 'NONE', #122802 ) ;
#67409=DIRECTION ( 'NONE',  ( -0.000000000000000000, 1.000000000000000000, 6.352154140967427193E-15 ) ) ;
#67440=ORIENTED_EDGE ( 'NONE', *, *, #238713, .F. ) ;
#67446=CARTESIAN_POINT ( 'NONE',  ( -22.50000000000096989, 75.89914163091383159, -181.7726746080137445 ) ) ;
#67500=VERTEX_POINT ( 'NONE', #218373 ) ;
#67537=DIRECTION ( 'NONE',  ( -1.000000000000000000, 0.000000000000000000, 0.000000000000000000 ) ) ;
#67584=LINE ( 'NONE', #207107, #223493 ) ;
#67602=DIRECTION ( 'NONE',  ( 0.000000000000000000, 0.000000000000000000, -1.000000000000000000 ) ) ;
#67610=AXIS2_PLACEMENT_3D ( 'NONE', #70211, #108031, #147140 ) ;
#67629=AXIS2_PLACEMENT_3D ( 'NONE', #136412, #80287, #197690 ) ;
#67645=VECTOR ( 'NONE', #78549, 1000.000000000000000 ) ;
#67677=CIRCLE ( 'NONE', #42736, 4.149999999999987033 ) ;
#67684=VECTOR ( 'NONE', #162550, 999.9999999999998863 ) ;
#67703=AXIS2_PLACEMENT_3D ( 'NONE', #51989, #114554, #211088 ) ;
#67718=ADVANCED_FACE ( 'NONE', ( #127003 ), #90430, .F. ) ;
#67726=CARTESIAN_POINT ( 'NONE',  ( -23.25000000000000000, 76.00000000001213607, -136.5231074845243313 ) ) ;
#67729=CARTESIAN_POINT ( 'NONE',  ( -18.50000000000000000, 77.63717271298267519, -158.4409541190523214 ) ) ;
#67762=DIRECTION ( 'NONE',  ( -2.978066053179069723E-16, -1.000000000000000000, -7.147358527629766941E-15 ) ) ;
#67826=LINE ( 'NONE', #87375, #149068 ) ;
#67846=CARTESIAN_POINT ( 'NONE',  ( 19.87657994472041523, 64.25000000001220712, -145.2573193598975081 ) ) ;
#67847=DIRECTION ( 'NONE',  ( 1.000000000000000000, -2.952720810173289112E-16, -2.061873921506763405E-30 ) ) ;
#67855=ADVANCED_FACE ( 'NONE', ( #210411 ), #248795, .T. ) ;
#67868=CARTESIAN_POINT ( 'NONE',  ( 21.05000000000000071, 67.22371710471985295, -161.4644784893834810 ) ) ;
#67886=ORIENTED_EDGE ( 'NONE', *, *, #128632, .F. ) ;
#67940=FACE_OUTER_BOUND ( 'NONE', #120811, .T. ) ;
#67951=PLANE ( 'NONE',  #15185 ) ;
#67964=CARTESIAN_POINT ( 'NONE',  ( 21.08078803292165659, 69.66698703557526073, -170.1022934716822022 ) ) ;
#68007=ORIENTED_EDGE ( 'NONE', *, *, #97295, .T. ) ;
#68014=ADVANCED_FACE ( 'NONE', ( #148846 ), #5438, .T. ) ;
#68019=AXIS2_PLACEMENT_3D ( 'NONE', #225822, #138891, #140192 ) ;
#68029=ORIENTED_EDGE ( 'NONE', *, *, #248971, .F. ) ;
#68045=( BOUNDED_SURFACE ( )  B_SPLINE_SURFACE ( 3, 2, ( 
 ( #221383, #122310, #105268 ),
 ( #42771, #184837, #222670 ),
 ( #6198, #46596, #66185 ),
 ( #203123, #145703, #225229 ) ),
 .UNSPECIFIED., .F., .F., .T. ) 
 B_SPLINE_SURFACE_WITH_KNOTS ( ( 4, 4 ),
 ( 3, 3 ),
 ( 0.0006461284895273780972, 0.0007503702773985888950 ),
 ( 0.000000000000000000, 1.000000000000000000 ),
 .UNSPECIFIED. ) 
 GEOMETRIC_REPRESENTATION_ITEM ( )  RATIONAL_B_SPLINE_SURFACE ( (
 ( 1.000000000000000000, 0.7071067811865475727, 1.000000000000000000),
 ( 1.000000000000000000, 0.7076476444649381081, 1.000000000000000000),
 ( 1.000000000000000000, 0.7075727925191463985, 1.000000000000000000),
 ( 1.000000000000000000, 0.7071067811865475727, 1.000000000000000000) ) ) 
 REPRESENTATION_ITEM ( '' )  SURFACE ( )  );
#68058=CARTESIAN_POINT ( 'NONE',  ( 18.59999999999999076, 69.55000000001230376, -160.0060803140843859 ) ) ;
#68081=AXIS2_PLACEMENT_3D ( 'NONE', #221387, #218827, #182300 ) ;
#68119=DIRECTION ( 'NONE',  ( -1.000000000000000000, 0.000000000000000000, 0.000000000000000000 ) ) ;
#68129=ORIENTED_EDGE ( 'NONE', *, *, #93372, .T. ) ;
#68147=DIRECTION ( 'NONE',  ( 0.000000000000000000, 0.000000000000000000, -1.000000000000000000 ) ) ;
#68159=CARTESIAN_POINT ( 'NONE',  ( 22.50000000000000000, 75.95437663941604001, -181.6736118230765271 ) ) ;
#68195=DIRECTION ( 'NONE',  ( 0.000000000000000000, 0.000000000000000000, 1.000000000000000000 ) ) ;
#68204=AXIS2_PLACEMENT_3D ( 'NONE', #156514, #80763, #178637 ) ;
#68253=ORIENTED_EDGE ( 'NONE', *, *, #103714, .F. ) ;
#68286=DIRECTION ( 'NONE',  ( 0.000000000000000000, -6.608470384673580212E-15, 1.000000000000000000 ) ) ;
#68290=FACE_OUTER_BOUND ( 'NONE', #53377, .T. ) ;
#68302=AXIS2_PLACEMENT_3D ( 'NONE', #253498, #74905, #115279 ) ;
#68321=CIRCLE ( 'NONE', #209977, 0.09999999999998898659 ) ;
#68324=CARTESIAN_POINT ( 'NONE',  ( -22.50000000000000000, 68.20922040163897293, -170.1231074845244109 ) ) ;
#68345=CARTESIAN_POINT ( 'NONE',  ( 21.05000000000000071, 69.45934304831114048, -169.9231074845244223 ) ) ;
#68351=DIRECTION ( 'NONE',  ( -1.000000000000000000, 0.000000000000000000, -0.000000000000000000 ) ) ;
#68354=AXIS2_PLACEMENT_3D ( 'NONE', #3456, #205508, #103828 ) ;
#68355=CIRCLE ( 'NONE', #101627, 12.77500000000000924 ) ;
#68369=AXIS2_PLACEMENT_3D ( 'NONE', #223713, #103752, #26844 ) ;
#68375=AXIS2_PLACEMENT_3D ( 'NONE', #161694, #242481, #182539 ) ;
#68388=AXIS2_PLACEMENT_3D ( 'NONE', #169353, #208462, #130168 ) ;
#68394=ORIENTED_EDGE ( 'NONE', *, *, #131031, .T. ) ;
#68402=ORIENTED_EDGE ( 'NONE', *, *, #124887, .T. ) ;
#68425=ORIENTED_EDGE ( 'NONE', *, *, #215547, .F. ) ;
#68439=( BOUNDED_CURVE ( )  B_SPLINE_CURVE ( 3, ( #43078, #242548, #220437, #41814 ),
 .UNSPECIFIED., .F., .F. ) 
 B_SPLINE_CURVE_WITH_KNOTS ( ( 4, 4 ),
 ( 4.712388980384690562, 6.283185307179586232 ),
 .UNSPECIFIED. ) 
 CURVE ( )  GEOMETRIC_REPRESENTATION_ITEM ( )  RATIONAL_B_SPLINE_CURVE ( ( 1.000000000000000000, 0.8047378541243652705, 0.8047378541243652705, 1.000000000000000000 ) ) 
 REPRESENTATION_ITEM ( '' )  );
#68457=( BOUNDED_SURFACE ( )  B_SPLINE_SURFACE ( 3, 2, ( 
 ( #195226, #56929, #238157 ),
 ( #38696, #175646, #216025 ),
 ( #219887, #41289, #37423 ),
 ( #136478, #120820, #21702 ) ),
 .UNSPECIFIED., .F., .F., .F. ) 
 B_SPLINE_SURFACE_WITH_KNOTS ( ( 4, 4 ),
 ( 3, 3 ),
 ( 2.081668171172168513E-17, 0.001979672783031568434 ),
 ( 0.000000000000000000, 1.000000000000000000 ),
 .UNSPECIFIED. ) 
 GEOMETRIC_REPRESENTATION_ITEM ( )  RATIONAL_B_SPLINE_SURFACE ( (
 ( 1.000000000000000000, 0.7103081912007698229, 1.000000000000000000),
 ( 1.000000000000000000, 0.7104998333559727763, 1.000000000000000000),
 ( 1.000000000000000000, 0.7107238315755050051, 1.000000000000000000),
 ( 1.000000000000000000, 0.7110073749539208565, 1.000000000000000000) ) ) 
 REPRESENTATION_ITEM ( '' )  SURFACE ( )  );
#68477=EDGE_CURVE ( 'NONE', #74533, #127058, #194998, .T. ) ;
#68479=CIRCLE ( 'NONE', #189295, 0.09999999999998898659 ) ;
#68483=CARTESIAN_POINT ( 'NONE',  ( -20.99749315643149927, 64.25000000001220712, -143.5379132532823974 ) ) ;
#68498=DIRECTION ( 'NONE',  ( -1.000000000000000000, -0.000000000000000000, -0.000000000000000000 ) ) ;
#68500=CARTESIAN_POINT ( 'NONE',  ( -20.64999999999999858, 68.85000000001228670, -157.7731074845244166 ) ) ;
#68507=DIRECTION ( 'NONE',  ( 0.000000000000000000, -7.086529944415894657E-15, 1.000000000000000000 ) ) ;
#68509=DIRECTION ( 'NONE',  ( 0.000000000000000000, 0.000000000000000000, 1.000000000000000000 ) ) ;
#68515=CIRCLE ( 'NONE', #81150, 0.1000000000000028644 ) ;
#68534=AXIS2_PLACEMENT_3D ( 'NONE', #79368, #88342, #68825 ) ;
#68551=LINE ( 'NONE', #43852, #73928 ) ;
#68591=CARTESIAN_POINT ( 'NONE',  ( -18.59999999999999787, 64.35000000001234355, -163.0083017138704236 ) ) ;
#68614=AXIS2_PLACEMENT_3D ( 'NONE', #47123, #221909, #1592 ) ;
#68620=CARTESIAN_POINT ( 'NONE',  ( -20.85000000000000142, 64.25000000001220712, -143.3647081744214802 ) ) ;
#68625=AXIS2_PLACEMENT_3D ( 'NONE', #83636, #62831, #182799 ) ;
#68650=CARTESIAN_POINT ( 'NONE',  ( 21.11747605621531321, 67.22129199451940451, -157.7785443147346598 ) ) ;
#68653=ORIENTED_EDGE ( 'NONE', *, *, #193548, .F. ) ;
#68662=CARTESIAN_POINT ( 'NONE',  ( -21.05000000000000071, 76.00000000001240608, -174.3231074845243427 ) ) ;
#68669=DIRECTION ( 'NONE',  ( 0.000000000000000000, 0.000000000000000000, 1.000000000000000000 ) ) ;
#68671=CARTESIAN_POINT ( 'NONE',  ( -18.59999999999999787, 77.83585931145570669, -125.0186683157258045 ) ) ;
#68674=ORIENTED_EDGE ( 'NONE', *, *, #234613, .T. ) ;
#68675=ORIENTED_EDGE ( 'NONE', *, *, #116473, .T. ) ;
#68731=CARTESIAN_POINT ( 'NONE',  ( 21.05000000000000071, 76.00000000001215028, -138.4231074845243654 ) ) ;
#68761=VERTEX_POINT ( 'NONE', #195375 ) ;
#68766=ORIENTED_EDGE ( 'NONE', *, *, #255386, .F. ) ;
#68787=ORIENTED_EDGE ( 'NONE', *, *, #126510, .F. ) ;
#68813=CARTESIAN_POINT ( 'NONE',  ( -23.15000000000000213, 85.50000000001232081, -160.1291383618718385 ) ) ;
#68825=DIRECTION ( 'NONE',  ( 1.000000000000000000, 0.000000000000000000, 0.000000000000000000 ) ) ;
#68833=DIRECTION ( 'NONE',  ( -1.000000000000000000, -0.000000000000000000, -0.000000000000000000 ) ) ;
#68847=ORIENTED_EDGE ( 'NONE', *, *, #44358, .T. ) ;
#68872=EDGE_LOOP ( 'NONE', ( #130327, #12284, #10693, #128189 ) ) ;
#68878=DIRECTION ( 'NONE',  ( 1.000000000000000000, 0.000000000000000000, 0.000000000000000000 ) ) ;
#68897=DIRECTION ( 'NONE',  ( 1.000000000000000000, 0.000000000000000000, 0.000000000000000000 ) ) ;
#68902=TOROIDAL_SURFACE ( 'NONE', #118959, 4.149999999999999467, 0.1000000000000000056 ) ;
#68918=CARTESIAN_POINT ( 'NONE',  ( 20.19326291201646129, 65.84393901210839317, -162.2612456769175253 ) ) ;
#68924=DIRECTION ( 'NONE',  ( 0.000000000000000000, -1.000000000000000000, -6.982962677686265922E-15 ) ) ;
#68928=VERTEX_POINT ( 'NONE', #50367 ) ;
#68949=FACE_OUTER_BOUND ( 'NONE', #77115, .T. ) ;
#68961=CARTESIAN_POINT ( 'NONE',  ( -20.85000000000000142, 77.16412189325330928, -128.8082593989527425 ) ) ;
#68966=ORIENTED_EDGE ( 'NONE', *, *, #252765, .T. ) ;
#69006=ORIENTED_EDGE ( 'NONE', *, *, #53151, .F. ) ;
#69046=DIRECTION ( 'NONE',  ( 1.000000000000000000, 0.000000000000000000, 0.000000000000000000 ) ) ;
#69050=ORIENTED_EDGE ( 'NONE', *, *, #250377, .F. ) ;
#69052=DIRECTION ( 'NONE',  ( 1.000000000000000000, 0.000000000000000000, 0.000000000000000000 ) ) ;
#69055=EDGE_LOOP ( 'NONE', ( #148638, #3978, #192041, #4829 ) ) ;
#69112=CARTESIAN_POINT ( 'NONE',  ( -18.50000000000000000, 66.65000000001229807, -157.6731074845244223 ) ) ;
#69148=EDGE_CURVE ( 'NONE', #161999, #62202, #193315, .T. ) ;
#69213=DIRECTION ( 'NONE',  ( 1.000000000000000000, 0.000000000000000000, 0.000000000000000000 ) ) ;
#69237=DIRECTION ( 'NONE',  ( 0.000000000000000000, 0.9999631594459055250, 0.008583690987131395445 ) ) ;
#69260=FACE_OUTER_BOUND ( 'NONE', #67144, .T. ) ;
#69301=CARTESIAN_POINT ( 'NONE',  ( -23.25000000000000000, 76.00000000001237765, -170.0231074845243597 ) ) ;
#69317=DIRECTION ( 'NONE',  ( 0.000000000000000000, -1.000000000000000000, 0.000000000000000000 ) ) ;
#69325=DIRECTION ( 'NONE',  ( 0.000000000000000000, -7.026728003956695223E-15, 1.000000000000000000 ) ) ;
#69347=LINE ( 'NONE', #227106, #29619 ) ;
#69354=DIRECTION ( 'NONE',  ( 0.000000000000000000, 0.000000000000000000, 1.000000000000000000 ) ) ;
#69366=ORIENTED_EDGE ( 'NONE', *, *, #231613, .F. ) ;
#69400=ORIENTED_EDGE ( 'NONE', *, *, #195611, .T. ) ;
#69404=TOROIDAL_SURFACE ( 'NONE', #215133, 0.9750000000000019762, 0.1000000000000000056 ) ;
#69427=CIRCLE ( 'NONE', #7042, 0.1000000000000072220 ) ;
#69458=CARTESIAN_POINT ( 'NONE',  ( 20.94999999999999574, 64.37928932189353759, -143.3915241368653994 ) ) ;
#69462=CARTESIAN_POINT ( 'NONE',  ( 18.59999999999999076, 77.25000000001232081, -162.0231074845243313 ) ) ;
#69496=CARTESIAN_POINT ( 'NONE',  ( -20.94999999999999929, 64.25000000001232081, -163.0083017138704236 ) ) ;
#69500=CARTESIAN_POINT ( 'NONE',  ( 23.14999999999999503, 64.35000000001218723, -143.5379132551783812 ) ) ;
#69503=CARTESIAN_POINT ( 'NONE',  ( -18.59999999999999787, 61.95000000001234497, -164.5094124137634708 ) ) ;
#69533=DIRECTION ( 'NONE',  ( 1.000000000000000000, 0.000000000000000000, 0.000000000000000000 ) ) ;
#69560=FACE_OUTER_BOUND ( 'NONE', #120877, .T. ) ;
#69585=EDGE_CURVE ( 'NONE', #49440, #49697, #155910, .T. ) ;
#69616=CARTESIAN_POINT ( 'NONE',  ( -1.739115166359751801E-14, 64.35000000001230092, -157.7731074845244450 ) ) ;
#69623=DIRECTION ( 'NONE',  ( 0.000000000000000000, 0.000000000000000000, -1.000000000000000000 ) ) ;
#69629=FACE_OUTER_BOUND ( 'NONE', #148466, .T. ) ;
#69641=CARTESIAN_POINT ( 'NONE',  ( 22.39999999999999503, 76.10085836911117951, -181.7726746080137445 ) ) ;
#69665=AXIS2_PLACEMENT_3D ( 'NONE', #171176, #92862, #55003 ) ;
#69668=CARTESIAN_POINT ( 'NONE',  ( -20.00857864376270001, 66.85000000001228670, -157.6731074845244223 ) ) ;
#69683=ORIENTED_EDGE ( 'NONE', *, *, #208940, .T. ) ;
#69685=AXIS2_PLACEMENT_3D ( 'NONE', #164411, #169589, #89988 ) ;
#69690=CARTESIAN_POINT ( 'NONE',  ( 23.14999999999999858, 71.00000000001230660, -157.6178414656113205 ) ) ;
#69695=VERTEX_POINT ( 'NONE', #104282 ) ;
#69711=VERTEX_POINT ( 'NONE', #246386 ) ;
#69713=VERTEX_POINT ( 'NONE', #109421 ) ;
#69720=EDGE_CURVE ( 'NONE', #86120, #35577, #47724, .T. ) ;
#69727=VERTEX_POINT ( 'NONE', #144699 ) ;
#69744=ORIENTED_EDGE ( 'NONE', *, *, #53434, .T. ) ;
#69747=DIRECTION ( 'NONE',  ( -1.000000000000000000, 0.000000000000000000, 0.000000000000000000 ) ) ;
#69781=ADVANCED_FACE ( 'NONE', ( #194134 ), #10343, .T. ) ;
#69805=CIRCLE ( 'NONE', #253118, 12.87499999999999822 ) ;
#69808=FACE_OUTER_BOUND ( 'NONE', #207628, .T. ) ;
#69809=CARTESIAN_POINT ( 'NONE',  ( -23.15000000000000213, 76.00000000001216449, -140.5231074845243597 ) ) ;
#69869=EDGE_LOOP ( 'NONE', ( #30491, #87417, #7517, #238928, #31517, #165659, #116952, #92870, #64880, #112698, #97136, #143300 ) ) ;
#69889=VECTOR ( 'NONE', #128736, 1000.000000000000000 ) ;
#69971=CARTESIAN_POINT ( 'NONE',  ( 18.59999999999998721, 69.06610602788578035, -132.7374616501508342 ) ) ;
#69983=DIRECTION ( 'NONE',  ( -2.827886303505249259E-16, -0.8660254037844378194, -0.5000000000000016653 ) ) ;
#70015=VERTEX_POINT ( 'NONE', #247342 ) ;
#70114=CARTESIAN_POINT ( 'NONE',  ( -23.15000000000000213, 85.00000000001222134, -145.8170766071767446 ) ) ;
#70124=DIRECTION ( 'NONE',  ( -1.000000000000000000, 1.836970198721029934E-16, 1.282749433769087757E-30 ) ) ;
#70140=ORIENTED_EDGE ( 'NONE', *, *, #158617, .F. ) ;
#70155=CARTESIAN_POINT ( 'NONE',  ( -23.25000000000000000, 71.65000000001228386, -157.8731074845243825 ) ) ;
#70204=DIRECTION ( 'NONE',  ( 0.000000000000000000, 0.8660254037844420383, -0.4999999999999943379 ) ) ;
#70207=CARTESIAN_POINT ( 'NONE',  ( 20.97565083910961548, 65.52538259873351478, -162.4451643079358973 ) ) ;
#70211=CARTESIAN_POINT ( 'NONE',  ( -23.15000000000000213, 76.00000000001234923, -165.8731074845243825 ) ) ;
#70218=AXIS2_PLACEMENT_3D ( 'NONE', #34009, #229607, #10565 ) ;
#70227=CARTESIAN_POINT ( 'NONE',  ( -21.93340585972067558, 68.67585297715902470, -170.0231074845244166 ) ) ;
#70237=AXIS2_PLACEMENT_3D ( 'NONE', #142335, #64096, #186625 ) ;
#70242=VERTEX_POINT ( 'NONE', #191255 ) ;
#70251=AXIS2_PLACEMENT_3D ( 'NONE', #209849, #113301, #228129 ) ;
#70256=AXIS2_PLACEMENT_3D ( 'NONE', #42970, #122514, #102910 ) ;
#70331=LINE ( 'NONE', #49451, #49737 ) ;
#70362=AXIS2_PLACEMENT_3D ( 'NONE', #215009, #91230, #35138 ) ;
#70372=EDGE_CURVE ( 'NONE', #77802, #212831, #77143, .T. ) ;
#70374=TOROIDAL_SURFACE ( 'NONE', #182788, 0.2000000000000000111, 0.1000000000000000056 ) ;
#70411=CARTESIAN_POINT ( 'NONE',  ( 20.94999999999999574, 74.83729825007431202, -162.0231074845243597 ) ) ;
#70454=ORIENTED_EDGE ( 'NONE', *, *, #94419, .T. ) ;
#70489=DIRECTION ( 'NONE',  ( 1.000000000000000000, 0.000000000000000000, 0.000000000000000000 ) ) ;
#70500=CARTESIAN_POINT ( 'NONE',  ( 20.94999999999999929, 76.00000000001237765, -170.0231074845243597 ) ) ;
#70518=DIRECTION ( 'NONE',  ( 0.000000000000000000, 7.086529944415886769E-15, -1.000000000000000000 ) ) ;
#70519=EDGE_CURVE ( 'NONE', #212171, #232077, #150521, .T. ) ;
#70561=CARTESIAN_POINT ( 'NONE',  ( -21.10320863425827298, 75.97497774878530663, -176.4233848709835684 ) ) ;
#70573=VERTEX_POINT ( 'NONE', #193506 ) ;
#70598=CARTESIAN_POINT ( 'NONE',  ( 18.49999999999998934, 69.45000000001222418, -148.7731074845244166 ) ) ;
#70609=EDGE_CURVE ( 'NONE', #99805, #135741, #10697, .T. ) ;
#70626=CARTESIAN_POINT ( 'NONE',  ( 20.85000000000000142, 76.00000000001213607, -136.5231074845243313 ) ) ;
#70627=ADVANCED_FACE ( 'NONE', ( #117800 ), #14985, .F. ) ;
#70630=EDGE_LOOP ( 'NONE', ( #98173, #168089, #16462 ) ) ;
#70633=CARTESIAN_POINT ( 'NONE',  ( 21.05000000000000071, 76.08561306081638520, -176.4368672183346405 ) ) ;
#70637=DIRECTION ( 'NONE',  ( -1.000000000000000000, 0.000000000000000000, -0.000000000000000000 ) ) ;
#70638=ADVANCED_FACE ( 'NONE', ( #198616 ), #158256, .T. ) ;
#70642=ADVANCED_FACE ( 'NONE', ( #219452 ), #74862, .F. ) ;
#70645=VERTEX_POINT ( 'NONE', #138613 ) ;
#70656=ORIENTED_EDGE ( 'NONE', *, *, #93223, .T. ) ;
#70677=ORIENTED_EDGE ( 'NONE', *, *, #130194, .T. ) ;
#70695=VERTEX_POINT ( 'NONE', #21303 ) ;
#70751=CARTESIAN_POINT ( 'NONE',  ( 20.99142135623731065, 64.40000000001218439, -143.4513107147999165 ) ) ;
#70753=DIRECTION ( 'NONE',  ( 0.000000000000000000, 1.000000000000000000, 6.982962677686266711E-15 ) ) ;
#70765=AXIS2_PLACEMENT_3D ( 'NONE', #212863, #158065, #34250 ) ;
#70779=SURFACE_STYLE_FILL_AREA ( #231130 ) ;
#70797=CARTESIAN_POINT ( 'NONE',  ( 23.25000000000000000, 87.75000000001246292, -181.7731074845242745 ) ) ;
#70811=( BOUNDED_SURFACE ( )  B_SPLINE_SURFACE ( 3, 2, ( 
 ( #165715, #146122, #41920 ),
 ( #65303, #125287, #221780 ),
 ( #202254, #143553, #164416 ),
 ( #6610, #83554, #121463 ) ),
 .UNSPECIFIED., .F., .F., .F. ) 
 B_SPLINE_SURFACE_WITH_KNOTS ( ( 4, 4 ),
 ( 3, 3 ),
 ( 0.0002700421466196637442, 0.0004789321604330607179 ),
 ( 0.000000000000000000, 1.000000000000000000 ),
 .UNSPECIFIED. ) 
 GEOMETRIC_REPRESENTATION_ITEM ( )  RATIONAL_B_SPLINE_SURFACE ( (
 ( 1.000000000000000000, 0.7071067811865475727, 1.000000000000000000),
 ( 1.000000000000000000, 0.7163411249511738577, 1.000000000000000000),
 ( 1.000000000000000000, 0.7221957104842052777, 1.000000000000000000),
 ( 1.000000000000000000, 0.7250110520819876836, 1.000000000000000000) ) ) 
 REPRESENTATION_ITEM ( '' )  SURFACE ( )  );
#70838=DIRECTION ( 'NONE',  ( 0.000000000000000000, -1.000000000000000000, -6.352154140967427193E-15 ) ) ;
#70855=ADVANCED_FACE ( 'NONE', ( #190640 ), #181587, .F. ) ;
#70869=ORIENTED_EDGE ( 'NONE', *, *, #35503, .F. ) ;
#70876=DIRECTION ( 'NONE',  ( -1.000000000000000000, 2.952720810173289112E-16, 2.061873921506763405E-30 ) ) ;
#70883=DIRECTION ( 'NONE',  ( 0.000000000000000000, -7.086529944415886769E-15, 1.000000000000000000 ) ) ;
#70884=CARTESIAN_POINT ( 'NONE',  ( 20.94999999999999929, 74.63912941282028157, -161.9501095574334215 ) ) ;
#70890=AXIS2_PLACEMENT_3D ( 'NONE', #255082, #15267, #256357 ) ;
#70905=DIRECTION ( 'NONE',  ( -0.000000000000000000, 1.000000000000000000, 6.982962677686266711E-15 ) ) ;
#70914=ORIENTED_EDGE ( 'NONE', *, *, #129223, .F. ) ;
#70938=DIRECTION ( 'NONE',  ( 1.000000000000000000, 0.000000000000000000, 0.000000000000000000 ) ) ;
#70964=FACE_BOUND ( 'NONE', #120590, .T. ) ;
#70968=DIRECTION ( 'NONE',  ( 0.000000000000000000, -1.000000000000000000, 0.000000000000000000 ) ) ;
#71018=VECTOR ( 'NONE', #239431, 1000.000000000000000 ) ;
#71053=CARTESIAN_POINT ( 'NONE',  ( -23.25000000000000000, 64.25000000001229239, -157.8731074845244393 ) ) ;
#71080=VERTEX_POINT ( 'NONE', #145897 ) ;
#71104=EDGE_LOOP ( 'NONE', ( #108206, #166985, #124183, #225464, #16621 ) ) ;
#71119=AXIS2_PLACEMENT_3D ( 'NONE', #190118, #32351, #168019 ) ;
#71129=DIRECTION ( 'NONE',  ( 3.469446951953635015E-14, 6.982962677686266711E-15, -1.000000000000000000 ) ) ;
#71140=EDGE_CURVE ( 'NONE', #203407, #208166, #173436, .T. ) ;
#71163=ORIENTED_EDGE ( 'NONE', *, *, #63780, .T. ) ;
#71188=CARTESIAN_POINT ( 'NONE',  ( 18.59999999999999076, 64.35000000001220144, -145.1731074845244507 ) ) ;
#71203=CARTESIAN_POINT ( 'NONE',  ( 23.14999999999998437, 76.00000000001237765, -170.0231074845243597 ) ) ;
#71214=CIRCLE ( 'NONE', #137816, 11.65000000000000746 ) ;
#71290=ORIENTED_EDGE ( 'NONE', *, *, #10641, .F. ) ;
#71341=CARTESIAN_POINT ( 'NONE',  ( 20.85000000000000142, 87.65000000001214175, -136.5231074845242745 ) ) ;
#71377=VECTOR ( 'NONE', #116514, 1000.000000000000000 ) ;
#71425=ADVANCED_FACE ( 'NONE', ( #157275 ), #215916, .F. ) ;
#71466=CARTESIAN_POINT ( 'NONE',  ( 21.08804281139604342, 65.37816569817111656, -157.6731075171456098 ) ) ;
#71488=CARTESIAN_POINT ( 'NONE',  ( 20.97107704358301916, 67.12452184799103350, -161.4641342551351784 ) ) ;
#71508=FACE_OUTER_BOUND ( 'NONE', #161384, .T. ) ;
#71517=ADVANCED_FACE ( 'NONE', ( #245778 ), #131859, .T. ) ;
#71523=DIRECTION ( 'NONE',  ( 0.000000000000000000, 0.9915357197604862671, -0.1298341882519953583 ) ) ;
#71548=FACE_OUTER_BOUND ( 'NONE', #6809, .T. ) ;
#71557=ORIENTED_EDGE ( 'NONE', *, *, #199435, .F. ) ;
#71562=CARTESIAN_POINT ( 'NONE',  ( -21.05000000000000071, 87.48912529308842068, -167.0231074845242745 ) ) ;
#71568=AXIS2_PLACEMENT_3D ( 'NONE', #185021, #106755, #88460 ) ;
#71581=CARTESIAN_POINT ( 'NONE',  ( -20.85000000000000142, 77.16412189325330928, -128.6082593989527254 ) ) ;
#71585=CARTESIAN_POINT ( 'NONE',  ( -20.54999999999999716, 76.00000000001212186, -134.5231074845243313 ) ) ;
#71592=VERTEX_POINT ( 'NONE', #210504 ) ;
#71632=EDGE_LOOP ( 'NONE', ( #11773, #52486, #26893, #182306, #119232 ) ) ;
#71641=VECTOR ( 'NONE', #13694, 1000.000000000000000 ) ;
#71737=ORIENTED_EDGE ( 'NONE', *, *, #204115, .F. ) ;
#71751=CARTESIAN_POINT ( 'NONE',  ( -18.59999999999999787, 64.25000000001233502, -163.0083017138704236 ) ) ;
#71758=EDGE_CURVE ( 'NONE', #2383, #217847, #152928, .T. ) ;
#71769=DIRECTION ( 'NONE',  ( 0.000000000000000000, -7.189901751995769991E-15, 1.000000000000000000 ) ) ;
#71794=CIRCLE ( 'NONE', #221588, 0.09999999999998898659 ) ;
#71799=DIRECTION ( 'NONE',  ( 1.000000000000000000, 0.000000000000000000, 0.000000000000000000 ) ) ;
#71820=DIRECTION ( 'NONE',  ( -1.000000000000000000, -0.000000000000000000, -0.000000000000000000 ) ) ;
#71830=CARTESIAN_POINT ( 'NONE',  ( -21.08376601933334271, 75.93622398908254922, -176.3650547558000881 ) ) ;
#71838=CARTESIAN_POINT ( 'NONE',  ( 21.08884785362045378, 69.64280663258713844, -170.0728905795912453 ) ) ;
#71854=CARTESIAN_POINT ( 'NONE',  ( -23.25000000000000000, 68.97833521811203639, -132.6895420826271277 ) ) ;
#71872=VECTOR ( 'NONE', #223714, 1000.000000000000000 ) ;
#71882=VECTOR ( 'NONE', #190511, 1000.000000000000000 ) ;
#71911=AXIS2_PLACEMENT_3D ( 'NONE', #86263, #82407, #2884 ) ;
#71968=CARTESIAN_POINT ( 'NONE',  ( 20.94999999999999929, 69.35000000001228670, -157.8731074845244109 ) ) ;
#71982=CIRCLE ( 'NONE', #125940, 0.09999999999998898659 ) ;
#72021=CARTESIAN_POINT ( 'NONE',  ( -23.15000000000000213, 64.35000000001218723, -143.5379132551784096 ) ) ;
#72031=AXIS2_PLACEMENT_3D ( 'NONE', #132908, #110759, #29975 ) ;
#72044=( NAMED_UNIT ( * ) SI_UNIT ( $, .STERADIAN. ) SOLID_ANGLE_UNIT ( ) );
#72112=CIRCLE ( 'NONE', #251129, 0.2000000000000057288 ) ;
#72138=EDGE_LOOP ( 'NONE', ( #63652, #251855, #139215, #109778 ) ) ;
#72146=DIRECTION ( 'NONE',  ( 1.000000000000000000, 0.000000000000000000, 0.000000000000000000 ) ) ;
#72181=CARTESIAN_POINT ( 'NONE',  ( -18.44204374631838661, 85.49103638961042861, -129.8969062143032716 ) ) ;
#72216=AXIS2_PLACEMENT_3D ( 'NONE', #44020, #103967, #151806 ) ;
#72220=DIRECTION ( 'NONE',  ( -1.000000000000000000, 0.000000000000000000, 0.000000000000000000 ) ) ;
#72223=DIRECTION ( 'NONE',  ( 0.000000000000000000, 0.000000000000000000, -1.000000000000000000 ) ) ;
#72234=CARTESIAN_POINT ( 'NONE',  ( 20.85000000000000142, 76.00000000001213607, -136.5231074845243313 ) ) ;
#72245=ORIENTED_EDGE ( 'NONE', *, *, #72261, .F. ) ;
#72261=EDGE_CURVE ( 'NONE', #9997, #147041, #111378, .T. ) ;
#72288=CARTESIAN_POINT ( 'NONE',  ( 23.14999999999999503, 64.35000000001222986, -148.6731074845244507 ) ) ;
#72290=DIRECTION ( 'NONE',  ( 1.734723475976757112E-13, 0.9999176327611370985, 0.01283462868040226822 ) ) ;
#72308=ADVANCED_FACE ( 'NONE', ( #230411 ), #171754, .F. ) ;
#72311=AXIS2_PLACEMENT_3D ( 'NONE', #139474, #100335, #37848 ) ;
#72338=CARTESIAN_POINT ( 'NONE',  ( 23.14999999999999503, 64.35000000001218723, -143.5379132551783812 ) ) ;
#72340=CIRCLE ( 'NONE', #155745, 0.09999999999999939493 ) ;
#72350=VECTOR ( 'NONE', #61059, 1000.000000000000000 ) ;
#72402=ORIENTED_EDGE ( 'NONE', *, *, #79648, .F. ) ;
#72407=SPHERICAL_SURFACE ( 'NONE', #256563, 0.1000000000000000056 ) ;
#72410=CARTESIAN_POINT ( 'NONE',  ( 23.14999999999999503, 61.95000000001218154, -142.0368025552853624 ) ) ;
#72436=CARTESIAN_POINT ( 'NONE',  ( -22.49544290803737212, 64.25012976215484173, -170.0884194437827261 ) ) ;
#72466=ORIENTED_EDGE ( 'NONE', *, *, #161091, .F. ) ;
#72471=DIRECTION ( 'NONE',  ( 0.000000000000000000, -0.4999999999999088507, 0.8660254037844913322 ) ) ;
#72474=CIRCLE ( 'NONE', #130712, 0.09999999999998898659 ) ;
#72496=CARTESIAN_POINT ( 'NONE',  ( 21.00000000000000000, 66.25000000001223555, -148.7731074845244450 ) ) ;
#72520=AXIS2_PLACEMENT_3D ( 'NONE', #119839, #199367, #39010 ) ;
#72526=ORIENTED_EDGE ( 'NONE', *, *, #12477, .T. ) ;
#72584=VECTOR ( 'NONE', #54230, 1000.000000000000114 ) ;
#72596=CARTESIAN_POINT ( 'NONE',  ( -23.15000000000000213, 73.50000000001229239, -156.7984855617622770 ) ) ;
#72610=FACE_OUTER_BOUND ( 'NONE', #91794, .T. ) ;
#72638=DIRECTION ( 'NONE',  ( -0.000000000000000000, 1.000000000000000000, 6.982962677686267499E-15 ) ) ;
#72702=ORIENTED_EDGE ( 'NONE', *, *, #244760, .F. ) ;
#72720=ORIENTED_EDGE ( 'NONE', *, *, #136347, .F. ) ;
#72750=VERTEX_POINT ( 'NONE', #230101 ) ;
#72751=ORIENTED_EDGE ( 'NONE', *, *, #21132, .F. ) ;
#72762=CARTESIAN_POINT ( 'NONE',  ( 21.06089410995835109, 65.27470446788869651, -157.8207267534812104 ) ) ;
#72770=VECTOR ( 'NONE', #92511, 1000.000000000000000 ) ;
#72775=ADVANCED_FACE ( 'NONE', ( #131003 ), #207997, .T. ) ;
#72793=CARTESIAN_POINT ( 'NONE',  ( 20.85000000000000142, 64.35000000001218723, -143.3069731475025037 ) ) ;
#72801=LINE ( 'NONE', #134016, #38098 ) ;
#72805=ORIENTED_EDGE ( 'NONE', *, *, #82829, .F. ) ;
#72842=EDGE_CURVE ( 'NONE', #251542, #30528, #50170, .T. ) ;
#72854=CIRCLE ( 'NONE', #172831, 11.64999999999999325 ) ;
#72876=DIRECTION ( 'NONE',  ( 0.000000000000000000, -6.467318590049456648E-15, 1.000000000000000000 ) ) ;
#72887=DIRECTION ( 'NONE',  ( -0.000000000000000000, -6.982962677686266711E-15, 1.000000000000000000 ) ) ;
#72915=AXIS2_PLACEMENT_3D ( 'NONE', #154088, #114914, #131907 ) ;
#72960=EDGE_LOOP ( 'NONE', ( #180258, #207085, #31545, #183311 ) ) ;
#72998=ORIENTED_EDGE ( 'NONE', *, *, #131888, .F. ) ;
#73006=ORIENTED_EDGE ( 'NONE', *, *, #151316, .T. ) ;
#73019=EDGE_CURVE ( 'NONE', #223792, #46071, #181695, .T. ) ;
#73023=MECHANICAL_DESIGN_GEOMETRIC_PRESENTATION_REPRESENTATION('',(#206075),#147824);
#73025=CARTESIAN_POINT ( 'NONE',  ( -21.14999999999999858, 69.45934304831114048, -169.9231074845244223 ) ) ;
#73048=DIRECTION ( 'NONE',  ( 0.000000000000000000, 0.1350103645451945777, -0.9908441862701589109 ) ) ;
#73060=FACE_OUTER_BOUND ( 'NONE', #247929, .T. ) ;
#73063=VECTOR ( 'NONE', #141524, 1000.000000000000000 ) ;
#73067=DIRECTION ( 'NONE',  ( 0.000000000000000000, -6.467318590049456648E-15, 1.000000000000000000 ) ) ;
#73082=EDGE_CURVE ( 'NONE', #168942, #35313, #180409, .T. ) ;
#73089=ADVANCED_FACE ( 'NONE', ( #128145 ), #234486, .T. ) ;
#73091=VECTOR ( 'NONE', #60016, 1000.000000000000000 ) ;
#73100=AXIS2_PLACEMENT_3D ( 'NONE', #256936, #20982, #155359 ) ;
#73111=CIRCLE ( 'NONE', #64690, 0.1000000000000033223 ) ;
#73115=AXIS2_PLACEMENT_3D ( 'NONE', #91173, #31249, #207293 ) ;
#73134=AXIS2_PLACEMENT_3D ( 'NONE', #237205, #157708, #160257 ) ;
#73158=AXIS2_PLACEMENT_3D ( 'NONE', #115448, #154619, #114169 ) ;
#73164=DIRECTION ( 'NONE',  ( 0.000000000000000000, 0.000000000000000000, 1.000000000000000000 ) ) ;
#73187=CARTESIAN_POINT ( 'NONE',  ( 21.30000000000002558, 76.00000000001237765, -170.0231074845243597 ) ) ;
#73231=VECTOR ( 'NONE', #77011, 1000.000000000000000 ) ;
#73239=ADVANCED_FACE ( 'NONE', ( #214093 ), #21058, .F. ) ;
#73243=VERTEX_POINT ( 'NONE', #180117 ) ;
#73249=VECTOR ( 'NONE', #125088, 999.9999999999998863 ) ;
#73252=DIRECTION ( 'NONE',  ( 0.000000000000000000, 0.000000000000000000, 1.000000000000000000 ) ) ;
#73259=DIRECTION ( 'NONE',  ( 0.000000000000000000, -0.5000000000000016653, 0.8660254037844377084 ) ) ;
#73260=ORIENTED_EDGE ( 'NONE', *, *, #7249, .T. ) ;
#73263=EDGE_CURVE ( 'NONE', #195708, #219226, #44459, .T. ) ;
#73295=ORIENTED_EDGE ( 'NONE', *, *, #114926, .F. ) ;
#73314=TOROIDAL_SURFACE ( 'NONE', #239694, 0.2000000000000000111, 0.1000000000000000056 ) ;
#73319=ORIENTED_EDGE ( 'NONE', *, *, #210169, .F. ) ;
#73322=CARTESIAN_POINT ( 'NONE',  ( 18.46082813847984383, 85.48074965091987565, -162.9387373818086644 ) ) ;
#73325=DIRECTION ( 'NONE',  ( -1.000000000000000000, -0.000000000000000000, -0.000000000000000000 ) ) ;
#73338=ORIENTED_EDGE ( 'NONE', *, *, #31839, .F. ) ;
#73361=DIRECTION ( 'NONE',  ( 0.000000000000000000, -0.4999999999999088507, -0.8660254037844913322 ) ) ;
#73376=LINE ( 'NONE', #96726, #180592 ) ;
#73383=EDGE_LOOP ( 'NONE', ( #187326, #232818, #36674, #89967 ) ) ;
#73396=AXIS2_PLACEMENT_3D ( 'NONE', #105205, #139221, #218766 ) ;
#73408=VECTOR ( 'NONE', #14180, 1000.000000000000000 ) ;
#73414=ORIENTED_EDGE ( 'NONE', *, *, #35201, .F. ) ;
#73478=ORIENTED_EDGE ( 'NONE', *, *, #6689, .F. ) ;
#73499=DIRECTION ( 'NONE',  ( 1.000000000000000000, 0.000000000000000000, 0.000000000000000000 ) ) ;
#73521=ORIENTED_EDGE ( 'NONE', *, *, #184504, .T. ) ;
#73529=ADVANCED_FACE ( 'NONE', ( #86101 ), #147396, .T. ) ;
#73665=EDGE_CURVE ( 'NONE', #127337, #99016, #222754, .T. ) ;
#73684=LINE ( 'NONE', #232744, #106952 ) ;
#73758=ORIENTED_EDGE ( 'NONE', *, *, #134141, .F. ) ;
#73779=DIRECTION ( 'NONE',  ( 0.000000000000000000, 1.000000000000000000, 6.853228547068871147E-15 ) ) ;
#73802=VERTEX_POINT ( 'NONE', #7574 ) ;
#73808=ORIENTED_EDGE ( 'NONE', *, *, #73019, .F. ) ;
#73823=LINE ( 'NONE', #131188, #49023 ) ;
#73825=CARTESIAN_POINT ( 'NONE',  ( -20.91682497891423154, 65.67736539654967487, -130.9625116876572406 ) ) ;
#73830=CIRCLE ( 'NONE', #23940, 11.64999999999999325 ) ;
#73832=CARTESIAN_POINT ( 'NONE',  ( 23.14999999999999858, 71.18691588786271041, -148.4646252410481964 ) ) ;
#73907=CYLINDRICAL_SURFACE ( 'NONE', #48954, 0.5000000000000004441 ) ;
#73920=LINE ( 'NONE', #212129, #148996 ) ;
#73928=VECTOR ( 'NONE', #166396, 1000.000000000000000 ) ;
#73937=DIRECTION ( 'NONE',  ( 0.000000000000000000, -0.8660254037844377084, -0.5000000000000016653 ) ) ;
#73957=AXIS2_PLACEMENT_3D ( 'NONE', #63684, #4973, #68507 ) ;
#73960=ORIENTED_EDGE ( 'NONE', *, *, #198243, .T. ) ;
#73972=EDGE_LOOP ( 'NONE', ( #196215, #53172, #114834, #150559 ) ) ;
#73985=DIRECTION ( 'NONE',  ( -1.000000000000000000, -0.000000000000000000, -0.000000000000000000 ) ) ;
#73986=DIRECTION ( 'NONE',  ( -0.000000000000000000, 0.4791956752371485107, 0.8777080977375185666 ) ) ;
#73991=ORIENTED_EDGE ( 'NONE', *, *, #52719, .F. ) ;
#74033=CYLINDRICAL_SURFACE ( 'NONE', #171074, 0.1000000000000026007 ) ;
#74039=CARTESIAN_POINT ( 'NONE',  ( 20.94999999999999929, 76.00000000001212186, -134.6231074845243256 ) ) ;
#74041=ORIENTED_EDGE ( 'NONE', *, *, #89850, .F. ) ;
#74045=CARTESIAN_POINT ( 'NONE',  ( 21.13461538461538680, 65.38541703798675542, -157.6731074845244223 ) ) ;
#74052=CIRCLE ( 'NONE', #40734, 7.899999999999990585 ) ;
#74055=CARTESIAN_POINT ( 'NONE',  ( -18.50000000000000000, 76.00000000001213607, -136.5231074845243313 ) ) ;
#74063=CARTESIAN_POINT ( 'NONE',  ( 21.05000000000000071, 77.16270174995034381, -162.1231074845243540 ) ) ;
#74078=CARTESIAN_POINT ( 'NONE',  ( -20.64999999999999858, 85.40000000001221281, -146.4170766071767389 ) ) ;
#74090=CIRCLE ( 'NONE', #194873, 0.1000000000000028644 ) ;
#74100=CARTESIAN_POINT ( 'NONE',  ( 21.17356465864818205, 75.90108875899855434, -176.4459106107660773 ) ) ;
#74128=CIRCLE ( 'NONE', #90820, 0.1000000000000028644 ) ;
#74134=ORIENTED_EDGE ( 'NONE', *, *, #54532, .T. ) ;
#74157=FACE_OUTER_BOUND ( 'NONE', #11025, .T. ) ;
#74173=EDGE_CURVE ( 'NONE', #3474, #164498, #12108, .T. ) ;
#74174=ORIENTED_EDGE ( 'NONE', *, *, #191812, .F. ) ;
#74208=ORIENTED_EDGE ( 'NONE', *, *, #201831, .F. ) ;
#74214=ORIENTED_EDGE ( 'NONE', *, *, #144735, .F. ) ;
#74215=AXIS2_PLACEMENT_3D ( 'NONE', #82085, #177398, #256844 ) ;
#74268=DIRECTION ( 'NONE',  ( 0.000000000000000000, -7.487053152578134969E-15, 1.000000000000000000 ) ) ;
#74285=DIRECTION ( 'NONE',  ( 1.000000000000000000, 0.000000000000000000, 0.000000000000000000 ) ) ;
#74286=DIRECTION ( 'NONE',  ( -1.000000000000000000, 2.952720810173289112E-16, 2.061873921506763405E-30 ) ) ;
#74305=DIRECTION ( 'NONE',  ( 0.000000000000000000, 1.000000000000000000, 6.982962677686266711E-15 ) ) ;
#74344=TOROIDAL_SURFACE ( 'NONE', #36928, 0.6000000000000009770, 0.1000000000000000056 ) ;
#74352=FACE_OUTER_BOUND ( 'NONE', #103068, .T. ) ;
#74370=EDGE_CURVE ( 'NONE', #10361, #52922, #7690, .T. ) ;
#74384=DIRECTION ( 'NONE',  ( 0.000000000000000000, 0.000000000000000000, 1.000000000000000000 ) ) ;
#74456=DIRECTION ( 'NONE',  ( 1.000000000000000000, 0.000000000000000000, 0.000000000000000000 ) ) ;
#74458=DIRECTION ( 'NONE',  ( 0.000000000000000000, -6.467318590049456648E-15, 1.000000000000000000 ) ) ;
#74460=ORIENTED_EDGE ( 'NONE', *, *, #56787, .T. ) ;
#74490=DIRECTION ( 'NONE',  ( 0.000000000000000000, 0.9999176327611370985, -0.01283462868041286391 ) ) ;
#74491=CIRCLE ( 'NONE', #37058, 0.09999999999998898659 ) ;
#74495=CARTESIAN_POINT ( 'NONE',  ( 21.04999999999999716, 76.01681986839808758, -176.3305327040897055 ) ) ;
#74505=EDGE_CURVE ( 'NONE', #5643, #241641, #101383, .T. ) ;
#74525=VECTOR ( 'NONE', #133569, 1000.000000000000000 ) ;
#74533=VERTEX_POINT ( 'NONE', #122888 ) ;
#74540=ORIENTED_EDGE ( 'NONE', *, *, #173922, .F. ) ;
#74552=VECTOR ( 'NONE', #196151, 1000.000000000000000 ) ;
#74563=AXIS2_PLACEMENT_3D ( 'NONE', #66349, #140743, #179890 ) ;
#74577=( BOUNDED_SURFACE ( )  B_SPLINE_SURFACE ( 3, 2, ( 
 ( #102339, #59358, #180637 ),
 ( #82769, #161080, #22868 ),
 ( #673, #58088, #1974 ),
 ( #181918, #43689, #137629 ) ),
 .UNSPECIFIED., .F., .F., .F. ) 
 B_SPLINE_SURFACE_WITH_KNOTS ( ( 4, 4 ),
 ( 3, 3 ),
 ( -3.469446951953614189E-18, 0.001979672783031543714 ),
 ( 0.000000000000000000, 1.000000000000000000 ),
 .UNSPECIFIED. ) 
 GEOMETRIC_REPRESENTATION_ITEM ( )  RATIONAL_B_SPLINE_SURFACE ( (
 ( 1.000000000000000000, 0.7103081912007699339, 1.000000000000000000),
 ( 1.000000000000000000, 0.7104998333558610879, 1.000000000000000000),
 ( 1.000000000000000000, 0.7107238315755344260, 1.000000000000000000),
 ( 1.000000000000000000, 0.7110073749539295163, 1.000000000000000000) ) ) 
 REPRESENTATION_ITEM ( '' )  SURFACE ( )  );
#74601=AXIS2_PLACEMENT_3D ( 'NONE', #72021, #151577, #14625 ) ;
#74612=FACE_OUTER_BOUND ( 'NONE', #178820, .T. ) ;
#74640=DIRECTION ( 'NONE',  ( 1.000000000000000000, 0.000000000000000000, 0.000000000000000000 ) ) ;
#74659=SPHERICAL_SURFACE ( 'NONE', #232019, 0.1000000000000000056 ) ;
#74673=CIRCLE ( 'NONE', #82960, 0.1000000000000033362 ) ;
#74677=EDGE_CURVE ( 'NONE', #189423, #94999, #62033, .T. ) ;
#74698=DIRECTION ( 'NONE',  ( -1.000000000000000000, 7.304098846218134667E-16, 5.100424963727256530E-30 ) ) ;
#74700=AXIS2_PLACEMENT_3D ( 'NONE', #118860, #40634, #80980 ) ;
#74712=ADVANCED_FACE ( 'NONE', ( #90144 ), #94003, .F. ) ;
#74759=ORIENTED_EDGE ( 'NONE', *, *, #189420, .T. ) ;
#74762=DIRECTION ( 'NONE',  ( 1.000000000000000000, 0.000000000000000000, 0.000000000000000000 ) ) ;
#74763=VERTEX_POINT ( 'NONE', #213969 ) ;
#74773=CARTESIAN_POINT ( 'NONE',  ( -18.39999999999999858, 85.50000000001212186, -129.6009576351939074 ) ) ;
#74778=CARTESIAN_POINT ( 'NONE',  ( -18.59999999999999787, 68.97833521811203639, -132.6895420826271277 ) ) ;
#74795=CIRCLE ( 'NONE', #91676, 0.2000000000000057288 ) ;
#74796=DIRECTION ( 'NONE',  ( -0.000000000000000000, -6.982962677686266711E-15, 1.000000000000000000 ) ) ;
#74834=DIRECTION ( 'NONE',  ( 1.000000000000000000, 0.000000000000000000, 0.000000000000000000 ) ) ;
#74862=CYLINDRICAL_SURFACE ( 'NONE', #52364, 0.09999999999999939493 ) ;
#74865=VECTOR ( 'NONE', #76628, 1000.000000000000114 ) ;
#74905=DIRECTION ( 'NONE',  ( -1.000000000000000000, -0.000000000000000000, -0.000000000000000000 ) ) ;
#74933=AXIS2_PLACEMENT_3D ( 'NONE', #188292, #9662, #12256 ) ;
#74957=CARTESIAN_POINT ( 'NONE',  ( -21.14999999999999858, 64.25000000001233502, -163.2392418215462726 ) ) ;
#74964=VERTEX_POINT ( 'NONE', #67729 ) ;
#74990=ADVANCED_FACE ( 'NONE', ( #51993, #173301 ), #208541, .T. ) ;
#74993=ORIENTED_EDGE ( 'NONE', *, *, #157964, .T. ) ;
#75010=DIRECTION ( 'NONE',  ( 0.000000000000000000, -0.1568667991644355497, 0.9876197685951332295 ) ) ;
#75017=EDGE_CURVE ( 'NONE', #141149, #133516, #70331, .T. ) ;
#75019=AXIS2_PLACEMENT_3D ( 'NONE', #95237, #17004, #57376 ) ;
#75028=VECTOR ( 'NONE', #179226, 1000.000000000000114 ) ;
#75067=DIRECTION ( 'NONE',  ( 1.000000000000000000, 0.000000000000000000, 0.000000000000000000 ) ) ;
#75071=CARTESIAN_POINT ( 'NONE',  ( -18.59999999999999787, 74.83729825007431202, -161.9231074845243654 ) ) ;
#75087=EDGE_CURVE ( 'NONE', #87344, #179596, #170406, .T. ) ;
#75106=CARTESIAN_POINT ( 'NONE',  ( -18.59999999999999787, 66.65000000001229807, -157.6731074845244223 ) ) ;
#75114=EDGE_CURVE ( 'NONE', #75851, #194825, #175833, .T. ) ;
#75144=DIRECTION ( 'NONE',  ( 1.000000000000000000, 7.304098846218135653E-16, 5.311601492717085047E-30 ) ) ;
#75155=EDGE_CURVE ( 'NONE', #66273, #129641, #158111, .T. ) ;
#75165=CARTESIAN_POINT ( 'NONE',  ( -2.995603634470891112E-16, 87.75000000001223555, -148.7731074845242745 ) ) ;
#75210=DIRECTION ( 'NONE',  ( 0.000000000000000000, 0.000000000000000000, 1.000000000000000000 ) ) ;
#75213=CYLINDRICAL_SURFACE ( 'NONE', #207054, 0.09999999999999939493 ) ;
#75215=DIRECTION ( 'NONE',  ( 0.000000000000000000, 0.9915357197604982575, -0.1298341882519033486 ) ) ;
#75220=ORIENTED_EDGE ( 'NONE', *, *, #246677, .T. ) ;
#75256=CARTESIAN_POINT ( 'NONE',  ( -18.50000000000000000, 68.97833521811203639, -132.8895420826271163 ) ) ;
#75291=EDGE_CURVE ( 'NONE', #174920, #65240, #154029, .T. ) ;
#75362=DIRECTION ( 'NONE',  ( 1.000000000000000000, 0.000000000000000000, 0.000000000000000000 ) ) ;
#75366=DIRECTION ( 'NONE',  ( -1.000000000000000000, 2.952720810173289112E-16, 2.061873921506763405E-30 ) ) ;
#75376=CARTESIAN_POINT ( 'NONE',  ( 21.59780538579342490, 75.90102133041445143, -176.8701980144676043 ) ) ;
#75413=VERTEX_POINT ( 'NONE', #116499 ) ;
#75459=EDGE_CURVE ( 'NONE', #134685, #43942, #203846, .T. ) ;
#75488=ORIENTED_EDGE ( 'NONE', *, *, #173922, .T. ) ;
#75519=DIRECTION ( 'NONE',  ( 0.000000000000000000, -0.9998779222360104635, -0.01562499999996343723 ) ) ;
#75529=VERTEX_POINT ( 'NONE', #201160 ) ;
#75535=ORIENTED_EDGE ( 'NONE', *, *, #46532, .T. ) ;
#75564=AXIS2_PLACEMENT_3D ( 'NONE', #77445, #114019, #76175 ) ;
#75612=DIRECTION ( 'NONE',  ( 0.000000000000000000, -6.982962677686266711E-15, 1.000000000000000000 ) ) ;
#75615=EDGE_CURVE ( 'NONE', #135478, #168421, #33387, .T. ) ;
#75633=DIRECTION ( 'NONE',  ( -2.952720810173289605E-16, -1.000000000000000000, -7.086529944415894657E-15 ) ) ;
#75649=TOROIDAL_SURFACE ( 'NONE', #221344, 4.099999999999999645, 0.1000000000000000056 ) ;
#75676=AXIS2_PLACEMENT_3D ( 'NONE', #238977, #77309, #257188 ) ;
#75678=CIRCLE ( 'NONE', #83983, 0.4000000000000114575 ) ;
#75683=DIRECTION ( 'NONE',  ( -1.000000000000000000, -0.000000000000000000, -0.000000000000000000 ) ) ;
#75691=DIRECTION ( 'NONE',  ( -1.000000000000000000, 3.265361837132813093E-16, 2.280189983783949500E-30 ) ) ;
#75707=ORIENTED_EDGE ( 'NONE', *, *, #57878, .T. ) ;
#75756=CIRCLE ( 'NONE', #79989, 0.4000000000000114575 ) ;
#75757=VERTEX_POINT ( 'NONE', #90183 ) ;
#75792=CIRCLE ( 'NONE', #250562, 0.2000000000000057288 ) ;
#75794=ORIENTED_EDGE ( 'NONE', *, *, #2752, .F. ) ;
#75808=TOROIDAL_SURFACE ( 'NONE', #196597, 0.4000000000000012990, 0.1000000000000000056 ) ;
#75815=ADVANCED_FACE ( 'NONE', ( #152784 ), #249296, .T. ) ;
#75820=ORIENTED_EDGE ( 'NONE', *, *, #190099, .F. ) ;
#75837=EDGE_LOOP ( 'NONE', ( #114434, #85662, #15426, #185144 ) ) ;
#75851=VERTEX_POINT ( 'NONE', #52344 ) ;
#75886=AXIS2_PLACEMENT_3D ( 'NONE', #214041, #194497, #56223 ) ;
#75942=ORIENTED_EDGE ( 'NONE', *, *, #157563, .F. ) ;
#75946=EDGE_CURVE ( 'NONE', #167063, #91225, #66855, .T. ) ;
#75951=EDGE_CURVE ( 'NONE', #42521, #110495, #154378, .T. ) ;
#75976=DIRECTION ( 'NONE',  ( 1.000000000000000000, 0.000000000000000000, 0.000000000000000000 ) ) ;
#75988=CARTESIAN_POINT ( 'NONE',  ( 18.60000000000000142, 85.40000000001226965, -162.7258477248609836 ) ) ;
#75999=ORIENTED_EDGE ( 'NONE', *, *, #72842, .F. ) ;
#76007=CARTESIAN_POINT ( 'NONE',  ( -20.64999999999999858, 85.40000000001231228, -160.1291383618718385 ) ) ;
#76013=CARTESIAN_POINT ( 'NONE',  ( -18.46154800491001069, 85.48020627425415796, -129.8656566461428099 ) ) ;
#76051=DIRECTION ( 'NONE',  ( 2.342056488767301376E-15, 0.1350103645451835865, 0.9908441862701605762 ) ) ;
#76058=EDGE_CURVE ( 'NONE', #258015, #78383, #187680, .T. ) ;
#76072=VECTOR ( 'NONE', #159628, 1000.000000000000000 ) ;
#76100=VERTEX_POINT ( 'NONE', #163046 ) ;
#76117=EDGE_CURVE ( 'NONE', #49587, #157237, #116919, .T. ) ;
#76133=DIRECTION ( 'NONE',  ( -1.000000000000000000, 0.000000000000000000, -0.000000000000000000 ) ) ;
#76143=DIRECTION ( 'NONE',  ( 1.000000000000000000, 0.000000000000000000, 0.000000000000000000 ) ) ;
#76175=DIRECTION ( 'NONE',  ( 0.000000000000000000, -7.116814260417660624E-15, 1.000000000000000000 ) ) ;
#76205=LINE ( 'NONE', #99602, #231616 ) ;
#76222=VECTOR ( 'NONE', #21348, 1000.000000000000000 ) ;
#76223=CARTESIAN_POINT ( 'NONE',  ( 20.94999999999999574, 74.15091558138529138, -158.3670969630772447 ) ) ;
#76236=CIRCLE ( 'NONE', #209516, 0.1000000000000070832 ) ;
#76257=VECTOR ( 'NONE', #176211, 1000.000000000000114 ) ;
#76267=EDGE_CURVE ( 'NONE', #48052, #88042, #181001, .T. ) ;
#76283=CIRCLE ( 'NONE', #109604, 0.09999999999999080458 ) ;
#76300=CARTESIAN_POINT ( 'NONE',  ( 21.07946286933444568, 75.92331615675604439, -176.3521448035320986 ) ) ;
#76301=DIRECTION ( 'NONE',  ( 0.000000000000000000, 0.9915357197604982575, -0.1298341882519033486 ) ) ;
#76302=DIRECTION ( 'NONE',  ( 0.000000000000000000, -6.982962677686266711E-15, 1.000000000000000000 ) ) ;
#76304=DIRECTION ( 'NONE',  ( 0.000000000000000000, -1.000000000000000000, -6.982962677686265922E-15 ) ) ;
#76308=DIRECTION ( 'NONE',  ( 0.7071067811865474617, -0.7071067811865474617, -4.937700262164531476E-15 ) ) ;
#76314=VERTEX_POINT ( 'NONE', #238389 ) ;
#76340=FACE_OUTER_BOUND ( 'NONE', #143050, .T. ) ;
#76423=DIRECTION ( 'NONE',  ( 0.000000000000000000, 1.000000000000000000, 6.982962677686266711E-15 ) ) ;
#76424=AXIS2_PLACEMENT_3D ( 'NONE', #248308, #207921, #30568 ) ;
#76426=DIRECTION ( 'NONE',  ( 0.000000000000000000, 0.000000000000000000, 1.000000000000000000 ) ) ;
#76452=ORIENTED_EDGE ( 'NONE', *, *, #14978, .T. ) ;
#76458=DIRECTION ( 'NONE',  ( -1.000000000000000000, 0.000000000000000000, -0.000000000000000000 ) ) ;
#76481=ORIENTED_EDGE ( 'NONE', *, *, #179163, .F. ) ;
#76509=ORIENTED_EDGE ( 'NONE', *, *, #69585, .F. ) ;
#76567=CARTESIAN_POINT ( 'NONE',  ( 21.11344571971268280, 65.38212097649376631, -157.7770865921222594 ) ) ;
#76591=LINE ( 'NONE', #156164, #127322 ) ;
#76599=CARTESIAN_POINT ( 'NONE',  ( 23.15000000000000213, 85.00000000001222134, -145.9170766071767389 ) ) ;
#76602=DIRECTION ( 'NONE',  ( 0.000000000000000000, 6.982962677686266711E-15, -1.000000000000000000 ) ) ;
#76628=DIRECTION ( 'NONE',  ( 0.000000000000000000, 0.8700118002898356018, -0.4930308989875170078 ) ) ;
#76632=DIRECTION ( 'NONE',  ( -1.000000000000000000, 0.000000000000000000, -0.000000000000000000 ) ) ;
#76652=TOROIDAL_SURFACE ( 'NONE', #39276, 11.65000000000000036, 0.1000000000000000056 ) ;
#76675=DIRECTION ( 'NONE',  ( -1.000000000000000000, 0.000000000000000000, 0.000000000000000000 ) ) ;
#76686=DIRECTION ( 'NONE',  ( -1.000000000000000000, 0.000000000000000000, 0.000000000000000000 ) ) ;
#76687=VECTOR ( 'NONE', #26980, 1000.000000000000000 ) ;
#76691=CARTESIAN_POINT ( 'NONE',  ( -23.25000000000000000, 76.00000000001237765, -170.0231074845243597 ) ) ;
#76732=CIRCLE ( 'NONE', #47503, 0.09999999999998898659 ) ;
#76760=FACE_OUTER_BOUND ( 'NONE', #115403, .T. ) ;
#76766=DIRECTION ( 'NONE',  ( 1.000000000000000000, 0.000000000000000000, 0.000000000000000000 ) ) ;
#76785=DIRECTION ( 'NONE',  ( 1.000000000000000000, 0.000000000000000000, 0.000000000000000000 ) ) ;
#76790=AXIS2_PLACEMENT_3D ( 'NONE', #61883, #82686, #100946 ) ;
#76806=DIRECTION ( 'NONE',  ( -1.000000000000000000, 0.000000000000000000, -0.000000000000000000 ) ) ;
#76829=EDGE_CURVE ( 'NONE', #176651, #206737, #142227, .T. ) ;
#76858=CARTESIAN_POINT ( 'NONE',  ( -21.05000000000000071, 74.83729825007431202, -161.9231074845243654 ) ) ;
#76864=ORIENTED_EDGE ( 'NONE', *, *, #34800, .T. ) ;
#76888=VERTEX_POINT ( 'NONE', #129695 ) ;
#76897=DIRECTION ( 'NONE',  ( 0.000000000000000000, -7.189901751995743170E-15, 1.000000000000000000 ) ) ;
#76918=CIRCLE ( 'NONE', #89558, 0.1000000000000033362 ) ;
#76919=CARTESIAN_POINT ( 'NONE',  ( -20.64999999999999858, 71.65000000001228386, -157.7731074845243882 ) ) ;
#76920=ORIENTED_EDGE ( 'NONE', *, *, #239684, .T. ) ;
#76933=CARTESIAN_POINT ( 'NONE',  ( 21.30000000000002558, 76.00000000001240608, -174.0731074845243711 ) ) ;
#76964=TOROIDAL_SURFACE ( 'NONE', #181039, 3.899999999999999467, 0.1000000000000000056 ) ;
#76970=DIRECTION ( 'NONE',  ( 1.000000000000000000, 7.304098846218134667E-16, 5.100424963727256530E-30 ) ) ;
#76971=DIRECTION ( 'NONE',  ( 0.000000000000000000, -3.208737065390626061E-15, 1.000000000000000000 ) ) ;
#77011=DIRECTION ( 'NONE',  ( -1.000000000000000000, 0.000000000000000000, 0.000000000000000000 ) ) ;
#77015=DIRECTION ( 'NONE',  ( 1.000000000000000000, 0.000000000000000000, 0.000000000000000000 ) ) ;
#77045=AXIS2_PLACEMENT_3D ( 'NONE', #164003, #166592, #243528 ) ;
#77060=AXIS2_PLACEMENT_3D ( 'NONE', #212378, #195390, #76686 ) ;
#77115=EDGE_LOOP ( 'NONE', ( #17486, #166770, #168255, #177714 ) ) ;
#77131=CARTESIAN_POINT ( 'NONE',  ( 18.42595409746874680, 85.49999981257727200, -163.0237451327774068 ) ) ;
#77140=DIRECTION ( 'NONE',  ( 0.000000000000000000, -1.000000000000000000, -6.982962677686265922E-15 ) ) ;
#77143=CIRCLE ( 'NONE', #152183, 0.1000000000000072220 ) ;
#77161=CARTESIAN_POINT ( 'NONE',  ( -23.25000000000000000, 77.14957036958777792, -128.7071950000224092 ) ) ;
#77166=AXIS2_PLACEMENT_3D ( 'NONE', #100075, #84333, #3559 ) ;
#77194=VERTEX_POINT ( 'NONE', #224313 ) ;
#77197=EDGE_CURVE ( 'NONE', #218463, #31922, #141836, .T. ) ;
#77202=DIRECTION ( 'NONE',  ( -1.000000000000000000, 0.000000000000000000, 0.000000000000000000 ) ) ;
#77222=AXIS2_PLACEMENT_3D ( 'NONE', #80734, #42919, #118622 ) ;
#77279=DIRECTION ( 'NONE',  ( 1.000000000000000000, 0.000000000000000000, 0.000000000000000000 ) ) ;
#77286=CARTESIAN_POINT ( 'NONE',  ( 23.15000000000000213, 85.50000000001222134, -146.4170766071767389 ) ) ;
#77309=DIRECTION ( 'NONE',  ( 0.000000000000000000, -6.982962677686267499E-15, 1.000000000000000000 ) ) ;
#77322=CIRCLE ( 'NONE', #73100, 0.09999999999999939493 ) ;
#77381=DIRECTION ( 'NONE',  ( -1.000000000000000000, 0.000000000000000000, 0.000000000000000000 ) ) ;
#77387=CARTESIAN_POINT ( 'NONE',  ( 21.08489247129321598, 67.12232480914222776, -157.6731074845244223 ) ) ;
#77404=EDGE_LOOP ( 'NONE', ( #179512, #56735, #181079, #148471 ) ) ;
#77423=CARTESIAN_POINT ( 'NONE',  ( 20.94999999999999574, 87.41227409416205774, -167.0231074845242745 ) ) ;
#77433=ORIENTED_EDGE ( 'NONE', *, *, #221326, .F. ) ;
#77434=AXIS2_PLACEMENT_3D ( 'NONE', #120004, #198216, #221611 ) ;
#77445=CARTESIAN_POINT ( 'NONE',  ( 21.05000000000000071, 76.00000000001237765, -170.0231074845243597 ) ) ;
#77448=CARTESIAN_POINT ( 'NONE',  ( 21.05000000000000071, 74.65091558138531980, -162.0366085209788878 ) ) ;
#77497=DIRECTION ( 'NONE',  ( 1.000000000000000000, 7.304098846218133681E-16, 4.639676173203992654E-30 ) ) ;
#77531=CARTESIAN_POINT ( 'NONE',  ( 18.59999999999999076, 65.79142135624952914, -148.7731074845244450 ) ) ;
#77543=CARTESIAN_POINT ( 'NONE',  ( 21.05000000000000071, 75.90220970870319661, -176.2809220950059057 ) ) ;
#77586=CARTESIAN_POINT ( 'NONE',  ( -18.46946985241236661, 85.50931722872408614, -163.0364449190248877 ) ) ;
#77608=DIRECTION ( 'NONE',  ( 0.000000000000000000, 0.000000000000000000, 1.000000000000000000 ) ) ;
#77611=ORIENTED_EDGE ( 'NONE', *, *, #118274, .F. ) ;
#77620=DIRECTION ( 'NONE',  ( -1.000000000000000000, 0.000000000000000000, 0.000000000000000000 ) ) ;
#77721=LINE ( 'NONE', #81558, #88909 ) ;
#77731=DIRECTION ( 'NONE',  ( 0.000000000000000000, -0.6728971962617102953, -0.7397360091702507301 ) ) ;
#77740=CARTESIAN_POINT ( 'NONE',  ( 18.39999999999999858, 85.50000000001233502, -162.9910380878246201 ) ) ;
#77744=ORIENTED_EDGE ( 'NONE', *, *, #55442, .F. ) ;
#77748=VERTEX_POINT ( 'NONE', #179455 ) ;
#77757=LINE ( 'NONE', #142856, #142066 ) ;
#77760=VERTEX_POINT ( 'NONE', #19072 ) ;
#77802=VERTEX_POINT ( 'NONE', #52624 ) ;
#77875=DIRECTION ( 'NONE',  ( -1.000000000000000000, 0.000000000000000000, 0.000000000000000000 ) ) ;
#77907=CARTESIAN_POINT ( 'NONE',  ( -23.25000000000000000, 76.00000000001213607, -138.6231074845243256 ) ) ;
#77982=DIRECTION ( 'NONE',  ( 0.000000000000000000, 0.000000000000000000, 1.000000000000000000 ) ) ;
#78003=CARTESIAN_POINT ( 'NONE',  ( 18.44206774312965180, 85.49102735755222682, -129.8968799798263092 ) ) ;
#78023=AXIS2_PLACEMENT_3D ( 'NONE', #182421, #19488, #121183 ) ;
#78042=CIRCLE ( 'NONE', #219696, 11.70000000000001528 ) ;
#78045=ORIENTED_EDGE ( 'NONE', *, *, #140638, .T. ) ;
#78063=ORIENTED_EDGE ( 'NONE', *, *, #46487, .F. ) ;
#78078=VERTEX_POINT ( 'NONE', #42078 ) ;
#78085=CARTESIAN_POINT ( 'NONE',  ( 23.24999999999999289, 64.35000000001218723, -143.5379132551783812 ) ) ;
#78145=ORIENTED_EDGE ( 'NONE', *, *, #245430, .T. ) ;
#78155=ADVANCED_FACE ( 'NONE', ( #201266 ), #181717, .F. ) ;
#78157=CARTESIAN_POINT ( 'NONE',  ( -18.39999999999999858, 85.50000000001210765, -129.9229180933022576 ) ) ;
#78184=AXIS2_PLACEMENT_3D ( 'NONE', #177450, #82138, #39218 ) ;
#78187=DIRECTION ( 'NONE',  ( 1.000000000000000000, 0.000000000000000000, 0.000000000000000000 ) ) ;
#78198=ORIENTED_EDGE ( 'NONE', *, *, #170316, .T. ) ;
#78245=EDGE_LOOP ( 'NONE', ( #164753, #105910, #26670, #93602, #16851 ) ) ;
#78254=CARTESIAN_POINT ( 'NONE',  ( 18.56579813702274961, 65.66974365629688748, -130.9360145562605169 ) ) ;
#78284=ORIENTED_EDGE ( 'NONE', *, *, #111501, .F. ) ;
#78308=DIRECTION ( 'NONE',  ( 0.000000000000000000, -6.982962677686266711E-15, 1.000000000000000000 ) ) ;
#78332=AXIS2_PLACEMENT_3D ( 'NONE', #70884, #130821, #228663 ) ;
#78383=VERTEX_POINT ( 'NONE', #134557 ) ;
#78421=CARTESIAN_POINT ( 'NONE',  ( 21.07888907270776002, 65.27493078649706604, -157.8019138976912359 ) ) ;
#78430=EDGE_LOOP ( 'NONE', ( #228515, #121843, #60371, #10040 ) ) ;
#78479=CIRCLE ( 'NONE', #178480, 0.5000000000000004441 ) ;
#78484=DIRECTION ( 'NONE',  ( 1.000000000000000000, 0.000000000000000000, 0.000000000000000000 ) ) ;
#78497=DIRECTION ( 'NONE',  ( 0.000000000000000000, -6.467318590049456648E-15, 1.000000000000000000 ) ) ;
#78520=CARTESIAN_POINT ( 'NONE',  ( 20.94999999999999929, 69.55000000001230376, -160.0060803140843859 ) ) ;
#78535=EDGE_CURVE ( 'NONE', #226308, #199740, #143022, .T. ) ;
#78548=EDGE_CURVE ( 'NONE', #245009, #70573, #237541, .T. ) ;
#78549=DIRECTION ( 'NONE',  ( 0.000000000000000000, -1.000000000000000000, -6.352154140967427193E-15 ) ) ;
#78562=VECTOR ( 'NONE', #27782, 1000.000000000000000 ) ;
#78571=CIRCLE ( 'NONE', #173921, 4.049999999999998046 ) ;
#78589=DIRECTION ( 'NONE',  ( -1.836970198721029934E-16, -1.000000000000000000, -6.982962677686266711E-15 ) ) ;
#78607=ORIENTED_EDGE ( 'NONE', *, *, #96709, .T. ) ;
#78645=DIRECTION ( 'NONE',  ( 1.000000000000000000, 0.000000000000000000, 0.000000000000000000 ) ) ;
#78704=CARTESIAN_POINT ( 'NONE',  ( 20.94999999999999929, 65.52661458509942349, -162.4444530202758870 ) ) ;
#78706=FACE_OUTER_BOUND ( 'NONE', #128027, .T. ) ;
#78724=ADVANCED_FACE ( 'NONE', ( #129150 ), #103141, .T. ) ;
#78757=LINE ( 'NONE', #158354, #112269 ) ;
#78777=FACE_OUTER_BOUND ( 'NONE', #43102, .T. ) ;
#78785=DIRECTION ( 'NONE',  ( 0.000000000000000000, 0.000000000000000000, -1.000000000000000000 ) ) ;
#78796=CARTESIAN_POINT ( 'NONE',  ( -21.14999999999999858, 76.00000000001237765, -170.0231074845243597 ) ) ;
#78825=CARTESIAN_POINT ( 'NONE',  ( -20.85000000000000142, 68.92903212821327941, -132.7765432626560766 ) ) ;
#78855=CIRCLE ( 'NONE', #8161, 3.900000000000000799 ) ;
#78875=AXIS2_PLACEMENT_3D ( 'NONE', #233490, #92665, #109652 ) ;
#78895=CARTESIAN_POINT ( 'NONE',  ( -18.59999999999999787, 77.83585931145570669, -125.0186683157258045 ) ) ;
#78902=DIRECTION ( 'NONE',  ( 1.000000000000000000, 0.000000000000000000, 0.000000000000000000 ) ) ;
#78935=ORIENTED_EDGE ( 'NONE', *, *, #199048, .T. ) ;
#78936=FACE_OUTER_BOUND ( 'NONE', #213450, .T. ) ;
#78941=DIRECTION ( 'NONE',  ( 1.000000000000000000, 0.000000000000000000, 0.000000000000000000 ) ) ;
#78992=AXIS2_PLACEMENT_3D ( 'NONE', #170937, #71799, #109612 ) ;
#78996=CYLINDRICAL_SURFACE ( 'NONE', #205456, 0.09999999999999939493 ) ;
#79001=DIRECTION ( 'NONE',  ( -0.000000000000000000, 1.000000000000000000, 6.982962677686266711E-15 ) ) ;
#79006=ADVANCED_FACE ( 'NONE', ( #4687 ), #202905, .T. ) ;
#79029=EDGE_CURVE ( 'NONE', #238847, #146731, #44056, .T. ) ;
#79043=DIRECTION ( 'NONE',  ( 0.000000000000000000, 0.000000000000000000, 1.000000000000000000 ) ) ;
#79047=DIRECTION ( 'NONE',  ( 0.000000000000000000, 0.000000000000000000, -1.000000000000000000 ) ) ;
#79070=AXIS2_PLACEMENT_3D ( 'NONE', #44830, #25284, #124378 ) ;
#79095=DIRECTION ( 'NONE',  ( 0.000000000000000000, -1.000000000000000000, -6.352154140967427193E-15 ) ) ;
#79133=EDGE_LOOP ( 'NONE', ( #125553, #6083, #20897, #109770 ) ) ;
#79136=LINE ( 'NONE', #255165, #137707 ) ;
#79174=CARTESIAN_POINT ( 'NONE',  ( 21.11833042828143547, 69.55435530615680761, -170.0302079935837014 ) ) ;
#79195=DIRECTION ( 'NONE',  ( 2.952720810173289112E-16, 1.000000000000000000, 6.982962677686266711E-15 ) ) ;
#79200=AXIS2_PLACEMENT_3D ( 'NONE', #243348, #64713, #223773 ) ;
#79252=ORIENTED_EDGE ( 'NONE', *, *, #120330, .T. ) ;
#79256=ADVANCED_FACE ( 'NONE', ( #114065 ), #72407, .F. ) ;
#79273=EDGE_CURVE ( 'NONE', #207248, #40059, #19293, .T. ) ;
#79276=CARTESIAN_POINT ( 'NONE',  ( 18.33996824403561376, 85.56963985944319973, -129.7040418470071472 ) ) ;
#79302=CIRCLE ( 'NONE', #225049, 0.2000000000000057288 ) ;
#79310=AXIS2_PLACEMENT_3D ( 'NONE', #196476, #33618, #54408 ) ;
#79313=DIRECTION ( 'NONE',  ( 0.000000000000000000, 6.982962677686266711E-15, -1.000000000000000000 ) ) ;
#79331=LINE ( 'NONE', #59757, #247229 ) ;
#79368=CARTESIAN_POINT ( 'NONE',  ( 20.94999999999999929, 67.22371710471982453, -157.8731074845244109 ) ) ;
#79379=EDGE_LOOP ( 'NONE', ( #143755, #80929, #213516, #253451 ) ) ;
#79381=CARTESIAN_POINT ( 'NONE',  ( 18.49999999999999289, 69.55000000001223270, -148.8731074845244109 ) ) ;
#79408=ORIENTED_EDGE ( 'NONE', *, *, #76058, .F. ) ;
#79422=AXIS2_PLACEMENT_3D ( 'NONE', #31697, #190773, #171227 ) ;
#79432=EDGE_CURVE ( 'NONE', #73243, #59416, #140071, .T. ) ;
#79447=CIRCLE ( 'NONE', #212751, 0.5999999999999894307 ) ;
#79452=ORIENTED_EDGE ( 'NONE', *, *, #18595, .F. ) ;
#79453=CARTESIAN_POINT ( 'NONE',  ( 21.05000000000000071, 71.00000000001223555, -148.9283735034374843 ) ) ;
#79468=EDGE_LOOP ( 'NONE', ( #158588, #92654, #132428, #110690 ) ) ;
#79470=EDGE_CURVE ( 'NONE', #4036, #6721, #85900, .T. ) ;
#79486=CARTESIAN_POINT ( 'NONE',  ( 23.14999999999999858, 76.00000000001213607, -136.5231074845243313 ) ) ;
#79510=CARTESIAN_POINT ( 'NONE',  ( 21.05000000000000071, 77.36087058720436005, -161.9501095574333931 ) ) ;
#79518=VECTOR ( 'NONE', #170716, 1000.000000000000000 ) ;
#79522=DIRECTION ( 'NONE',  ( 1.000000000000000000, 0.000000000000000000, 0.000000000000000000 ) ) ;
#79524=DIRECTION ( 'NONE',  ( -1.000000000000000000, 1.836970198721029934E-16, 1.601412966608202925E-30 ) ) ;
#79539=VERTEX_POINT ( 'NONE', #155507 ) ;
#79566=AXIS2_PLACEMENT_3D ( 'NONE', #23409, #220306, #2509 ) ;
#79578=ORIENTED_EDGE ( 'NONE', *, *, #247778, .F. ) ;
#79585=ORIENTED_EDGE ( 'NONE', *, *, #153694, .T. ) ;
#79618=ORIENTED_EDGE ( 'NONE', *, *, #208437, .T. ) ;
#79625=CIRCLE ( 'NONE', #225376, 0.09999999999999939493 ) ;
#79629=VERTEX_POINT ( 'NONE', #57635 ) ;
#79632=VECTOR ( 'NONE', #155841, 1000.000000000000000 ) ;
#79635=DIRECTION ( 'NONE',  ( 0.000000000000000000, 6.982962677686266711E-15, -1.000000000000000000 ) ) ;
#79646=VERTEX_POINT ( 'NONE', #56347 ) ;
#79648=EDGE_CURVE ( 'NONE', #91629, #166025, #81988, .T. ) ;
#79690=DIRECTION ( 'NONE',  ( 0.000000000000000000, 0.8777080977375655291, -0.4791956752370622463 ) ) ;
#79716=VECTOR ( 'NONE', #167846, 1000.000000000000000 ) ;
#79733=DIRECTION ( 'NONE',  ( 1.000000000000000000, 0.000000000000000000, 0.000000000000000000 ) ) ;
#79804=EDGE_LOOP ( 'NONE', ( #178189, #12974, #231192, #105354, #110969, #141010, #46623, #56626, #198944, #21722, #89067 ) ) ;
#79811=CIRCLE ( 'NONE', #204711, 0.09999999999999646672 ) ;
#79830=DIRECTION ( 'NONE',  ( 1.000000000000000000, -2.952720810173289112E-16, -2.061873921506763405E-30 ) ) ;
#79862=DIRECTION ( 'NONE',  ( -1.000000000000000000, 7.304098846218164250E-16, -4.217023435051628197E-16 ) ) ;
#79896=AXIS2_PLACEMENT_3D ( 'NONE', #189272, #74490, #50998 ) ;
#79900=AXIS2_PLACEMENT_3D ( 'NONE', #210370, #151705, #171287 ) ;
#79904=ORIENTED_EDGE ( 'NONE', *, *, #231613, .T. ) ;
#79907=ORIENTED_EDGE ( 'NONE', *, *, #107210, .F. ) ;
#79912=ORIENTED_EDGE ( 'NONE', *, *, #138256, .T. ) ;
#79976=AXIS2_PLACEMENT_3D ( 'NONE', #158844, #42718, #201785 ) ;
#79989=AXIS2_PLACEMENT_3D ( 'NONE', #121906, #142721, #202706 ) ;
#79997=DIRECTION ( 'NONE',  ( 0.000000000000000000, -0.8700118002898356018, 0.4930308989875170078 ) ) ;
#80012=ORIENTED_EDGE ( 'NONE', *, *, #233630, .F. ) ;
#80058=TOROIDAL_SURFACE ( 'NONE', #92565, 4.099999999999999645, 0.1000000000000000056 ) ;
#80074=EDGE_CURVE ( 'NONE', #84708, #34506, #241143, .T. ) ;
#80098=CARTESIAN_POINT ( 'NONE',  ( 21.05000000000000071, 75.94851711813097950, -176.3232873024375920 ) ) ;
#80107=ADVANCED_FACE ( 'NONE', ( #102868 ), #39095, .T. ) ;
#80145=VECTOR ( 'NONE', #74698, 1000.000000000000000 ) ;
#80172=EDGE_LOOP ( 'NONE', ( #183797, #98919, #218443, #172175 ) ) ;
#80175=EDGE_CURVE ( 'NONE', #230504, #200038, #217208, .T. ) ;
#80222=ORIENTED_EDGE ( 'NONE', *, *, #149231, .F. ) ;
#80235=CIRCLE ( 'NONE', #146889, 0.09999999999998898659 ) ;
#80241=ORIENTED_EDGE ( 'NONE', *, *, #116402, .T. ) ;
#80243=VERTEX_POINT ( 'NONE', #153627 ) ;
#80244=DIRECTION ( 'NONE',  ( 1.000000000000000000, 0.000000000000000000, 0.000000000000000000 ) ) ;
#80287=DIRECTION ( 'NONE',  ( -1.000000000000000000, -0.000000000000000000, -0.000000000000000000 ) ) ;
#80295=ADVANCED_FACE ( 'NONE', ( #248836 ), #11513, .F. ) ;
#80299=ORIENTED_EDGE ( 'NONE', *, *, #64019, .F. ) ;
#80316=ORIENTED_EDGE ( 'NONE', *, *, #200050, .T. ) ;
#80321=VERTEX_POINT ( 'NONE', #152321 ) ;
#80322=AXIS2_PLACEMENT_3D ( 'NONE', #14405, #93906, #233449 ) ;
#80326=ORIENTED_EDGE ( 'NONE', *, *, #17210, .F. ) ;
#80338=CIRCLE ( 'NONE', #100982, 0.1000000000000033223 ) ;
#80342=CIRCLE ( 'NONE', #155428, 0.1000000000000028644 ) ;
#80418=CARTESIAN_POINT ( 'NONE',  ( 21.14999999999999858, 64.25000000001237765, -169.9231074845244507 ) ) ;
#80420=ORIENTED_EDGE ( 'NONE', *, *, #142693, .T. ) ;
#80434=LINE ( 'NONE', #177041, #182407 ) ;
#80501=DIRECTION ( 'NONE',  ( 0.000000000000000000, 1.000000000000000000, 8.717686153663073805E-15 ) ) ;
#80527=CYLINDRICAL_SURFACE ( 'NONE', #225152, 0.1000000000000070832 ) ;
#80531=ADVANCED_FACE ( 'NONE', ( #43897 ), #222505, .F. ) ;
#80534=ORIENTED_EDGE ( 'NONE', *, *, #82121, .F. ) ;
#80568=CARTESIAN_POINT ( 'NONE',  ( 20.94999999999999929, 87.48912529308822172, -139.6231074845242688 ) ) ;
#80583=ORIENTED_EDGE ( 'NONE', *, *, #105570, .T. ) ;
#80599=FACE_OUTER_BOUND ( 'NONE', #87326, .T. ) ;
#80628=ORIENTED_EDGE ( 'NONE', *, *, #62158, .T. ) ;
#80647=AXIS2_PLACEMENT_3D ( 'NONE', #14141, #93651, #255234 ) ;
#80657=( BOUNDED_SURFACE ( )  B_SPLINE_SURFACE ( 3, 2, ( 
 ( #14788, #137262, #211693 ),
 ( #194707, #236368, #250792 ),
 ( #96825, #176422, #13484 ),
 ( #255880, #175165, #231258 ),
 ( #76013, #93006, #172599 ),
 ( #72181, #135968, #232548 ),
 ( #53887, #133424, #55131 ),
 ( #212959, #12213, #94283 ),
 ( #115144, #254623, #34349 ),
 ( #173881, #74773, #134682 ) ),
 .UNSPECIFIED., .F., .F., .T. ) 
 B_SPLINE_SURFACE_WITH_KNOTS ( ( 4, 2, 2, 2, 4 ),
 ( 3, 3 ),
 ( 0.0001836757140119112878, 0.0004000170051583592156, 0.0005081876507315832067, 0.0005622729735181951479, 0.0006163582963048070892 ),
 ( 0.000000000000000000, 1.000000000000000000 ),
 .UNSPECIFIED. ) 
 GEOMETRIC_REPRESENTATION_ITEM ( )  RATIONAL_B_SPLINE_SURFACE ( (
 ( 1.000000000000000000, 0.7071067811865870967, 1.000000000000000000),
 ( 1.000000000000000000, 0.6461995200020528296, 1.000000000000000000),
 ( 1.000000000000000000, 0.5776453529561198508, 1.000000000000000000),
 ( 1.000000000000000000, 0.4585233068345995755, 1.000000000000000000),
 ( 1.000000000000000000, 0.4154092989941690628, 1.000000000000000000),
 ( 1.000000000000000000, 0.3550093145835241937, 1.000000000000000000),
 ( 1.000000000000000000, 0.3354498651686700361, 1.000000000000000000),
 ( 1.000000000000000000, 0.3060347992254511817, 1.000000000000000000),
 ( 1.000000000000000000, 0.2963555829627100846, 1.000000000000000000),
 ( 1.000000000000000000, 0.2966190024561151661, 1.000000000000000000) ) ) 
 REPRESENTATION_ITEM ( '' )  SURFACE ( )  );
#80667=DIRECTION ( 'NONE',  ( 0.000000000000000000, -7.056502275159890043E-15, 1.000000000000000000 ) ) ;
#80669=DIRECTION ( 'NONE',  ( 1.000000000000000000, 0.000000000000000000, 0.000000000000000000 ) ) ;
#80691=CIRCLE ( 'NONE', #226421, 11.80000000000000426 ) ;
#80712=LINE ( 'NONE', #40367, #184023 ) ;
#80714=CARTESIAN_POINT ( 'NONE',  ( -18.60000000000000142, 85.52395432076488646, -129.6410904276969518 ) ) ;
#80720=LINE ( 'NONE', #121190, #99488 ) ;
#80723=VERTEX_POINT ( 'NONE', #115107 ) ;
#80734=CARTESIAN_POINT ( 'NONE',  ( -23.15000000000000213, 64.35000000001228670, -157.8731074845244393 ) ) ;
#80743=ORIENTED_EDGE ( 'NONE', *, *, #151432, .T. ) ;
#80747=CARTESIAN_POINT ( 'NONE',  ( -20.85000000000000142, 68.97833521811203639, -132.6895420826271277 ) ) ;
#80752=DIRECTION ( 'NONE',  ( 0.000000000000000000, 0.8660254037844377084, 0.5000000000000015543 ) ) ;
#80763=DIRECTION ( 'NONE',  ( 0.000000000000000000, 6.982962677686266711E-15, -1.000000000000000000 ) ) ;
#80768=DIRECTION ( 'NONE',  ( 0.000000000000000000, -7.429790795770644761E-15, 1.000000000000000000 ) ) ;
#80784=DIRECTION ( 'NONE',  ( -1.000000000000000000, -0.000000000000000000, -0.000000000000000000 ) ) ;
#80804=CYLINDRICAL_SURFACE ( 'NONE', #166221, 0.09999999999999939493 ) ;
#80813=CARTESIAN_POINT ( 'NONE',  ( 18.49999999999998934, 65.70711192142385926, -131.0651054685122858 ) ) ;
#80852=AXIS2_PLACEMENT_3D ( 'NONE', #15767, #215217, #36616 ) ;
#80860=CARTESIAN_POINT ( 'NONE',  ( -21.76363531954647357, 75.90099812571297377, -177.0360440323960916 ) ) ;
#80880=AXIS2_PLACEMENT_3D ( 'NONE', #46344, #68498, #125883 ) ;
#80929=ORIENTED_EDGE ( 'NONE', *, *, #184504, .F. ) ;
#80940=DIRECTION ( 'NONE',  ( 1.000000000000000000, 0.000000000000000000, 0.000000000000000000 ) ) ;
#80942=VERTEX_POINT ( 'NONE', #28895 ) ;
#80963=AXIS2_PLACEMENT_3D ( 'NONE', #28492, #208390, #106678 ) ;
#80975=CARTESIAN_POINT ( 'NONE',  ( 20.94999999999999929, 71.00000000001223555, -148.9283735034374843 ) ) ;
#80980=DIRECTION ( 'NONE',  ( -1.000000000000000000, 0.000000000000000000, 0.000000000000000000 ) ) ;
#80986=AXIS2_PLACEMENT_3D ( 'NONE', #34122, #135734, #53646 ) ;
#81015=AXIS2_PLACEMENT_3D ( 'NONE', #91125, #111987, #191543 ) ;
#81024=DIRECTION ( 'NONE',  ( 1.000000000000000000, -0.000000000000000000, -0.000000000000000000 ) ) ;
#81031=DIRECTION ( 'NONE',  ( 2.952720810173289112E-16, 1.000000000000000000, 6.982962677686266711E-15 ) ) ;
#81054=ORIENTED_EDGE ( 'NONE', *, *, #170316, .F. ) ;
#81063=CARTESIAN_POINT ( 'NONE',  ( -20.85000000000000142, 76.00000000001213607, -136.5231074845243313 ) ) ;
#81073=VERTEX_POINT ( 'NONE', #95233 ) ;
#81075=DIRECTION ( 'NONE',  ( 0.000000000000000000, 6.982962677686267499E-15, -1.000000000000000000 ) ) ;
#81121=DIRECTION ( 'NONE',  ( -1.000000000000000000, -0.000000000000000000, -0.000000000000000000 ) ) ;
#81142=ORIENTED_EDGE ( 'NONE', *, *, #221326, .T. ) ;
#81150=AXIS2_PLACEMENT_3D ( 'NONE', #169734, #131847, #28952 ) ;
#81157=( GEOMETRIC_REPRESENTATION_CONTEXT ( 3 ) GLOBAL_UNCERTAINTY_ASSIGNED_CONTEXT ( ( #154644 ) ) GLOBAL_UNIT_ASSIGNED_CONTEXT ( ( #152890, #250651, #72044 ) ) REPRESENTATION_CONTEXT ( 'NONE', 'WORKASPACE' ) );
#81168=AXIS2_PLACEMENT_3D ( 'NONE', #87207, #226728, #10274 ) ;
#81174=CARTESIAN_POINT ( 'NONE',  ( -18.47690164073605956, 85.46484453802433734, -129.8217265446881754 ) ) ;
#81175=CARTESIAN_POINT ( 'NONE',  ( 18.39999999999999858, 85.40000000001246860, -181.7731074845243029 ) ) ;
#81195=EDGE_CURVE ( 'NONE', #103678, #123954, #153536, .T. ) ;
#81205=ORIENTED_EDGE ( 'NONE', *, *, #155746, .F. ) ;
#81215=ORIENTED_EDGE ( 'NONE', *, *, #206222, .F. ) ;
#81275=CARTESIAN_POINT ( 'NONE',  ( 18.59999999999999432, 74.83729825007431202, -161.9231074845243654 ) ) ;
#81310=CIRCLE ( 'NONE', #35415, 0.09999999999998898659 ) ;
#81317=ORIENTED_EDGE ( 'NONE', *, *, #254906, .T. ) ;
#81321=ORIENTED_EDGE ( 'NONE', *, *, #20499, .T. ) ;
#81340=ORIENTED_EDGE ( 'NONE', *, *, #97102, .F. ) ;
#81414=ADVANCED_FACE ( 'NONE', ( #131484 ), #187019, .F. ) ;
#81495=DIRECTION ( 'NONE',  ( 0.000000000000000000, -6.982962677686266711E-15, 1.000000000000000000 ) ) ;
#81499=EDGE_CURVE ( 'NONE', #99805, #244509, #241170, .T. ) ;
#81501=CARTESIAN_POINT ( 'NONE',  ( -23.25000000000000000, 76.00000000001237765, -170.0231074845243597 ) ) ;
#81531=EDGE_CURVE ( 'NONE', #89486, #15940, #53707, .T. ) ;
#81558=CARTESIAN_POINT ( 'NONE',  ( 23.24999999999999289, 64.35000000001245724, -181.7731074845244450 ) ) ;
#81561=VERTEX_POINT ( 'NONE', #160057 ) ;
#81571=CARTESIAN_POINT ( 'NONE',  ( 21.05000000000000071, 84.66355140188136374, -146.0472086025916099 ) ) ;
#81594=DIRECTION ( 'NONE',  ( 0.000000000000000000, 0.000000000000000000, 1.000000000000000000 ) ) ;
#81603=CARTESIAN_POINT ( 'NONE',  ( -20.94999999999999929, 87.75000000001236344, -166.9231074845242802 ) ) ;
#81617=EDGE_LOOP ( 'NONE', ( #179112, #125545, #110806, #10406 ) ) ;
#81629=AXIS2_PLACEMENT_3D ( 'NONE', #5332, #84858, #243968 ) ;
#81655=EDGE_LOOP ( 'NONE', ( #243943, #5910, #160348, #68653 ) ) ;
#81668=ORIENTED_EDGE ( 'NONE', *, *, #147242, .T. ) ;
#81674=AXIS2_PLACEMENT_3D ( 'NONE', #84239, #47722, #105105 ) ;
#81685=DIRECTION ( 'NONE',  ( 4.504528286903032433E-15, 0.1298341882520054891, 0.9915357197604850459 ) ) ;
#81749=DIRECTION ( 'NONE',  ( 0.000000000000000000, -7.116814260417660624E-15, 1.000000000000000000 ) ) ;
#81762=DIRECTION ( 'NONE',  ( 0.000000000000000000, -1.000000000000000000, -6.982962677686267499E-15 ) ) ;
#81773=LINE ( 'NONE', #160088, #185908 ) ;
#81797=AXIS2_PLACEMENT_3D ( 'NONE', #128819, #188776, #20432 ) ;
#81800=FACE_OUTER_BOUND ( 'NONE', #191061, .T. ) ;
#81808=CYLINDRICAL_SURFACE ( 'NONE', #54861, 0.1000000000000038219 ) ;
#81825=CARTESIAN_POINT ( 'NONE',  ( 18.33683296300455012, 85.51114997114484595, -129.6174000718142736 ) ) ;
#81863=DIRECTION ( 'NONE',  ( -0.000000000000000000, 6.982962677686266711E-15, -1.000000000000000000 ) ) ;
#81915=DIRECTION ( 'NONE',  ( -2.252264143451594314E-15, 0.1298341882520054891, 0.9915357197604850459 ) ) ;
#81934=DIRECTION ( 'NONE',  ( 1.000000000000000000, 0.000000000000000000, 0.000000000000000000 ) ) ;
#81943=ORIENTED_EDGE ( 'NONE', *, *, #56019, .F. ) ;
#81988=CIRCLE ( 'NONE', #40374, 0.09999999999998898659 ) ;
#82028=ADVANCED_FACE ( 'NONE', ( #38484 ), #254892, .F. ) ;
#82039=CARTESIAN_POINT ( 'NONE',  ( -21.05000000000000071, 87.48912529308822172, -139.5231074845243029 ) ) ;
#82053=CARTESIAN_POINT ( 'NONE',  ( -20.94999999999999929, 87.75000000001236344, -167.1231074845242688 ) ) ;
#82060=EDGE_CURVE ( 'NONE', #101850, #20227, #143986, .T. ) ;
#82077=ORIENTED_EDGE ( 'NONE', *, *, #225997, .T. ) ;
#82085=CARTESIAN_POINT ( 'NONE',  ( 20.94999999999999929, 69.35000000001222986, -148.7731074845244166 ) ) ;
#82106=DIRECTION ( 'NONE',  ( 1.000000000000000000, -7.304098846218134667E-16, -5.100424963727256530E-30 ) ) ;
#82117=CARTESIAN_POINT ( 'NONE',  ( 23.14999999999999858, 76.00000000001213607, -136.5231074845243313 ) ) ;
#82120=AXIS2_PLACEMENT_3D ( 'NONE', #137704, #56868, #140270 ) ;
#82121=EDGE_CURVE ( 'NONE', #206325, #18470, #166352, .T. ) ;
#82128=TOROIDAL_SURFACE ( 'NONE', #107100, 0.2000000000000000111, 0.1000000000000000056 ) ;
#82136=DIRECTION ( 'NONE',  ( 0.000000000000000000, 6.982962677686266711E-15, -1.000000000000000000 ) ) ;
#82137=EDGE_LOOP ( 'NONE', ( #215344, #112743, #221488, #204243, #10000 ) ) ;
#82138=DIRECTION ( 'NONE',  ( 0.000000000000000000, 1.000000000000000000, 6.982962677686266711E-15 ) ) ;
#82160=CYLINDRICAL_SURFACE ( 'NONE', #168729, 0.1000000000000106914 ) ;
#82163=CARTESIAN_POINT ( 'NONE',  ( -18.59999999999999787, 68.97833521811203639, -132.6895420826271277 ) ) ;
#82207=EDGE_LOOP ( 'NONE', ( #170942, #176637, #181846 ) ) ;
#82215=ORIENTED_EDGE ( 'NONE', *, *, #123934, .T. ) ;
#82217=CIRCLE ( 'NONE', #115566, 0.1000000000000046685 ) ;
#82248=CARTESIAN_POINT ( 'NONE',  ( -23.25000000000000000, 64.35000000001245724, -181.7731074845244450 ) ) ;
#82269=DIRECTION ( 'NONE',  ( 0.000000000000000000, -1.000000000000000000, 0.000000000000000000 ) ) ;
#82323=LINE ( 'NONE', #217986, #200604 ) ;
#82325=CARTESIAN_POINT ( 'NONE',  ( 20.41140022480505323, 65.58956915761068274, -162.4081061808921902 ) ) ;
#82334=ADVANCED_FACE ( 'NONE', ( #91737, #90434 ), #108729, .F. ) ;
#82373=ORIENTED_EDGE ( 'NONE', *, *, #24691, .F. ) ;
#82407=DIRECTION ( 'NONE',  ( -0.000000000000000000, -0.01283462868040327436, 0.9999176327611370985 ) ) ;
#82438=DIRECTION ( 'NONE',  ( 1.000000000000000000, 0.000000000000000000, 0.000000000000000000 ) ) ;
#82455=CARTESIAN_POINT ( 'NONE',  ( 21.08804582317328169, 67.12183383292037320, -157.6731076551165245 ) ) ;
#82470=CIRCLE ( 'NONE', #3377, 6.258578643762724880 ) ;
#82491=ORIENTED_EDGE ( 'NONE', *, *, #231279, .F. ) ;
#82510=CARTESIAN_POINT ( 'NONE',  ( -18.54148534481894117, 65.67467670974440352, -130.9531731826884879 ) ) ;
#82525=VERTEX_POINT ( 'NONE', #26331 ) ;
#82530=ORIENTED_EDGE ( 'NONE', *, *, #52719, .T. ) ;
#82548=CARTESIAN_POINT ( 'NONE',  ( 20.04142135623730070, 64.35000000001222986, -148.6731074845244507 ) ) ;
#82585=LINE ( 'NONE', #65621, #61608 ) ;
#82589=CARTESIAN_POINT ( 'NONE',  ( -20.94999999999999929, 64.25000000001233502, -163.0083017138704236 ) ) ;
#82671=CARTESIAN_POINT ( 'NONE',  ( 21.05000000000000071, 75.96798630682472719, -176.2819502080616871 ) ) ;
#82686=DIRECTION ( 'NONE',  ( 1.000000000000000000, 0.000000000000000000, 0.000000000000000000 ) ) ;
#82689=DIRECTION ( 'NONE',  ( 0.000000000000000000, -1.000000000000000000, -6.860497997771532351E-15 ) ) ;
#82708=DIRECTION ( 'NONE',  ( -4.408576920032448588E-17, -0.1350103645451807832, -0.9908441862701610203 ) ) ;
#82735=ORIENTED_EDGE ( 'NONE', *, *, #126226, .F. ) ;
#82746=LINE ( 'NONE', #162346, #248837 ) ;
#82752=ORIENTED_EDGE ( 'NONE', *, *, #217362, .T. ) ;
#82769=CARTESIAN_POINT ( 'NONE',  ( 21.93340585898254247, 76.00000000001243450, -177.3472545066566681 ) ) ;
#82781=CIRCLE ( 'NONE', #45418, 0.09999999999999939493 ) ;
#82803=ORIENTED_EDGE ( 'NONE', *, *, #141988, .F. ) ;
#82819=ORIENTED_EDGE ( 'NONE', *, *, #34800, .F. ) ;
#82829=EDGE_CURVE ( 'NONE', #141897, #110495, #26987, .T. ) ;
#82837=CIRCLE ( 'NONE', #166124, 11.89999999999999325 ) ;
#82863=CARTESIAN_POINT ( 'NONE',  ( 20.86777300164945004, 65.66799936921553638, -130.9299399888601272 ) ) ;
#82885=DIRECTION ( 'NONE',  ( 1.000000000000000000, 0.000000000000000000, 0.000000000000000000 ) ) ;
#82888=CARTESIAN_POINT ( 'NONE',  ( -22.39999999999999858, 76.00000000001237765, -170.1231074845243540 ) ) ;
#82898=CARTESIAN_POINT ( 'NONE',  ( 20.95512820512820440, 65.37615131630040821, -157.8731074845244393 ) ) ;
#82913=ADVANCED_FACE ( 'NONE', ( #227713 ), #24422, .T. ) ;
#82914=AXIS2_PLACEMENT_3D ( 'NONE', #102724, #181025, #41524 ) ;
#82943=DIRECTION ( 'NONE',  ( 0.000000000000000000, 6.982962677686267499E-15, -1.000000000000000000 ) ) ;
#82960=AXIS2_PLACEMENT_3D ( 'NONE', #133672, #248490, #90686 ) ;
#82967=CARTESIAN_POINT ( 'NONE',  ( -20.94999999999999929, 64.40000000001234071, -163.0949042542488883 ) ) ;
#82992=ORIENTED_EDGE ( 'NONE', *, *, #201617, .F. ) ;
#83003=ORIENTED_EDGE ( 'NONE', *, *, #129127, .T. ) ;
#83028=ORIENTED_EDGE ( 'NONE', *, *, #38334, .F. ) ;
#83062=CYLINDRICAL_SURFACE ( 'NONE', #144076, 0.09999999999998898659 ) ;
#83066=ORIENTED_EDGE ( 'NONE', *, *, #98787, .T. ) ;
#83107=DIRECTION ( 'NONE',  ( 0.000000000000000000, 0.000000000000000000, -1.000000000000000000 ) ) ;
#83110=DIRECTION ( 'NONE',  ( 0.000000000000000000, -7.272083257015735086E-15, 1.000000000000000000 ) ) ;
#83117=DIRECTION ( 'NONE',  ( 0.000000000000000000, 0.9908441862701791170, -0.1350103645450472789 ) ) ;
#83133=CARTESIAN_POINT ( 'NONE',  ( 20.94999999999999574, 87.48912529308842068, -167.1231074845242688 ) ) ;
#83194=ADVANCED_FACE ( 'NONE', ( #136297 ), #215842, .F. ) ;
#83203=CARTESIAN_POINT ( 'NONE',  ( 18.49999999999999289, 65.79142135624951493, -145.2559501969990379 ) ) ;
#83226=CIRCLE ( 'NONE', #112312, 2.000000000000001776 ) ;
#83228=CARTESIAN_POINT ( 'NONE',  ( 23.24999999999999289, 64.35000000001237197, -170.0231074845244166 ) ) ;
#83231=ORIENTED_EDGE ( 'NONE', *, *, #239697, .T. ) ;
#83247=DIRECTION ( 'NONE',  ( 0.000000000000000000, -0.9915357197604982575, 0.1298341882519033486 ) ) ;
#83249=CARTESIAN_POINT ( 'NONE',  ( 20.94999999999999574, 87.48912529308842068, -166.9231074845242802 ) ) ;
#83258=CIRCLE ( 'NONE', #245605, 0.1999999999999987899 ) ;
#83283=VECTOR ( 'NONE', #103847, 1000.000000000000000 ) ;
#83299=CARTESIAN_POINT ( 'NONE',  ( 22.47110162079220785, 75.97120258720977404, -181.6730434212086891 ) ) ;
#83321=EDGE_CURVE ( 'NONE', #91629, #141665, #162793, .T. ) ;
#83333=AXIS2_PLACEMENT_3D ( 'NONE', #127646, #89782, #247587 ) ;
#83347=AXIS2_PLACEMENT_3D ( 'NONE', #170601, #68897, #169305 ) ;
#83376=DIRECTION ( 'NONE',  ( 0.000000000000000000, -0.1298341882519953583, -0.9915357197604861561 ) ) ;
#83385=DIRECTION ( 'NONE',  ( 0.000000000000000000, 0.000000000000000000, 1.000000000000000000 ) ) ;
#83388=EDGE_LOOP ( 'NONE', ( #135275, #15419, #153833 ) ) ;
#83401=DIRECTION ( 'NONE',  ( 0.000000000000000000, -0.4999999999999088507, -0.8660254037844913322 ) ) ;
#83404=ADVANCED_FACE ( 'NONE', ( #52632 ), #133466, .F. ) ;
#83459=TOROIDAL_SURFACE ( 'NONE', #137630, 0.2000000000000000111, 0.1000000000000000056 ) ;
#83464=CARTESIAN_POINT ( 'NONE',  ( -23.15000000000000213, 71.65000000001228386, -157.7731074845243882 ) ) ;
#83487=CIRCLE ( 'NONE', #17101, 0.09999999999999938105 ) ;
#83527=CARTESIAN_POINT ( 'NONE',  ( 19.97071067695833690, 64.27928932305385956, -145.3468540517209249 ) ) ;
#83554=CARTESIAN_POINT ( 'NONE',  ( 21.04999999999999716, 67.12872031401667527, -161.4644784893834810 ) ) ;
#83557=DIRECTION ( 'NONE',  ( -1.000000000000000000, 2.952720810173289112E-16, 2.061873921506763405E-30 ) ) ;
#83561=DIRECTION ( 'NONE',  ( 0.000000000000000000, -0.4999999999999088507, 0.8660254037844913322 ) ) ;
#83566=DIRECTION ( 'NONE',  ( 0.000000000000000000, 0.000000000000000000, 1.000000000000000000 ) ) ;
#83622=CIRCLE ( 'NONE', #8653, 0.5999999999999894307 ) ;
#83623=CARTESIAN_POINT ( 'NONE',  ( -20.94999999999999929, 77.16412189325330928, -128.6082593989527254 ) ) ;
#83636=CARTESIAN_POINT ( 'NONE',  ( -21.29999999999995808, 76.00000000001237765, -170.0231074845243597 ) ) ;
#83637=LINE ( 'NONE', #203626, #132582 ) ;
#83653=EDGE_CURVE ( 'NONE', #208166, #56768, #137424, .T. ) ;
#83669=AXIS2_PLACEMENT_3D ( 'NONE', #5480, #22527, #60335 ) ;
#83694=CIRCLE ( 'NONE', #250156, 7.791421356237310469 ) ;
#83731=FACE_OUTER_BOUND ( 'NONE', #180631, .T. ) ;
#83749=ORIENTED_EDGE ( 'NONE', *, *, #250783, .T. ) ;
#83769=ORIENTED_EDGE ( 'NONE', *, *, #145704, .T. ) ;
#83770=AXIS2_PLACEMENT_3D ( 'NONE', #241982, #42493, #63332 ) ;
#83775=DIRECTION ( 'NONE',  ( 7.304098846218134667E-16, 1.000000000000000000, 6.982962677686267499E-15 ) ) ;
#83806=AXIS2_PLACEMENT_3D ( 'NONE', #169010, #112845, #33349 ) ;
#83811=EDGE_LOOP ( 'NONE', ( #50708, #79585, #85714, #104605, #85388 ) ) ;
#83838=ORIENTED_EDGE ( 'NONE', *, *, #2752, .T. ) ;
#83846=AXIS2_PLACEMENT_3D ( 'NONE', #25274, #23996, #78785 ) ;
#83914=ORIENTED_EDGE ( 'NONE', *, *, #123623, .T. ) ;
#83939=EDGE_CURVE ( 'NONE', #90874, #200975, #91841, .T. ) ;
#83983=AXIS2_PLACEMENT_3D ( 'NONE', #13805, #93333, #172927 ) ;
#83995=CARTESIAN_POINT ( 'NONE',  ( -20.64999999999999858, 85.40000000001221281, -146.4170766071767389 ) ) ;
#84024=CIRCLE ( 'NONE', #34048, 0.09999999999998898659 ) ;
#84037=DIRECTION ( 'NONE',  ( 1.000000000000000000, 0.000000000000000000, 0.000000000000000000 ) ) ;
#84039=ORIENTED_EDGE ( 'NONE', *, *, #34128, .F. ) ;
#84042=CIRCLE ( 'NONE', #866, 0.1000000000000070832 ) ;
#84045=CARTESIAN_POINT ( 'NONE',  ( 20.94999999999999929, 77.83534155023671985, -158.4679561919613491 ) ) ;
#84051=ORIENTED_EDGE ( 'NONE', *, *, #192530, .F. ) ;
#84063=AXIS2_PLACEMENT_3D ( 'NONE', #251337, #110549, #90988 ) ;
#84069=CARTESIAN_POINT ( 'NONE',  ( -23.25000000000000000, 64.25000000001219291, -143.5379132551784096 ) ) ;
#84111=CARTESIAN_POINT ( 'NONE',  ( -18.59999999999999787, 64.35000000001247145, -181.7731074845244450 ) ) ;
#84130=CARTESIAN_POINT ( 'NONE',  ( 20.87600722750343252, 65.66887361445355964, -130.9329845918269370 ) ) ;
#84158=CARTESIAN_POINT ( 'NONE',  ( 20.97224591636398472, 65.37484658384866520, -157.7731815798608466 ) ) ;
#84164=CARTESIAN_POINT ( 'NONE',  ( 18.59999999999999076, 76.00000000001213607, -136.5231074845243313 ) ) ;
#84203=AXIS2_PLACEMENT_3D ( 'NONE', #59896, #118635, #78187 ) ;
#84214=AXIS2_PLACEMENT_3D ( 'NONE', #240763, #101193, #125921 ) ;
#84232=CARTESIAN_POINT ( 'NONE',  ( 18.50000000000000000, 85.50000000001244871, -181.7731074845243029 ) ) ;
#84239=CARTESIAN_POINT ( 'NONE',  ( 18.59999999999999076, 69.35000000001222986, -148.6731074845243938 ) ) ;
#84246=ORIENTED_EDGE ( 'NONE', *, *, #170074, .F. ) ;
#84266=EDGE_LOOP ( 'NONE', ( #223154, #199899, #150961, #130763 ) ) ;
#84277=LINE ( 'NONE', #64767, #156546 ) ;
#84290=DIRECTION ( 'NONE',  ( 0.000000000000000000, -0.1350103645451557199, -0.9908441862701644620 ) ) ;
#84333=DIRECTION ( 'NONE',  ( 1.000000000000000000, 0.000000000000000000, 0.000000000000000000 ) ) ;
#84338=DIRECTION ( 'NONE',  ( 0.000000000000000000, -1.000000000000000000, 0.000000000000000000 ) ) ;
#84362=ORIENTED_EDGE ( 'NONE', *, *, #76829, .F. ) ;
#84364=DIRECTION ( 'NONE',  ( 0.000000000000000000, 0.000000000000000000, 1.000000000000000000 ) ) ;
#84365=ORIENTED_EDGE ( 'NONE', *, *, #93076, .F. ) ;
#84484=DIRECTION ( 'NONE',  ( 1.000000000000000000, 0.000000000000000000, 0.000000000000000000 ) ) ;
#84539=AXIS2_PLACEMENT_3D ( 'NONE', #188906, #208490, #50651 ) ;
#84549=EDGE_LOOP ( 'NONE', ( #6913, #114779, #225236, #198748, #201467 ) ) ;
#84557=VECTOR ( 'NONE', #61576, 1000.000000000000000 ) ;
#84562=CARTESIAN_POINT ( 'NONE',  ( 22.49066049874202022, 75.94365674848023673, -181.6731197220414629 ) ) ;
#84596=CARTESIAN_POINT ( 'NONE',  ( 20.94999999999999929, 70.15000000001235492, -159.8906102602464330 ) ) ;
#84608=CARTESIAN_POINT ( 'NONE',  ( -23.25000000000000000, 87.48912529308822172, -139.6231074845242688 ) ) ;
#84618=EDGE_CURVE ( 'NONE', #994, #159949, #187395, .T. ) ;
#84627=EDGE_CURVE ( 'NONE', #58091, #70573, #208752, .T. ) ;
#84650=EDGE_CURVE ( 'NONE', #182460, #90874, #62863, .T. ) ;
#84657=EDGE_LOOP ( 'NONE', ( #230503, #126562, #201477, #251312 ) ) ;
#84708=VERTEX_POINT ( 'NONE', #235175 ) ;
#84721=CARTESIAN_POINT ( 'NONE',  ( -22.49231231312463208, 64.35001509633508476, -170.0841603721258082 ) ) ;
#84726=VECTOR ( 'NONE', #39242, 1000.000000000000000 ) ;
#84727=CIRCLE ( 'NONE', #209676, 0.09999999999998898659 ) ;
#84728=EDGE_CURVE ( 'NONE', #255891, #191184, #136038, .T. ) ;
#84761=DIRECTION ( 'NONE',  ( -1.000000000000000000, 0.000000000000000000, -0.000000000000000000 ) ) ;
#84763=EDGE_LOOP ( 'NONE', ( #47294, #103611, #6869, #44833 ) ) ;
#84778=EDGE_LOOP ( 'NONE', ( #143473, #12998, #70140 ) ) ;
#84790=ORIENTED_EDGE ( 'NONE', *, *, #188098, .F. ) ;
#84795=ORIENTED_EDGE ( 'NONE', *, *, #224177, .F. ) ;
#84798=EDGE_CURVE ( 'NONE', #88042, #176438, #104608, .T. ) ;
#84809=CARTESIAN_POINT ( 'NONE',  ( 19.81427058490525894, 64.33143601963044489, -145.2731074845244166 ) ) ;
#84817=ADVANCED_FACE ( 'NONE', ( #246713 ), #52355, .F. ) ;
#84842=ORIENTED_EDGE ( 'NONE', *, *, #68477, .F. ) ;
#84858=DIRECTION ( 'NONE',  ( 0.000000000000000000, 6.982962677686266711E-15, -1.000000000000000000 ) ) ;
#84867=EDGE_CURVE ( 'NONE', #5985, #11624, #111065, .T. ) ;
#84881=ORIENTED_EDGE ( 'NONE', *, *, #158617, .T. ) ;
#84896=DIRECTION ( 'NONE',  ( 0.000000000000000000, -1.000000000000000000, -7.272083257015735086E-15 ) ) ;
#84927=VERTEX_POINT ( 'NONE', #208881 ) ;
#84980=ORIENTED_EDGE ( 'NONE', *, *, #25759, .T. ) ;
#85009=CARTESIAN_POINT ( 'NONE',  ( -21.04999999999954241, 69.55922910635037226, -170.0055102975150021 ) ) ;
#85017=ADVANCED_FACE ( 'NONE', ( #27272 ), #169354, .T. ) ;
#85021=EDGE_CURVE ( 'NONE', #91225, #9710, #24696, .T. ) ;
#85082=AXIS2_PLACEMENT_3D ( 'NONE', #74078, #76602, #139108 ) ;
#85088=ORIENTED_EDGE ( 'NONE', *, *, #213514, .F. ) ;
#85089=DIRECTION ( 'NONE',  ( 1.000000000000000000, 0.000000000000000000, 0.000000000000000000 ) ) ;
#85103=EDGE_LOOP ( 'NONE', ( #55722, #59618, #202928, #168770 ) ) ;
#85104=ADVANCED_FACE ( 'NONE', ( #36244 ), #15389, .T. ) ;
#85108=DIRECTION ( 'NONE',  ( 0.000000000000000000, -1.000000000000000000, -6.982962677686265922E-15 ) ) ;
#85113=DIRECTION ( 'NONE',  ( 0.000000000000000000, -1.000000000000000000, -6.982962677686265922E-15 ) ) ;
#85130=VERTEX_POINT ( 'NONE', #16674 ) ;
#85142=CARTESIAN_POINT ( 'NONE',  ( 20.94999999999999929, 69.45000000001229523, -157.7731074845244166 ) ) ;
#85153=DIRECTION ( 'NONE',  ( 0.000000000000000000, 0.7397360091702792628, -0.6728971962616790981 ) ) ;
#85217=CIRCLE ( 'NONE', #197672, 4.300000000000025580 ) ;
#85225=CARTESIAN_POINT ( 'NONE',  ( 20.94999999999999574, 65.37642973952952730, -162.5311622812938879 ) ) ;
#85226=ORIENTED_EDGE ( 'NONE', *, *, #235456, .F. ) ;
#85233=DIRECTION ( 'NONE',  ( 1.000000000000000000, 0.000000000000000000, 0.000000000000000000 ) ) ;
#85245=TOROIDAL_SURFACE ( 'NONE', #163831, 0.2000000000000000111, 0.1000000000000000056 ) ;
#85259=CIRCLE ( 'NONE', #131084, 0.09999999999998898659 ) ;
#85263=ADVANCED_FACE ( 'NONE', ( #256482 ), #114915, .T. ) ;
#85277=DIRECTION ( 'NONE',  ( -0.000000000000000000, 0.1298341882520009927, 0.9915357197604854900 ) ) ;
#85280=CARTESIAN_POINT ( 'NONE',  ( -23.15000000000000213, 87.48912529308822172, -139.6231074845242688 ) ) ;
#85299=ORIENTED_EDGE ( 'NONE', *, *, #177498, .F. ) ;
#85307=TOROIDAL_SURFACE ( 'NONE', #205959, 0.2000000000000000111, 0.1000000000000000056 ) ;
#85323=DIRECTION ( 'NONE',  ( 0.000000000000000000, 0.4999999999999088507, -0.8660254037844913322 ) ) ;
#85373=DIRECTION ( 'NONE',  ( 1.000000000000000000, 0.000000000000000000, 0.000000000000000000 ) ) ;
#85387=CARTESIAN_POINT ( 'NONE',  ( 23.14999999999999858, 87.75000000001246292, -181.7731074845242745 ) ) ;
#85388=ORIENTED_EDGE ( 'NONE', *, *, #186854, .F. ) ;
#85419=CIRCLE ( 'NONE', #102174, 11.69999999999998863 ) ;
#85426=EDGE_CURVE ( 'NONE', #151457, #7914, #138335, .T. ) ;
#85442=ORIENTED_EDGE ( 'NONE', *, *, #122153, .T. ) ;
#85443=AXIS2_PLACEMENT_3D ( 'NONE', #100770, #142497, #216901 ) ;
#85534=ADVANCED_FACE ( 'NONE', ( #130007 ), #80058, .F. ) ;
#85539=ORIENTED_EDGE ( 'NONE', *, *, #92786, .F. ) ;
#85581=DIRECTION ( 'NONE',  ( 0.000000000000000000, 3.469446951953514729E-13, -1.000000000000000000 ) ) ;
#85589=CARTESIAN_POINT ( 'NONE',  ( 18.49505816908824229, 85.43787255322325791, -129.7454502828534260 ) ) ;
#85591=EDGE_LOOP ( 'NONE', ( #142621, #56189, #72702, #109811 ) ) ;
#85594=DIRECTION ( 'NONE',  ( 1.000000000000000000, 0.000000000000000000, 0.000000000000000000 ) ) ;
#85599=EDGE_CURVE ( 'NONE', #168004, #111850, #179897, .T. ) ;
#85638=EDGE_CURVE ( 'NONE', #176438, #205324, #188250, .T. ) ;
#85660=ORIENTED_EDGE ( 'NONE', *, *, #57942, .F. ) ;
#85662=ORIENTED_EDGE ( 'NONE', *, *, #175107, .T. ) ;
#85666=ADVANCED_FACE ( 'NONE', ( #176882 ), #157324, .T. ) ;
#85675=DIRECTION ( 'NONE',  ( 0.000000000000000000, 6.982962677686267499E-15, -1.000000000000000000 ) ) ;
#85693=ORIENTED_EDGE ( 'NONE', *, *, #133513, .F. ) ;
#85696=ADVANCED_FACE ( 'NONE', ( #122022 ), #21658, .F. ) ;
#85704=AXIS2_PLACEMENT_3D ( 'NONE', #210427, #111314, #190879 ) ;
#85709=ORIENTED_EDGE ( 'NONE', *, *, #153925, .F. ) ;
#85714=ORIENTED_EDGE ( 'NONE', *, *, #110891, .F. ) ;
#85718=AXIS2_PLACEMENT_3D ( 'NONE', #235954, #58591, #75633 ) ;
#85721=DIRECTION ( 'NONE',  ( 0.000000000000000000, -7.272083257015735086E-15, 1.000000000000000000 ) ) ;
#85741=ORIENTED_EDGE ( 'NONE', *, *, #255942, .F. ) ;
#85758=ORIENTED_EDGE ( 'NONE', *, *, #145611, .F. ) ;
#85767=ORIENTED_EDGE ( 'NONE', *, *, #189882, .T. ) ;
#85792=EDGE_LOOP ( 'NONE', ( #144205, #61521, #89837, #197215 ) ) ;
#85839=CARTESIAN_POINT ( 'NONE',  ( -18.59999999999999787, 64.35000000001247145, -181.7731074845244450 ) ) ;
#85842=CARTESIAN_POINT ( 'NONE',  ( -20.54999999999999716, 68.85000000001228670, -157.6731074845243938 ) ) ;
#85857=DIRECTION ( 'NONE',  ( -1.000000000000000000, 2.952720810173289112E-16, 2.061873921506763405E-30 ) ) ;
#85863=CARTESIAN_POINT ( 'NONE',  ( -21.07946286933445279, 69.67096268100465295, -170.0997913277808209 ) ) ;
#85864=CARTESIAN_POINT ( 'NONE',  ( 22.44352723754029810, 75.99072290496917503, -181.6728288298730547 ) ) ;
#85896=ADVANCED_FACE ( 'NONE', ( #171460 ), #34504, .T. ) ;
#85900=CIRCLE ( 'NONE', #160959, 0.09999999999999939493 ) ;
#85922=ADVANCED_FACE ( 'NONE', ( #154461 ), #196393, .T. ) ;
#85934=ADVANCED_FACE ( 'NONE', ( #90584 ), #55284, .T. ) ;
#85951=DIRECTION ( 'NONE',  ( 0.000000000000000000, 0.000000000000000000, -1.000000000000000000 ) ) ;
#85953=EDGE_CURVE ( 'NONE', #164268, #183531, #1159, .T. ) ;
#86021=VERTEX_POINT ( 'NONE', #230104 ) ;
#86034=AXIS2_PLACEMENT_3D ( 'NONE', #203754, #246718, #86337 ) ;
#86043=ADVANCED_FACE ( 'NONE', ( #136110 ), #40928, .T. ) ;
#86101=FACE_OUTER_BOUND ( 'NONE', #107098, .T. ) ;
#86112=EDGE_CURVE ( 'NONE', #133329, #23498, #80235, .T. ) ;
#86119=CARTESIAN_POINT ( 'NONE',  ( -21.05000000000000071, 76.00000000001234923, -165.7231074845244052 ) ) ;
#86120=VERTEX_POINT ( 'NONE', #177861 ) ;
#86166=DIRECTION ( 'NONE',  ( 1.734723475976817507E-14, -6.982962677686266711E-15, 1.000000000000000000 ) ) ;
#86182=CIRCLE ( 'NONE', #69665, 0.09999999999999939493 ) ;
#86183=VERTEX_POINT ( 'NONE', #23930 ) ;
#86189=ORIENTED_EDGE ( 'NONE', *, *, #246957, .T. ) ;
#86198=DIRECTION ( 'NONE',  ( 0.000000000000000000, 0.000000000000000000, 1.000000000000000000 ) ) ;
#86208=ADVANCED_FACE ( 'NONE', ( #63016 ), #203815, .T. ) ;
#86214=DIRECTION ( 'NONE',  ( -1.000000000000000000, 0.000000000000000000, 0.000000000000000000 ) ) ;
#86242=CARTESIAN_POINT ( 'NONE',  ( -18.39999999999999858, 85.60000000001211617, -129.9229180933022576 ) ) ;
#86262=DIRECTION ( 'NONE',  ( 0.000000000000000000, -6.982962677686266711E-15, 1.000000000000000000 ) ) ;
#86263=CARTESIAN_POINT ( 'NONE',  ( -22.39999999999999858, 68.20922040163897293, -170.1231074845244109 ) ) ;
#86281=EDGE_LOOP ( 'NONE', ( #106151, #13261 ) ) ;
#86301=EDGE_LOOP ( 'NONE', ( #85442, #249332, #22361, #202841 ) ) ;
#86337=DIRECTION ( 'NONE',  ( 0.000000000000000000, -6.454785026890489601E-15, 1.000000000000000000 ) ) ;
#86389=CARTESIAN_POINT ( 'NONE',  ( -23.15000000000000213, 64.25000000001217870, -139.6231074845244393 ) ) ;
#86402=CYLINDRICAL_SURFACE ( 'NONE', #253518, 4.000000000000003553 ) ;
#86408=DIRECTION ( 'NONE',  ( 1.000000000000000000, 0.000000000000000000, 0.000000000000000000 ) ) ;
#86426=CARTESIAN_POINT ( 'NONE',  ( 21.05000000000000071, 76.00000000001213607, -136.5231074845243313 ) ) ;
#86463=EDGE_CURVE ( 'NONE', #997, #244808, #176175, .T. ) ;
#86513=LINE ( 'NONE', #85225, #37948 ) ;
#86567=CARTESIAN_POINT ( 'NONE',  ( -23.25000000000000000, 77.83585931145570669, -125.0186683157258329 ) ) ;
#86572=CARTESIAN_POINT ( 'NONE',  ( 18.59999999999999432, 74.83729825007431202, -162.0231074845243597 ) ) ;
#86592=AXIS2_PLACEMENT_3D ( 'NONE', #40041, #223763, #182095 ) ;
#86600=ORIENTED_EDGE ( 'NONE', *, *, #109601, .F. ) ;
#86638=ORIENTED_EDGE ( 'NONE', *, *, #245943, .F. ) ;
#86645=ORIENTED_EDGE ( 'NONE', *, *, #196107, .T. ) ;
#86719=AXIS2_PLACEMENT_3D ( 'NONE', #91593, #74640, #250646 ) ;
#86728=CARTESIAN_POINT ( 'NONE',  ( -21.05000000000000071, 64.40000000001219860, -143.4513107147999449 ) ) ;
#86805=DIRECTION ( 'NONE',  ( 0.000000000000000000, -6.853228547068871147E-15, 1.000000000000000000 ) ) ;
#86837=FACE_OUTER_BOUND ( 'NONE', #123631, .T. ) ;
#86853=CARTESIAN_POINT ( 'NONE',  ( -18.59999999999999787, 77.26327546522934142, -128.6212428177779543 ) ) ;
#86873=DIRECTION ( 'NONE',  ( 0.000000000000000000, -5.551115123125777653E-14, 1.000000000000000000 ) ) ;
#86886=VERTEX_POINT ( 'NONE', #161200 ) ;
#86890=EDGE_LOOP ( 'NONE', ( #237165, #94800, #44100, #86638 ) ) ;
#86891=DIRECTION ( 'NONE',  ( 1.000000000000000000, 0.000000000000000000, 0.000000000000000000 ) ) ;
#86921=CARTESIAN_POINT ( 'NONE',  ( 23.14999999999999147, 76.00000000001237765, -170.0231074845243597 ) ) ;
#86937=CARTESIAN_POINT ( 'NONE',  ( -21.05000000000000071, 70.10000000001235776, -159.8040077198679683 ) ) ;
#86938=EDGE_LOOP ( 'NONE', ( #173091, #200245, #108424, #117501 ) ) ;
#86942=DIRECTION ( 'NONE',  ( 0.000000000000000000, 1.000000000000000000, 1.387778780781444413E-14 ) ) ;
#86946=CARTESIAN_POINT ( 'NONE',  ( -20.64999999999999858, 68.85000000001228670, -157.7731074845244166 ) ) ;
#86968=EDGE_CURVE ( 'NONE', #80243, #90604, #151598, .T. ) ;
#86996=AXIS2_PLACEMENT_3D ( 'NONE', #167286, #168592, #188105 ) ;
#87036=EDGE_CURVE ( 'NONE', #256686, #229236, #39164, .T. ) ;
#87099=AXIS2_PLACEMENT_3D ( 'NONE', #87191, #166787, #246295 ) ;
#87108=DIRECTION ( 'NONE',  ( 1.000000000000000000, 0.000000000000000000, 0.000000000000000000 ) ) ;
#87113=DIRECTION ( 'NONE',  ( -0.000000000000000000, -0.6132151058540604716, 0.7899159663865477077 ) ) ;
#87126=CARTESIAN_POINT ( 'NONE',  ( -20.94999999999999929, 68.87972903831452243, -132.8635444426850825 ) ) ;
#87137=DIRECTION ( 'NONE',  ( 0.000000000000000000, -7.304098846218085561E-15, 1.000000000000000000 ) ) ;
#87139=DIRECTION ( 'NONE',  ( 2.827886303505249259E-16, 0.8660254037844377084, 0.5000000000000016653 ) ) ;
#87149=EDGE_LOOP ( 'NONE', ( #117793, #22849, #244485, #244556 ) ) ;
#87155=CARTESIAN_POINT ( 'NONE',  ( 20.22483756094572271, 66.49809532114194610, -161.8835683558092171 ) ) ;
#87165=DIRECTION ( 'NONE',  ( 1.000000000000000000, 0.000000000000000000, 0.000000000000000000 ) ) ;
#87168=LINE ( 'NONE', #250114, #245807 ) ;
#87191=CARTESIAN_POINT ( 'NONE',  ( -18.59999999999999787, 69.15387683765952431, -132.7853812176745407 ) ) ;
#87193=DIRECTION ( 'NONE',  ( 6.938893903907991995E-14, 0.000000000000000000, -1.000000000000000000 ) ) ;
#87207=CARTESIAN_POINT ( 'NONE',  ( 21.05000000000000071, 76.00000000001213607, -136.5231074845243313 ) ) ;
#87287=ORIENTED_EDGE ( 'NONE', *, *, #78548, .T. ) ;
#87326=EDGE_LOOP ( 'NONE', ( #233369, #126040, #146523, #184395 ) ) ;
#87344=VERTEX_POINT ( 'NONE', #23967 ) ;
#87360=EDGE_CURVE ( 'NONE', #167384, #41308, #222454, .T. ) ;
#87375=CARTESIAN_POINT ( 'NONE',  ( -21.05000000000000071, 76.10000000001245724, -181.6731074845243654 ) ) ;
#87392=EDGE_CURVE ( 'NONE', #128506, #224580, #239234, .T. ) ;
#87417=ORIENTED_EDGE ( 'NONE', *, *, #195762, .T. ) ;
#87424=FACE_OUTER_BOUND ( 'NONE', #224210, .T. ) ;
#87452=CARTESIAN_POINT ( 'NONE',  ( 20.94999999999999929, 65.27628289530476025, -157.8731074845244393 ) ) ;
#87476=EDGE_LOOP ( 'NONE', ( #107951, #227417, #180577, #132572 ) ) ;
#87480=ORIENTED_EDGE ( 'NONE', *, *, #89774, .T. ) ;
#87509=CARTESIAN_POINT ( 'NONE',  ( 21.14250536705908345, 69.48182782313165262, -170.0231074845243882 ) ) ;
#87536=EDGE_CURVE ( 'NONE', #38206, #33088, #193464, .T. ) ;
#87537=CARTESIAN_POINT ( 'NONE',  ( -20.64999999999999858, 74.00000000001223555, -149.7477294072864709 ) ) ;
#87559=LINE ( 'NONE', #148854, #30743 ) ;
#87579=CIRCLE ( 'NONE', #95952, 7.899999999999990585 ) ;
#87586=LINE ( 'NONE', #189289, #146110 ) ;
#87627=ORIENTED_EDGE ( 'NONE', *, *, #63780, .F. ) ;
#87706=ORIENTED_EDGE ( 'NONE', *, *, #217126, .T. ) ;
#87723=EDGE_CURVE ( 'NONE', #18470, #114980, #114992, .T. ) ;
#87730=CARTESIAN_POINT ( 'NONE',  ( -21.14999999999999858, 64.25000000001232081, -163.2392418215462726 ) ) ;
#87754=ORIENTED_EDGE ( 'NONE', *, *, #59711, .F. ) ;
#87757=EDGE_LOOP ( 'NONE', ( #142705, #62631, #57897, #166218 ) ) ;
#87770=CARTESIAN_POINT ( 'NONE',  ( 21.05000000000000071, 76.00000000001213607, -136.5231074845243313 ) ) ;
#87777=CYLINDRICAL_SURFACE ( 'NONE', #48565, 0.5000000000000004441 ) ;
#87805=CARTESIAN_POINT ( 'NONE',  ( -23.15000000000000213, 76.00000000001213607, -136.5231074845243313 ) ) ;
#87816=CARTESIAN_POINT ( 'NONE',  ( -23.15000000000000213, 76.00000000001237765, -170.0231074845243597 ) ) ;
#87822=EDGE_CURVE ( 'NONE', #44761, #128947, #248268, .T. ) ;
#87828=VECTOR ( 'NONE', #13724, 1000.000000000000000 ) ;
#87831=AXIS2_PLACEMENT_3D ( 'NONE', #144546, #105395, #201975 ) ;
#87864=CARTESIAN_POINT ( 'NONE',  ( 20.94999999999999929, 76.00000000001213607, -136.5231074845243313 ) ) ;
#87933=EDGE_CURVE ( 'NONE', #79539, #143129, #165056, .T. ) ;
#87947=DIRECTION ( 'NONE',  ( -1.000000000000000000, 0.000000000000000000, 0.000000000000000000 ) ) ;
#87973=AXIS2_PLACEMENT_3D ( 'NONE', #190734, #229822, #227250 ) ;
#87985=CARTESIAN_POINT ( 'NONE',  ( 20.94999999999999929, 70.60000000001228670, -157.6178414656113205 ) ) ;
#88009=CARTESIAN_POINT ( 'NONE',  ( -20.96428641294245310, 64.25000000001219291, -143.3482143065823209 ) ) ;
#88011=ORIENTED_EDGE ( 'NONE', *, *, #191434, .T. ) ;
#88015=ADVANCED_FACE ( 'NONE', ( #144218 ), #69404, .F. ) ;
#88025=CYLINDRICAL_SURFACE ( 'NONE', #237060, 0.09999999999999939493 ) ;
#88031=CARTESIAN_POINT ( 'NONE',  ( 20.94999999999999929, 64.25000000001219291, -143.3069731475025321 ) ) ;
#88035=CARTESIAN_POINT ( 'NONE',  ( 21.05000000000000071, 70.15000000001221281, -146.6556047088023149 ) ) ;
#88042=VERTEX_POINT ( 'NONE', #166404 ) ;
#88081=CARTESIAN_POINT ( 'NONE',  ( 20.85000000000000142, 64.25000000001215028, -136.5231074845244166 ) ) ;
#88109=DIRECTION ( 'NONE',  ( 1.000000000000000000, -1.836970198721029934E-16, -1.282749433769087582E-30 ) ) ;
#88112=CIRCLE ( 'NONE', #213035, 12.87499999999999822 ) ;
#88128=AXIS2_PLACEMENT_3D ( 'NONE', #251872, #12013, #189352 ) ;
#88145=CARTESIAN_POINT ( 'NONE',  ( 23.14999999999998437, 76.00000000001240608, -174.0731074845243711 ) ) ;
#88152=CIRCLE ( 'NONE', #9083, 0.09999999999998898659 ) ;
#88163=CARTESIAN_POINT ( 'NONE',  ( 18.45139536634708222, 85.48608172029329921, -129.8825958667136433 ) ) ;
#88167=DIRECTION ( 'NONE',  ( 0.000000000000000000, 6.982962677686266711E-15, -1.000000000000000000 ) ) ;
#88168=CARTESIAN_POINT ( 'NONE',  ( 21.13920837816993270, 67.21675294989238125, -157.7731074845244166 ) ) ;
#88175=ORIENTED_EDGE ( 'NONE', *, *, #141181, .T. ) ;
#88224=( BOUNDED_CURVE ( )  B_SPLINE_CURVE ( 3, ( #212443, #192875, #254103, #93756 ),
 .UNSPECIFIED., .F., .F. ) 
 B_SPLINE_CURVE_WITH_KNOTS ( ( 4, 4 ),
 ( 0.06456096931748350753, 3.077031684272309775 ),
 .UNSPECIFIED. ) 
 CURVE ( )  GEOMETRIC_REPRESENTATION_ITEM ( )  RATIONAL_B_SPLINE_CURVE ( ( 1.000000000000000000, 0.3763440860215095940, 0.3763440860215095940, 1.000000000000000000 ) ) 
 REPRESENTATION_ITEM ( '' )  );
#88230=EDGE_LOOP ( 'NONE', ( #175473, #160575, #168088 ) ) ;
#88238=ADVANCED_FACE ( 'NONE', ( #37148 ), #131924, .T. ) ;
#88256=CARTESIAN_POINT ( 'NONE',  ( -23.25000000000000000, 76.00000000001236344, -165.8731074845243825 ) ) ;
#88277=TOROIDAL_SURFACE ( 'NONE', #146559, 0.2000000000000000111, 0.1000000000000000056 ) ;
#88342=DIRECTION ( 'NONE',  ( 0.000000000000000000, 6.982962677686266711E-15, -1.000000000000000000 ) ) ;
#88355=CIRCLE ( 'NONE', #17632, 0.1000000000000072220 ) ;
#88358=CARTESIAN_POINT ( 'NONE',  ( -20.54999999999999716, 76.00000000001237765, -170.0231074845243597 ) ) ;
#88386=ORIENTED_EDGE ( 'NONE', *, *, #236932, .F. ) ;
#88419=EDGE_LOOP ( 'NONE', ( #204192, #140301, #249781, #14976 ) ) ;
#88437=SPHERICAL_SURFACE ( 'NONE', #208221, 0.1000000000000000056 ) ;
#88460=DIRECTION ( 'NONE',  ( 0.000000000000000000, -6.982962677686266711E-15, 1.000000000000000000 ) ) ;
#88465=AXIS2_PLACEMENT_3D ( 'NONE', #235767, #19298, #54565 ) ;
#88498=CIRCLE ( 'NONE', #59258, 0.09999999999999459321 ) ;
#88535=AXIS2_PLACEMENT_3D ( 'NONE', #230878, #52200, #15693 ) ;
#88568=VERTEX_POINT ( 'NONE', #151670 ) ;
#88624=EDGE_LOOP ( 'NONE', ( #63971, #178533, #128785, #41249 ) ) ;
#88639=ORIENTED_EDGE ( 'NONE', *, *, #246872, .T. ) ;
#88699=EDGE_CURVE ( 'NONE', #72750, #229354, #127847, .T. ) ;
#88706=AXIS2_PLACEMENT_3D ( 'NONE', #66126, #128683, #86942 ) ;
#88725=DIRECTION ( 'NONE',  ( 0.000000000000000000, -7.086529944415886769E-15, 1.000000000000000000 ) ) ;
#88731=CIRCLE ( 'NONE', #188695, 0.1000000000000026007 ) ;
#88770=EDGE_LOOP ( 'NONE', ( #164717, #37987, #17246, #200721 ) ) ;
#88782=CIRCLE ( 'NONE', #247007, 0.2000000000000057288 ) ;
#88789=CARTESIAN_POINT ( 'NONE',  ( 20.85000000000000142, 87.65000000001215597, -139.4231074845242802 ) ) ;
#88797=DIRECTION ( 'NONE',  ( 1.000000000000000000, 0.000000000000000000, 0.000000000000000000 ) ) ;
#88799=ORIENTED_EDGE ( 'NONE', *, *, #23208, .F. ) ;
#88804=ORIENTED_EDGE ( 'NONE', *, *, #90601, .T. ) ;
#88865=DIRECTION ( 'NONE',  ( -1.000000000000000000, 2.952720810173289112E-16, 2.061873921506763405E-30 ) ) ;
#88909=VECTOR ( 'NONE', #119451, 1000.000000000000000 ) ;
#88933=VECTOR ( 'NONE', #25403, 1000.000000000000000 ) ;
#88960=CYLINDRICAL_SURFACE ( 'NONE', #159120, 0.5000000000000004441 ) ;
#88965=EDGE_CURVE ( 'NONE', #120146, #210220, #138018, .T. ) ;
#89063=CIRCLE ( 'NONE', #122406, 0.09999999999999939493 ) ;
#89067=ORIENTED_EDGE ( 'NONE', *, *, #128632, .T. ) ;
#89071=ADVANCED_FACE ( 'NONE', ( #162923 ), #100328, .F. ) ;
#89088=AXIS2_PLACEMENT_3D ( 'NONE', #18054, #1026, #162719 ) ;
#89105=DIRECTION ( 'NONE',  ( -1.000000000000000000, 3.265361837132813093E-16, 2.280189983783949500E-30 ) ) ;
#89110=AXIS2_PLACEMENT_3D ( 'NONE', #231046, #66815, #168529 ) ;
#89115=CARTESIAN_POINT ( 'NONE',  ( 21.93340585971889212, 68.67585297715739046, -170.0231074845244166 ) ) ;
#89123=CARTESIAN_POINT ( 'NONE',  ( 20.12500000000000000, 66.25000000001227818, -148.8731074845244393 ) ) ;
#89127=FACE_OUTER_BOUND ( 'NONE', #65504, .T. ) ;
#89135=AXIS2_PLACEMENT_3D ( 'NONE', #205598, #27006, #229041 ) ;
#89154=DIRECTION ( 'NONE',  ( 0.000000000000000000, -6.982962677686266711E-15, 1.000000000000000000 ) ) ;
#89254=CARTESIAN_POINT ( 'NONE',  ( 21.05000000000000071, 85.50000000001232081, -160.1291383618718385 ) ) ;
#89288=DIRECTION ( 'NONE',  ( 1.000000000000000000, 0.000000000000000000, 0.000000000000000000 ) ) ;
#89309=CARTESIAN_POINT ( 'NONE',  ( -18.59999999999999787, 64.35000000001234355, -163.0083017138704236 ) ) ;
#89316=LINE ( 'NONE', #168918, #167709 ) ;
#89319=DIRECTION ( 'NONE',  ( -1.000000000000000000, 3.265361837132813093E-16, 2.280189983783949500E-30 ) ) ;
#89325=ORIENTED_EDGE ( 'NONE', *, *, #146075, .T. ) ;
#89330=ADVANCED_FACE ( 'NONE', ( #135306 ), #64154, .F. ) ;
#89371=EDGE_CURVE ( 'NONE', #238125, #59420, #239114, .T. ) ;
#89402=CARTESIAN_POINT ( 'NONE',  ( 18.59999999999999076, 65.50857864377491069, -145.2731074845244450 ) ) ;
#89415=SPHERICAL_SURFACE ( 'NONE', #175356, 0.1000000000000000056 ) ;
#89416=CYLINDRICAL_SURFACE ( 'NONE', #50505, 0.1000000000000028644 ) ;
#89422=AXIS2_PLACEMENT_3D ( 'NONE', #175802, #57089, #114528 ) ;
#89451=CIRCLE ( 'NONE', #68625, 4.049999999999998046 ) ;
#89486=VERTEX_POINT ( 'NONE', #908 ) ;
#89505=CARTESIAN_POINT ( 'NONE',  ( 18.49999999999999289, 69.55000000001246008, -181.7731074845244166 ) ) ;
#89531=EDGE_CURVE ( 'NONE', #89486, #80723, #197587, .T. ) ;
#89553=PLANE ( 'NONE',  #234451 ) ;
#89558=AXIS2_PLACEMENT_3D ( 'NONE', #35679, #76051, #156909 ) ;
#89568=AXIS2_PLACEMENT_3D ( 'NONE', #68731, #208251, #111703 ) ;
#89576=CIRCLE ( 'NONE', #64479, 0.1000000000000028644 ) ;
#89582=ORIENTED_EDGE ( 'NONE', *, *, #131852, .F. ) ;
#89615=ORIENTED_EDGE ( 'NONE', *, *, #243585, .F. ) ;
#89661=ORIENTED_EDGE ( 'NONE', *, *, #191434, .F. ) ;
#89677=DIRECTION ( 'NONE',  ( 1.040834085586049673E-13, 0.7899159663865300551, 0.6132151058540831201 ) ) ;
#89687=DIRECTION ( 'NONE',  ( 1.000000000000000000, 0.000000000000000000, 0.000000000000000000 ) ) ;
#89700=EDGE_LOOP ( 'NONE', ( #205658, #59463, #28490, #189971 ) ) ;
#89726=DIRECTION ( 'NONE',  ( 0.000000000000000000, 0.1350103645451974088, -0.9908441862701587999 ) ) ;
#89727=CARTESIAN_POINT ( 'NONE',  ( 20.74625933824083290, 67.11708647892803015, -161.4679364604013188 ) ) ;
#89757=ORIENTED_EDGE ( 'NONE', *, *, #128335, .T. ) ;
#89774=EDGE_CURVE ( 'NONE', #197213, #225207, #93552, .T. ) ;
#89782=DIRECTION ( 'NONE',  ( 1.000000000000000000, 0.000000000000000000, 0.000000000000000000 ) ) ;
#89792=B_SPLINE_CURVE_WITH_KNOTS ( 'NONE', 3,
 ( #18123, #36434, #96355, #175945, #196752, #97632, #177229, #38988, #118533, #198034, #59787, #128454, #208007, #179782, #247094, #62389, #220182, #29390, #218873, #222725, #41564, #9779 ),
 .UNSPECIFIED., .F., .F.,
 ( 4, 3, 3, 3, 3, 3, 3, 4 ),
 ( 0.000000000000000000, 7.307836821087015899E-06, 4.161455748548358328E-05, 7.576591810647013904E-05, 0.0001098090429817646371, 0.0001438003617351047054, 0.0001777914035423499054, 0.0002117966137402968007 ),
 .UNSPECIFIED. ) ;
#89801=DIRECTION ( 'NONE',  ( 0.000000000000000000, 0.8660254037844420383, -0.4999999999999941713 ) ) ;
#89810=DIRECTION ( 'NONE',  ( 0.000000000000000000, -6.938893903907222067E-15, 1.000000000000000000 ) ) ;
#89818=DIRECTION ( 'NONE',  ( 1.000000000000000000, 0.000000000000000000, 0.000000000000000000 ) ) ;
#89837=ORIENTED_EDGE ( 'NONE', *, *, #4964, .F. ) ;
#89850=EDGE_CURVE ( 'NONE', #90961, #70645, #247085, .T. ) ;
#89854=AXIS2_PLACEMENT_3D ( 'NONE', #132017, #192017, #108600 ) ;
#89881=DIRECTION ( 'NONE',  ( -1.000000000000000000, 0.000000000000000000, -0.000000000000000000 ) ) ;
#89901=ADVANCED_FACE ( 'NONE', ( #242772 ), #224499, .F. ) ;
#89907=EDGE_CURVE ( 'NONE', #95398, #26294, #130570, .T. ) ;
#89924=ORIENTED_EDGE ( 'NONE', *, *, #3429, .T. ) ;
#89933=LINE ( 'NONE', #208629, #256083 ) ;
#89967=ORIENTED_EDGE ( 'NONE', *, *, #95491, .F. ) ;
#89978=LINE ( 'NONE', #151265, #216102 ) ;
#89988=DIRECTION ( 'NONE',  ( 0.000000000000000000, 7.086529944415886769E-15, -1.000000000000000000 ) ) ;
#90047=ORIENTED_EDGE ( 'NONE', *, *, #53040, .T. ) ;
#90087=LINE ( 'NONE', #189213, #233048 ) ;
#90109=CARTESIAN_POINT ( 'NONE',  ( 23.14999999999999503, 69.35000000001222986, -148.8731074845244109 ) ) ;
#90133=FACE_OUTER_BOUND ( 'NONE', #172810, .T. ) ;
#90137=ORIENTED_EDGE ( 'NONE', *, *, #133513, .T. ) ;
#90138=CARTESIAN_POINT ( 'NONE',  ( 21.05000000000000071, 76.10000000001240039, -176.5001538663141503 ) ) ;
#90144=FACE_OUTER_BOUND ( 'NONE', #35356, .T. ) ;
#90149=DIRECTION ( 'NONE',  ( -1.000000000000000000, 0.000000000000000000, -0.000000000000000000 ) ) ;
#90158=LINE ( 'NONE', #91472, #201427 ) ;
#90171=ORIENTED_EDGE ( 'NONE', *, *, #206946, .F. ) ;
#90179=CIRCLE ( 'NONE', #135977, 0.09999999999998898659 ) ;
#90183=CARTESIAN_POINT ( 'NONE',  ( -23.15000000000000213, 71.75000000001223555, -148.8731074845244109 ) ) ;
#90199=EDGE_CURVE ( 'NONE', #243905, #79646, #23464, .T. ) ;
#90255=EDGE_CURVE ( 'NONE', #219226, #120146, #189031, .T. ) ;
#90267=LINE ( 'NONE', #109836, #78562 ) ;
#90269=CARTESIAN_POINT ( 'NONE',  ( 22.40000000000010516, 76.00000000001340084, -181.6726782920694632 ) ) ;
#90282=CARTESIAN_POINT ( 'NONE',  ( 23.24999999999997513, 64.35000000001218723, -143.5379132551784096 ) ) ;
#90303=CARTESIAN_POINT ( 'NONE',  ( -21.06715728752538652, 64.25000000001233502, -163.0083017138703951 ) ) ;
#90306=DIRECTION ( 'NONE',  ( -1.000000000000000000, -0.000000000000000000, -0.000000000000000000 ) ) ;
#90338=ORIENTED_EDGE ( 'NONE', *, *, #43177, .T. ) ;
#90357=ORIENTED_EDGE ( 'NONE', *, *, #80175, .F. ) ;
#90373=EDGE_LOOP ( 'NONE', ( #123510, #244166, #73478, #209341 ) ) ;
#90384=CARTESIAN_POINT ( 'NONE',  ( -20.94999999999999929, 87.65000000001235492, -167.0231074845242460 ) ) ;
#90395=DIRECTION ( 'NONE',  ( 2.952720810173289112E-16, 1.000000000000000000, -6.088138035986627436E-46 ) ) ;
#90411=ORIENTED_EDGE ( 'NONE', *, *, #12403, .F. ) ;
#90430=CYLINDRICAL_SURFACE ( 'NONE', #103019, 0.09999999999999939493 ) ;
#90434=FACE_BOUND ( 'NONE', #236372, .T. ) ;
#90472=DIRECTION ( 'NONE',  ( -0.000000000000000000, 1.000000000000000000, 6.982962677686266711E-15 ) ) ;
#90497=LINE ( 'NONE', #205303, #19175 ) ;
#90519=CARTESIAN_POINT ( 'NONE',  ( -23.25000000000000000, 84.59626168225520360, -145.9732350016745954 ) ) ;
#90523=ORIENTED_EDGE ( 'NONE', *, *, #91503, .T. ) ;
#90541=DIRECTION ( 'NONE',  ( -0.000000000000000000, -0.01283462868040327436, 0.9999176327611370985 ) ) ;
#90554=CARTESIAN_POINT ( 'NONE',  ( -21.14999999999999858, 76.10000000001245724, -181.6726782920691505 ) ) ;
#90562=CIRCLE ( 'NONE', #119634, 4.099999999999992539 ) ;
#90572=ORIENTED_EDGE ( 'NONE', *, *, #114556, .F. ) ;
#90584=FACE_OUTER_BOUND ( 'NONE', #131076, .T. ) ;
#90601=EDGE_CURVE ( 'NONE', #76888, #224580, #14263, .T. ) ;
#90604=VERTEX_POINT ( 'NONE', #141764 ) ;
#90615=CARTESIAN_POINT ( 'NONE',  ( 18.59999999999999076, 64.35000000001220144, -145.1731074845244507 ) ) ;
#90623=DIRECTION ( 'NONE',  ( -0.000000000000000000, 0.8660254037844377084, 0.5000000000000016653 ) ) ;
#90686=DIRECTION ( 'NONE',  ( 0.000000000000000000, 0.9908441862701791170, -0.1350103645450472789 ) ) ;
#90687=EDGE_CURVE ( 'NONE', #241247, #188351, #31030, .T. ) ;
#90695=CARTESIAN_POINT ( 'NONE',  ( -20.94999999999999929, 74.83729825007431202, -162.0231074845243597 ) ) ;
#90703=DIRECTION ( 'NONE',  ( -0.000000000000000000, 1.000000000000000000, 6.982962677686266711E-15 ) ) ;
#90727=DIRECTION ( 'NONE',  ( -0.000000000000000000, 6.982962677686266711E-15, -1.000000000000000000 ) ) ;
#90732=DIRECTION ( 'NONE',  ( 0.000000000000000000, 0.9999176327611370985, -0.01283462868041289687 ) ) ;
#90737=CARTESIAN_POINT ( 'NONE',  ( 18.49999999999998934, 69.45000000001222418, -148.8731074845244109 ) ) ;
#90814=CARTESIAN_POINT ( 'NONE',  ( -23.15000000000000213, 74.08971962618051066, -157.3917396293254285 ) ) ;
#90820=AXIS2_PLACEMENT_3D ( 'NONE', #242111, #63470, #98716 ) ;
#90854=ADVANCED_FACE ( 'NONE', ( #76340 ), #52939, .T. ) ;
#90859=FACE_OUTER_BOUND ( 'NONE', #124003, .T. ) ;
#90874=VERTEX_POINT ( 'NONE', #112925 ) ;
#90898=DIRECTION ( 'NONE',  ( -1.000000000000000000, 0.000000000000000000, -0.000000000000000000 ) ) ;
#90913=ORIENTED_EDGE ( 'NONE', *, *, #97469, .T. ) ;
#90919=DIRECTION ( 'NONE',  ( 0.000000000000000000, -0.8700118002898354908, 0.4930308989875170078 ) ) ;
#90961=VERTEX_POINT ( 'NONE', #645 ) ;
#90988=DIRECTION ( 'NONE',  ( 0.000000000000000000, -0.1350103645451807555, -0.9908441862701610203 ) ) ;
#91000=CARTESIAN_POINT ( 'NONE',  ( 21.05000000000000071, 65.27628289530476025, -157.8731074845244393 ) ) ;
#91019=EDGE_CURVE ( 'NONE', #132009, #109794, #110274, .T. ) ;
#91043=CARTESIAN_POINT ( 'NONE',  ( -22.00356870141227006, 68.74575763752082480, -170.0231074845244450 ) ) ;
#91059=LINE ( 'NONE', #109316, #149275 ) ;
#91089=AXIS2_PLACEMENT_3D ( 'NONE', #47712, #218979, #199449 ) ;
#91090=LINE ( 'NONE', #145913, #130364 ) ;
#91093=CARTESIAN_POINT ( 'NONE',  ( 18.39999999999999858, 85.50000000001209344, -129.9229180933022576 ) ) ;
#91103=DIRECTION ( 'NONE',  ( -1.000000000000000000, 0.000000000000000000, 0.000000000000000000 ) ) ;
#91104=CARTESIAN_POINT ( 'NONE',  ( 23.14999999999999858, 71.00000000001223555, -148.9283735034374843 ) ) ;
#91110=ORIENTED_EDGE ( 'NONE', *, *, #183934, .F. ) ;
#91118=EDGE_CURVE ( 'NONE', #16708, #255384, #105978, .T. ) ;
#91125=CARTESIAN_POINT ( 'NONE',  ( 18.59999999999997655, 77.16412189325330928, -128.6082593989527254 ) ) ;
#91154=CARTESIAN_POINT ( 'NONE',  ( 20.95159278453404283, 67.09210366206326626, -161.5383872994151773 ) ) ;
#91173=CARTESIAN_POINT ( 'NONE',  ( 22.57320508075688537, 64.35000000001238618, -170.0231074845244166 ) ) ;
#91195=ADVANCED_FACE ( 'NONE', ( #233861 ), #85307, .T. ) ;
#91224=CIRCLE ( 'NONE', #236965, 0.1999999999999987899 ) ;
#91225=VERTEX_POINT ( 'NONE', #130898 ) ;
#91227=VERTEX_POINT ( 'NONE', #196029 ) ;
#91230=DIRECTION ( 'NONE',  ( 1.000000000000000000, -2.952720810173289112E-16, -2.061873921506763405E-30 ) ) ;
#91245=ORIENTED_EDGE ( 'NONE', *, *, #156704, .T. ) ;
#91302=VERTEX_POINT ( 'NONE', #139871 ) ;
#91356=CYLINDRICAL_SURFACE ( 'NONE', #78992, 2.000000000000001776 ) ;
#91381=VECTOR ( 'NONE', #128529, 1000.000000000000000 ) ;
#91382=CARTESIAN_POINT ( 'NONE',  ( -21.09316766718153247, 75.96073659769774622, -176.3932607969990727 ) ) ;
#91392=DIRECTION ( 'NONE',  ( 1.000000000000000000, 0.000000000000000000, 0.000000000000000000 ) ) ;
#91422=DIRECTION ( 'NONE',  ( -1.000000000000000000, 2.952720810173289112E-16, 2.061873921506763405E-30 ) ) ;
#91448=VERTEX_POINT ( 'NONE', #64210 ) ;
#91454=CARTESIAN_POINT ( 'NONE',  ( -22.60000000000080789, 75.95218301954709261, -181.7731299156771172 ) ) ;
#91455=LINE ( 'NONE', #255601, #73231 ) ;
#91464=ORIENTED_EDGE ( 'NONE', *, *, #44551, .F. ) ;
#91468=CARTESIAN_POINT ( 'NONE',  ( -21.04999999999999716, 69.69982018209549324, -170.0745903664056016 ) ) ;
#91472=CARTESIAN_POINT ( 'NONE',  ( 20.94999999999999929, 76.00000000001229239, -157.1481074845243882 ) ) ;
#91489=VERTEX_POINT ( 'NONE', #31218 ) ;
#91503=EDGE_CURVE ( 'NONE', #168221, #138337, #172878, .T. ) ;
#91504=EDGE_LOOP ( 'NONE', ( #12759, #174468, #249871, #158278, #19689 ) ) ;
#91540=DIRECTION ( 'NONE',  ( 1.000000000000000000, 0.000000000000000000, 0.000000000000000000 ) ) ;
#91555=ORIENTED_EDGE ( 'NONE', *, *, #7249, .F. ) ;
#91558=AXIS2_PLACEMENT_3D ( 'NONE', #201065, #141102, #160691 ) ;
#91576=FACE_OUTER_BOUND ( 'NONE', #147463, .T. ) ;
#91578=CARTESIAN_POINT ( 'NONE',  ( 22.40000000000020819, 76.10085836911211743, -181.7726746080140572 ) ) ;
#91593=CARTESIAN_POINT ( 'NONE',  ( 22.39999999999999858, 76.00000000001237765, -170.0231074845243597 ) ) ;
#91598=CARTESIAN_POINT ( 'NONE',  ( 22.39999999999999503, 64.35000000001237197, -170.1231074845244393 ) ) ;
#91600=DIRECTION ( 'NONE',  ( 0.000000000000000000, -7.086529944415894657E-15, 1.000000000000000000 ) ) ;
#91629=VERTEX_POINT ( 'NONE', #94991 ) ;
#91635=AXIS2_PLACEMENT_3D ( 'NONE', #47734, #106414, #110284 ) ;
#91637=AXIS2_PLACEMENT_3D ( 'NONE', #59762, #62369, #161482 ) ;
#91641=CYLINDRICAL_SURFACE ( 'NONE', #79422, 0.09999999999998898659 ) ;
#91661=AXIS2_PLACEMENT_3D ( 'NONE', #45918, #22526, #204969 ) ;
#91664=CARTESIAN_POINT ( 'NONE',  ( 18.59999999999999076, 74.16465844978787914, -158.4679561919613775 ) ) ;
#91676=AXIS2_PLACEMENT_3D ( 'NONE', #116431, #197237, #215511 ) ;
#91716=ORIENTED_EDGE ( 'NONE', *, *, #257669, .T. ) ;
#91718=EDGE_CURVE ( 'NONE', #161528, #80243, #123544, .T. ) ;
#91727=ORIENTED_EDGE ( 'NONE', *, *, #123909, .F. ) ;
#91737=FACE_OUTER_BOUND ( 'NONE', #86281, .T. ) ;
#91759=CYLINDRICAL_SURFACE ( 'NONE', #93280, 2.000000000000001776 ) ;
#91792=CARTESIAN_POINT ( 'NONE',  ( -20.54999999999999716, 66.65000000001222702, -148.7731074845244166 ) ) ;
#91794=EDGE_LOOP ( 'NONE', ( #230324, #112825, #132702, #199917 ) ) ;
#91795=AXIS2_PLACEMENT_3D ( 'NONE', #171077, #194472, #73252 ) ;
#91836=ORIENTED_EDGE ( 'NONE', *, *, #25759, .F. ) ;
#91841=CIRCLE ( 'NONE', #237597, 0.09999999999999939493 ) ;
#91847=CARTESIAN_POINT ( 'NONE',  ( -23.25000000000000000, 87.75000000001216449, -139.6231074845242688 ) ) ;
#91856=ORIENTED_EDGE ( 'NONE', *, *, #235456, .T. ) ;
#91869=VECTOR ( 'NONE', #122799, 1000.000000000000000 ) ;
#91910=CIRCLE ( 'NONE', #4423, 11.80000000000000426 ) ;
#91921=ORIENTED_EDGE ( 'NONE', *, *, #57895, .T. ) ;
#91929=EDGE_LOOP ( 'NONE', ( #3636, #68394, #189510, #82215, #131640, #38693, #121905, #98479, #8181, #242012, #183395 ) ) ;
#91937=AXIS2_PLACEMENT_3D ( 'NONE', #41620, #199407, #97685 ) ;
#91964=ORIENTED_EDGE ( 'NONE', *, *, #142693, .F. ) ;
#91969=EDGE_LOOP ( 'NONE', ( #139632, #146054, #119094, #69744 ) ) ;
#91980=CARTESIAN_POINT ( 'NONE',  ( -1.820710678118657944, 85.92928932189354896, -145.2731074845243029 ) ) ;
#91987=ORIENTED_EDGE ( 'NONE', *, *, #236392, .T. ) ;
#92011=DIRECTION ( 'NONE',  ( -0.000000000000000000, -0.8660254037844468122, -0.4999999999999860112 ) ) ;
#92026=EDGE_CURVE ( 'NONE', #47890, #226308, #174272, .T. ) ;
#92034=AXIS2_PLACEMENT_3D ( 'NONE', #76007, #180250, #175156 ) ;
#92095=ORIENTED_EDGE ( 'NONE', *, *, #93268, .F. ) ;
#92114=DIRECTION ( 'NONE',  ( -1.000000000000000000, -0.000000000000000000, -0.000000000000000000 ) ) ;
#92148=CARTESIAN_POINT ( 'NONE',  ( -22.50000000000094147, 75.90000000001255387, -181.6726782920691790 ) ) ;
#92166=CARTESIAN_POINT ( 'NONE',  ( -22.59080734064478335, 64.25000000001237765, -170.0538571926214786 ) ) ;
#92176=CARTESIAN_POINT ( 'NONE',  ( -20.64999999999999858, 84.73084112150763758, -160.4250327655399531 ) ) ;
#92177=CARTESIAN_POINT ( 'NONE',  ( -20.94999999999999929, 70.15000000001235492, -159.8906102602464330 ) ) ;
#92178=DIRECTION ( 'NONE',  ( -1.000000000000000000, 0.000000000000000000, 0.000000000000000000 ) ) ;
#92181=ORIENTED_EDGE ( 'NONE', *, *, #156734, .T. ) ;
#92190=AXIS2_PLACEMENT_3D ( 'NONE', #173669, #73259, #148925 ) ;
#92195=ORIENTED_EDGE ( 'NONE', *, *, #133849, .T. ) ;
#92197=EDGE_LOOP ( 'NONE', ( #168211, #106328, #61294, #199834 ) ) ;
#92211=CARTESIAN_POINT ( 'NONE',  ( -21.05000000000000071, 87.65000000001215597, -139.4231074845242802 ) ) ;
#92251=EDGE_LOOP ( 'NONE', ( #13310, #203766, #122942, #237332 ) ) ;
#92278=CARTESIAN_POINT ( 'NONE',  ( 21.12400247839515899, 65.27851195598189804, -157.7731074845244166 ) ) ;
#92290=AXIS2_PLACEMENT_3D ( 'NONE', #129399, #31616, #133251 ) ;
#92298=CARTESIAN_POINT ( 'NONE',  ( -18.59999999999999787, 77.85102823015316176, -158.3691942151018566 ) ) ;
#92303=DIRECTION ( 'NONE',  ( 1.000000000000000000, -0.000000000000000000, 0.000000000000000000 ) ) ;
#92305=VECTOR ( 'NONE', #3857, 1000.000000000000000 ) ;
#92320=FACE_OUTER_BOUND ( 'NONE', #84549, .T. ) ;
#92370=VERTEX_POINT ( 'NONE', #31866 ) ;
#92457=EDGE_CURVE ( 'NONE', #177863, #194806, #94362, .T. ) ;
#92466=ORIENTED_EDGE ( 'NONE', *, *, #245899, .F. ) ;
#92503=AXIS2_PLACEMENT_3D ( 'NONE', #27197, #186242, #187542 ) ;
#92511=DIRECTION ( 'NONE',  ( 0.000000000000000000, -1.000000000000000000, -6.982962677686266711E-15 ) ) ;
#92538=CARTESIAN_POINT ( 'NONE',  ( 23.14999999999999858, 71.00000000001223555, -148.9283735034374843 ) ) ;
#92547=CYLINDRICAL_SURFACE ( 'NONE', #148295, 0.09999999999998898659 ) ;
#92565=AXIS2_PLACEMENT_3D ( 'NONE', #53053, #90898, #36080 ) ;
#92577=CYLINDRICAL_SURFACE ( 'NONE', #177748, 4.000000000000003553 ) ;
#92581=CARTESIAN_POINT ( 'NONE',  ( -18.52328366898032641, 85.64232108905335394, -129.8082881469542258 ) ) ;
#92585=LINE ( 'NONE', #213831, #33396 ) ;
#92586=EDGE_CURVE ( 'NONE', #14612, #134542, #158246, .T. ) ;
#92616=VERTEX_POINT ( 'NONE', #139902 ) ;
#92640=CARTESIAN_POINT ( 'NONE',  ( 22.39999999999999503, 64.35000000001237197, -170.0231074845244166 ) ) ;
#92641=EDGE_CURVE ( 'NONE', #91489, #23345, #25138, .T. ) ;
#92647=CARTESIAN_POINT ( 'NONE',  ( -21.08621493067320429, 75.94380516053638530, -176.3724017756962894 ) ) ;
#92653=ADVANCED_FACE ( 'NONE', ( #6835 ), #36015, .F. ) ;
#92654=ORIENTED_EDGE ( 'NONE', *, *, #245113, .F. ) ;
#92665=DIRECTION ( 'NONE',  ( 1.000000000000000000, 0.000000000000000000, 0.000000000000000000 ) ) ;
#92678=AXIS2_PLACEMENT_3D ( 'NONE', #78796, #236596, #256106 ) ;
#92701=AXIS2_PLACEMENT_3D ( 'NONE', #147506, #130500, #9276 ) ;
#92711=AXIS2_PLACEMENT_3D ( 'NONE', #105796, #22465, #240220 ) ;
#92715=CARTESIAN_POINT ( 'NONE',  ( -22.50485643085238863, 76.07878633908967458, -181.7729024236968485 ) ) ;
#92728=ORIENTED_EDGE ( 'NONE', *, *, #256443, .T. ) ;
#92729=CARTESIAN_POINT ( 'NONE',  ( -21.05000000000000071, 64.40000000001219860, -143.4513107147999449 ) ) ;
#92737=FACE_OUTER_BOUND ( 'NONE', #233258, .T. ) ;
#92750=ORIENTED_EDGE ( 'NONE', *, *, #75017, .F. ) ;
#92775=CARTESIAN_POINT ( 'NONE',  ( 23.24999999999999289, 64.35000000001245724, -181.7731074845244450 ) ) ;
#92778=VERTEX_POINT ( 'NONE', #216359 ) ;
#92784=VERTEX_POINT ( 'NONE', #237221 ) ;
#92786=EDGE_CURVE ( 'NONE', #228810, #67500, #15363, .T. ) ;
#92813=ORIENTED_EDGE ( 'NONE', *, *, #132410, .F. ) ;
#92821=CARTESIAN_POINT ( 'NONE',  ( 23.14999999999999858, 71.00000000001223555, -148.4283735034374843 ) ) ;
#92823=ORIENTED_EDGE ( 'NONE', *, *, #242690, .F. ) ;
#92862=DIRECTION ( 'NONE',  ( -2.602085213965226419E-14, -6.982962677686266711E-15, 1.000000000000000000 ) ) ;
#92870=ORIENTED_EDGE ( 'NONE', *, *, #132173, .T. ) ;
#92878=EDGE_LOOP ( 'NONE', ( #183151, #64604, #202340 ) ) ;
#92973=FACE_OUTER_BOUND ( 'NONE', #185524, .T. ) ;
#92975=CARTESIAN_POINT ( 'NONE',  ( 21.05000000000000426, 65.27628289530478867, -162.4286900929113528 ) ) ;
#92998=AXIS2_PLACEMENT_3D ( 'NONE', #188664, #150824, #10030 ) ;
#93006=CARTESIAN_POINT ( 'NONE',  ( -18.33981767444321065, 85.56957578981628387, -129.7039456407995033 ) ) ;
#93008=DIRECTION ( 'NONE',  ( -5.603264701231743991E-32, -7.172728831056617961E-15, 1.000000000000000000 ) ) ;
#93028=ORIENTED_EDGE ( 'NONE', *, *, #174750, .F. ) ;
#93048=CARTESIAN_POINT ( 'NONE',  ( 23.14999999999999503, 64.35000000001228670, -157.8731074845244393 ) ) ;
#93055=CARTESIAN_POINT ( 'NONE',  ( 18.59999999999999787, 77.83534155023670564, -158.4679561919613491 ) ) ;
#93076=EDGE_CURVE ( 'NONE', #195729, #216103, #55656, .T. ) ;
#93077=ORIENTED_EDGE ( 'NONE', *, *, #194644, .T. ) ;
#93089=ORIENTED_EDGE ( 'NONE', *, *, #52617, .T. ) ;
#93116=ORIENTED_EDGE ( 'NONE', *, *, #201049, .T. ) ;
#93132=CIRCLE ( 'NONE', #138882, 11.70000000000001528 ) ;
#93146=CARTESIAN_POINT ( 'NONE',  ( 23.14999999999999858, 76.00000000001213607, -136.5231074845243313 ) ) ;
#93157=CARTESIAN_POINT ( 'NONE',  ( -21.04999999999999716, 76.00000000001243450, -176.5637644362255969 ) ) ;
#93170=AXIS2_PLACEMENT_3D ( 'NONE', #220316, #241166, #179913 ) ;
#93223=EDGE_CURVE ( 'NONE', #36642, #207248, #139044, .T. ) ;
#93262=LINE ( 'NONE', #91980, #204304 ) ;
#93268=EDGE_CURVE ( 'NONE', #46365, #136655, #196479, .T. ) ;
#93272=FACE_OUTER_BOUND ( 'NONE', #32180, .T. ) ;
#93280=AXIS2_PLACEMENT_3D ( 'NONE', #168781, #68351, #231285 ) ;
#93301=AXIS2_PLACEMENT_3D ( 'NONE', #112638, #129630, #245730 ) ;
#93314=AXIS2_PLACEMENT_3D ( 'NONE', #223231, #185403, #62885 ) ;
#93317=TOROIDAL_SURFACE ( 'NONE', #68388, 0.2000000000000000111, 0.1000000000000000056 ) ;
#93323=ORIENTED_EDGE ( 'NONE', *, *, #47039, .T. ) ;
#93327=EDGE_LOOP ( 'NONE', ( #161000, #40491, #116373, #75820 ) ) ;
#93333=DIRECTION ( 'NONE',  ( -1.000000000000000000, -0.000000000000000000, -0.000000000000000000 ) ) ;
#93337=AXIS2_PLACEMENT_3D ( 'NONE', #206889, #227723, #68669 ) ;
#93342=EDGE_LOOP ( 'NONE', ( #72805, #222599, #89325, #41236 ) ) ;
#93346=ORIENTED_EDGE ( 'NONE', *, *, #246677, .F. ) ;
#93366=AXIS2_PLACEMENT_3D ( 'NONE', #234214, #195132, #132569 ) ;
#93372=EDGE_CURVE ( 'NONE', #60849, #246816, #256499, .T. ) ;
#93419=DIRECTION ( 'NONE',  ( -0.000000000000000000, 1.000000000000000000, 6.982962677686266711E-15 ) ) ;
#93421=CARTESIAN_POINT ( 'NONE',  ( -23.15000000000000213, 85.00000000001232081, -160.1291383618718385 ) ) ;
#93437=AXIS2_PLACEMENT_3D ( 'NONE', #246217, #130105, #109253 ) ;
#93483=CIRCLE ( 'NONE', #160166, 0.2000000000000057288 ) ;
#93518=EDGE_CURVE ( 'NONE', #4036, #248809, #188474, .T. ) ;
#93526=CARTESIAN_POINT ( 'NONE',  ( 20.94999999999999929, 71.00000000001223555, -148.9283735034374843 ) ) ;
#93552=CIRCLE ( 'NONE', #126871, 0.09999999999998898659 ) ;
#93578=AXIS2_PLACEMENT_3D ( 'NONE', #227873, #229167, #226568 ) ;
#93586=EDGE_LOOP ( 'NONE', ( #137115, #228232, #115293, #47580 ) ) ;
#93591=DIRECTION ( 'NONE',  ( 0.000000000000000000, 0.9908441862701420355, 0.1350103645453197554 ) ) ;
#93592=FACE_OUTER_BOUND ( 'NONE', #130257, .T. ) ;
#93596=DIRECTION ( 'NONE',  ( 0.000000000000000000, 0.000000000000000000, -1.000000000000000000 ) ) ;
#93602=ORIENTED_EDGE ( 'NONE', *, *, #149311, .F. ) ;
#93623=EDGE_CURVE ( 'NONE', #236193, #74533, #534, .T. ) ;
#93651=DIRECTION ( 'NONE',  ( 1.000000000000000000, -0.000000000000000000, 0.000000000000000000 ) ) ;
#93695=ORIENTED_EDGE ( 'NONE', *, *, #186367, .F. ) ;
#93714=VECTOR ( 'NONE', #25729, 1000.000000000000000 ) ;
#93756=CARTESIAN_POINT ( 'NONE',  ( 20.94999999999999574, 67.07338541492521244, -161.5514244653012952 ) ) ;
#93776=VERTEX_POINT ( 'NONE', #163478 ) ;
#93790=AXIS2_PLACEMENT_3D ( 'NONE', #45476, #42916, #67602 ) ;
#93794=ORIENTED_EDGE ( 'NONE', *, *, #34464, .F. ) ;
#93800=CARTESIAN_POINT ( 'NONE',  ( -23.15000000000000213, 85.00000000001232081, -160.1291383618718385 ) ) ;
#93811=VERTEX_POINT ( 'NONE', #220869 ) ;
#93814=VECTOR ( 'NONE', #192062, 1000.000000000000000 ) ;
#93830=DIRECTION ( 'NONE',  ( 0.000000000000000000, 1.000000000000000000, 0.000000000000000000 ) ) ;
#93843=ORIENTED_EDGE ( 'NONE', *, *, #40839, .F. ) ;
#93858=ADVANCED_FACE ( 'NONE', ( #189467 ), #57382, .T. ) ;
#93876=CARTESIAN_POINT ( 'NONE',  ( 23.14999999999999858, 71.18691588786276725, -158.0815897280005800 ) ) ;
#93906=DIRECTION ( 'NONE',  ( -1.000000000000000000, -0.000000000000000000, 0.000000000000000000 ) ) ;
#93944=DIRECTION ( 'NONE',  ( 0.000000000000000000, -6.652207440891554563E-15, 1.000000000000000000 ) ) ;
#93951=LINE ( 'NONE', #251747, #161936 ) ;
#93999=CARTESIAN_POINT ( 'NONE',  ( -22.57848426163147693, 76.00426432929559439, -181.7731657914146979 ) ) ;
#94003=CYLINDRICAL_SURFACE ( 'NONE', #220269, 0.5000000000000004441 ) ;
#94004=ADVANCED_FACE ( 'NONE', ( #195898 ), #14706, .F. ) ;
#94035=ORIENTED_EDGE ( 'NONE', *, *, #20499, .F. ) ;
#94083=ADVANCED_FACE ( 'NONE', ( #163184 ), #257434, .T. ) ;
#94086=EDGE_LOOP ( 'NONE', ( #242637, #76509, #16813, #184835 ) ) ;
#94101=ORIENTED_EDGE ( 'NONE', *, *, #55442, .T. ) ;
#94133=CARTESIAN_POINT ( 'NONE',  ( -20.00857864376270001, 66.85000000001222986, -148.7731074845244166 ) ) ;
#94142=ORIENTED_EDGE ( 'NONE', *, *, #195762, .F. ) ;
#94148=FACE_OUTER_BOUND ( 'NONE', #221951, .T. ) ;
#94188=EDGE_LOOP ( 'NONE', ( #105197, #137526, #163664, #202098, #91836 ) ) ;
#94225=CARTESIAN_POINT ( 'NONE',  ( -21.05000000000000071, 76.00000000001213607, -136.5231074845243313 ) ) ;
#94270=DIRECTION ( 'NONE',  ( 0.000000000000000000, 0.000000000000000000, 1.000000000000000000 ) ) ;
#94283=CARTESIAN_POINT ( 'NONE',  ( -18.43634282235119670, 85.67978719994012238, -129.8624555990704721 ) ) ;
#94300=CYLINDRICAL_SURFACE ( 'NONE', #123174, 0.5000000000000004441 ) ;
#94322=ORIENTED_EDGE ( 'NONE', *, *, #184423, .F. ) ;
#94324=EDGE_CURVE ( 'NONE', #166820, #29646, #66134, .T. ) ;
#94333=CARTESIAN_POINT ( 'NONE',  ( 23.14999999999999858, 69.35000000001228670, -157.6731074845243938 ) ) ;
#94344=ORIENTED_EDGE ( 'NONE', *, *, #116202, .T. ) ;
#94362=LINE ( 'NONE', #173969, #115123 ) ;
#94372=DIRECTION ( 'NONE',  ( 0.000000000000000000, -7.109473446599835262E-15, 1.000000000000000000 ) ) ;
#94409=FACE_OUTER_BOUND ( 'NONE', #254930, .T. ) ;
#94417=EDGE_CURVE ( 'NONE', #65247, #206663, #170245, .T. ) ;
#94419=EDGE_CURVE ( 'NONE', #123398, #170736, #116048, .T. ) ;
#94433=FACE_OUTER_BOUND ( 'NONE', #179409, .T. ) ;
#94441=DIRECTION ( 'NONE',  ( 0.000000000000000000, 6.982962677686266711E-15, -1.000000000000000000 ) ) ;
#94442=CARTESIAN_POINT ( 'NONE',  ( -21.05000000000000071, 76.02110330807200000, -176.3276238137887901 ) ) ;
#94456=DIRECTION ( 'NONE',  ( 0.000000000000000000, -7.147358527629766941E-15, 1.000000000000000000 ) ) ;
#94474=DIRECTION ( 'NONE',  ( -0.000000000000000000, -1.000000000000000000, -7.272083257015735086E-15 ) ) ;
#94492=EDGE_LOOP ( 'NONE', ( #51643, #228128, #138372, #35339, #898, #242282 ) ) ;
#94496=AXIS2_PLACEMENT_3D ( 'NONE', #115092, #55084, #254568 ) ;
#94497=ORIENTED_EDGE ( 'NONE', *, *, #175654, .T. ) ;
#94508=CARTESIAN_POINT ( 'NONE',  ( -18.50000000000000000, 76.00000000001237765, -170.0231074845243597 ) ) ;
#94515=VERTEX_POINT ( 'NONE', #90695 ) ;
#94526=CARTESIAN_POINT ( 'NONE',  ( 18.59999999999999787, 74.13328508995498112, -158.2704322382423641 ) ) ;
#94591=DIRECTION ( 'NONE',  ( 1.000000000000000000, 0.000000000000000000, 0.000000000000000000 ) ) ;
#94596=CARTESIAN_POINT ( 'NONE',  ( 18.49999999999999289, 65.75000000001220712, -145.3731074845244393 ) ) ;
#94621=EDGE_LOOP ( 'NONE', ( #213126, #206738, #129773, #166919 ) ) ;
#94631=CARTESIAN_POINT ( 'NONE',  ( -20.89192007715127986, 65.67101464000523947, -130.9404391622479977 ) ) ;
#94695=EDGE_CURVE ( 'NONE', #67500, #176291, #165746, .T. ) ;
#94706=VERTEX_POINT ( 'NONE', #77531 ) ;
#94737=CARTESIAN_POINT ( 'NONE',  ( 21.05000000000000071, 84.66355140188147743, -160.4990063664569959 ) ) ;
#94749=CARTESIAN_POINT ( 'NONE',  ( -20.94999999999999929, 64.35000000001214460, -136.5231074845244166 ) ) ;
#94754=VERTEX_POINT ( 'NONE', #102217 ) ;
#94756=ORIENTED_EDGE ( 'NONE', *, *, #58044, .F. ) ;
#94764=ORIENTED_EDGE ( 'NONE', *, *, #171039, .F. ) ;
#94800=ORIENTED_EDGE ( 'NONE', *, *, #205266, .T. ) ;
#94803=AXIS2_PLACEMENT_3D ( 'NONE', #71341, #167881, #49184 ) ;
#94804=AXIS2_PLACEMENT_3D ( 'NONE', #238515, #247505, #109260 ) ;
#94818=CARTESIAN_POINT ( 'NONE',  ( -21.05000000000000071, 75.74389420792016381, -170.0580039261966476 ) ) ;
#94828=ORIENTED_EDGE ( 'NONE', *, *, #177329, .F. ) ;
#94853=TOROIDAL_SURFACE ( 'NONE', #15791, 0.2000000000000000111, 0.1000000000000000056 ) ;
#94863=CARTESIAN_POINT ( 'NONE',  ( 22.39999999999999503, 64.35000000001237197, -170.1231074845244393 ) ) ;
#94869=DIRECTION ( 'NONE',  ( -1.000000000000000000, -0.000000000000000000, 0.000000000000000000 ) ) ;
#94874=AXIS2_PLACEMENT_3D ( 'NONE', #252877, #74285, #134207 ) ;
#94881=DIRECTION ( 'NONE',  ( -0.000000000000000000, -6.982962677686266711E-15, 1.000000000000000000 ) ) ;
#94884=FACE_OUTER_BOUND ( 'NONE', #94188, .T. ) ;
#94885=DIRECTION ( 'NONE',  ( 0.000000000000000000, -6.467318590049456648E-15, 1.000000000000000000 ) ) ;
#94890=VERTEX_POINT ( 'NONE', #143944 ) ;
#94899=DIRECTION ( 'NONE',  ( 1.000000000000000000, 0.000000000000000000, 0.000000000000000000 ) ) ;
#94909=ORIENTED_EDGE ( 'NONE', *, *, #120150, .F. ) ;
#94939=EDGE_CURVE ( 'NONE', #40931, #113219, #3197, .T. ) ;
#94962=DIRECTION ( 'NONE',  ( 0.000000000000000000, 0.000000000000000000, -1.000000000000000000 ) ) ;
#94981=LINE ( 'NONE', #194112, #101225 ) ;
#94991=CARTESIAN_POINT ( 'NONE',  ( 23.14999999999999503, 64.35000000001228670, -157.7731074845244450 ) ) ;
#94992=EDGE_CURVE ( 'NONE', #101907, #112448, #29195, .T. ) ;
#94999=VERTEX_POINT ( 'NONE', #168712 ) ;
#95009=CARTESIAN_POINT ( 'NONE',  ( 21.14999999999999858, 64.35000000001228670, -157.8731074845244393 ) ) ;
#95013=ORIENTED_EDGE ( 'NONE', *, *, #114926, .T. ) ;
#95025=DIRECTION ( 'NONE',  ( 0.000000000000000000, 0.1298341882519953583, 0.9915357197604862671 ) ) ;
#95082=ORIENTED_EDGE ( 'NONE', *, *, #15366, .F. ) ;
#95093=PLANE ( 'NONE',  #207207 ) ;
#95112=ORIENTED_EDGE ( 'NONE', *, *, #85953, .T. ) ;
#95129=TOROIDAL_SURFACE ( 'NONE', #240876, 0.6000000000000009770, 0.1000000000000000056 ) ;
#95157=DIRECTION ( 'NONE',  ( 0.000000000000000000, 6.938893903907222067E-15, -1.000000000000000000 ) ) ;
#95171=DIRECTION ( 'NONE',  ( 0.000000000000000000, 1.000000000000000000, 6.982962677686266711E-15 ) ) ;
#95172=AXIS2_PLACEMENT_3D ( 'NONE', #82053, #142053, #161653 ) ;
#95181=CARTESIAN_POINT ( 'NONE',  ( -20.85000000000000142, 76.00000000001213607, -136.5231074845243313 ) ) ;
#95210=VERTEX_POINT ( 'NONE', #101929 ) ;
#95221=DIRECTION ( 'NONE',  ( 1.000000000000000000, 0.000000000000000000, 0.000000000000000000 ) ) ;
#95233=CARTESIAN_POINT ( 'NONE',  ( 21.05000000000000071, 71.18691588786271041, -148.4646252410481964 ) ) ;
#95237=CARTESIAN_POINT ( 'NONE',  ( 20.94999999999999929, 77.16412189325330928, -128.6082593989527254 ) ) ;
#95244=AXIS2_PLACEMENT_3D ( 'NONE', #252733, #132818, #89810 ) ;
#95281=CIRCLE ( 'NONE', #174443, 12.87499999999999822 ) ;
#95291=ORIENTED_EDGE ( 'NONE', *, *, #47966, .F. ) ;
#95303=EDGE_CURVE ( 'NONE', #6721, #147377, #83637, .T. ) ;
#95341=EDGE_CURVE ( 'NONE', #44088, #174960, #82470, .T. ) ;
#95363=FACE_OUTER_BOUND ( 'NONE', #254980, .T. ) ;
#95380=DIRECTION ( 'NONE',  ( 0.000000000000000000, -6.982962677686266711E-15, 1.000000000000000000 ) ) ;
#95391=ORIENTED_EDGE ( 'NONE', *, *, #257687, .F. ) ;
#95398=VERTEX_POINT ( 'NONE', #213895 ) ;
#95410=AXIS2_PLACEMENT_3D ( 'NONE', #95492, #56348, #78484 ) ;
#95419=DIRECTION ( 'NONE',  ( 0.000000000000000000, 6.467318590049456648E-15, -1.000000000000000000 ) ) ;
#95423=FACE_OUTER_BOUND ( 'NONE', #25159, .T. ) ;
#95427=AXIS2_PLACEMENT_3D ( 'NONE', #87452, #187874, #30094 ) ;
#95472=AXIS2_PLACEMENT_3D ( 'NONE', #209098, #70905, #150433 ) ;
#95491=EDGE_CURVE ( 'NONE', #18113, #118231, #153672, .T. ) ;
#95492=CARTESIAN_POINT ( 'NONE',  ( 23.14999999999999503, 69.55000000001246008, -181.7731074845244166 ) ) ;
#95551=LINE ( 'NONE', #198505, #67645 ) ;
#95560=EDGE_LOOP ( 'NONE', ( #11616, #90523, #122381, #56456 ) ) ;
#95574=CARTESIAN_POINT ( 'NONE',  ( -21.14999999999999858, 76.10000000001245724, -181.6726782920691505 ) ) ;
#95578=DIRECTION ( 'NONE',  ( -1.000000000000000000, 2.952720810173289112E-16, 2.061873921506763405E-30 ) ) ;
#95593=VECTOR ( 'NONE', #133419, 1000.000000000000000 ) ;
#95679=EDGE_CURVE ( 'NONE', #121929, #209214, #45274, .T. ) ;
#95682=ADVANCED_FACE ( 'NONE', ( #203326 ), #221572, .T. ) ;
#95684=VERTEX_POINT ( 'NONE', #62531 ) ;
#95687=ORIENTED_EDGE ( 'NONE', *, *, #11040, .F. ) ;
#95707=DIRECTION ( 'NONE',  ( 1.000000000000000000, 0.000000000000000000, 0.000000000000000000 ) ) ;
#95723=DIRECTION ( 'NONE',  ( 0.000000000000000000, 0.000000000000000000, 1.000000000000000000 ) ) ;
#95744=AXIS2_PLACEMENT_3D ( 'NONE', #9623, #130856, #89154 ) ;
#95783=CARTESIAN_POINT ( 'NONE',  ( -18.50000000000000000, 70.65875701002080689, -179.8297576910124178 ) ) ;
#95821=ORIENTED_EDGE ( 'NONE', *, *, #133045, .F. ) ;
#95866=ORIENTED_EDGE ( 'NONE', *, *, #239231, .T. ) ;
#95901=ORIENTED_EDGE ( 'NONE', *, *, #94324, .T. ) ;
#95952=AXIS2_PLACEMENT_3D ( 'NONE', #81063, #40715, #160653 ) ;
#95989=EDGE_CURVE ( 'NONE', #80321, #176854, #53837, .T. ) ;
#96014=ADVANCED_FACE ( 'NONE', ( #144283 ), #62038, .T. ) ;
#96040=ORIENTED_EDGE ( 'NONE', *, *, #242088, .T. ) ;
#96051=FACE_OUTER_BOUND ( 'NONE', #51258, .T. ) ;
#96057=FACE_OUTER_BOUND ( 'NONE', #46170, .T. ) ;
#96152=CARTESIAN_POINT ( 'NONE',  ( -18.59999999999999787, 68.97833521811203639, -132.8895420826271163 ) ) ;
#96158=EDGE_CURVE ( 'NONE', #167205, #244509, #46481, .T. ) ;
#96182=CARTESIAN_POINT ( 'NONE',  ( -21.05000000000000071, 77.83534155023670564, -158.4679561919613491 ) ) ;
#96204=EDGE_CURVE ( 'NONE', #231632, #59304, #120679, .T. ) ;
#96231=CARTESIAN_POINT ( 'NONE',  ( 23.25000000000000000, 84.59626168225530307, -160.5729799673740104 ) ) ;
#96235=EDGE_LOOP ( 'NONE', ( #182519, #95391, #234625, #59648 ) ) ;
#96237=DIRECTION ( 'NONE',  ( -6.938893903907222856E-15, -1.000000000000000000, -7.272083257015735086E-15 ) ) ;
#96269=DIRECTION ( 'NONE',  ( -1.000000000000000000, -7.304098846218105085E-16, -4.217023435051676515E-16 ) ) ;
#96304=DIRECTION ( 'NONE',  ( 0.000000000000000000, -4.744542840278440942E-15, 1.000000000000000000 ) ) ;
#96324=ORIENTED_EDGE ( 'NONE', *, *, #46542, .F. ) ;
#96333=CARTESIAN_POINT ( 'NONE',  ( -23.25000000000000000, 76.00000000001207923, -128.6231074845243540 ) ) ;
#96334=ORIENTED_EDGE ( 'NONE', *, *, #193360, .F. ) ;
#96355=CARTESIAN_POINT ( 'NONE',  ( 20.95035502843362707, 65.52236167323586358, -162.4468077757880451 ) ) ;
#96380=DIRECTION ( 'NONE',  ( 1.000000000000000000, -2.952720810173289112E-16, -2.061873921506763405E-30 ) ) ;
#96406=EDGE_CURVE ( 'NONE', #238847, #118231, #107304, .T. ) ;
#96421=CARTESIAN_POINT ( 'NONE',  ( -23.15000000000000213, 64.35000000001218723, -143.5379132551784096 ) ) ;
#96467=CARTESIAN_POINT ( 'NONE',  ( 23.24999999999999645, 71.22429906543278832, -148.3718755885703331 ) ) ;
#96476=CARTESIAN_POINT ( 'NONE',  ( -20.94999999999999929, 74.16465844978787914, -158.4679561919613775 ) ) ;
#96493=ADVANCED_FACE ( 'NONE', ( #200871 ), #37471, .F. ) ;
#96502=ORIENTED_EDGE ( 'NONE', *, *, #75291, .F. ) ;
#96513=ORIENTED_EDGE ( 'NONE', *, *, #188599, .F. ) ;
#96515=ADVANCED_FACE ( 'NONE', ( #163058 ), #199618, .F. ) ;
#96526=CARTESIAN_POINT ( 'NONE',  ( 23.24999999999999289, 69.35000000001222986, -148.8731074845244109 ) ) ;
#96527=CARTESIAN_POINT ( 'NONE',  ( -23.25000000000000000, 76.10000000001245724, -181.6726782920691505 ) ) ;
#96592=( BOUNDED_SURFACE ( )  B_SPLINE_SURFACE ( 3, 2, ( 
 ( #155778, #120505, #74957 ),
 ( #154498, #134867, #35820 ),
 ( #214423, #115326, #194892 ),
 ( #244253, #200018, #102156 ),
 ( #166046, #103452, #26526 ),
 ( #160903, #63054, #82589 ) ),
 .UNSPECIFIED., .F., .F., .F. ) 
 B_SPLINE_SURFACE_WITH_KNOTS ( ( 4, 2, 4 ),
 ( 3, 3 ),
 ( 1.570796326794895448, 2.356194490192343505, 3.141592653589791784 ),
 ( 0.000000000000000000, 1.000000000000000000 ),
 .UNSPECIFIED. ) 
 GEOMETRIC_REPRESENTATION_ITEM ( )  RATIONAL_B_SPLINE_SURFACE ( (
 ( 1.000000000000000000, 0.7071067811865475727, 1.000000000000000000),
 ( 1.000000000000000000, 0.6611148371779108635, 1.000000000000000000),
 ( 1.000000000000000000, 0.6092287576696373552, 1.000000000000000000),
 ( 1.000000000000000000, 0.5278258667057376119, 1.000000000000000000),
 ( 1.000000000000000000, 0.4993418825334632327, 1.000000000000000000),
 ( 1.000000000000000000, 0.5000000000000456302, 1.000000000000000000) ) ) 
 REPRESENTATION_ITEM ( '' )  SURFACE ( )  );
#96620=VECTOR ( 'NONE', #149159, 1000.000000000000000 ) ;
#96638=VERTEX_POINT ( 'NONE', #249006 ) ;
#96673=CARTESIAN_POINT ( 'NONE',  ( 21.06490991615909891, 65.27510865242517468, -157.8193961309912936 ) ) ;
#96676=CARTESIAN_POINT ( 'NONE',  ( -23.25000000000000000, 71.85000000001228670, -157.6731074845243654 ) ) ;
#96690=AXIS2_PLACEMENT_3D ( 'NONE', #106697, #65016, #87137 ) ;
#96709=EDGE_CURVE ( 'NONE', #222373, #211242, #204032, .T. ) ;
#96726=CARTESIAN_POINT ( 'NONE',  ( 18.49999999999999645, 70.30054753569086756, -182.5653814410942459 ) ) ;
#96738=EDGE_CURVE ( 'NONE', #146933, #122358, #151181, .T. ) ;
#96761=EDGE_CURVE ( 'NONE', #123954, #243905, #14249, .T. ) ;
#96770=ORIENTED_EDGE ( 'NONE', *, *, #133629, .F. ) ;
#96808=EDGE_CURVE ( 'NONE', #15766, #90604, #88224, .T. ) ;
#96814=LINE ( 'NONE', #176409, #84557 ) ;
#96817=DIRECTION ( 'NONE',  ( 2.978066053179066272E-16, 1.000000000000000000, 7.147358527629759053E-15 ) ) ;
#96819=CARTESIAN_POINT ( 'NONE',  ( -23.15000000000000213, 71.75000000001223555, -148.7731074845243882 ) ) ;
#96825=CARTESIAN_POINT ( 'NONE',  ( -18.49372193242229301, 85.44248452337028255, -129.7583262244892808 ) ) ;
#96842=ORIENTED_EDGE ( 'NONE', *, *, #181646, .T. ) ;
#96871=AXIS2_PLACEMENT_3D ( 'NONE', #94526, #34589, #75010 ) ;
#96889=CARTESIAN_POINT ( 'NONE',  ( -22.57320508075687115, 64.25000000001237765, -170.0231074845244166 ) ) ;
#96890=AXIS2_PLACEMENT_3D ( 'NONE', #234207, #217202, #58123 ) ;
#96906=EDGE_CURVE ( 'NONE', #195729, #69727, #79302, .T. ) ;
#96911=ORIENTED_EDGE ( 'NONE', *, *, #107918, .F. ) ;
#96923=CARTESIAN_POINT ( 'NONE',  ( -20.94999999999999929, 87.39257802171783851, -139.5970570643562212 ) ) ;
#96974=ADVANCED_FACE ( 'NONE', ( #59740 ), #139280, .T. ) ;
#97036=AXIS2_PLACEMENT_3D ( 'NONE', #151573, #135811, #52423 ) ;
#97057=EDGE_LOOP ( 'NONE', ( #1856, #145473, #202248, #197699 ) ) ;
#97061=DIRECTION ( 'NONE',  ( 0.000000000000000000, -1.000000000000000000, -6.982962677686265922E-15 ) ) ;
#97088=CARTESIAN_POINT ( 'NONE',  ( 20.94999999999999929, 87.65000000001215597, -139.5231074845243029 ) ) ;
#97092=CARTESIAN_POINT ( 'NONE',  ( 21.05000000000000071, 76.09999993531950224, -176.5011857056192639 ) ) ;
#97102=EDGE_CURVE ( 'NONE', #217847, #128659, #252513, .T. ) ;
#97109=VERTEX_POINT ( 'NONE', #213388 ) ;
#97129=CARTESIAN_POINT ( 'NONE',  ( 18.49999999999999289, 65.74999999739320344, -145.3359355348928261 ) ) ;
#97136=ORIENTED_EDGE ( 'NONE', *, *, #245899, .T. ) ;
#97152=DIRECTION ( 'NONE',  ( 1.000000000000000000, 0.000000000000000000, 0.000000000000000000 ) ) ;
#97165=ORIENTED_EDGE ( 'NONE', *, *, #230785, .F. ) ;
#97187=FACE_OUTER_BOUND ( 'NONE', #47562, .T. ) ;
#97205=AXIS2_PLACEMENT_3D ( 'NONE', #117587, #200980, #118888 ) ;
#97241=DIRECTION ( 'NONE',  ( 1.000000000000000000, 0.000000000000000000, 0.000000000000000000 ) ) ;
#97255=CARTESIAN_POINT ( 'NONE',  ( -20.64999999999999858, 71.75000000001229239, -157.6731074845243654 ) ) ;
#97257=ORIENTED_EDGE ( 'NONE', *, *, #112456, .T. ) ;
#97281=ADVANCED_FACE ( 'NONE', ( #220786 ), #200788, .F. ) ;
#97295=EDGE_CURVE ( 'NONE', #123863, #9710, #184205, .T. ) ;
#97358=DIRECTION ( 'NONE',  ( 0.000000000000000000, 1.000000000000000000, -1.387778780781444413E-14 ) ) ;
#97379=ORIENTED_EDGE ( 'NONE', *, *, #146481, .F. ) ;
#97385=AXIS2_PLACEMENT_3D ( 'NONE', #164567, #165858, #65447 ) ;
#97386=CIRCLE ( 'NONE', #105765, 4.049999999999998046 ) ;
#97412=EDGE_CURVE ( 'NONE', #145174, #56292, #113300, .T. ) ;
#97420=DIRECTION ( 'NONE',  ( 1.000000000000000000, 0.000000000000000000, 0.000000000000000000 ) ) ;
#97453=DIRECTION ( 'NONE',  ( 0.000000000000000000, -7.116814260417660624E-15, 1.000000000000000000 ) ) ;
#97456=ADVANCED_FACE ( 'NONE', ( #188084 ), #88960, .F. ) ;
#97469=EDGE_CURVE ( 'NONE', #122358, #225207, #135790, .T. ) ;
#97480=CARTESIAN_POINT ( 'NONE',  ( 23.14999999999999503, 64.35000000001222986, -148.6731074845244507 ) ) ;
#97488=B_SPLINE_CURVE_WITH_KNOTS ( 'NONE', 3,
 ( #150157, #90138, #70633, #124171, #74495, #36643, #194422, #171038 ),
 .UNSPECIFIED., .F., .F.,
 ( 4, 2, 2, 4 ),
 ( 0.000000000000000000, 0.0001881495939909204459, 0.0002822243909863701521, 0.0003762991879818198583 ),
 .UNSPECIFIED. ) ;
#97502=CARTESIAN_POINT ( 'NONE',  ( 20.94999999999999929, 76.00000000001215028, -138.5231074845243313 ) ) ;
#97536=ORIENTED_EDGE ( 'NONE', *, *, #175999, .T. ) ;
#97543=CARTESIAN_POINT ( 'NONE',  ( 18.41832399655371688, 85.68240326668606599, -129.8662638644967728 ) ) ;
#97578=ORIENTED_EDGE ( 'NONE', *, *, #46308, .T. ) ;
#97601=CARTESIAN_POINT ( 'NONE',  ( 23.24999999999999645, 76.00000000001213607, -136.5231074845243313 ) ) ;
#97610=CIRCLE ( 'NONE', #76790, 11.64999999999999325 ) ;
#97632=CARTESIAN_POINT ( 'NONE',  ( 20.95203847575071521, 65.49893946073831330, -162.4560361359008596 ) ) ;
#97635=PLANE ( 'NONE',  #167816 ) ;
#97669=ORIENTED_EDGE ( 'NONE', *, *, #101550, .F. ) ;
#97685=DIRECTION ( 'NONE',  ( 0.000000000000000000, 6.938893903907030216E-14, -1.000000000000000000 ) ) ;
#97697=DIRECTION ( 'NONE',  ( 0.000000000000000000, 0.000000000000000000, -1.000000000000000000 ) ) ;
#97733=DIRECTION ( 'NONE',  ( 0.000000000000000000, -6.661338147750933721E-15, 1.000000000000000000 ) ) ;
#97782=DIRECTION ( 'NONE',  ( 1.000000000000000000, 0.000000000000000000, 0.000000000000000000 ) ) ;
#97799=CARTESIAN_POINT ( 'NONE',  ( 18.54148534481893407, 65.67467670974440352, -130.9531731826884879 ) ) ;
#97861=CARTESIAN_POINT ( 'NONE',  ( 21.14999999999999858, 87.65000000001236913, -170.0231074845242745 ) ) ;
#97870=ORIENTED_EDGE ( 'NONE', *, *, #53434, .F. ) ;
#97887=ORIENTED_EDGE ( 'NONE', *, *, #31816, .F. ) ;
#97900=CARTESIAN_POINT ( 'NONE',  ( -23.15000000000000213, 76.00000000001210765, -132.5231074845243313 ) ) ;
#97908=ORIENTED_EDGE ( 'NONE', *, *, #74505, .F. ) ;
#97910=DIRECTION ( 'NONE',  ( 1.000000000000000000, 0.000000000000000000, 0.000000000000000000 ) ) ;
#97951=ORIENTED_EDGE ( 'NONE', *, *, #171261, .F. ) ;
#97964=FACE_OUTER_BOUND ( 'NONE', #110264, .T. ) ;
#97965=CARTESIAN_POINT ( 'NONE',  ( 21.05193202509564543, 65.27606398031511503, -157.8505728811986728 ) ) ;
#97995=DIRECTION ( 'NONE',  ( 1.000000000000000000, 0.000000000000000000, 0.000000000000000000 ) ) ;
#98023=CARTESIAN_POINT ( 'NONE',  ( -18.59999999999999787, 77.16412189325330928, -128.8082593989527425 ) ) ;
#98078=CARTESIAN_POINT ( 'NONE',  ( 23.25000000000000000, 87.65000000001238334, -170.0231074845242745 ) ) ;
#98082=EDGE_CURVE ( 'NONE', #217454, #176291, #167858, .T. ) ;
#98111=ORIENTED_EDGE ( 'NONE', *, *, #231841, .T. ) ;
#98130=ADVANCED_FACE ( 'NONE', ( #140625 ), #178506, .T. ) ;
#98170=ADVANCED_FACE ( 'NONE', ( #61091 ), #220177, .F. ) ;
#98173=ORIENTED_EDGE ( 'NONE', *, *, #41436, .T. ) ;
#98174=DIRECTION ( 'NONE',  ( -0.000000000000000000, 0.9875055080513808203, -0.1575844902526395142 ) ) ;
#98271=EDGE_LOOP ( 'NONE', ( #184505, #206213, #209964, #73319, #61950 ) ) ;
#98295=DIRECTION ( 'NONE',  ( -1.000000000000000000, 0.000000000000000000, -0.000000000000000000 ) ) ;
#98310=AXIS2_PLACEMENT_3D ( 'NONE', #123571, #127421, #47860 ) ;
#98317=CIRCLE ( 'NONE', #56628, 0.09999999999998898659 ) ;
#98327=CYLINDRICAL_SURFACE ( 'NONE', #19351, 0.1000000000000028644 ) ;
#98333=ORIENTED_EDGE ( 'NONE', *, *, #32797, .T. ) ;
#98369=DIRECTION ( 'NONE',  ( 1.000000000000000000, -0.000000000000000000, 0.000000000000000000 ) ) ;
#98370=CARTESIAN_POINT ( 'NONE',  ( 21.11825140030056502, 75.99279637937949872, -176.4685150499438180 ) ) ;
#98402=CARTESIAN_POINT ( 'NONE',  ( -20.54999999999999716, 87.75000000001226397, -153.2731074845242745 ) ) ;
#98404=DIRECTION ( 'NONE',  ( 1.000000000000000000, 0.000000000000000000, 0.000000000000000000 ) ) ;
#98407=CARTESIAN_POINT ( 'NONE',  ( -18.59999999999999787, 76.00000000001213607, -136.5231074845243313 ) ) ;
#98414=CARTESIAN_POINT ( 'NONE',  ( -18.51991288638526711, 85.39243678968618667, -162.8798410805651429 ) ) ;
#98455=ORIENTED_EDGE ( 'NONE', *, *, #139117, .F. ) ;
#98465=CARTESIAN_POINT ( 'NONE',  ( 20.85000000000000142, 76.32388570108247450, -136.5655178952103768 ) ) ;
#98479=ORIENTED_EDGE ( 'NONE', *, *, #14512, .T. ) ;
#98480=EDGE_CURVE ( 'NONE', #176041, #140162, #179510, .T. ) ;
#98483=TOROIDAL_SURFACE ( 'NONE', #190136, 1.900000000000002576, 0.1000000000000000056 ) ;
#98490=EDGE_CURVE ( 'NONE', #138337, #59420, #77757, .T. ) ;
#98502=SPHERICAL_SURFACE ( 'NONE', #199355, 0.1000000000000000056 ) ;
#98562=CARTESIAN_POINT ( 'NONE',  ( 23.14999999999999858, 76.00000000001215028, -138.5231074845243313 ) ) ;
#98593=DIRECTION ( 'NONE',  ( 0.000000000000000000, -1.000000000000000000, -8.717686153663073805E-15 ) ) ;
#98613=ORIENTED_EDGE ( 'NONE', *, *, #11019, .T. ) ;
#98634=CARTESIAN_POINT ( 'NONE',  ( -23.15000000000000213, 76.00000000001237765, -170.0231074845243597 ) ) ;
#98665=FACE_OUTER_BOUND ( 'NONE', #91969, .T. ) ;
#98703=DIRECTION ( 'NONE',  ( 0.000000000000000000, -6.938893903907222067E-15, 1.000000000000000000 ) ) ;
#98716=DIRECTION ( 'NONE',  ( 0.000000000000000000, -1.000000000000000000, 0.000000000000000000 ) ) ;
#98723=CARTESIAN_POINT ( 'NONE',  ( -23.25000000000000000, 70.05000000001221849, -146.8288097895591875 ) ) ;
#98727=AXIS2_PLACEMENT_3D ( 'NONE', #187591, #68924, #87165 ) ;
#98733=ORIENTED_EDGE ( 'NONE', *, *, #251721, .T. ) ;
#98752=EDGE_CURVE ( 'NONE', #44711, #206438, #62967, .T. ) ;
#98787=EDGE_CURVE ( 'NONE', #28696, #60057, #13649, .T. ) ;
#98791=CARTESIAN_POINT ( 'NONE',  ( 18.59999999999999432, 74.73821383144729680, -161.9366085209788935 ) ) ;
#98795=ADVANCED_FACE ( 'NONE', ( #17492 ), #56588, .F. ) ;
#98806=CARTESIAN_POINT ( 'NONE',  ( -20.64999999999999858, 85.00000000001222134, -146.0170766071767332 ) ) ;
#98836=AXIS2_PLACEMENT_3D ( 'NONE', #215478, #277, #159378 ) ;
#98919=ORIENTED_EDGE ( 'NONE', *, *, #239231, .F. ) ;
#98921=AXIS2_PLACEMENT_3D ( 'NONE', #50603, #170629, #55711 ) ;
#98935=EDGE_CURVE ( 'NONE', #45573, #9997, #246318, .T. ) ;
#98953=DIRECTION ( 'NONE',  ( 1.000000000000000000, 0.000000000000000000, 0.000000000000000000 ) ) ;
#99001=ADVANCED_FACE ( 'NONE', ( #205101 ), #75649, .F. ) ;
#99016=VERTEX_POINT ( 'NONE', #43490 ) ;
#99019=CARTESIAN_POINT ( 'NONE',  ( -21.40925344232282512, 69.34148114062192292, -170.1220576731440417 ) ) ;
#99053=VERTEX_POINT ( 'NONE', #237219 ) ;
#99088=CARTESIAN_POINT ( 'NONE',  ( 18.50016250449482413, 65.70233904877132147, -131.0487410911965753 ) ) ;
#99165=DIRECTION ( 'NONE',  ( -1.000000000000000000, 0.000000000000000000, -0.000000000000000000 ) ) ;
#99197=AXIS2_PLACEMENT_3D ( 'NONE', #56899, #777, #215992 ) ;
#99230=EDGE_CURVE ( 'NONE', #203751, #22319, #200146, .T. ) ;
#99234=VECTOR ( 'NONE', #149044, 1000.000000000000114 ) ;
#99255=CARTESIAN_POINT ( 'NONE',  ( -20.85000000000000142, 69.15387683765952431, -132.7853812176745407 ) ) ;
#99277=VERTEX_POINT ( 'NONE', #70155 ) ;
#99359=CARTESIAN_POINT ( 'NONE',  ( -21.05000000000000071, 77.83534155023670564, -158.3679561919613548 ) ) ;
#99383=CIRCLE ( 'NONE', #245152, 12.97499999999999964 ) ;
#99384=VERTEX_POINT ( 'NONE', #247475 ) ;
#99412=CIRCLE ( 'NONE', #174499, 2.000000000000001776 ) ;
#99440=VECTOR ( 'NONE', #77381, 1000.000000000000000 ) ;
#99442=EDGE_LOOP ( 'NONE', ( #64868, #179765, #1260, #205436 ) ) ;
#99455=EDGE_CURVE ( 'NONE', #25682, #65247, #46003, .T. ) ;
#99488=VECTOR ( 'NONE', #62473, 1000.000000000000000 ) ;
#99493=CARTESIAN_POINT ( 'NONE',  ( -21.05000000000000071, 85.51932773110476660, -163.0501311079649440 ) ) ;
#99540=AXIS2_PLACEMENT_3D ( 'NONE', #17238, #14681, #117602 ) ;
#99543=CARTESIAN_POINT ( 'NONE',  ( 18.59999999999999787, 87.75000000001219291, -145.1731074845242802 ) ) ;
#99561=CIRCLE ( 'NONE', #74700, 0.09999999999999939493 ) ;
#99588=DIRECTION ( 'NONE',  ( 0.000000000000000000, -6.938893903907222067E-15, 1.000000000000000000 ) ) ;
#99596=ORIENTED_EDGE ( 'NONE', *, *, #25728, .T. ) ;
#99602=CARTESIAN_POINT ( 'NONE',  ( 20.94999999999999574, 77.25000000001232081, -162.0231074845243313 ) ) ;
#99648=CARTESIAN_POINT ( 'NONE',  ( -23.25000000000000000, 76.00000000001213607, -136.5231074845243313 ) ) ;
#99659=CARTESIAN_POINT ( 'NONE',  ( -21.14999999999999858, 69.45934304831114048, -170.0231074845243882 ) ) ;
#99682=ORIENTED_EDGE ( 'NONE', *, *, #250862, .F. ) ;
#99683=EDGE_LOOP ( 'NONE', ( #196473, #156345, #167009 ) ) ;
#99705=DIRECTION ( 'NONE',  ( 0.000000000000000000, -0.1298341882519953860, -0.9915357197604862671 ) ) ;
#99717=CARTESIAN_POINT ( 'NONE',  ( -18.60000000000000142, 85.32100840337361092, -162.7871692354464415 ) ) ;
#99751=DIRECTION ( 'NONE',  ( 0.000000000000000000, 0.000000000000000000, 1.000000000000000000 ) ) ;
#99753=DIRECTION ( 'NONE',  ( 1.000000000000000000, -1.836970198721029934E-16, -1.282749433769087582E-30 ) ) ;
#99766=CARTESIAN_POINT ( 'NONE',  ( 18.59999999999999076, 64.25000000001220712, -145.1731074845244507 ) ) ;
#99780=DIRECTION ( 'NONE',  ( 0.000000000000000000, -6.982962677686266711E-15, 1.000000000000000000 ) ) ;
#99796=AXIS2_PLACEMENT_3D ( 'NONE', #47608, #58517, #38997 ) ;
#99805=VERTEX_POINT ( 'NONE', #165063 ) ;
#99828=DIRECTION ( 'NONE',  ( -1.000000000000000000, 2.952720810173289112E-16, 2.061873921506763405E-30 ) ) ;
#99830=CARTESIAN_POINT ( 'NONE',  ( 23.14999999999999503, 64.35000000001228670, -157.8731074845244393 ) ) ;
#99840=EDGE_CURVE ( 'NONE', #23345, #34074, #146749, .T. ) ;
#99841=DIRECTION ( 'NONE',  ( -1.000000000000000000, 0.000000000000000000, 0.000000000000000000 ) ) ;
#99855=AXIS2_PLACEMENT_3D ( 'NONE', #98634, #58253, #73067 ) ;
#99882=ORIENTED_EDGE ( 'NONE', *, *, #161878, .F. ) ;
#99928=CARTESIAN_POINT ( 'NONE',  ( 21.05000000000000071, 87.65000000001215597, -139.5231074845243029 ) ) ;
#99939=ORIENTED_EDGE ( 'NONE', *, *, #20980, .F. ) ;
#99963=CARTESIAN_POINT ( 'NONE',  ( 20.94999999999999929, 69.55000000001230376, -160.0060803140843859 ) ) ;
#99965=CARTESIAN_POINT ( 'NONE',  ( -20.94999999999999929, 77.83534155023671985, -158.4679561919613491 ) ) ;
#99967=EDGE_CURVE ( 'NONE', #212994, #3049, #192334, .T. ) ;
#99981=VECTOR ( 'NONE', #36799, 1000.000000000000000 ) ;
#99983=( BOUNDED_SURFACE ( )  B_SPLINE_SURFACE ( 3, 2, ( 
 ( #193719, #232859, #17625 ),
 ( #34661, #179313, #158470 ),
 ( #115451, #155900, #77586 ),
 ( #54189, #15083, #237964 ),
 ( #174192, #197556, #18919 ),
 ( #153346, #98414, #218390 ),
 ( #154620, #39808, #198843 ),
 ( #213261, #20223, #99717 ) ),
 .UNSPECIFIED., .F., .F., .T. ) 
 B_SPLINE_SURFACE_WITH_KNOTS ( ( 4, 2, 2, 4 ),
 ( 3, 3 ),
 ( 0.0001723339234021429623, 0.0002782939632049933449, 0.0003842540030078437545, 0.0005961740826135445738 ),
 ( 0.000000000000000000, 1.000000000000000000 ),
 .UNSPECIFIED. ) 
 GEOMETRIC_REPRESENTATION_ITEM ( )  RATIONAL_B_SPLINE_SURFACE ( (
 ( 1.000000000000000000, 0.9504532311154486601, 1.000000000000000000),
 ( 1.000000000000000000, 0.9506023220705525079, 1.000000000000000000),
 ( 1.000000000000000000, 0.9395774818187484501, 1.000000000000000000),
 ( 1.000000000000000000, 0.9079328464641823748, 1.000000000000000000),
 ( 1.000000000000000000, 0.8875702416206456835, 1.000000000000000000),
 ( 1.000000000000000000, 0.8205919608039227153, 1.000000000000000000),
 ( 1.000000000000000000, 0.7666842783598419864, 1.000000000000000000),
 ( 1.000000000000000000, 0.7071067811865088260, 1.000000000000000000) ) ) 
 REPRESENTATION_ITEM ( '' )  SURFACE ( )  );
#99995=DIRECTION ( 'NONE',  ( 1.000000000000000000, 0.000000000000000000, 0.000000000000000000 ) ) ;
#100028=EDGE_LOOP ( 'NONE', ( #239348, #173580, #217902, #234514 ) ) ;
#100037=EDGE_LOOP ( 'NONE', ( #149374, #201270, #101353, #6784 ) ) ;
#100060=ORIENTED_EDGE ( 'NONE', *, *, #247730, .T. ) ;
#100075=CARTESIAN_POINT ( 'NONE',  ( 20.85000000000000142, 77.16412189325330928, -128.6082593989527254 ) ) ;
#100092=DIRECTION ( 'NONE',  ( -1.000000000000000000, 0.000000000000000000, -0.000000000000000000 ) ) ;
#100174=ORIENTED_EDGE ( 'NONE', *, *, #48729, .F. ) ;
#100207=AXIS2_PLACEMENT_3D ( 'NONE', #23997, #103485, #542 ) ;
#100211=AXIS2_PLACEMENT_3D ( 'NONE', #188522, #52852, #111560 ) ;
#100238=DIRECTION ( 'NONE',  ( 1.000000000000000000, -0.000000000000000000, 0.000000000000000000 ) ) ;
#100273=CARTESIAN_POINT ( 'NONE',  ( -18.54270223418606633, 85.62410550289501998, -129.7821724341168590 ) ) ;
#100275=LINE ( 'NONE', #177309, #191612 ) ;
#100297=DIRECTION ( 'NONE',  ( 0.000000000000000000, 0.000000000000000000, 1.000000000000000000 ) ) ;
#100312=CARTESIAN_POINT ( 'NONE',  ( -18.50000000000000000, 72.08710075277885210, -158.5412845115134246 ) ) ;
#100328=PLANE ( 'NONE',  #93170 ) ;
#100335=DIRECTION ( 'NONE',  ( 0.000000000000000000, -6.982962677686266711E-15, 1.000000000000000000 ) ) ;
#100346=CARTESIAN_POINT ( 'NONE',  ( 21.05000000000000071, 87.48912529308842068, -166.9231074845242802 ) ) ;
#100348=ORIENTED_EDGE ( 'NONE', *, *, #10641, .T. ) ;
#100352=ORIENTED_EDGE ( 'NONE', *, *, #40637, .T. ) ;
#100373=ADVANCED_FACE ( 'NONE', ( #67940 ), #28868, .T. ) ;
#100380=ORIENTED_EDGE ( 'NONE', *, *, #203043, .F. ) ;
#100388=EDGE_CURVE ( 'NONE', #69713, #188264, #75792, .T. ) ;
#100389=ORIENTED_EDGE ( 'NONE', *, *, #134969, .F. ) ;
#100581=ORIENTED_EDGE ( 'NONE', *, *, #197105, .F. ) ;
#100687=CARTESIAN_POINT ( 'NONE',  ( 20.94999999999999929, 77.83534155023671985, -158.4679561919613491 ) ) ;
#100745=CARTESIAN_POINT ( 'NONE',  ( -21.14999999999999858, 76.00000000001242029, -176.5637644362255969 ) ) ;
#100751=CARTESIAN_POINT ( 'NONE',  ( -18.50000000000000000, 66.75000000001223555, -148.6731074845244223 ) ) ;
#100770=CARTESIAN_POINT ( 'NONE',  ( 21.00000000000000000, 66.25000000001229239, -157.6731074845244223 ) ) ;
#100772=CARTESIAN_POINT ( 'NONE',  ( -18.57399277249657032, 65.66887361445355964, -130.9329845918269370 ) ) ;
#100783=ORIENTED_EDGE ( 'NONE', *, *, #222094, .F. ) ;
#100810=CARTESIAN_POINT ( 'NONE',  ( 20.95595624212450048, 65.37610879691814603, -162.3934745703977001 ) ) ;
#100886=CIRCLE ( 'NONE', #142608, 0.09999999999999939493 ) ;
#100912=AXIS2_PLACEMENT_3D ( 'NONE', #144931, #224476, #66704 ) ;
#100920=CARTESIAN_POINT ( 'NONE',  ( -18.41353343127310893, 85.50000000001232081, -162.9910380878245917 ) ) ;
#100938=VECTOR ( 'NONE', #121126, 1000.000000000000000 ) ;
#100946=DIRECTION ( 'NONE',  ( 0.000000000000000000, -7.147358527629766941E-15, 1.000000000000000000 ) ) ;
#100949=CIRCLE ( 'NONE', #167670, 11.74999999999999645 ) ;
#100982=AXIS2_PLACEMENT_3D ( 'NONE', #75988, #113822, #252052 ) ;
#100993=EDGE_CURVE ( 'NONE', #40059, #35313, #196947, .T. ) ;
#100994=ORIENTED_EDGE ( 'NONE', *, *, #127667, .T. ) ;
#101008=CARTESIAN_POINT ( 'NONE',  ( 21.05000000000000071, 85.00000000001222134, -145.9170766071767389 ) ) ;
#101020=AXIS2_PLACEMENT_3D ( 'NONE', #125901, #142880, #122069 ) ;
#101062=DIRECTION ( 'NONE',  ( -1.000000000000000000, 0.000000000000000000, -0.000000000000000000 ) ) ;
#101093=ORIENTED_EDGE ( 'NONE', *, *, #158665, .T. ) ;
#101128=CARTESIAN_POINT ( 'NONE',  ( 20.89878130938411616, 65.67252876774553272, -130.9457041994994881 ) ) ;
#101164=AXIS2_PLACEMENT_3D ( 'NONE', #222674, #79313, #238408 ) ;
#101173=EDGE_LOOP ( 'NONE', ( #191259, #31238, #200556, #44727 ) ) ;
#101179=ADVANCED_FACE ( 'NONE', ( #25032 ), #155301, .T. ) ;
#101185=EDGE_LOOP ( 'NONE', ( #82735, #169585, #236519, #171143 ) ) ;
#101193=DIRECTION ( 'NONE',  ( 0.9880948137434723000, -0.1538461538461484146, -1.074301950413233906E-15 ) ) ;
#101195=DIRECTION ( 'NONE',  ( 0.000000000000000000, -6.853228547068871147E-15, 1.000000000000000000 ) ) ;
#101225=VECTOR ( 'NONE', #38883, 1000.000000000000000 ) ;
#101260=DIRECTION ( 'NONE',  ( 1.000000000000000000, 0.000000000000000000, 0.000000000000000000 ) ) ;
#101261=ORIENTED_EDGE ( 'NONE', *, *, #176747, .F. ) ;
#101266=CARTESIAN_POINT ( 'NONE',  ( 21.04999999999999716, 69.70076908992551523, -170.1215449845244052 ) ) ;
#101280=LINE ( 'NONE', #102585, #173030 ) ;
#101346=CIRCLE ( 'NONE', #247137, 0.09999999999998898659 ) ;
#101353=ORIENTED_EDGE ( 'NONE', *, *, #111554, .F. ) ;
#101383=LINE ( 'NONE', #257889, #124391 ) ;
#101471=LINE ( 'NONE', #44118, #141284 ) ;
#101496=VERTEX_POINT ( 'NONE', #17013 ) ;
#101550=EDGE_CURVE ( 'NONE', #75757, #203324, #109643, .T. ) ;
#101567=DIRECTION ( 'NONE',  ( -1.000000000000000000, 0.000000000000000000, 0.000000000000000000 ) ) ;
#101572=CARTESIAN_POINT ( 'NONE',  ( -21.07928932188134041, 69.67148334361908724, -170.1220026301787982 ) ) ;
#101576=FACE_OUTER_BOUND ( 'NONE', #224502, .T. ) ;
#101581=CYLINDRICAL_SURFACE ( 'NONE', #246245, 0.09999999999999939493 ) ;
#101602=DIRECTION ( 'NONE',  ( 0.000000000000000000, 1.000000000000000000, 6.938893903907222067E-15 ) ) ;
#101627=AXIS2_PLACEMENT_3D ( 'NONE', #76691, #2278, #175826 ) ;
#101637=CARTESIAN_POINT ( 'NONE',  ( -18.50000000000000000, 64.25000000001246292, -181.7731074845244450 ) ) ;
#101647=DIRECTION ( 'NONE',  ( 0.000000000000000000, -2.775557561562888827E-14, 1.000000000000000000 ) ) ;
#101679=FACE_OUTER_BOUND ( 'NONE', #140874, .T. ) ;
#101692=CARTESIAN_POINT ( 'NONE',  ( -20.94999999999999929, 87.65000000001215597, -139.5231074845243029 ) ) ;
#101717=AXIS2_PLACEMENT_3D ( 'NONE', #103751, #223709, #226266 ) ;
#101756=CIRCLE ( 'NONE', #147589, 0.09999999999998898659 ) ;
#101807=ORIENTED_EDGE ( 'NONE', *, *, #54510, .T. ) ;
#101809=CARTESIAN_POINT ( 'NONE',  ( 18.47149038651510367, 85.67145715801882488, -129.8503211497859127 ) ) ;
#101813=CARTESIAN_POINT ( 'NONE',  ( 21.11701782572532693, 65.27839088400483547, -157.7780700550132167 ) ) ;
#101822=VECTOR ( 'NONE', #239322, 1000.000000000000000 ) ;
#101835=CIRCLE ( 'NONE', #247606, 0.09999999999998898659 ) ;
#101850=VERTEX_POINT ( 'NONE', #51936 ) ;
#101880=EDGE_LOOP ( 'NONE', ( #49840, #162052, #231792, #243496 ) ) ;
#101892=CARTESIAN_POINT ( 'NONE',  ( 20.21494484322215968, 66.69682926214346708, -161.6828422927512179 ) ) ;
#101907=VERTEX_POINT ( 'NONE', #91093 ) ;
#101929=CARTESIAN_POINT ( 'NONE',  ( -18.50000000000000000, 85.40000000001209912, -129.6410656363516125 ) ) ;
#101934=LINE ( 'NONE', #181524, #133078 ) ;
#101935=CARTESIAN_POINT ( 'NONE',  ( -23.25000000000000000, 71.85000000001224407, -148.7731074845243882 ) ) ;
#101945=ORIENTED_EDGE ( 'NONE', *, *, #250377, .T. ) ;
#101993=DIRECTION ( 'NONE',  ( -4.391705002472927119E-16, -1.000000000000000000, -7.026728003956683390E-15 ) ) ;
#102003=AXIS2_PLACEMENT_3D ( 'NONE', #214871, #131485, #194051 ) ;
#102010=CARTESIAN_POINT ( 'NONE',  ( -18.46907102845853998, 85.47372736477618105, -129.8470727457877558 ) ) ;
#102051=ORIENTED_EDGE ( 'NONE', *, *, #95341, .T. ) ;
#102070=ORIENTED_EDGE ( 'NONE', *, *, #73082, .F. ) ;
#102073=CARTESIAN_POINT ( 'NONE',  ( 22.39999999999999503, 64.25000000001237765, -170.1231074845244393 ) ) ;
#102079=AXIS2_PLACEMENT_3D ( 'NONE', #123699, #182393, #83247 ) ;
#102085=CARTESIAN_POINT ( 'NONE',  ( -23.15000000000000213, 71.85000000001245724, -181.7731074845243882 ) ) ;
#102156=CARTESIAN_POINT ( 'NONE',  ( -21.05439746398122836, 64.25000000001233502, -163.0331909970394406 ) ) ;
#102174=AXIS2_PLACEMENT_3D ( 'NONE', #242225, #144389, #29640 ) ;
#102191=FACE_OUTER_BOUND ( 'NONE', #138005, .T. ) ;
#102202=DIRECTION ( 'NONE',  ( 0.000000000000000000, 6.938893903907222067E-15, -1.000000000000000000 ) ) ;
#102215=ORIENTED_EDGE ( 'NONE', *, *, #183081, .F. ) ;
#102217=CARTESIAN_POINT ( 'NONE',  ( 20.84999999999998721, 65.66751761918692409, -130.9282609406112670 ) ) ;
#102224=CARTESIAN_POINT ( 'NONE',  ( -18.59999999999999787, 76.00000000001207923, -128.6231074845243540 ) ) ;
#102230=CARTESIAN_POINT ( 'NONE',  ( 21.04999999999999716, 75.90156250001210481, -176.3223383946166507 ) ) ;
#102232=EDGE_CURVE ( 'NONE', #29869, #65240, #29553, .T. ) ;
#102244=CARTESIAN_POINT ( 'NONE',  ( -21.05000000000000071, 76.00000000001240608, -174.3231074845243427 ) ) ;
#102268=VERTEX_POINT ( 'NONE', #244698 ) ;
#102269=FACE_OUTER_BOUND ( 'NONE', #99442, .T. ) ;
#102270=CARTESIAN_POINT ( 'NONE',  ( 18.59999999999999432, 74.27191306321800823, -183.1386724793566145 ) ) ;
#102324=CYLINDRICAL_SURFACE ( 'NONE', #117954, 0.1000000000000046685 ) ;
#102327=ORIENTED_EDGE ( 'NONE', *, *, #60059, .T. ) ;
#102339=CARTESIAN_POINT ( 'NONE',  ( 22.39999999999999503, 76.00000000001243450, -177.8138870828977360 ) ) ;
#102340=CARTESIAN_POINT ( 'NONE',  ( 21.14999999999998082, 87.75000000001237765, -170.0231074845242745 ) ) ;
#102401=EDGE_LOOP ( 'NONE', ( #11611, #36979, #48007, #81215 ) ) ;
#102409=CARTESIAN_POINT ( 'NONE',  ( -20.05000000000000426, 66.75000000001223555, -148.8731074845244393 ) ) ;
#102421=ORIENTED_EDGE ( 'NONE', *, *, #122282, .F. ) ;
#102430=CARTESIAN_POINT ( 'NONE',  ( -21.04999999999999716, 69.69257478044694665, -170.0062876161386782 ) ) ;
#102450=ORIENTED_EDGE ( 'NONE', *, *, #195079, .T. ) ;
#102472=CARTESIAN_POINT ( 'NONE',  ( 18.50000000000000000, 85.50000000001233502, -162.9910380878246201 ) ) ;
#102473=DIRECTION ( 'NONE',  ( 0.000000000000000000, -6.982962677686266711E-15, 1.000000000000000000 ) ) ;
#102491=LINE ( 'NONE', #199064, #113598 ) ;
#102492=EDGE_CURVE ( 'NONE', #209999, #97109, #180939, .T. ) ;
#102507=CARTESIAN_POINT ( 'NONE',  ( -23.25000000000000000, 64.35000000001228670, -157.8731074845244393 ) ) ;
#102508=ORIENTED_EDGE ( 'NONE', *, *, #75087, .T. ) ;
#102518=FACE_OUTER_BOUND ( 'NONE', #29315, .T. ) ;
#102553=EDGE_CURVE ( 'NONE', #39887, #201875, #68515, .T. ) ;
#102562=CARTESIAN_POINT ( 'NONE',  ( 21.05000000000000071, 76.00000000001237765, -170.0231074845243597 ) ) ;
#102571=CARTESIAN_POINT ( 'NONE',  ( -20.54999999999999716, 85.50000000001232081, -160.1291383618718385 ) ) ;
#102585=CARTESIAN_POINT ( 'NONE',  ( -21.14999999999999858, 87.75000000001237765, -170.0231074845242745 ) ) ;
#102594=CARTESIAN_POINT ( 'NONE',  ( 21.05543885634738643, 67.22422895316475433, -157.8387230138097266 ) ) ;
#102600=CARTESIAN_POINT ( 'NONE',  ( 20.94999999999999574, 77.16270174995034381, -162.0231074845243313 ) ) ;
#102634=ADVANCED_FACE ( 'NONE', ( #90133 ), #64417, .T. ) ;
#102646=VECTOR ( 'NONE', #245875, 1000.000000000000000 ) ;
#102661=B_SPLINE_CURVE_WITH_KNOTS ( 'NONE', 3,
 ( #181290, #1323, #63887, #143419, #237393, #238671, #80860, #160451, #58720, #39215 ),
 .UNSPECIFIED., .F., .F.,
 ( 4, 3, 3, 4 ),
 ( 0.000000000000000000, 0.0002000000000002785953, 0.001000000000045107602, 0.001967863649472123035 ),
 .UNSPECIFIED. ) ;
#102671=AXIS2_PLACEMENT_3D ( 'NONE', #256909, #78308, #198263 ) ;
#102682=DIRECTION ( 'NONE',  ( 1.000000000000000000, 0.000000000000000000, 0.000000000000000000 ) ) ;
#102688=CARTESIAN_POINT ( 'NONE',  ( -21.05000000000000071, 74.25000000001229239, -158.3535959266227451 ) ) ;
#102708=DIRECTION ( 'NONE',  ( 0.000000000000000000, 0.000000000000000000, 1.000000000000000000 ) ) ;
#102710=ORIENTED_EDGE ( 'NONE', *, *, #97412, .T. ) ;
#102717=DIRECTION ( 'NONE',  ( 1.000000000000000000, 0.000000000000000000, 0.000000000000000000 ) ) ;
#102724=CARTESIAN_POINT ( 'NONE',  ( 21.05000000000000071, 70.60000000001228670, -157.6178414656113205 ) ) ;
#102746=ORIENTED_EDGE ( 'NONE', *, *, #40528, .T. ) ;
#102751=CARTESIAN_POINT ( 'NONE',  ( -21.07928932188134041, 75.90110485435802445, -176.3516241409176644 ) ) ;
#102782=DIRECTION ( 'NONE',  ( 1.000000000000000000, 0.000000000000000000, 0.000000000000000000 ) ) ;
#102803=EDGE_LOOP ( 'NONE', ( #195744, #104505, #195728, #82752, #63583 ) ) ;
#102821=ORIENTED_EDGE ( 'NONE', *, *, #70519, .F. ) ;
#102848=AXIS2_PLACEMENT_3D ( 'NONE', #148066, #12426, #208056 ) ;
#102852=ORIENTED_EDGE ( 'NONE', *, *, #137499, .T. ) ;
#102863=DIRECTION ( 'NONE',  ( 1.000000000000000000, 0.000000000000000000, 0.000000000000000000 ) ) ;
#102866=CYLINDRICAL_SURFACE ( 'NONE', #118139, 0.1000000000000072220 ) ;
#102868=FACE_OUTER_BOUND ( 'NONE', #241329, .T. ) ;
#102910=DIRECTION ( 'NONE',  ( 1.000000000000000000, 0.000000000000000000, 0.000000000000000000 ) ) ;
#102940=CYLINDRICAL_SURFACE ( 'NONE', #74215, 0.09999999999999939493 ) ;
#102943=CARTESIAN_POINT ( 'NONE',  ( -20.54999999999999716, 68.75000000001223555, -148.8731074845244109 ) ) ;
#102975=ORIENTED_EDGE ( 'NONE', *, *, #35491, .F. ) ;
#102977=EDGE_LOOP ( 'NONE', ( #104981, #118748, #129364, #131330 ) ) ;
#103009=EDGE_CURVE ( 'NONE', #247434, #5863, #81310, .T. ) ;
#103019=AXIS2_PLACEMENT_3D ( 'NONE', #47444, #150441, #164854 ) ;
#103044=ORIENTED_EDGE ( 'NONE', *, *, #180106, .F. ) ;
#103064=DIRECTION ( 'NONE',  ( -1.000000000000000000, -0.000000000000000000, -0.000000000000000000 ) ) ;
#103068=EDGE_LOOP ( 'NONE', ( #37370, #172397, #79252, #143375 ) ) ;
#103086=SPHERICAL_SURFACE ( 'NONE', #227632, 0.1000000000000000056 ) ;
#103090=AXIS2_PLACEMENT_3D ( 'NONE', #231753, #73985, #132646 ) ;
#103096=ADVANCED_FACE ( 'NONE', ( #109394 ), #6329, .F. ) ;
#103114=ADVANCED_FACE ( 'NONE', ( #51983 ), #131536, .F. ) ;
#103141=CYLINDRICAL_SURFACE ( 'NONE', #1379, 0.1000000000000072220 ) ;
#103165=EDGE_CURVE ( 'NONE', #181798, #238125, #189506, .T. ) ;
#103171=TOROIDAL_SURFACE ( 'NONE', #140797, 11.65000000000000036, 0.1000000000000000056 ) ;
#103236=ORIENTED_EDGE ( 'NONE', *, *, #245113, .T. ) ;
#103244=DIRECTION ( 'NONE',  ( -0.7071067811865474617, 0.7071067811865474617, 5.142139384388980375E-15 ) ) ;
#103282=EDGE_LOOP ( 'NONE', ( #160746, #97951, #15807, #75942 ) ) ;
#103383=CARTESIAN_POINT ( 'NONE',  ( 18.59999999999999076, 65.50857864377491069, -145.1731074845244507 ) ) ;
#103400=DIRECTION ( 'NONE',  ( -1.000000000000000000, 0.000000000000000000, 0.000000000000000000 ) ) ;
#103404=AXIS2_PLACEMENT_3D ( 'NONE', #151689, #113808, #51238 ) ;
#103427=DIRECTION ( 'NONE',  ( -1.000000000000000000, 0.000000000000000000, -0.000000000000000000 ) ) ;
#103428=VERTEX_POINT ( 'NONE', #189922 ) ;
#103431=DIRECTION ( 'NONE',  ( 1.000000000000000000, 0.000000000000000000, 0.000000000000000000 ) ) ;
#103442=CARTESIAN_POINT ( 'NONE',  ( 21.14999999999999858, 76.00000000001237765, -170.0231074845243597 ) ) ;
#103447=EDGE_CURVE ( 'NONE', #103678, #132498, #28314, .T. ) ;
#103452=CARTESIAN_POINT ( 'NONE',  ( -20.94684162548487194, 64.25000000001233502, -163.1814634889771014 ) ) ;
#103485=DIRECTION ( 'NONE',  ( 1.000000000000000000, 0.000000000000000000, 0.000000000000000000 ) ) ;
#103507=CARTESIAN_POINT ( 'NONE',  ( -21.05000000000000071, 76.10000000001241460, -176.5637644362255969 ) ) ;
#103566=DIRECTION ( 'NONE',  ( 0.000000000000000000, 0.4930308989874980785, 0.8700118002898462599 ) ) ;
#103579=CARTESIAN_POINT ( 'NONE',  ( -20.64999999999999858, 74.07476635515241981, -149.2533510176504876 ) ) ;
#103611=ORIENTED_EDGE ( 'NONE', *, *, #201371, .T. ) ;
#103627=FACE_OUTER_BOUND ( 'NONE', #230717, .T. ) ;
#103628=ADVANCED_FACE ( 'NONE', ( #97187 ), #176794, .F. ) ;
#103629=AXIS2_PLACEMENT_3D ( 'NONE', #205332, #28034, #145373 ) ;
#103640=FACE_OUTER_BOUND ( 'NONE', #68872, .T. ) ;
#103660=DIRECTION ( 'NONE',  ( 0.000000000000000000, 0.000000000000000000, -1.000000000000000000 ) ) ;
#103665=DIRECTION ( 'NONE',  ( -1.000000000000000000, 2.952720810173289112E-16, 2.061873921506763405E-30 ) ) ;
#103671=DIRECTION ( 'NONE',  ( 0.000000000000000000, -1.000000000000000000, 0.000000000000000000 ) ) ;
#103678=VERTEX_POINT ( 'NONE', #222284 ) ;
#103714=EDGE_CURVE ( 'NONE', #127304, #247235, #10807, .T. ) ;
#103717=CARTESIAN_POINT ( 'NONE',  ( -20.96077737575351918, 64.37609936600742344, -143.3823155274181147 ) ) ;
#103720=DIRECTION ( 'NONE',  ( 1.000000000000000000, 0.000000000000000000, 0.000000000000000000 ) ) ;
#103730=ADVANCED_FACE ( 'NONE', ( #103627 ), #210157, .F. ) ;
#103751=CARTESIAN_POINT ( 'NONE',  ( 18.59999999999999076, 65.79142135624952914, -148.6731074845244223 ) ) ;
#103752=DIRECTION ( 'NONE',  ( 0.000000000000000000, -6.982962677686266711E-15, 1.000000000000000000 ) ) ;
#103803=EDGE_CURVE ( 'NONE', #208786, #60353, #90497, .T. ) ;
#103822=AXIS2_PLACEMENT_3D ( 'NONE', #229926, #133399, #212931 ) ;
#103828=DIRECTION ( 'NONE',  ( 0.000000000000000000, 0.000000000000000000, 1.000000000000000000 ) ) ;
#103847=DIRECTION ( 'NONE',  ( 1.000000000000000000, 0.000000000000000000, 0.000000000000000000 ) ) ;
#103854=CARTESIAN_POINT ( 'NONE',  ( 18.49999999999999289, 65.79142135624977072, -181.7731074845244450 ) ) ;
#103891=DIRECTION ( 'NONE',  ( 1.000000000000000000, 0.000000000000000000, 0.000000000000000000 ) ) ;
#103914=DIRECTION ( 'NONE',  ( 0.000000000000000000, 0.000000000000000000, 1.000000000000000000 ) ) ;
#103937=CARTESIAN_POINT ( 'NONE',  ( 22.57320508075687115, 64.25000000001237765, -170.0231074845244166 ) ) ;
#103939=DIRECTION ( 'NONE',  ( 0.000000000000000000, 0.000000000000000000, 1.000000000000000000 ) ) ;
#103954=EDGE_CURVE ( 'NONE', #172545, #165339, #168686, .T. ) ;
#103959=DIRECTION ( 'NONE',  ( 0.000000000000000000, 1.000000000000000000, 6.982962677686266711E-15 ) ) ;
#103967=DIRECTION ( 'NONE',  ( 0.000000000000000000, 0.4999999999999943379, 0.8660254037844420383 ) ) ;
#103975=LINE ( 'NONE', #182270, #24441 ) ;
#103979=CARTESIAN_POINT ( 'NONE',  ( -18.59999999999999787, 77.85161776048096272, -124.9199177649206689 ) ) ;
#104001=VECTOR ( 'NONE', #232775, 1000.000000000000000 ) ;
#104025=CARTESIAN_POINT ( 'NONE',  ( 21.05000000000000071, 87.48912529308822172, -139.6231074845242688 ) ) ;
#104031=CARTESIAN_POINT ( 'NONE',  ( -23.15000000000000213, 76.00000000001213607, -136.5231074845243313 ) ) ;
#104057=AXIS2_PLACEMENT_3D ( 'NONE', #2282, #41458, #143081 ) ;
#104106=VERTEX_POINT ( 'NONE', #25770 ) ;
#104128=CARTESIAN_POINT ( 'NONE',  ( 18.59999999999999076, 61.95000000001233076, -164.5094124137634708 ) ) ;
#104133=ADVANCED_FACE ( 'NONE', ( #183565 ), #64567, .F. ) ;
#104137=DIRECTION ( 'NONE',  ( -1.000000000000000000, 0.000000000000000000, 0.000000000000000000 ) ) ;
#104153=CARTESIAN_POINT ( 'NONE',  ( -21.05000000000000071, 74.83729825007431202, -161.9231074845243654 ) ) ;
#104180=AXIS2_PLACEMENT_3D ( 'NONE', #11790, #170891, #151292 ) ;
#104247=CARTESIAN_POINT ( 'NONE',  ( -2.995603634470891112E-16, 69.35000000001222986, -148.7731074845244166 ) ) ;
#104277=DIRECTION ( 'NONE',  ( 0.000000000000000000, -6.547589603894034005E-15, 1.000000000000000000 ) ) ;
#104282=CARTESIAN_POINT ( 'NONE',  ( 21.13461538461538325, 65.38541703798675542, -157.6731074845244223 ) ) ;
#104306=DIRECTION ( 'NONE',  ( 0.000000000000000000, -6.982962677686267499E-15, 1.000000000000000000 ) ) ;
#104316=DIRECTION ( 'NONE',  ( 0.000000000000000000, 6.982962677686267499E-15, -1.000000000000000000 ) ) ;
#104357=AXIS2_PLACEMENT_3D ( 'NONE', #203871, #23982, #146450 ) ;
#104381=CARTESIAN_POINT ( 'NONE',  ( 19.94784844284954417, 64.28691006698312549, -145.3209087672257454 ) ) ;
#104414=CARTESIAN_POINT ( 'NONE',  ( -18.59999999999999787, 72.08710075277885210, -158.5412845115134246 ) ) ;
#104427=AXIS2_PLACEMENT_3D ( 'NONE', #160484, #60058, #139579 ) ;
#104452=DIRECTION ( 'NONE',  ( 0.000000000000000000, 7.086529944415886769E-15, -1.000000000000000000 ) ) ;
#104483=VECTOR ( 'NONE', #222211, 1000.000000000000000 ) ;
#104491=CARTESIAN_POINT ( 'NONE',  ( -20.54999999999999716, 71.65000000001222702, -148.8731074845244109 ) ) ;
#104505=ORIENTED_EDGE ( 'NONE', *, *, #204809, .T. ) ;
#104522=FACE_OUTER_BOUND ( 'NONE', #90373, .T. ) ;
#104542=DIRECTION ( 'NONE',  ( 1.296989514748957922E-15, 0.9887567792719351711, -0.1495327102803594987 ) ) ;
#104548=ORIENTED_EDGE ( 'NONE', *, *, #139478, .T. ) ;
#104581=EDGE_LOOP ( 'NONE', ( #34704, #172989, #34123 ) ) ;
#104605=ORIENTED_EDGE ( 'NONE', *, *, #13951, .F. ) ;
#104608=LINE ( 'NONE', #47220, #229591 ) ;
#104659=ORIENTED_EDGE ( 'NONE', *, *, #14512, .F. ) ;
#104675=DIRECTION ( 'NONE',  ( 0.000000000000000000, 1.000000000000000000, 7.272083257015735086E-15 ) ) ;
#104689=CIRCLE ( 'NONE', #150533, 0.09999999999999938105 ) ;
#104719=CIRCLE ( 'NONE', #242121, 4.000000000000003553 ) ;
#104771=DIRECTION ( 'NONE',  ( -1.000000000000000000, 2.952720810173289112E-16, 2.061873921506763405E-30 ) ) ;
#104795=CARTESIAN_POINT ( 'NONE',  ( 20.94999999999999929, 87.29603075034764004, -166.9752083248604038 ) ) ;
#104810=VECTOR ( 'NONE', #232715, 1000.000000000000000 ) ;
#104843=EDGE_CURVE ( 'NONE', #246816, #132867, #139938, .T. ) ;
#104858=VERTEX_POINT ( 'NONE', #92821 ) ;
#104862=EDGE_CURVE ( 'NONE', #5558, #223147, #206408, .T. ) ;
#104935=CARTESIAN_POINT ( 'NONE',  ( -18.50000000000000000, 66.65000000001229807, -157.6731074845244223 ) ) ;
#104964=FACE_OUTER_BOUND ( 'NONE', #4338, .T. ) ;
#104981=ORIENTED_EDGE ( 'NONE', *, *, #161784, .F. ) ;
#104984=DIRECTION ( 'NONE',  ( 1.000000000000000000, -7.304098846218163263E-16, 4.217023435051626718E-16 ) ) ;
#104988=CIRCLE ( 'NONE', #234606, 11.64999999999999325 ) ;
#105011=CIRCLE ( 'NONE', #221745, 11.64999999999999325 ) ;
#105030=CARTESIAN_POINT ( 'NONE',  ( 23.14999999999999858, 70.40000000001222702, -148.9283735034374843 ) ) ;
#105047=CIRCLE ( 'NONE', #9235, 0.09999999999998898659 ) ;
#105069=ORIENTED_EDGE ( 'NONE', *, *, #177340, .T. ) ;
#105070=ORIENTED_EDGE ( 'NONE', *, *, #201617, .T. ) ;
#105084=AXIS2_PLACEMENT_3D ( 'NONE', #46229, #21554, #219730 ) ;
#105105=DIRECTION ( 'NONE',  ( 0.000000000000000000, 0.000000000000000000, 1.000000000000000000 ) ) ;
#105126=DIRECTION ( 'NONE',  ( -1.000000000000000000, 0.000000000000000000, -0.000000000000000000 ) ) ;
#105142=DIRECTION ( 'NONE',  ( 1.000000000000000000, 0.000000000000000000, 0.000000000000000000 ) ) ;
#105147=CARTESIAN_POINT ( 'NONE',  ( 21.10710606213542562, 67.22310597611910055, -157.7821109581250028 ) ) ;
#105162=FACE_OUTER_BOUND ( 'NONE', #232593, .T. ) ;
#105197=ORIENTED_EDGE ( 'NONE', *, *, #11192, .T. ) ;
#105201=CARTESIAN_POINT ( 'NONE',  ( 22.60000000000000142, 64.25043287652299284, -170.1239658536231616 ) ) ;
#105205=CARTESIAN_POINT ( 'NONE',  ( 21.05000000000000071, 76.00000000001213607, -136.5231074845243313 ) ) ;
#105233=DIRECTION ( 'NONE',  ( 0.000000000000000000, -6.467318590049456648E-15, 1.000000000000000000 ) ) ;
#105252=CARTESIAN_POINT ( 'NONE',  ( -20.94999999999999929, 74.75000000001232081, -162.0231074845243597 ) ) ;
#105268=CARTESIAN_POINT ( 'NONE',  ( 22.49999999999999645, 64.35042919246758686, -170.1231074845244393 ) ) ;
#105271=ORIENTED_EDGE ( 'NONE', *, *, #206818, .F. ) ;
#105289=CIRCLE ( 'NONE', #159515, 0.09999999999998898659 ) ;
#105299=ORIENTED_EDGE ( 'NONE', *, *, #211355, .F. ) ;
#105321=ORIENTED_EDGE ( 'NONE', *, *, #102232, .T. ) ;
#105326=CARTESIAN_POINT ( 'NONE',  ( 21.30740335185486245, 69.44334207798438285, -170.1220420103002482 ) ) ;
#105338=EDGE_CURVE ( 'NONE', #80723, #125708, #27751, .T. ) ;
#105345=CARTESIAN_POINT ( 'NONE',  ( -21.64999999999999858, 68.65000000001229807, -157.7731074845244166 ) ) ;
#105354=ORIENTED_EDGE ( 'NONE', *, *, #94695, .T. ) ;
#105375=AXIS2_PLACEMENT_3D ( 'NONE', #224656, #86408, #50817 ) ;
#105395=DIRECTION ( 'NONE',  ( 0.000000000000000000, -6.982962677686266711E-15, 1.000000000000000000 ) ) ;
#105474=ORIENTED_EDGE ( 'NONE', *, *, #208437, .F. ) ;
#105499=ORIENTED_EDGE ( 'NONE', *, *, #247698, .F. ) ;
#105516=EDGE_CURVE ( 'NONE', #15766, #160550, #89792, .T. ) ;
#105518=VERTEX_POINT ( 'NONE', #24565 ) ;
#105528=DIRECTION ( 'NONE',  ( 0.000000000000000000, -6.997203936713175802E-15, 1.000000000000000000 ) ) ;
#105568=CARTESIAN_POINT ( 'NONE',  ( 20.85000000000000142, 77.13501884592227498, -128.8061306010920362 ) ) ;
#105570=EDGE_CURVE ( 'NONE', #244761, #56847, #69427, .T. ) ;
#105575=CARTESIAN_POINT ( 'NONE',  ( -22.48660254037843487, 64.35000000001238618, -170.0731074845244279 ) ) ;
#105579=CARTESIAN_POINT ( 'NONE',  ( -21.14999999999999858, 75.90220970870363715, -176.2809220950004487 ) ) ;
#105592=DIRECTION ( 'NONE',  ( 1.000000000000000000, 0.000000000000000000, 0.000000000000000000 ) ) ;
#105639=DIRECTION ( 'NONE',  ( 0.000000000000000000, -0.9876197685951263461, 0.1568667991644794590 ) ) ;
#105659=ORIENTED_EDGE ( 'NONE', *, *, #250406, .F. ) ;
#105663=EDGE_CURVE ( 'NONE', #61430, #74964, #210560, .T. ) ;
#105666=ORIENTED_EDGE ( 'NONE', *, *, #128335, .F. ) ;
#105668=FACE_OUTER_BOUND ( 'NONE', #177837, .T. ) ;
#105723=EDGE_CURVE ( 'NONE', #186771, #229354, #61219, .T. ) ;
#105730=VECTOR ( 'NONE', #117000, 1000.000000000000000 ) ;
#105741=CARTESIAN_POINT ( 'NONE',  ( 21.05000000000000071, 75.90220970870363715, -176.2809220950004772 ) ) ;
#105765=AXIS2_PLACEMENT_3D ( 'NONE', #71203, #132440, #73779 ) ;
#105778=DIRECTION ( 'NONE',  ( -0.000000000000000000, 6.982962677686266711E-15, -1.000000000000000000 ) ) ;
#105796=CARTESIAN_POINT ( 'NONE',  ( 18.59999999999999076, 69.35000000001222986, -148.8731074845244109 ) ) ;
#105801=CIRCLE ( 'NONE', #72520, 0.5000000000000004441 ) ;
#105803=EDGE_LOOP ( 'NONE', ( #153005, #156326, #165328, #35621 ) ) ;
#105811=DIRECTION ( 'NONE',  ( 0.000000000000000000, 0.4999999999999088507, 0.8660254037844913322 ) ) ;
#105820=VERTEX_POINT ( 'NONE', #38350 ) ;
#105822=ORIENTED_EDGE ( 'NONE', *, *, #165972, .F. ) ;
#105860=CARTESIAN_POINT ( 'NONE',  ( -21.09107601085566230, 69.63612202465257894, -170.0624146492417879 ) ) ;
#105861=FACE_OUTER_BOUND ( 'NONE', #188807, .T. ) ;
#105866=FACE_OUTER_BOUND ( 'NONE', #79133, .T. ) ;
#105874=ORIENTED_EDGE ( 'NONE', *, *, #155138, .F. ) ;
#105878=AXIS2_PLACEMENT_3D ( 'NONE', #210455, #168797, #211740 ) ;
#105910=ORIENTED_EDGE ( 'NONE', *, *, #75615, .T. ) ;
#105948=DIRECTION ( 'NONE',  ( 0.000000000000000000, 0.000000000000000000, -1.000000000000000000 ) ) ;
#105964=ORIENTED_EDGE ( 'NONE', *, *, #198794, .T. ) ;
#105967=CARTESIAN_POINT ( 'NONE',  ( -20.85000000000000142, 68.97833521811203639, -132.8895420826271163 ) ) ;
#105970=AXIS2_PLACEMENT_3D ( 'NONE', #63848, #83376, #200793 ) ;
#105978=CIRCLE ( 'NONE', #131127, 0.1000000000000072220 ) ;
#105982=CIRCLE ( 'NONE', #239285, 0.09999999999998898659 ) ;
#105995=CARTESIAN_POINT ( 'NONE',  ( -20.54999999999999716, 85.50000000001222134, -146.4170766071767389 ) ) ;
#105996=ORIENTED_EDGE ( 'NONE', *, *, #200033, .F. ) ;
#106003=CIRCLE ( 'NONE', #214368, 0.09999999999999939493 ) ;
#106027=ORIENTED_EDGE ( 'NONE', *, *, #99455, .T. ) ;
#106070=CARTESIAN_POINT ( 'NONE',  ( -21.44999999999999929, 68.85000000001228670, -157.7731074845244166 ) ) ;
#106082=VERTEX_POINT ( 'NONE', #111157 ) ;
#106094=CARTESIAN_POINT ( 'NONE',  ( -20.54999999999999716, 68.75000000001230660, -157.7731074845244166 ) ) ;
#106131=ORIENTED_EDGE ( 'NONE', *, *, #93223, .F. ) ;
#106136=DIRECTION ( 'NONE',  ( 0.000000000000000000, -0.9654727137038715545, 0.2605042016806676242 ) ) ;
#106137=ORIENTED_EDGE ( 'NONE', *, *, #22622, .T. ) ;
#106151=ORIENTED_EDGE ( 'NONE', *, *, #3047, .T. ) ;
#106156=CARTESIAN_POINT ( 'NONE',  ( -20.64999999999999858, 76.00000000001227818, -157.0481074845243938 ) ) ;
#106157=EDGE_CURVE ( 'NONE', #61299, #133057, #223873, .T. ) ;
#106170=DIRECTION ( 'NONE',  ( -1.836970198721029934E-16, -1.000000000000000000, -6.982962677686266711E-15 ) ) ;
#106204=ADVANCED_FACE ( 'NONE', ( #57584 ), #60154, .T. ) ;
#106219=ORIENTED_EDGE ( 'NONE', *, *, #215653, .F. ) ;
#106266=VECTOR ( 'NONE', #203890, 1000.000000000000000 ) ;
#106272=EDGE_LOOP ( 'NONE', ( #143772, #179343, #203404, #247939 ) ) ;
#106295=CARTESIAN_POINT ( 'NONE',  ( 20.94999027547553894, 65.70673848566998743, -131.0638252334829588 ) ) ;
#106300=ORIENTED_EDGE ( 'NONE', *, *, #242456, .T. ) ;
#106307=DIRECTION ( 'NONE',  ( -1.000000000000000000, 0.000000000000000000, -0.000000000000000000 ) ) ;
#106311=CARTESIAN_POINT ( 'NONE',  ( 20.85000000000000142, 77.73670573947964613, -125.0056848969006182 ) ) ;
#106328=ORIENTED_EDGE ( 'NONE', *, *, #145019, .T. ) ;
#106329=DIRECTION ( 'NONE',  ( 0.000000000000000000, -1.000000000000000000, -7.105427357601001859E-15 ) ) ;
#106347=DIRECTION ( 'NONE',  ( 0.000000000000000000, 0.000000000000000000, -1.000000000000000000 ) ) ;
#106348=AXIS2_PLACEMENT_3D ( 'NONE', #47022, #126585, #27527 ) ;
#106350=CARTESIAN_POINT ( 'NONE',  ( 18.52928932188134326, 65.72071067813087097, -145.3145288407617386 ) ) ;
#106358=VERTEX_POINT ( 'NONE', #11781 ) ;
#106414=DIRECTION ( 'NONE',  ( 1.000000000000000000, 0.000000000000000000, 0.000000000000000000 ) ) ;
#106428=DIRECTION ( 'NONE',  ( 0.000000000000000000, 0.8660254037844420383, -0.4999999999999943379 ) ) ;
#106474=DIRECTION ( 'NONE',  ( -1.000000000000000000, -0.000000000000000000, -0.000000000000000000 ) ) ;
#106505=ORIENTED_EDGE ( 'NONE', *, *, #111760, .F. ) ;
#106513=ORIENTED_EDGE ( 'NONE', *, *, #138143, .T. ) ;
#106520=DIRECTION ( 'NONE',  ( -0.7071067811865214825, -0.7071067811865735520, 0.000000000000000000 ) ) ;
#106539=DIRECTION ( 'NONE',  ( -0.000000000000000000, 0.1350103645451974088, -0.9908441862701587999 ) ) ;
#106615=FACE_OUTER_BOUND ( 'NONE', #206662, .T. ) ;
#106624=ORIENTED_EDGE ( 'NONE', *, *, #98082, .F. ) ;
#106627=EDGE_CURVE ( 'NONE', #203324, #30979, #2439, .T. ) ;
#106674=TOROIDAL_SURFACE ( 'NONE', #169085, 0.4000000000000017431, 0.1000000000000000056 ) ;
#106676=ORIENTED_EDGE ( 'NONE', *, *, #108538, .F. ) ;
#106678=DIRECTION ( 'NONE',  ( 0.000000000000000000, 1.000000000000000000, 0.000000000000000000 ) ) ;
#106697=CARTESIAN_POINT ( 'NONE',  ( -20.54999999999999716, 76.00000000001213607, -136.5231074845243313 ) ) ;
#106706=CARTESIAN_POINT ( 'NONE',  ( 21.14999999999999858, 64.35000000001237197, -169.9231074845244507 ) ) ;
#106715=CARTESIAN_POINT ( 'NONE',  ( 20.77526135991770317, 67.06799098339197940, -161.5545389417991657 ) ) ;
#106741=AXIS2_PLACEMENT_3D ( 'NONE', #157127, #49342, #168050 ) ;
#106755=DIRECTION ( 'NONE',  ( 1.000000000000000000, 0.000000000000000000, 0.000000000000000000 ) ) ;
#106764=CARTESIAN_POINT ( 'NONE',  ( 18.59999999999999787, 77.83585931145570669, -125.0186683157258329 ) ) ;
#106857=DIRECTION ( 'NONE',  ( 0.000000000000000000, -2.775557561562888827E-14, 1.000000000000000000 ) ) ;
#106899=SHAPE_REPRESENTATION ( 'Injection Molded Chain Links 12', ( #2425 ), #81157 ) ;
#106952=VECTOR ( 'NONE', #54082, 1000.000000000000000 ) ;
#106957=ORIENTED_EDGE ( 'NONE', *, *, #64019, .T. ) ;
#106965=CARTESIAN_POINT ( 'NONE',  ( 20.94999999999999574, 74.83729825007431202, -161.9231074845243654 ) ) ;
#106991=CARTESIAN_POINT ( 'NONE',  ( -23.15000000000000213, 85.00000000001222134, -146.4170766071767389 ) ) ;
#107071=CARTESIAN_POINT ( 'NONE',  ( 23.24999999999999645, 79.90000000001214175, -136.5231074845243029 ) ) ;
#107083=CARTESIAN_POINT ( 'NONE',  ( 21.09813707148777340, 69.61493789427588297, -170.0544589840539231 ) ) ;
#107098=EDGE_LOOP ( 'NONE', ( #94909, #146162, #131552 ) ) ;
#107100=AXIS2_PLACEMENT_3D ( 'NONE', #240117, #1484, #83566 ) ;
#107124=EDGE_LOOP ( 'NONE', ( #130523, #15415, #14299, #96513 ) ) ;
#107174=DIRECTION ( 'NONE',  ( 0.000000000000000000, -0.6728971962617862346, 0.7397360091701815632 ) ) ;
#107175=FACE_OUTER_BOUND ( 'NONE', #241521, .T. ) ;
#107198=PRODUCT_DEFINITION_FORMATION_WITH_SPECIFIED_SOURCE ( 'ANY', '', #5496, .NOT_KNOWN. ) ;
#107207=ORIENTED_EDGE ( 'NONE', *, *, #84798, .T. ) ;
#107210=EDGE_CURVE ( 'NONE', #47267, #242166, #214451, .T. ) ;
#107214=DIRECTION ( 'NONE',  ( 1.000000000000000000, 0.000000000000000000, 0.000000000000000000 ) ) ;
#107219=CARTESIAN_POINT ( 'NONE',  ( -20.00857864376270001, 66.85000000001228670, -157.7731074845244166 ) ) ;
#107224=CIRCLE ( 'NONE', #148943, 0.1000000000000028644 ) ;
#107236=ORIENTED_EDGE ( 'NONE', *, *, #248474, .T. ) ;
#107247=AXIS2_PLACEMENT_3D ( 'NONE', #195942, #216759, #75976 ) ;
#107264=DIRECTION ( 'NONE',  ( 0.000000000000000000, -1.000000000000000000, -6.982962677686266711E-15 ) ) ;
#107282=CARTESIAN_POINT ( 'NONE',  ( 22.59999954896768770, 76.00882823225497020, -181.7736161585923469 ) ) ;
#107294=LINE ( 'NONE', #248088, #165884 ) ;
#107304=LINE ( 'NONE', #129446, #174696 ) ;
#107307=CYLINDRICAL_SURFACE ( 'NONE', #158025, 0.1000000000000106914 ) ;
#107343=CIRCLE ( 'NONE', #94874, 0.09999999999998898659 ) ;
#107385=FACE_OUTER_BOUND ( 'NONE', #88419, .T. ) ;
#107391=B_SPLINE_CURVE_WITH_KNOTS ( 'NONE', 3,
 ( #182683, #178850, #58834, #160558, #217911, #101809, #237511, #61435 ),
 .UNSPECIFIED., .F., .F.,
 ( 4, 2, 2, 4 ),
 ( 0.000000000000000000, 0.0002181133598169243877, 0.0003271700397253575520, 0.0004362267196337907705 ),
 .UNSPECIFIED. ) ;
#107407=B_SPLINE_CURVE_WITH_KNOTS ( 'NONE', 3,
 ( #177953, #100920, #257413, #220900, #160962, #158413, #39745, #240480, #237907, #59227 ),
 .UNSPECIFIED., .F., .F.,
 ( 4, 2, 2, 2, 4 ),
 ( 0.000000000000000000, 3.990160268011951094E-05, 7.980320536023902188E-05, 0.0001596064107204957434, 0.0003192128214409947935 ),
 .UNSPECIFIED. ) ;
#107432=CIRCLE ( 'NONE', #140756, 4.000000000000003553 ) ;
#107448=AXIS2_PLACEMENT_3D ( 'NONE', #26867, #8566, #106347 ) ;
#107456=ADVANCED_FACE ( 'NONE', ( #121137 ), #129250, .F. ) ;
#107459=CARTESIAN_POINT ( 'NONE',  ( -20.85000000000000142, 69.06610602788578035, -132.7374616501508342 ) ) ;
#107504=DIRECTION ( 'NONE',  ( 2.952720810173289112E-16, 1.000000000000000000, -6.088138035986627436E-46 ) ) ;
#107518=CIRCLE ( 'NONE', #166200, 0.09999999999999939493 ) ;
#107531=DIRECTION ( 'NONE',  ( 1.000000000000000000, 0.000000000000000000, 0.000000000000000000 ) ) ;
#107565=CARTESIAN_POINT ( 'NONE',  ( -20.85000000000000142, 77.16412189325330928, -128.6082593989527254 ) ) ;
#107590=ADVANCED_FACE ( 'NONE', ( #244893 ), #187518, .T. ) ;
#107603=CIRCLE ( 'NONE', #186746, 0.09999999999999939493 ) ;
#107605=ORIENTED_EDGE ( 'NONE', *, *, #126217, .T. ) ;
#107682=DIRECTION ( 'NONE',  ( 0.000000000000000000, -6.982962677686266711E-15, 1.000000000000000000 ) ) ;
#107700=DIRECTION ( 'NONE',  ( 0.000000000000000000, 0.000000000000000000, 1.000000000000000000 ) ) ;
#107710=AXIS2_PLACEMENT_3D ( 'NONE', #235920, #100238, #136822 ) ;
#107806=AXIS2_PLACEMENT_3D ( 'NONE', #30209, #131857, #109713 ) ;
#107813=CARTESIAN_POINT ( 'NONE',  ( 20.46382478191414833, 65.40137955871495024, -162.3452930151790099 ) ) ;
#107884=AXIS2_PLACEMENT_3D ( 'NONE', #211481, #76766, #255352 ) ;
#107890=CARTESIAN_POINT ( 'NONE',  ( -21.44999999999999929, 68.65000000001229807, -157.6731074845243938 ) ) ;
#107894=ADVANCED_FACE ( 'NONE', ( #36141 ), #68457, .F. ) ;
#107918=EDGE_CURVE ( 'NONE', #96638, #113005, #135906, .T. ) ;
#107951=ORIENTED_EDGE ( 'NONE', *, *, #113904, .F. ) ;
#107967=ORIENTED_EDGE ( 'NONE', *, *, #62543, .T. ) ;
#107984=EDGE_LOOP ( 'NONE', ( #100352, #100174, #174290, #162423 ) ) ;
#107988=CARTESIAN_POINT ( 'NONE',  ( 20.94999999999999574, 76.00000000001237765, -170.0231074845243597 ) ) ;
#108000=DIRECTION ( 'NONE',  ( -0.000000000000000000, 6.982962677686266711E-15, -1.000000000000000000 ) ) ;
#108009=DIRECTION ( 'NONE',  ( 0.000000000000000000, -7.172728831056617961E-15, 1.000000000000000000 ) ) ;
#108028=CARTESIAN_POINT ( 'NONE',  ( 20.54374330479327426, 65.49498968578932079, -162.2974238496363171 ) ) ;
#108031=DIRECTION ( 'NONE',  ( -0.000000000000000000, 1.000000000000000000, 6.982962677686267499E-15 ) ) ;
#108063=FACE_OUTER_BOUND ( 'NONE', #164165, .T. ) ;
#108116=ORIENTED_EDGE ( 'NONE', *, *, #159900, .F. ) ;
#108117=ORIENTED_EDGE ( 'NONE', *, *, #148858, .T. ) ;
#108125=CARTESIAN_POINT ( 'NONE',  ( 20.94999999999999929, 76.00000000001213607, -136.5231074845243313 ) ) ;
#108145=VECTOR ( 'NONE', #148736, 1000.000000000000000 ) ;
#108149=CARTESIAN_POINT ( 'NONE',  ( 20.94999999999999929, 85.50000000001222134, -146.4170766071767389 ) ) ;
#108172=EDGE_CURVE ( 'NONE', #194825, #216685, #76205, .T. ) ;
#108194=AXIS2_PLACEMENT_3D ( 'NONE', #33395, #60295, #15085 ) ;
#108206=ORIENTED_EDGE ( 'NONE', *, *, #51999, .T. ) ;
#108225=EDGE_CURVE ( 'NONE', #204905, #99384, #181903, .T. ) ;
#108252=VERTEX_POINT ( 'NONE', #1801 ) ;
#108264=VERTEX_POINT ( 'NONE', #242987 ) ;
#108314=ORIENTED_EDGE ( 'NONE', *, *, #257599, .F. ) ;
#108334=CARTESIAN_POINT ( 'NONE',  ( -20.94999999999999929, 76.00000000001216449, -140.5231074845243597 ) ) ;
#108348=CYLINDRICAL_SURFACE ( 'NONE', #232988, 0.1000000000000028644 ) ;
#108363=CARTESIAN_POINT ( 'NONE',  ( 20.85000000000000142, 87.65000000001214175, -136.5231074845242745 ) ) ;
#108367=ORIENTED_EDGE ( 'NONE', *, *, #117433, .F. ) ;
#108383=ORIENTED_EDGE ( 'NONE', *, *, #29301, .T. ) ;
#108392=FACE_OUTER_BOUND ( 'NONE', #168533, .T. ) ;
#108424=ORIENTED_EDGE ( 'NONE', *, *, #113262, .T. ) ;
#108442=CIRCLE ( 'NONE', #100211, 0.09999999999998898659 ) ;
#108501=ORIENTED_EDGE ( 'NONE', *, *, #103165, .T. ) ;
#108519=CYLINDRICAL_SURFACE ( 'NONE', #240642, 2.000000000000001776 ) ;
#108536=ADVANCED_FACE ( 'NONE', ( #149058 ), #109892, .T. ) ;
#108538=EDGE_CURVE ( 'NONE', #165339, #157651, #248528, .T. ) ;
#108549=ORIENTED_EDGE ( 'NONE', *, *, #46958, .T. ) ;
#108583=CYLINDRICAL_SURFACE ( 'NONE', #224163, 0.1000000000000028644 ) ;
#108584=DIRECTION ( 'NONE',  ( 0.000000000000000000, -1.000000000000000000, -6.982962677686265922E-15 ) ) ;
#108600=DIRECTION ( 'NONE',  ( 0.000000000000000000, -0.9908441862701420355, -0.1350103645453197554 ) ) ;
#108603=ORIENTED_EDGE ( 'NONE', *, *, #210341, .T. ) ;
#108632=EDGE_LOOP ( 'NONE', ( #80, #250536, #130346, #178658 ) ) ;
#108638=DIRECTION ( 'NONE',  ( 0.7071359030028288029, 0.000000000000000000, 0.7070776581708504427 ) ) ;
#108674=CYLINDRICAL_SURFACE ( 'NONE', #57628, 0.09999999999999939493 ) ;
#108676=AXIS2_PLACEMENT_3D ( 'NONE', #37924, #178732, #77015 ) ;
#108694=LINE ( 'NONE', #129550, #172003 ) ;
#108714=ORIENTED_EDGE ( 'NONE', *, *, #3047, .F. ) ;
#108723=VERTEX_POINT ( 'NONE', #123721 ) ;
#108729=PLANE ( 'NONE',  #95744 ) ;
#108742=ORIENTED_EDGE ( 'NONE', *, *, #52617, .F. ) ;
#108765=ORIENTED_EDGE ( 'NONE', *, *, #34464, .T. ) ;
#108786=CIRCLE ( 'NONE', #179724, 11.90000000000000746 ) ;
#108835=VECTOR ( 'NONE', #130145, 1000.000000000000114 ) ;
#108881=CARTESIAN_POINT ( 'NONE',  ( -21.05000000000000071, 64.25000000001220712, -143.3647081744215086 ) ) ;
#108893=CARTESIAN_POINT ( 'NONE',  ( -20.54999999999999716, 74.00000000001223555, -149.7477294072864709 ) ) ;
#108895=CARTESIAN_POINT ( 'NONE',  ( -23.15000000000000213, 76.00000000001213607, -136.5231074845243313 ) ) ;
#108901=CARTESIAN_POINT ( 'NONE',  ( 20.96428641294248862, 64.25000000001219291, -143.3482143065823777 ) ) ;
#108978=DIRECTION ( 'NONE',  ( 0.000000000000000000, -1.000000000000000000, 0.000000000000000000 ) ) ;
#109024=AXIS2_PLACEMENT_3D ( 'NONE', #175532, #78941, #154690 ) ;
#109035=CARTESIAN_POINT ( 'NONE',  ( 18.59999999999999076, 65.79142135624951493, -145.2731074845244450 ) ) ;
#109068=LINE ( 'NONE', #146898, #231287 ) ;
#109076=ADVANCED_FACE ( 'NONE', ( #6003 ), #187246, .F. ) ;
#109107=ORIENTED_EDGE ( 'NONE', *, *, #19582, .T. ) ;
#109114=FACE_OUTER_BOUND ( 'NONE', #157305, .T. ) ;
#109127=DIRECTION ( 'NONE',  ( -1.000000000000000000, 2.952720810173289112E-16, 2.061873921506763405E-30 ) ) ;
#109131=EDGE_CURVE ( 'NONE', #58292, #236311, #203109, .T. ) ;
#109133=CARTESIAN_POINT ( 'NONE',  ( -22.59999970745345976, 76.00935637733996941, -181.7736206921935889 ) ) ;
#109160=CARTESIAN_POINT ( 'NONE',  ( 20.85000000000000142, 68.92903212821327941, -132.7765432626560766 ) ) ;
#109171=ORIENTED_EDGE ( 'NONE', *, *, #207720, .T. ) ;
#109180=CIRCLE ( 'NONE', #171774, 0.09999999999999939493 ) ;
#109209=AXIS2_PLACEMENT_3D ( 'NONE', #235892, #54699, #136795 ) ;
#109211=CARTESIAN_POINT ( 'NONE',  ( 20.85000000000000142, 69.15387683765952431, -132.7853812176745407 ) ) ;
#109221=CYLINDRICAL_SURFACE ( 'NONE', #169128, 12.87499999999999822 ) ;
#109230=FACE_OUTER_BOUND ( 'NONE', #42783, .T. ) ;
#109250=EDGE_LOOP ( 'NONE', ( #91921, #234729, #246807, #250704 ) ) ;
#109253=DIRECTION ( 'NONE',  ( 1.000000000000000000, 0.000000000000000000, 0.000000000000000000 ) ) ;
#109260=DIRECTION ( 'NONE',  ( 0.000000000000000000, 0.000000000000000000, 1.000000000000000000 ) ) ;
#109275=DIRECTION ( 'NONE',  ( 1.000000000000000000, 0.000000000000000000, 0.000000000000000000 ) ) ;
#109302=ADVANCED_FACE ( 'NONE', ( #220891 ), #59217, .F. ) ;
#109316=CARTESIAN_POINT ( 'NONE',  ( -21.05000000000000071, 74.16465844978787914, -158.3679561919613832 ) ) ;
#109336=EDGE_CURVE ( 'NONE', #243465, #148976, #28178, .T. ) ;
#109394=FACE_OUTER_BOUND ( 'NONE', #84657, .T. ) ;
#109396=CARTESIAN_POINT ( 'NONE',  ( -23.15000000000000213, 87.75000000001216449, -139.6231074845242688 ) ) ;
#109416=VERTEX_POINT ( 'NONE', #157101 ) ;
#109418=CARTESIAN_POINT ( 'NONE',  ( 20.95346350065193519, 67.11282275083783588, -161.5113755374890445 ) ) ;
#109421=CARTESIAN_POINT ( 'NONE',  ( 18.49999999999999645, 77.36242903720540198, -128.6342262366031548 ) ) ;
#109423=CARTESIAN_POINT ( 'NONE',  ( 21.05000000000000071, 71.00000000001223555, -148.9283735034374843 ) ) ;
#109454=VERTEX_POINT ( 'NONE', #103507 ) ;
#109484=DIRECTION ( 'NONE',  ( 0.000000000000000000, 6.982962677686266711E-15, -1.000000000000000000 ) ) ;
#109498=VERTEX_POINT ( 'NONE', #166107 ) ;
#109527=EDGE_LOOP ( 'NONE', ( #858, #87480, #211487, #147389 ) ) ;
#109552=ORIENTED_EDGE ( 'NONE', *, *, #108172, .F. ) ;
#109554=DIRECTION ( 'NONE',  ( 1.000000000000000000, 0.000000000000000000, 0.000000000000000000 ) ) ;
#109573=DIRECTION ( 'NONE',  ( 0.000000000000000000, -6.467318590049456648E-15, 1.000000000000000000 ) ) ;
#109598=LINE ( 'NONE', #108334, #749 ) ;
#109601=EDGE_CURVE ( 'NONE', #208658, #222829, #211647, .T. ) ;
#109604=AXIS2_PLACEMENT_3D ( 'NONE', #38898, #118433, #257875 ) ;
#109612=DIRECTION ( 'NONE',  ( 0.000000000000000000, -6.938893903907222067E-15, 1.000000000000000000 ) ) ;
#109613=CARTESIAN_POINT ( 'NONE',  ( 21.93642651522410603, 68.67283376068658640, -170.0231074845243882 ) ) ;
#109624=EDGE_CURVE ( 'NONE', #141624, #19886, #107432, .T. ) ;
#109639=CARTESIAN_POINT ( 'NONE',  ( -21.14999999999999858, 76.00000000001242029, -176.5637644362255969 ) ) ;
#109643=CIRCLE ( 'NONE', #59737, 0.09999999999998898659 ) ;
#109652=DIRECTION ( 'NONE',  ( 0.000000000000000000, -7.056502275159890043E-15, 1.000000000000000000 ) ) ;
#109713=DIRECTION ( 'NONE',  ( 0.000000000000000000, -7.056502275159890832E-15, 1.000000000000000000 ) ) ;
#109724=VERTEX_POINT ( 'NONE', #175109 ) ;
#109755=EDGE_LOOP ( 'NONE', ( #211842, #206665, #239037, #110123, #251738 ) ) ;
#109764=ADVANCED_FACE ( 'NONE', ( #218008 ), #74344, .T. ) ;
#109770=ORIENTED_EDGE ( 'NONE', *, *, #1581, .F. ) ;
#109778=ORIENTED_EDGE ( 'NONE', *, *, #257453, .F. ) ;
#109794=VERTEX_POINT ( 'NONE', #56371 ) ;
#109811=ORIENTED_EDGE ( 'NONE', *, *, #144735, .T. ) ;
#109836=CARTESIAN_POINT ( 'NONE',  ( -23.25000000000000000, 87.65000000001215597, -139.5231074845243029 ) ) ;
#109859=CYLINDRICAL_SURFACE ( 'NONE', #124692, 11.74999999999999645 ) ;
#109875=VERTEX_POINT ( 'NONE', #6682 ) ;
#109889=ORIENTED_EDGE ( 'NONE', *, *, #180856, .F. ) ;
#109892=CYLINDRICAL_SURFACE ( 'NONE', #148599, 7.899999999999990585 ) ;
#109911=ADVANCED_FACE ( 'NONE', ( #240179 ), #61534, .T. ) ;
#110009=DIRECTION ( 'NONE',  ( 0.000000000000000000, 7.147358527629766941E-15, -1.000000000000000000 ) ) ;
#110022=AXIS2_PLACEMENT_3D ( 'NONE', #50511, #131355, #110506 ) ;
#110034=VECTOR ( 'NONE', #128018, 1000.000000000000000 ) ;
#110037=ORIENTED_EDGE ( 'NONE', *, *, #57895, .F. ) ;
#110083=ORIENTED_EDGE ( 'NONE', *, *, #20975, .F. ) ;
#110123=ORIENTED_EDGE ( 'NONE', *, *, #71140, .T. ) ;
#110137=TOROIDAL_SURFACE ( 'NONE', #35360, 11.65000000000000036, 0.1000000000000000056 ) ;
#110153=DIRECTION ( 'NONE',  ( 0.000000000000000000, 1.000000000000000000, 0.000000000000000000 ) ) ;
#110174=CARTESIAN_POINT ( 'NONE',  ( 18.49999999999999645, 76.00000000001213607, -136.5231074845243313 ) ) ;
#110182=CARTESIAN_POINT ( 'NONE',  ( 20.85000000000000142, 64.25000000001219291, -143.3069731475025037 ) ) ;
#110256=EDGE_LOOP ( 'NONE', ( #243318, #190320, #127440, #203907 ) ) ;
#110261=DIRECTION ( 'NONE',  ( 0.000000000000000000, 0.000000000000000000, -1.000000000000000000 ) ) ;
#110264=EDGE_LOOP ( 'NONE', ( #168623, #163968, #179771 ) ) ;
#110274=CIRCLE ( 'NONE', #1925, 0.09999999999998898659 ) ;
#110284=DIRECTION ( 'NONE',  ( 0.000000000000000000, 0.000000000000000000, 1.000000000000000000 ) ) ;
#110321=AXIS2_PLACEMENT_3D ( 'NONE', #80975, #161843, #160557 ) ;
#110338=ORIENTED_EDGE ( 'NONE', *, *, #135727, .T. ) ;
#110357=B_SPLINE_CURVE_WITH_KNOTS ( 'NONE', 3,
 ( #210838, #115580, #92166, #189992 ),
 .UNSPECIFIED., .F., .F.,
 ( 4, 4 ),
 ( 0.000000000000000000, 0.0001048066582182725969 ),
 .UNSPECIFIED. ) ;
#110361=DIRECTION ( 'NONE',  ( 0.000000000000000000, 0.4999999999999608646, -0.8660254037844612451 ) ) ;
#110381=( BOUNDED_SURFACE ( )  B_SPLINE_SURFACE ( 3, 2, ( 
 ( #40827, #61642, #244119 ),
 ( #82455, #145013, #43371 ),
 ( #241561, #163320, #204978 ),
 ( #141185, #224555, #45928 ),
 ( #223269, #25110, #44653 ),
 ( #26377, #185446, #42105 ) ),
 .UNSPECIFIED., .F., .F., .T. ) 
 B_SPLINE_SURFACE_WITH_KNOTS ( ( 4, 2, 4 ),
 ( 3, 3 ),
 ( 0.0001381104793128061785, 0.0002947094729387477754, 0.0004513084665646893722 ),
 ( 0.000000000000000000, 1.000000000000000000 ),
 .UNSPECIFIED. ) 
 GEOMETRIC_REPRESENTATION_ITEM ( )  RATIONAL_B_SPLINE_SURFACE ( (
 ( 1.000000000000000000, 0.7071067811865494601, 1.000000000000000000),
 ( 1.000000000000000000, 0.6919563088097517856, 1.000000000000000000),
 ( 1.000000000000000000, 0.6959445945719651139, 1.000000000000000000),
 ( 1.000000000000000000, 0.7137882985310910477, 1.000000000000000000),
 ( 1.000000000000000000, 0.7257496306098256689, 1.000000000000000000),
 ( 1.000000000000000000, 0.7250110520819876836, 1.000000000000000000) ) ) 
 REPRESENTATION_ITEM ( '' )  SURFACE ( )  );
#110408=CARTESIAN_POINT ( 'NONE',  ( 18.59999999999999432, 74.36282728704190959, -158.4409541190523498 ) ) ;
#110416=CARTESIAN_POINT ( 'NONE',  ( 20.94999999999999929, 70.50000000001223555, -148.9283735034374843 ) ) ;
#110426=CARTESIAN_POINT ( 'NONE',  ( -22.39999999999999858, 76.10085836911117951, -181.7726746080137445 ) ) ;
#110495=VERTEX_POINT ( 'NONE', #102244 ) ;
#110501=CARTESIAN_POINT ( 'NONE',  ( -18.50000000000000000, 66.65000000001229807, -157.8731074845244393 ) ) ;
#110506=DIRECTION ( 'NONE',  ( 1.000000000000000000, 0.000000000000000000, 0.000000000000000000 ) ) ;
#110522=VECTOR ( 'NONE', #149341, 1000.000000000000000 ) ;
#110549=DIRECTION ( 'NONE',  ( 0.000000000000000000, -0.9908441862701610203, 0.1350103645451807555 ) ) ;
#110566=CARTESIAN_POINT ( 'NONE',  ( 20.94999999999999929, 85.40000000001221281, -146.4170766071767389 ) ) ;
#110571=CARTESIAN_POINT ( 'NONE',  ( 23.24999999999999645, 76.00000000001213607, -136.5231074845243313 ) ) ;
#110588=CARTESIAN_POINT ( 'NONE',  ( -18.50000000000000355, 77.26327546522934142, -128.6212428177779543 ) ) ;
#110622=CARTESIAN_POINT ( 'NONE',  ( -23.25000000000000000, 77.25000000001209344, -128.7226267301092548 ) ) ;
#110645=ORIENTED_EDGE ( 'NONE', *, *, #132398, .T. ) ;
#110652=VECTOR ( 'NONE', #253742, 1000.000000000000000 ) ;
#110683=CIRCLE ( 'NONE', #164673, 11.75000000000001066 ) ;
#110690=ORIENTED_EDGE ( 'NONE', *, *, #46532, .F. ) ;
#110709=DIRECTION ( 'NONE',  ( 0.7071359030028113724, 0.000000000000000000, -0.7070776581708677622 ) ) ;
#110724=CIRCLE ( 'NONE', #73158, 0.1000000000000118433 ) ;
#110759=DIRECTION ( 'NONE',  ( 0.000000000000000000, 6.982962677686266711E-15, -1.000000000000000000 ) ) ;
#110764=ADVANCED_FACE ( 'NONE', ( #5280 ), #228225, .T. ) ;
#110806=ORIENTED_EDGE ( 'NONE', *, *, #75951, .F. ) ;
#110836=CARTESIAN_POINT ( 'NONE',  ( -18.59999999999999787, 85.50000000001229239, -157.8731074845242972 ) ) ;
#110846=AXIS2_PLACEMENT_3D ( 'NONE', #82888, #140316, #41267 ) ;
#110857=AXIS2_PLACEMENT_3D ( 'NONE', #220613, #221861, #241461 ) ;
#110870=DIRECTION ( 'NONE',  ( -6.938893903907222067E-15, -1.000000000000000000, -6.982962677686266711E-15 ) ) ;
#110877=DIRECTION ( 'NONE',  ( 1.000000000000000000, 0.000000000000000000, 0.000000000000000000 ) ) ;
#110878=CARTESIAN_POINT ( 'NONE',  ( 20.04142135623730070, 64.25000000001220712, -145.3731074845244393 ) ) ;
#110891=EDGE_CURVE ( 'NONE', #54225, #86886, #120110, .T. ) ;
#110906=CARTESIAN_POINT ( 'NONE',  ( 22.39999999999999503, 68.20922040163900135, -170.0231074845243882 ) ) ;
#110939=VERTEX_POINT ( 'NONE', #34206 ) ;
#110969=ORIENTED_EDGE ( 'NONE', *, *, #240057, .T. ) ;
#111014=AXIS2_PLACEMENT_3D ( 'NONE', #138927, #114270, #253762 ) ;
#111051=ORIENTED_EDGE ( 'NONE', *, *, #57280, .T. ) ;
#111065=LINE ( 'NONE', #92775, #113051 ) ;
#111108=ORIENTED_EDGE ( 'NONE', *, *, #224821, .T. ) ;
#111129=CARTESIAN_POINT ( 'NONE',  ( -21.70464131381649509, 68.90464198104452009, -170.0231074845243882 ) ) ;
#111147=ORIENTED_EDGE ( 'NONE', *, *, #243850, .T. ) ;
#111149=TOROIDAL_SURFACE ( 'NONE', #211114, 12.97499999999999609, 0.1000000000000000056 ) ;
#111157=CARTESIAN_POINT ( 'NONE',  ( -18.50000000000000000, 74.13328508995498112, -158.2704322382423641 ) ) ;
#111158=ORIENTED_EDGE ( 'NONE', *, *, #12227, .F. ) ;
#111182=DIRECTION ( 'NONE',  ( -1.000000000000000000, 2.952720810173289112E-16, 2.061873921506763405E-30 ) ) ;
#111187=VECTOR ( 'NONE', #153181, 1000.000000000000000 ) ;
#111197=EDGE_CURVE ( 'NONE', #176651, #223292, #246493, .T. ) ;
#111233=CARTESIAN_POINT ( 'NONE',  ( -20.94999999999999929, 64.40000000001234071, -163.0949042542488883 ) ) ;
#111256=CARTESIAN_POINT ( 'NONE',  ( 21.53699400380727269, 69.21228820682173932, -170.0231074845244166 ) ) ;
#111307=EDGE_CURVE ( 'NONE', #59389, #77760, #89978, .T. ) ;
#111309=CARTESIAN_POINT ( 'NONE',  ( 18.59999999999999076, 64.35000000001220144, -145.1731074845244507 ) ) ;
#111314=DIRECTION ( 'NONE',  ( 1.000000000000000000, 0.000000000000000000, 0.000000000000000000 ) ) ;
#111322=CYLINDRICAL_SURFACE ( 'NONE', #503, 11.80000000000000426 ) ;
#111363=LINE ( 'NONE', #168815, #178354 ) ;
#111369=CARTESIAN_POINT ( 'NONE',  ( 23.14999999999999858, 76.00000000001216449, -140.5231074845243597 ) ) ;
#111378=CIRCLE ( 'NONE', #177490, 0.09999999999999939493 ) ;
#111395=ORIENTED_EDGE ( 'NONE', *, *, #132292, .F. ) ;
#111399=ORIENTED_EDGE ( 'NONE', *, *, #23240, .F. ) ;
#111468=ORIENTED_EDGE ( 'NONE', *, *, #16643, .F. ) ;
#111478=CARTESIAN_POINT ( 'NONE',  ( 21.05000000000000071, 64.25000000001219291, -143.3647081744214802 ) ) ;
#111481=AXIS2_PLACEMENT_3D ( 'NONE', #219048, #18295, #161682 ) ;
#111487=AXIS2_PLACEMENT_3D ( 'NONE', #48930, #247125, #68509 ) ;
#111495=VERTEX_POINT ( 'NONE', #83228 ) ;
#111501=EDGE_CURVE ( 'NONE', #20561, #36642, #91224, .T. ) ;
#111520=DIRECTION ( 'NONE',  ( 0.000000000000000000, 6.997203936713175802E-15, -1.000000000000000000 ) ) ;
#111529=VERTEX_POINT ( 'NONE', #217610 ) ;
#111554=EDGE_CURVE ( 'NONE', #7639, #199740, #174479, .T. ) ;
#111560=DIRECTION ( 'NONE',  ( -3.469446951953995998E-14, 0.000000000000000000, -1.000000000000000000 ) ) ;
#111561=DIRECTION ( 'NONE',  ( -0.000000000000000000, 1.000000000000000000, 6.982962677686266711E-15 ) ) ;
#111564=FACE_OUTER_BOUND ( 'NONE', #150605, .T. ) ;
#111600=EDGE_CURVE ( 'NONE', #71592, #81073, #66077, .T. ) ;
#111602=( NAMED_UNIT ( * ) SI_UNIT ( $, .STERADIAN. ) SOLID_ANGLE_UNIT ( ) );
#111625=CARTESIAN_POINT ( 'NONE',  ( 20.85000000000000142, 77.83585931145570669, -125.0186683157258329 ) ) ;
#111628=EDGE_LOOP ( 'NONE', ( #252112, #52086, #79618, #205190 ) ) ;
#111630=DIRECTION ( 'NONE',  ( -1.836970198721029934E-16, -1.000000000000000000, -6.982962677686266711E-15 ) ) ;
#111636=CARTESIAN_POINT ( 'NONE',  ( -20.88420186297724612, 65.66974365629688748, -130.9360145562605169 ) ) ;
#111701=CARTESIAN_POINT ( 'NONE',  ( -22.48970261584618058, 64.35000000001238618, -170.0784769727418393 ) ) ;
#111703=DIRECTION ( 'NONE',  ( 0.000000000000000000, 0.000000000000000000, -1.000000000000000000 ) ) ;
#111746=AXIS2_PLACEMENT_3D ( 'NONE', #116357, #238859, #77202 ) ;
#111760=EDGE_CURVE ( 'NONE', #149556, #174107, #78757, .T. ) ;
#111819=ADVANCED_FACE ( 'NONE', ( #219555 ), #96592, .T. ) ;
#111825=ORIENTED_EDGE ( 'NONE', *, *, #211593, .T. ) ;
#111850=VERTEX_POINT ( 'NONE', #65625 ) ;
#111858=DIRECTION ( 'NONE',  ( -1.000000000000000000, -0.000000000000000000, -0.000000000000000000 ) ) ;
#111896=CIRCLE ( 'NONE', #66075, 0.5000000000000004441 ) ;
#111916=EDGE_CURVE ( 'NONE', #249154, #1901, #237149, .T. ) ;
#111926=CARTESIAN_POINT ( 'NONE',  ( 21.07928932188134397, 75.90110485435802445, -176.3516241409176644 ) ) ;
#111934=DIRECTION ( 'NONE',  ( 0.000000000000000000, 0.000000000000000000, 1.000000000000000000 ) ) ;
#111970=CARTESIAN_POINT ( 'NONE',  ( 18.59999999999999432, 85.48068669529105534, -129.5819923157664562 ) ) ;
#111987=DIRECTION ( 'NONE',  ( 1.000000000000000000, -3.265361837132813093E-16, -2.280189983783949500E-30 ) ) ;
#111992=CARTESIAN_POINT ( 'NONE',  ( -21.45000000000000284, 68.29142135624960019, -157.6731074845243938 ) ) ;
#112040=ORIENTED_EDGE ( 'NONE', *, *, #216492, .F. ) ;
#112066=ORIENTED_EDGE ( 'NONE', *, *, #172255, .T. ) ;
#112087=SPHERICAL_SURFACE ( 'NONE', #146578, 0.1000000000000000056 ) ;
#112103=EDGE_LOOP ( 'NONE', ( #221699, #25554, #97669, #7299 ) ) ;
#112125=VERTEX_POINT ( 'NONE', #17242 ) ;
#112127=EDGE_CURVE ( 'NONE', #157651, #67356, #212409, .T. ) ;
#112163=VERTEX_POINT ( 'NONE', #24950 ) ;
#112166=ORIENTED_EDGE ( 'NONE', *, *, #47966, .T. ) ;
#112183=DIRECTION ( 'NONE',  ( -1.000000000000000000, -0.000000000000000000, -0.000000000000000000 ) ) ;
#112184=CARTESIAN_POINT ( 'NONE',  ( -18.47140463609786210, 85.67147468523300802, -129.8503470262502049 ) ) ;
#112190=AXIS2_PLACEMENT_3D ( 'NONE', #46982, #168286, #6587 ) ;
#112234=DIRECTION ( 'NONE',  ( 1.000000000000000000, 0.000000000000000000, 0.000000000000000000 ) ) ;
#112237=EDGE_CURVE ( 'NONE', #31671, #30979, #245532, .T. ) ;
#112247=CARTESIAN_POINT ( 'NONE',  ( 21.08134388332232234, 69.66531941949442341, -170.0989264020314522 ) ) ;
#112252=EDGE_CURVE ( 'NONE', #14224, #222470, #121492, .T. ) ;
#112264=ORIENTED_EDGE ( 'NONE', *, *, #158843, .T. ) ;
#112269=VECTOR ( 'NONE', #94474, 1000.000000000000000 ) ;
#112287=ORIENTED_EDGE ( 'NONE', *, *, #101550, .T. ) ;
#112312=AXIS2_PLACEMENT_3D ( 'NONE', #215792, #157146, #52873 ) ;
#112329=CYLINDRICAL_SURFACE ( 'NONE', #147854, 0.09999999999999939493 ) ;
#112383=CARTESIAN_POINT ( 'NONE',  ( 20.94999999999999574, 87.65000000001235492, -167.1231074845242688 ) ) ;
#112393=ADVANCED_FACE ( 'NONE', ( #146147 ), #41714, .T. ) ;
#112426=CARTESIAN_POINT ( 'NONE',  ( 18.40000000000000213, 85.50000000001236344, -163.0237453873441780 ) ) ;
#112434=DIRECTION ( 'NONE',  ( -0.000000000000000000, 6.982962677686266711E-15, -1.000000000000000000 ) ) ;
#112448=VERTEX_POINT ( 'NONE', #78157 ) ;
#112456=EDGE_CURVE ( 'NONE', #230504, #73243, #254222, .T. ) ;
#112459=SURFACE_STYLE_USAGE ( .BOTH. , #214115 ) ;
#112478=FACE_OUTER_BOUND ( 'NONE', #17715, .T. ) ;
#112479=DIRECTION ( 'NONE',  ( 0.000000000000000000, -6.982962677686266711E-15, 1.000000000000000000 ) ) ;
#112489=ORIENTED_EDGE ( 'NONE', *, *, #245032, .T. ) ;
#112492=LINE ( 'NONE', #214147, #148676 ) ;
#112511=FACE_OUTER_BOUND ( 'NONE', #234956, .T. ) ;
#112536=CARTESIAN_POINT ( 'NONE',  ( -18.59999999999999787, 64.25000000001222134, -148.7731074845244450 ) ) ;
#112605=DIRECTION ( 'NONE',  ( 0.000000000000000000, -7.487053152578134969E-15, 1.000000000000000000 ) ) ;
#112638=CARTESIAN_POINT ( 'NONE',  ( 21.05000000000000071, 84.73084112150763758, -160.4250327655399531 ) ) ;
#112678=AXIS2_PLACEMENT_3D ( 'NONE', #8861, #145782, #222753 ) ;
#112698=ORIENTED_EDGE ( 'NONE', *, *, #126416, .T. ) ;
#112702=EDGE_LOOP ( 'NONE', ( #92813, #31406, #194175, #82373 ) ) ;
#112732=CARTESIAN_POINT ( 'NONE',  ( -21.05000000000000071, 76.08579911628598325, -176.4370863660123518 ) ) ;
#112742=ADVANCED_FACE ( 'NONE', ( #184976 ), #6325, .T. ) ;
#112743=ORIENTED_EDGE ( 'NONE', *, *, #6689, .T. ) ;
#112748=CARTESIAN_POINT ( 'NONE',  ( 21.05000000000000071, 76.00000000001237765, -170.0231074845243597 ) ) ;
#112768=LINE ( 'NONE', #249711, #36693 ) ;
#112819=ORIENTED_EDGE ( 'NONE', *, *, #235713, .F. ) ;
#112825=ORIENTED_EDGE ( 'NONE', *, *, #108538, .T. ) ;
#112845=DIRECTION ( 'NONE',  ( 0.000000000000000000, -7.172728831056617961E-15, 1.000000000000000000 ) ) ;
#112881=LINE ( 'NONE', #150726, #153586 ) ;
#112890=AXIS2_PLACEMENT_3D ( 'NONE', #49080, #128640, #15107 ) ;
#112891=CARTESIAN_POINT ( 'NONE',  ( 18.53691006697079757, 65.69784844286128589, -145.3209087672253474 ) ) ;
#112904=EDGE_LOOP ( 'NONE', ( #253315, #250383, #203892, #123000 ) ) ;
#112925=CARTESIAN_POINT ( 'NONE',  ( -22.39999999999999858, 76.00000000001243450, -177.8138870828977360 ) ) ;
#112932=CARTESIAN_POINT ( 'NONE',  ( 18.49999999999998934, 64.35000000001220144, -145.2731074845244450 ) ) ;
#113005=VERTEX_POINT ( 'NONE', #180824 ) ;
#113026=DIRECTION ( 'NONE',  ( 1.000000000000000000, -2.952720810173289112E-16, -2.061873921506763405E-30 ) ) ;
#113031=FACE_OUTER_BOUND ( 'NONE', #162855, .T. ) ;
#113051=VECTOR ( 'NONE', #231039, 1000.000000000000000 ) ;
#113091=FACE_OUTER_BOUND ( 'NONE', #113652, .T. ) ;
#113096=CIRCLE ( 'NONE', #171570, 0.09999999999999939493 ) ;
#113152=DIRECTION ( 'NONE',  ( 1.000000000000000000, 0.000000000000000000, 0.000000000000000000 ) ) ;
#113154=CARTESIAN_POINT ( 'NONE',  ( -20.64999999999999858, 76.00000000001237765, -170.0231074845243597 ) ) ;
#113164=ORIENTED_EDGE ( 'NONE', *, *, #247947, .F. ) ;
#113175=EDGE_CURVE ( 'NONE', #60353, #92616, #55376, .T. ) ;
#113191=FACE_OUTER_BOUND ( 'NONE', #129768, .T. ) ;
#113219=VERTEX_POINT ( 'NONE', #32031 ) ;
#113262=EDGE_CURVE ( 'NONE', #205324, #58091, #125460, .T. ) ;
#113300=CIRCLE ( 'NONE', #845, 0.09999999999998898659 ) ;
#113301=DIRECTION ( 'NONE',  ( -1.000000000000000000, 2.952720810173289112E-16, 2.061873921506763405E-30 ) ) ;
#113310=EDGE_LOOP ( 'NONE', ( #116748, #135827, #81205, #167455 ) ) ;
#113324=CIRCLE ( 'NONE', #171622, 0.09999999999999939493 ) ;
#113423=ORIENTED_EDGE ( 'NONE', *, *, #230785, .T. ) ;
#113449=CARTESIAN_POINT ( 'NONE',  ( 21.14999999999999858, 69.45934304831114048, -169.9231074845244223 ) ) ;
#113493=ORIENTED_EDGE ( 'NONE', *, *, #32115, .F. ) ;
#113505=CARTESIAN_POINT ( 'NONE',  ( -21.14250536705909411, 76.00000000001242029, -176.5412796614051274 ) ) ;
#113527=CARTESIAN_POINT ( 'NONE',  ( 23.24999999999999645, 70.40000000001246860, -181.7731074845244166 ) ) ;
#113546=VERTEX_POINT ( 'NONE', #76919 ) ;
#113576=CARTESIAN_POINT ( 'NONE',  ( -22.59999999999999787, 75.89914163091376054, -181.7726746080137445 ) ) ;
#113597=CARTESIAN_POINT ( 'NONE',  ( 23.24999999999999645, 78.10000000001214460, -136.5231074845243029 ) ) ;
#113598=VECTOR ( 'NONE', #124667, 1000.000000000000000 ) ;
#113617=VECTOR ( 'NONE', #148553, 1000.000000000000000 ) ;
#113635=VERTEX_POINT ( 'NONE', #200728 ) ;
#113636=DIRECTION ( 'NONE',  ( -1.000000000000000000, 0.000000000000000000, 0.000000000000000000 ) ) ;
#113643=ORIENTED_EDGE ( 'NONE', *, *, #122780, .F. ) ;
#113652=EDGE_LOOP ( 'NONE', ( #222244, #113423, #237418, #151852 ) ) ;
#113659=CARTESIAN_POINT ( 'NONE',  ( -20.85000000000000497, 64.25000000001220712, -143.4422547304831710 ) ) ;
#113690=ADVANCED_FACE ( 'NONE', ( #24684 ), #61215, .T. ) ;
#113695=CARTESIAN_POINT ( 'NONE',  ( 18.58703555225036297, 85.40633674080073945, -162.8981628432770208 ) ) ;
#113765=DIRECTION ( 'NONE',  ( 0.000000000000000000, 7.026728003956695223E-15, -1.000000000000000000 ) ) ;
#113769=CARTESIAN_POINT ( 'NONE',  ( -18.50000000000000711, 64.25000000001233502, -163.0083017138704236 ) ) ;
#113788=ORIENTED_EDGE ( 'NONE', *, *, #151834, .F. ) ;
#113790=ADVANCED_FACE ( 'NONE', ( #230568 ), #46768, .T. ) ;
#113808=DIRECTION ( 'NONE',  ( -1.000000000000000000, -0.000000000000000000, -0.000000000000000000 ) ) ;
#113820=DIRECTION ( 'NONE',  ( 0.000000000000000000, -7.147358527629766941E-15, 1.000000000000000000 ) ) ;
#113822=DIRECTION ( 'NONE',  ( 2.659396599871503635E-15, -0.6132151058540604716, 0.7899159663865477077 ) ) ;
#113824=LINE ( 'NONE', #53861, #190854 ) ;
#113849=CIRCLE ( 'NONE', #197035, 0.09999999999998898659 ) ;
#113874=DIRECTION ( 'NONE',  ( -1.000000000000000000, 0.000000000000000000, -0.000000000000000000 ) ) ;
#113882=CIRCLE ( 'NONE', #59680, 7.800000000000001599 ) ;
#113904=EDGE_CURVE ( 'NONE', #218857, #218618, #50771, .T. ) ;
#113924=EDGE_CURVE ( 'NONE', #228499, #168221, #179998, .T. ) ;
#113938=ORIENTED_EDGE ( 'NONE', *, *, #134187, .T. ) ;
#114019=DIRECTION ( 'NONE',  ( -1.000000000000000000, -0.000000000000000000, -0.000000000000000000 ) ) ;
#114025=LINE ( 'NONE', #247117, #110522 ) ;
#114035=DIRECTION ( 'NONE',  ( 0.000000000000000000, 0.1350103645451835865, 0.9908441862701605762 ) ) ;
#114056=CIRCLE ( 'NONE', #118170, 0.1000000000000028644 ) ;
#114065=FACE_OUTER_BOUND ( 'NONE', #109527, .T. ) ;
#114127=AXIS2_PLACEMENT_3D ( 'NONE', #177236, #201905, #37722 ) ;
#114146=AXIS2_PLACEMENT_3D ( 'NONE', #132199, #29290, #188317 ) ;
#114168=CARTESIAN_POINT ( 'NONE',  ( 18.49999999999999289, 65.55993210786904513, -145.2559897356427996 ) ) ;
#114169=DIRECTION ( 'NONE',  ( 0.000000000000000000, 0.4930308989874980785, 0.8700118002898462599 ) ) ;
#114173=ADVANCED_FACE ( 'NONE', ( #119613 ), #242096, .T. ) ;
#114270=DIRECTION ( 'NONE',  ( 0.000000000000000000, -0.8660254037844419273, 0.4999999999999942824 ) ) ;
#114276=DIRECTION ( 'NONE',  ( 0.000000000000000000, 0.000000000000000000, 1.000000000000000000 ) ) ;
#114277=ORIENTED_EDGE ( 'NONE', *, *, #111197, .F. ) ;
#114281=CARTESIAN_POINT ( 'NONE',  ( -18.59999999999999787, 77.83585931145570669, -125.0186683157258329 ) ) ;
#114293=AXIS2_PLACEMENT_3D ( 'NONE', #43338, #5457, #181575 ) ;
#114295=VECTOR ( 'NONE', #230506, 1000.000000000000000 ) ;
#114313=DIRECTION ( 'NONE',  ( -0.7071067811865474617, 0.7071067811865474617, 4.937700262164531476E-15 ) ) ;
#114317=ORIENTED_EDGE ( 'NONE', *, *, #171731, .T. ) ;
#114337=CIRCLE ( 'NONE', #85082, 0.09999999999999939493 ) ;
#114420=CARTESIAN_POINT ( 'NONE',  ( 23.14999999999999858, 76.00000000001210765, -132.5231074845243313 ) ) ;
#114423=CARTESIAN_POINT ( 'NONE',  ( 21.05000000000000071, 65.27628288308724791, -157.8468678833862100 ) ) ;
#114434=ORIENTED_EDGE ( 'NONE', *, *, #10558, .F. ) ;
#114464=AXIS2_PLACEMENT_3D ( 'NONE', #220710, #141178, #25106 ) ;
#114476=DIRECTION ( 'NONE',  ( 1.000000000000000000, 0.000000000000000000, 0.000000000000000000 ) ) ;
#114498=ORIENTED_EDGE ( 'NONE', *, *, #160460, .F. ) ;
#114513=LINE ( 'NONE', #173259, #65979 ) ;
#114528=DIRECTION ( 'NONE',  ( 0.000000000000000000, 0.000000000000000000, -1.000000000000000000 ) ) ;
#114536=COLOUR_RGB ( '', 0.08235294, 0.09019608, 0.10196078) ;
#114540=EDGE_CURVE ( 'NONE', #115854, #73802, #14531, .T. ) ;
#114554=DIRECTION ( 'NONE',  ( 1.000000000000000000, 0.000000000000000000, 0.000000000000000000 ) ) ;
#114556=EDGE_CURVE ( 'NONE', #108264, #187685, #242693, .T. ) ;
#114580=CIRCLE ( 'NONE', #160577, 0.1000000000000028644 ) ;
#114581=ORIENTED_EDGE ( 'NONE', *, *, #195990, .T. ) ;
#114626=ORIENTED_EDGE ( 'NONE', *, *, #35219, .F. ) ;
#114632=EDGE_CURVE ( 'NONE', #47348, #28076, #255628, .T. ) ;
#114633=ORIENTED_EDGE ( 'NONE', *, *, #35281, .T. ) ;
#114657=DIRECTION ( 'NONE',  ( 0.000000000000000000, 0.000000000000000000, 1.000000000000000000 ) ) ;
#114701=EDGE_CURVE ( 'NONE', #194619, #196891, #105289, .T. ) ;
#114745=DIRECTION ( 'NONE',  ( -3.469446951953515108E-14, -1.000000000000000000, 0.000000000000000000 ) ) ;
#114779=ORIENTED_EDGE ( 'NONE', *, *, #79029, .T. ) ;
#114790=EDGE_CURVE ( 'NONE', #75757, #116101, #66468, .T. ) ;
#114798=CIRCLE ( 'NONE', #2342, 1.900000000000012790 ) ;
#114834=ORIENTED_EDGE ( 'NONE', *, *, #82060, .T. ) ;
#114843=CARTESIAN_POINT ( 'NONE',  ( 23.14999999999999503, 69.35000000001222986, -148.6731074845243938 ) ) ;
#114844=DIRECTION ( 'NONE',  ( 1.000000000000000000, 7.304098846218134667E-16, 5.100424963727256530E-30 ) ) ;
#114875=CARTESIAN_POINT ( 'NONE',  ( -20.94999999999999574, 64.37928932189355180, -143.3915241368654279 ) ) ;
#114885=VERTEX_POINT ( 'NONE', #166889 ) ;
#114914=DIRECTION ( 'NONE',  ( -1.000000000000000000, 3.265361837132813093E-16, 2.280189983783949500E-30 ) ) ;
#114915=( BOUNDED_SURFACE ( )  B_SPLINE_SURFACE ( 3, 2, ( 
 ( #175752, #101266, #197848 ),
 ( #201704, #217403, #216125 ),
 ( #178323, #239557, #140436 ),
 ( #79174, #42631, #41379 ),
 ( #17925, #120919, #257774 ),
 ( #199144, #59597, #158760 ) ),
 .UNSPECIFIED., .F., .F., .F. ) 
 B_SPLINE_SURFACE_WITH_KNOTS ( ( 4, 2, 4 ),
 ( 3, 3 ),
 ( 0.0001792624049599534481, 0.0003686986002124517745, 0.0005581347954649500467 ),
 ( 0.000000000000000000, 1.000000000000000000 ),
 .UNSPECIFIED. ) 
 GEOMETRIC_REPRESENTATION_ITEM ( )  RATIONAL_B_SPLINE_SURFACE ( (
 ( 1.000000000000000000, 0.9238795325112856283, 1.000000000000000000),
 ( 1.000000000000000000, 0.9229318695237381798, 1.000000000000000000),
 ( 1.000000000000000000, 0.8926288119231814422, 1.000000000000000000),
 ( 1.000000000000000000, 0.8123777807270232687, 1.000000000000000000),
 ( 1.000000000000000000, 0.7629087100932465670, 1.000000000000000000),
 ( 1.000000000000000000, 0.7071067811865475727, 1.000000000000000000) ) ) 
 REPRESENTATION_ITEM ( '' )  SURFACE ( )  );
#114924=ORIENTED_EDGE ( 'NONE', *, *, #28411, .F. ) ;
#114926=EDGE_CURVE ( 'NONE', #64653, #52602, #226103, .T. ) ;
#114931=LINE ( 'NONE', #194488, #47878 ) ;
#114936=EDGE_LOOP ( 'NONE', ( #129780, #198565, #140557, #10103 ) ) ;
#114942=DIRECTION ( 'NONE',  ( 1.000000000000000000, 0.000000000000000000, 0.000000000000000000 ) ) ;
#114980=VERTEX_POINT ( 'NONE', #115864 ) ;
#114992=CIRCLE ( 'NONE', #164881, 11.80000000000000426 ) ;
#115005=DIRECTION ( 'NONE',  ( 7.589415207398576792E-15, 1.000000000000000000, 6.982962677686266711E-15 ) ) ;
#115026=CARTESIAN_POINT ( 'NONE',  ( -20.54999999999999716, 85.40000000001221281, -146.4170766071767389 ) ) ;
#115062=DIRECTION ( 'NONE',  ( 0.000000000000000000, 0.000000000000000000, 1.000000000000000000 ) ) ;
#115067=DIRECTION ( 'NONE',  ( 0.000000000000000000, 0.000000000000000000, 1.000000000000000000 ) ) ;
#115080=CIRCLE ( 'NONE', #2638, 0.5000000000000004441 ) ;
#115087=ORIENTED_EDGE ( 'NONE', *, *, #113175, .F. ) ;
#115092=CARTESIAN_POINT ( 'NONE',  ( 21.05000000000000071, 87.48912529308822172, -139.6231074845242688 ) ) ;
#115107=CARTESIAN_POINT ( 'NONE',  ( -23.15000000000000213, 85.00000000001222134, -145.9170766071767389 ) ) ;
#115108=ADVANCED_FACE ( 'NONE', ( #216226 ), #159844, .T. ) ;
#115123=VECTOR ( 'NONE', #214328, 1000.000000000000000 ) ;
#115136=AXIS2_PLACEMENT_3D ( 'NONE', #104795, #186970, #249497 ) ;
#115144=CARTESIAN_POINT ( 'NONE',  ( -18.40904629823847571, 85.50000000001210765, -129.9229179220422452 ) ) ;
#115148=ORIENTED_EDGE ( 'NONE', *, *, #248808, .F. ) ;
#115150=CARTESIAN_POINT ( 'NONE',  ( 23.14999999999999858, 76.00000000001213607, -136.5231074845243313 ) ) ;
#115153=AXIS2_PLACEMENT_3D ( 'NONE', #93146, #249673, #211834 ) ;
#115157=ADVANCED_FACE ( 'NONE', ( #190936 ), #144373, .T. ) ;
#115163=DIRECTION ( 'NONE',  ( 0.000000000000000000, 0.000000000000000000, -1.000000000000000000 ) ) ;
#115200=VECTOR ( 'NONE', #194867, 1000.000000000000114 ) ;
#115228=ORIENTED_EDGE ( 'NONE', *, *, #242261, .F. ) ;
#115230=ORIENTED_EDGE ( 'NONE', *, *, #93518, .T. ) ;
#115279=DIRECTION ( 'NONE',  ( 0.000000000000000000, -1.176083712526648525E-14, 1.000000000000000000 ) ) ;
#115293=ORIENTED_EDGE ( 'NONE', *, *, #245430, .F. ) ;
#115298=ADVANCED_FACE ( 'NONE', ( #215593 ), #236447, .T. ) ;
#115319=LINE ( 'NONE', #237842, #141552 ) ;
#115326=CARTESIAN_POINT ( 'NONE',  ( -21.00448002041592233, 64.25000000001232081, -163.1747666222132409 ) ) ;
#115403=EDGE_LOOP ( 'NONE', ( #152489, #67337, #236692, #255143 ) ) ;
#115426=DIRECTION ( 'NONE',  ( 0.000000000000000000, 1.000000000000000000, 0.000000000000000000 ) ) ;
#115433=ORIENTED_EDGE ( 'NONE', *, *, #20114, .T. ) ;
#115447=CARTESIAN_POINT ( 'NONE',  ( 18.59999999999999076, 65.50857864377491069, -145.2731074845244166 ) ) ;
#115448=CARTESIAN_POINT ( 'NONE',  ( -18.59999999999999787, 68.87972903831452243, -132.8635444426850825 ) ) ;
#115451=CARTESIAN_POINT ( 'NONE',  ( -18.43473496883401097, 85.49495241101172383, -162.9772359122965781 ) ) ;
#115479=CARTESIAN_POINT ( 'NONE',  ( -20.94403535211772294, 65.69367753730678317, -131.0189238066348594 ) ) ;
#115511=CARTESIAN_POINT ( 'NONE',  ( -18.50000000000000000, 64.35000000001247145, -181.7731074845244450 ) ) ;
#115527=VERTEX_POINT ( 'NONE', #227156 ) ;
#115544=DIRECTION ( 'NONE',  ( 0.000000000000000000, -6.982962677686266711E-15, 1.000000000000000000 ) ) ;
#115566=AXIS2_PLACEMENT_3D ( 'NONE', #179566, #81685, #160006 ) ;
#115578=CARTESIAN_POINT ( 'NONE',  ( -20.94999999999999929, 87.41227409416205774, -167.0231074845242745 ) ) ;
#115580=CARTESIAN_POINT ( 'NONE',  ( -22.59999999999999787, 64.25012875563587045, -170.0885370755381132 ) ) ;
#115591=FACE_OUTER_BOUND ( 'NONE', #223308, .T. ) ;
#115614=EDGE_CURVE ( 'NONE', #151389, #168873, #172387, .T. ) ;
#115675=DIRECTION ( 'NONE',  ( 1.000000000000000000, 0.000000000000000000, 0.000000000000000000 ) ) ;
#115690=AXIS2_PLACEMENT_3D ( 'NONE', #35328, #17024, #254312 ) ;
#115699=VERTEX_POINT ( 'NONE', #14563 ) ;
#115717=EDGE_CURVE ( 'NONE', #104106, #198025, #57493, .T. ) ;
#115729=CARTESIAN_POINT ( 'NONE',  ( 20.94999999999999574, 77.83534155023670564, -158.4679561919613491 ) ) ;
#115766=CARTESIAN_POINT ( 'NONE',  ( 23.14999999999999858, 64.40000000001218439, -143.4513107147999449 ) ) ;
#115852=ORIENTED_EDGE ( 'NONE', *, *, #54722, .T. ) ;
#115854=VERTEX_POINT ( 'NONE', #83464 ) ;
#115863=ORIENTED_EDGE ( 'NONE', *, *, #86112, .F. ) ;
#115864=CARTESIAN_POINT ( 'NONE',  ( -23.15000000000000213, 76.00000000001222134, -148.3231074845243427 ) ) ;
#115912=DIRECTION ( 'NONE',  ( 0.000000000000000000, 7.086529944415886769E-15, -1.000000000000000000 ) ) ;
#115929=DIRECTION ( 'NONE',  ( 1.000000000000000000, 0.000000000000000000, 0.000000000000000000 ) ) ;
#115963=ORIENTED_EDGE ( 'NONE', *, *, #162743, .T. ) ;
#116033=CARTESIAN_POINT ( 'NONE',  ( 22.39999999999999503, 76.00000000001243450, -177.7731074845243597 ) ) ;
#116037=DIRECTION ( 'NONE',  ( 1.000000000000000000, 0.000000000000000000, 0.000000000000000000 ) ) ;
#116048=CIRCLE ( 'NONE', #91089, 0.09999999999998898659 ) ;
#116081=ADVANCED_FACE ( 'NONE', ( #76760 ), #242247, .F. ) ;
#116094=CARTESIAN_POINT ( 'NONE',  ( 18.49999999999999645, 76.00000000001213607, -136.5231074845243313 ) ) ;
#116097=CARTESIAN_POINT ( 'NONE',  ( -21.05000000000000071, 77.83534155023670564, -158.4679561919613491 ) ) ;
#116101=VERTEX_POINT ( 'NONE', #3635 ) ;
#116144=DIRECTION ( 'NONE',  ( 0.000000000000000000, 0.000000000000000000, 1.000000000000000000 ) ) ;
#116167=TOROIDAL_SURFACE ( 'NONE', #53790, 12.97499999999999787, 0.1000000000000000056 ) ;
#116187=DIRECTION ( 'NONE',  ( 1.000000000000000000, 0.000000000000000000, 0.000000000000000000 ) ) ;
#116193=EDGE_CURVE ( 'NONE', #116101, #218186, #155425, .T. ) ;
#116202=EDGE_CURVE ( 'NONE', #143129, #33310, #181018, .T. ) ;
#116234=ORIENTED_EDGE ( 'NONE', *, *, #155616, .F. ) ;
#116252=EDGE_LOOP ( 'NONE', ( #102746, #9737, #84842, #102975 ) ) ;
#116281=CARTESIAN_POINT ( 'NONE',  ( 18.46947024752544309, 85.50929715716830515, -163.0364180358262445 ) ) ;
#116286=FACE_OUTER_BOUND ( 'NONE', #254968, .T. ) ;
#116288=CARTESIAN_POINT ( 'NONE',  ( 18.57071067811864040, 65.82071067813089371, -148.6731074845244223 ) ) ;
#116299=TOROIDAL_SURFACE ( 'NONE', #203765, 0.2000000000000000111, 0.1000000000000000056 ) ;
#116311=PRESENTATION_STYLE_ASSIGNMENT (( #112459 ) ) ;
#116312=EDGE_CURVE ( 'NONE', #69711, #7639, #88731, .T. ) ;
#116332=DIRECTION ( 'NONE',  ( 1.000000000000000000, 0.000000000000000000, 0.000000000000000000 ) ) ;
#116357=CARTESIAN_POINT ( 'NONE',  ( -22.39999999999999858, 75.90000000001236913, -170.0231074845243597 ) ) ;
#116361=CARTESIAN_POINT ( 'NONE',  ( -20.00857864376270001, 66.65000000001229807, -157.7731074845244166 ) ) ;
#116372=DIRECTION ( 'NONE',  ( 1.000000000000000000, 0.000000000000000000, 0.000000000000000000 ) ) ;
#116373=ORIENTED_EDGE ( 'NONE', *, *, #155642, .F. ) ;
#116390=DIRECTION ( 'NONE',  ( 0.000000000000000000, 0.000000000000000000, 1.000000000000000000 ) ) ;
#116402=EDGE_CURVE ( 'NONE', #176438, #244844, #209555, .T. ) ;
#116431=CARTESIAN_POINT ( 'NONE',  ( -20.94999999999999929, 68.97833521811203639, -132.6895420826271277 ) ) ;
#116434=CARTESIAN_POINT ( 'NONE',  ( -21.14999999999999858, 76.10000000001241460, -176.5637644362255969 ) ) ;
#116442=EDGE_CURVE ( 'NONE', #237280, #20561, #110357, .T. ) ;
#116473=EDGE_CURVE ( 'NONE', #94706, #140520, #205619, .T. ) ;
#116496=CARTESIAN_POINT ( 'NONE',  ( 18.49999999999999289, 68.97833521811203639, -132.6895420826271277 ) ) ;
#116499=CARTESIAN_POINT ( 'NONE',  ( 18.49999999999999645, 77.83585931145570669, -125.0186683157258045 ) ) ;
#116502=ORIENTED_EDGE ( 'NONE', *, *, #18135, .F. ) ;
#116503=EDGE_CURVE ( 'NONE', #141665, #111495, #77721, .T. ) ;
#116513=VERTEX_POINT ( 'NONE', #20361 ) ;
#116514=DIRECTION ( 'NONE',  ( -0.000000000000000000, -1.000000000000000000, -6.982962677686266711E-15 ) ) ;
#116535=EDGE_LOOP ( 'NONE', ( #253428, #31480, #151541, #208041 ) ) ;
#116540=CARTESIAN_POINT ( 'NONE',  ( -18.59999999999999787, 65.66751761918692409, -130.9282609406112670 ) ) ;
#116550=ORIENTED_EDGE ( 'NONE', *, *, #34909, .F. ) ;
#116661=DIRECTION ( 'NONE',  ( -1.000000000000000000, 0.000000000000000000, -0.000000000000000000 ) ) ;
#116684=ADVANCED_FACE ( 'NONE', ( #104964 ), #18208, .T. ) ;
#116713=CARTESIAN_POINT ( 'NONE',  ( 18.59999999999999787, 76.00000000001237765, -170.0231074845243597 ) ) ;
#116730=DIRECTION ( 'NONE',  ( 0.000000000000000000, -6.938893903907222067E-15, 1.000000000000000000 ) ) ;
#116748=ORIENTED_EDGE ( 'NONE', *, *, #90255, .T. ) ;
#116792=EDGE_CURVE ( 'NONE', #176760, #61299, #118150, .T. ) ;
#116806=CYLINDRICAL_SURFACE ( 'NONE', #193448, 11.80000000000000426 ) ;
#116845=LINE ( 'NONE', #17721, #217822 ) ;
#116855=ORIENTED_EDGE ( 'NONE', *, *, #245508, .T. ) ;
#116884=TOROIDAL_SURFACE ( 'NONE', #16949, 0.2000000000000000111, 0.1000000000000000056 ) ;
#116892=DIRECTION ( 'NONE',  ( -1.000000000000000000, 0.000000000000000000, 0.000000000000000000 ) ) ;
#116919=CIRCLE ( 'NONE', #150260, 0.1000000000000028644 ) ;
#116929=CARTESIAN_POINT ( 'NONE',  ( 21.05000000000000071, 76.00000000001210765, -132.5231074845243313 ) ) ;
#116952=ORIENTED_EDGE ( 'NONE', *, *, #137452, .T. ) ;
#116988=ORIENTED_EDGE ( 'NONE', *, *, #120330, .F. ) ;
#117000=DIRECTION ( 'NONE',  ( -0.000000000000000000, 6.982962677686266711E-15, -1.000000000000000000 ) ) ;
#117004=CARTESIAN_POINT ( 'NONE',  ( 18.59999999999997655, 76.00000000001207923, -128.6231074845243540 ) ) ;
#117019=CARTESIAN_POINT ( 'NONE',  ( 23.14999999999999503, 64.35000000001228670, -157.8731074845244393 ) ) ;
#117047=CARTESIAN_POINT ( 'NONE',  ( 22.24259225415828212, 75.90093411655959699, -177.5150453550897680 ) ) ;
#117136=EDGE_CURVE ( 'NONE', #194619, #160806, #164146, .T. ) ;
#117150=CARTESIAN_POINT ( 'NONE',  ( 18.39999999999999858, 85.50000000001209344, -129.6009576351939074 ) ) ;
#117213=ORIENTED_EDGE ( 'NONE', *, *, #49037, .T. ) ;
#117221=DIRECTION ( 'NONE',  ( 0.000000000000000000, -0.9654727137038715545, -0.2605042016806676242 ) ) ;
#117234=ORIENTED_EDGE ( 'NONE', *, *, #143595, .T. ) ;
#117258=FACE_OUTER_BOUND ( 'NONE', #134744, .T. ) ;
#117294=ORIENTED_EDGE ( 'NONE', *, *, #235106, .F. ) ;
#117301=EDGE_CURVE ( 'NONE', #218857, #62106, #201718, .T. ) ;
#117313=ORIENTED_EDGE ( 'NONE', *, *, #92026, .T. ) ;
#117320=DIRECTION ( 'NONE',  ( 0.000000000000000000, 7.086529944415886769E-15, -1.000000000000000000 ) ) ;
#117325=CARTESIAN_POINT ( 'NONE',  ( -23.25000000000000000, 64.35000000001222986, -148.7731074845244450 ) ) ;
#117332=EDGE_CURVE ( 'NONE', #195092, #69727, #256677, .T. ) ;
#117419=ADVANCED_FACE ( 'NONE', ( #40289 ), #110137, .T. ) ;
#117433=EDGE_CURVE ( 'NONE', #110939, #6455, #168468, .T. ) ;
#117439=CIRCLE ( 'NONE', #184240, 0.2000000000000057288 ) ;
#117441=CARTESIAN_POINT ( 'NONE',  ( -23.25000000000000000, 84.59626168225530307, -160.5729799673740104 ) ) ;
#117458=AXIS2_PLACEMENT_3D ( 'NONE', #123712, #188805, #164125 ) ;
#117472=VERTEX_POINT ( 'NONE', #45382 ) ;
#117478=ORIENTED_EDGE ( 'NONE', *, *, #145611, .T. ) ;
#117495=VERTEX_POINT ( 'NONE', #68813 ) ;
#117501=ORIENTED_EDGE ( 'NONE', *, *, #125992, .F. ) ;
#117536=ADVANCED_FACE ( 'NONE', ( #106615 ), #7540, .T. ) ;
#117562=CIRCLE ( 'NONE', #122226, 0.1000000000000026007 ) ;
#117587=CARTESIAN_POINT ( 'NONE',  ( -21.65000000000000213, 68.29142135624952914, -148.8731074845244109 ) ) ;
#117602=DIRECTION ( 'NONE',  ( 0.000000000000000000, 0.000000000000000000, 1.000000000000000000 ) ) ;
#117699=CARTESIAN_POINT ( 'NONE',  ( -20.94999999999999929, 77.83534155023670564, -158.4679561919613491 ) ) ;
#117718=ORIENTED_EDGE ( 'NONE', *, *, #191812, .T. ) ;
#117734=EDGE_CURVE ( 'NONE', #44761, #251678, #256349, .T. ) ;
#117752=CYLINDRICAL_SURFACE ( 'NONE', #156189, 0.09999999999999939493 ) ;
#117793=ORIENTED_EDGE ( 'NONE', *, *, #236614, .T. ) ;
#117800=FACE_OUTER_BOUND ( 'NONE', #202439, .T. ) ;
#117810=ORIENTED_EDGE ( 'NONE', *, *, #96204, .F. ) ;
#117819=AXIS2_PLACEMENT_3D ( 'NONE', #178886, #217947, #159305 ) ;
#117822=EDGE_LOOP ( 'NONE', ( #126173, #203528, #214051, #166409 ) ) ;
#117930=CARTESIAN_POINT ( 'NONE',  ( -20.54999999999999716, 85.50000000001222134, -146.4170766071767389 ) ) ;
#117954=AXIS2_PLACEMENT_3D ( 'NONE', #98465, #18963, #181907 ) ;
#117959=EDGE_CURVE ( 'NONE', #112448, #95210, #6861, .T. ) ;
#118011=FACE_OUTER_BOUND ( 'NONE', #200794, .T. ) ;
#118031=ADVANCED_FACE ( 'NONE', ( #199881 ), #20562, .T. ) ;
#118033=ORIENTED_EDGE ( 'NONE', *, *, #38828, .T. ) ;
#118041=AXIS2_PLACEMENT_3D ( 'NONE', #146904, #69983, #110361 ) ;
#118084=CARTESIAN_POINT ( 'NONE',  ( 22.39999999999999503, 64.25000000001237765, -170.1231074845244393 ) ) ;
#118131=VECTOR ( 'NONE', #124218, 1000.000000000000000 ) ;
#118139=AXIS2_PLACEMENT_3D ( 'NONE', #161609, #122470, #40395 ) ;
#118150=CIRCLE ( 'NONE', #5692, 0.09999999999999344136 ) ;
#118154=CIRCLE ( 'NONE', #151324, 0.9750000000000036415 ) ;
#118163=CARTESIAN_POINT ( 'NONE',  ( -20.64999999999999858, 74.00000000001223555, -149.3477294072864652 ) ) ;
#118169=DIRECTION ( 'NONE',  ( -0.000000000000000000, 0.1298341882520054891, 0.9915357197604850459 ) ) ;
#118170=AXIS2_PLACEMENT_3D ( 'NONE', #69668, #249583, #70968 ) ;
#118174=ORIENTED_EDGE ( 'NONE', *, *, #155855, .T. ) ;
#118231=VERTEX_POINT ( 'NONE', #15595 ) ;
#118274=EDGE_CURVE ( 'NONE', #61430, #167205, #12199, .T. ) ;
#118324=ORIENTED_EDGE ( 'NONE', *, *, #129573, .F. ) ;
#118334=DIRECTION ( 'NONE',  ( 0.000000000000000000, 0.000000000000000000, -1.000000000000000000 ) ) ;
#118374=DIRECTION ( 'NONE',  ( 0.000000000000000000, 6.982962677686266711E-15, -1.000000000000000000 ) ) ;
#118391=EDGE_CURVE ( 'NONE', #50939, #140576, #8262, .T. ) ;
#118418=DIRECTION ( 'NONE',  ( 1.000000000000000000, -0.000000000000000000, 0.000000000000000000 ) ) ;
#118429=DIRECTION ( 'NONE',  ( 0.000000000000000000, 0.000000000000000000, -1.000000000000000000 ) ) ;
#118433=DIRECTION ( 'NONE',  ( 0.000000000000000000, 0.9887567792719329507, 0.1495327102803732933 ) ) ;
#118533=CARTESIAN_POINT ( 'NONE',  ( 20.95378194480896639, 65.46508800846955012, -162.4580533363765937 ) ) ;
#118622=DIRECTION ( 'NONE',  ( 0.000000000000000000, 0.000000000000000000, -1.000000000000000000 ) ) ;
#118629=VECTOR ( 'NONE', #39293, 1000.000000000000000 ) ;
#118635=DIRECTION ( 'NONE',  ( -0.000000000000000000, -6.982962677686266711E-15, 1.000000000000000000 ) ) ;
#118636=CARTESIAN_POINT ( 'NONE',  ( -21.22070241538126112, 69.53005372714277144, -170.1220265150594173 ) ) ;
#118641=ADVANCED_FACE ( 'NONE', ( #145126 ), #20745, .F. ) ;
#118648=DIRECTION ( 'NONE',  ( 0.000000000000000000, 0.000000000000000000, 1.000000000000000000 ) ) ;
#118657=DIRECTION ( 'NONE',  ( 2.694716079187273439E-16, 1.000000000000000000, 6.467318590049456648E-15 ) ) ;
#118679=AXIS2_PLACEMENT_3D ( 'NONE', #169408, #148525, #228060 ) ;
#118683=EDGE_CURVE ( 'NONE', #20561, #187685, #175078, .T. ) ;
#118696=CARTESIAN_POINT ( 'NONE',  ( -23.25000000000000000, 87.65000000001235492, -166.9231074845242802 ) ) ;
#118704=DIRECTION ( 'NONE',  ( 0.000000000000000000, -6.982962677686266711E-15, 1.000000000000000000 ) ) ;
#118719=DIRECTION ( 'NONE',  ( 0.000000000000000000, 6.853228547068871147E-15, -1.000000000000000000 ) ) ;
#118748=ORIENTED_EDGE ( 'NONE', *, *, #250941, .F. ) ;
#118752=CARTESIAN_POINT ( 'NONE',  ( -23.15000000000000213, 87.65000000001215597, -139.6231074845242688 ) ) ;
#118765=AXIS2_PLACEMENT_3D ( 'NONE', #121635, #64208, #240286 ) ;
#118802=ORIENTED_EDGE ( 'NONE', *, *, #96808, .T. ) ;
#118835=ADVANCED_FACE ( 'NONE', ( #146405 ), #154231, .T. ) ;
#118860=CARTESIAN_POINT ( 'NONE',  ( 23.14999999999999503, 69.55000000001223270, -148.8731074845244109 ) ) ;
#118888=DIRECTION ( 'NONE',  ( 0.000000000000000000, 0.000000000000000000, 1.000000000000000000 ) ) ;
#118889=EDGE_CURVE ( 'NONE', #206438, #1901, #237537, .T. ) ;
#118900=ORIENTED_EDGE ( 'NONE', *, *, #105723, .T. ) ;
#118923=VECTOR ( 'NONE', #241691, 1000.000000000000114 ) ;
#118942=DIRECTION ( 'NONE',  ( 1.000000000000000000, -3.265361837132813093E-16, -2.280189983783949500E-30 ) ) ;
#118959=AXIS2_PLACEMENT_3D ( 'NONE', #57516, #97910, #139612 ) ;
#118976=CARTESIAN_POINT ( 'NONE',  ( 23.14999999999999858, 76.00000000001213607, -136.5231074845243313 ) ) ;
#119008=ORIENTED_EDGE ( 'NONE', *, *, #35281, .F. ) ;
#119015=CARTESIAN_POINT ( 'NONE',  ( 18.49999999999999289, 64.35000000001220144, -145.1731074845244507 ) ) ;
#119032=EDGE_CURVE ( 'NONE', #146731, #238847, #179156, .T. ) ;
#119038=AXIS2_PLACEMENT_3D ( 'NONE', #254696, #156956, #38275 ) ;
#119053=VECTOR ( 'NONE', #24905, 1000.000000000000114 ) ;
#119056=AXIS2_PLACEMENT_3D ( 'NONE', #43848, #60821, #120847 ) ;
#119094=ORIENTED_EDGE ( 'NONE', *, *, #48001, .F. ) ;
#119106=ORIENTED_EDGE ( 'NONE', *, *, #198635, .F. ) ;
#119131=EDGE_CURVE ( 'NONE', #229236, #40931, #141879, .T. ) ;
#119172=CARTESIAN_POINT ( 'NONE',  ( -20.94999999999999929, 76.00000000001210765, -132.5231074845243313 ) ) ;
#119182=LINE ( 'NONE', #77448, #122793 ) ;
#119183=VERTEX_POINT ( 'NONE', #208698 ) ;
#119227=DIRECTION ( 'NONE',  ( 0.000000000000000000, -1.000000000000000000, -6.982962677686265922E-15 ) ) ;
#119232=ORIENTED_EDGE ( 'NONE', *, *, #218691, .F. ) ;
#119267=CARTESIAN_POINT ( 'NONE',  ( -23.15000000000000213, 76.00000000001222134, -149.3981074845243313 ) ) ;
#119276=EDGE_LOOP ( 'NONE', ( #144090, #133433, #8095, #200990 ) ) ;
#119293=ORIENTED_EDGE ( 'NONE', *, *, #20980, .T. ) ;
#119320=CIRCLE ( 'NONE', #239950, 11.80000000000000426 ) ;
#119335=AXIS2_PLACEMENT_3D ( 'NONE', #24148, #141499, #243167 ) ;
#119339=EDGE_LOOP ( 'NONE', ( #221392, #117718, #34175, #115230 ) ) ;
#119355=DIRECTION ( 'NONE',  ( 1.000000000000000000, 0.000000000000000000, 0.000000000000000000 ) ) ;
#119382=CARTESIAN_POINT ( 'NONE',  ( 21.14999999999999503, 87.75000000001234923, -167.1231074845242688 ) ) ;
#119427=LINE ( 'NONE', #197658, #1206 ) ;
#119444=DIRECTION ( 'NONE',  ( 0.000000000000000000, -0.01562499999996560217, -0.9998779222360102414 ) ) ;
#119451=DIRECTION ( 'NONE',  ( -0.000000000000000000, 6.982962677686266711E-15, -1.000000000000000000 ) ) ;
#119456=CARTESIAN_POINT ( 'NONE',  ( 21.14999999999999858, 69.35000000001228670, -157.7731074845243882 ) ) ;
#119461=CARTESIAN_POINT ( 'NONE',  ( -22.50000000000000000, 75.90736249940297853, -181.6728046915650907 ) ) ;
#119526=CIRCLE ( 'NONE', #57118, 0.09999999999999459321 ) ;
#119591=CARTESIAN_POINT ( 'NONE',  ( 22.50000000000000000, 68.20922040163900135, -170.1231074845244109 ) ) ;
#119613=FACE_OUTER_BOUND ( 'NONE', #61558, .T. ) ;
#119634=AXIS2_PLACEMENT_3D ( 'NONE', #152285, #111858, #229243 ) ;
#119660=CARTESIAN_POINT ( 'NONE',  ( -23.15000000000000213, 71.65000000001228386, -157.8731074845243825 ) ) ;
#119683=DIRECTION ( 'NONE',  ( -2.952720810173289112E-16, -1.000000000000000000, -6.982962677686266711E-15 ) ) ;
#119722=CARTESIAN_POINT ( 'NONE',  ( 18.49362639424882104, 85.44260436790048630, -129.7586665510135049 ) ) ;
#119728=CARTESIAN_POINT ( 'NONE',  ( 20.94999999999999574, 74.16465844978787914, -158.4679561919613775 ) ) ;
#119767=DIRECTION ( 'NONE',  ( 2.952720810173289112E-16, 1.000000000000000000, 6.982962677686266711E-15 ) ) ;
#119783=CARTESIAN_POINT ( 'NONE',  ( 20.04142135623730070, 64.35000000001222986, -148.6731074845244507 ) ) ;
#119796=LINE ( 'NONE', #96333, #251796 ) ;
#119800=ORIENTED_EDGE ( 'NONE', *, *, #244689, .F. ) ;
#119810=DIRECTION ( 'NONE',  ( 0.000000000000000000, 0.6728971962617102953, -0.7397360091702507301 ) ) ;
#119832=ORIENTED_EDGE ( 'NONE', *, *, #128845, .F. ) ;
#119839=CARTESIAN_POINT ( 'NONE',  ( -23.15000000000000213, 85.00000000001232081, -160.1291383618718385 ) ) ;
#119845=CARTESIAN_POINT ( 'NONE',  ( -23.25000000000000000, 69.06610602788578035, -132.7374616501508342 ) ) ;
#119915=B_SPLINE_CURVE_WITH_KNOTS ( 'NONE', 3,
 ( #234245, #119461, #195165, #59430, #138972, #176877, #156031, #133870, #16514, #255034, #235530, #17756, #198980, #56867, #179439, #214686 ),
 .UNSPECIFIED., .F., .F.,
 ( 4, 3, 3, 3, 3, 4 ),
 ( 0.000000000000000000, 2.209075297431620268E-05, 5.594258369009782919E-05, 8.979524372342005711E-05, 0.0001236472815274570580, 0.0001574990747609547690 ),
 .UNSPECIFIED. ) ;
#119935=ADVANCED_FACE ( 'NONE', ( #244608 ), #5986, .F. ) ;
#119939=ORIENTED_EDGE ( 'NONE', *, *, #160265, .F. ) ;
#119969=DIRECTION ( 'NONE',  ( 0.000000000000000000, -1.000000000000000000, 2.771150684185008344E-14 ) ) ;
#119999=DIRECTION ( 'NONE',  ( -1.000000000000000000, -0.000000000000000000, -0.000000000000000000 ) ) ;
#120001=DIRECTION ( 'NONE',  ( -0.000000000000000000, -6.982962677686266711E-15, 1.000000000000000000 ) ) ;
#120004=CARTESIAN_POINT ( 'NONE',  ( -18.59999999999999787, 64.35000000001222986, -148.6731074845244507 ) ) ;
#120010=FACE_OUTER_BOUND ( 'NONE', #75837, .T. ) ;
#120039=ORIENTED_EDGE ( 'NONE', *, *, #127167, .F. ) ;
#120110=CIRCLE ( 'NONE', #153438, 0.09999999999998898659 ) ;
#120122=DIRECTION ( 'NONE',  ( 1.000000000000000000, 0.000000000000000000, 0.000000000000000000 ) ) ;
#120146=VERTEX_POINT ( 'NONE', #243977 ) ;
#120150=EDGE_CURVE ( 'NONE', #61430, #146933, #584, .T. ) ;
#120168=DIRECTION ( 'NONE',  ( 0.000000000000000000, -1.000000000000000000, -8.717686153663073805E-15 ) ) ;
#120185=DIRECTION ( 'NONE',  ( -3.265361837132813093E-16, -1.000000000000000000, 7.445645354460596589E-46 ) ) ;
#120186=DIRECTION ( 'NONE',  ( 1.000000000000000000, 0.000000000000000000, 0.000000000000000000 ) ) ;
#120222=VERTEX_POINT ( 'NONE', #9220 ) ;
#120319=CYLINDRICAL_SURFACE ( 'NONE', #178475, 0.09999999999998898659 ) ;
#120330=EDGE_CURVE ( 'NONE', #141624, #145447, #109598, .T. ) ;
#120332=ORIENTED_EDGE ( 'NONE', *, *, #247196, .T. ) ;
#120333=EDGE_CURVE ( 'NONE', #190389, #34228, #42472, .T. ) ;
#120335=CARTESIAN_POINT ( 'NONE',  ( 21.05000000000000071, 77.84908441863932183, -158.3670969630772163 ) ) ;
#120336=DIRECTION ( 'NONE',  ( 1.000000000000000000, -0.000000000000000000, 0.000000000000000000 ) ) ;
#120363=CARTESIAN_POINT ( 'NONE',  ( -18.49513951962167013, 85.43772502668979030, -129.7450349094951605 ) ) ;
#120369=DIRECTION ( 'NONE',  ( 0.000000000000000000, 1.000000000000000000, 0.000000000000000000 ) ) ;
#120385=ORIENTED_EDGE ( 'NONE', *, *, #162986, .T. ) ;
#120390=ADVANCED_FACE ( 'NONE', ( #194313 ), #258064, .F. ) ;
#120392=ORIENTED_EDGE ( 'NONE', *, *, #132292, .T. ) ;
#120403=ORIENTED_EDGE ( 'NONE', *, *, #95679, .F. ) ;
#120414=ORIENTED_EDGE ( 'NONE', *, *, #244569, .T. ) ;
#120428=CARTESIAN_POINT ( 'NONE',  ( -18.59999999999999787, 76.00000000001237765, -170.0231074845243597 ) ) ;
#120439=ORIENTED_EDGE ( 'NONE', *, *, #235228, .F. ) ;
#120480=DIRECTION ( 'NONE',  ( 1.000000000000000000, 0.000000000000000000, 0.000000000000000000 ) ) ;
#120482=CARTESIAN_POINT ( 'NONE',  ( 20.94999999999999929, 69.15387683765952431, -132.7853812176745407 ) ) ;
#120505=CARTESIAN_POINT ( 'NONE',  ( -21.05000000000000071, 64.25000000001233502, -163.2392418215462726 ) ) ;
#120512=ADVANCED_FACE ( 'NONE', ( #201991 ), #75808, .F. ) ;
#120526=LINE ( 'NONE', #142605, #76072 ) ;
#120528=DIRECTION ( 'NONE',  ( 0.000000000000000000, -6.982962677686266711E-15, 1.000000000000000000 ) ) ;
#120536=DIRECTION ( 'NONE',  ( 0.000000000000000000, -1.000000000000000000, 0.000000000000000000 ) ) ;
#120554=CIRCLE ( 'NONE', #49794, 0.5000000000000004441 ) ;
#120575=CARTESIAN_POINT ( 'NONE',  ( -18.50000000000000000, 76.00000000001213607, -136.5231074845243313 ) ) ;
#120590=EDGE_LOOP ( 'NONE', ( #50426, #25322 ) ) ;
#120592=ADVANCED_FACE ( 'NONE', ( #184995 ), #24667, .T. ) ;
#120618=ORIENTED_EDGE ( 'NONE', *, *, #228975, .F. ) ;
#120619=CARTESIAN_POINT ( 'NONE',  ( -18.50000000000000000, 66.85000000001222986, -148.8731074845244393 ) ) ;
#120679=CIRCLE ( 'NONE', #108194, 4.049999999999998046 ) ;
#120683=VECTOR ( 'NONE', #183996, 1000.000000000000000 ) ;
#120686=EDGE_CURVE ( 'NONE', #86183, #30145, #250934, .T. ) ;
#120749=EDGE_LOOP ( 'NONE', ( #176780, #36307, #10630, #153632 ) ) ;
#120794=CIRCLE ( 'NONE', #124869, 0.2000000000000057288 ) ;
#120808=CARTESIAN_POINT ( 'NONE',  ( -21.05000000000000071, 77.25000000001232081, -162.0231074845243313 ) ) ;
#120810=ORIENTED_EDGE ( 'NONE', *, *, #72261, .T. ) ;
#120811=EDGE_LOOP ( 'NONE', ( #215953, #122213, #111468, #105996 ) ) ;
#120820=CARTESIAN_POINT ( 'NONE',  ( -21.07016717457010557, 76.00000000001243450, -176.3440483226252411 ) ) ;
#120847=DIRECTION ( 'NONE',  ( 1.000000000000000000, 0.000000000000000000, 0.000000000000000000 ) ) ;
#120877=EDGE_LOOP ( 'NONE', ( #192316, #141628, #109889, #102421 ) ) ;
#120884=DIRECTION ( 'NONE',  ( 0.000000000000000000, -7.056502275159890832E-15, 1.000000000000000000 ) ) ;
#120919=CARTESIAN_POINT ( 'NONE',  ( 21.04999999999999716, 69.50331341424582376, -170.0084513660146683 ) ) ;
#120923=LINE ( 'NONE', #200431, #164434 ) ;
#120935=DIRECTION ( 'NONE',  ( 0.000000000000000000, -0.6728971962617102953, 0.7397360091702507301 ) ) ;
#120939=CARTESIAN_POINT ( 'NONE',  ( 20.94999999999999929, 76.00000000001237765, -170.0231074845243597 ) ) ;
#121025=ORIENTED_EDGE ( 'NONE', *, *, #10517, .F. ) ;
#121077=AXIS2_PLACEMENT_3D ( 'NONE', #4046, #83557, #163144 ) ;
#121089=CARTESIAN_POINT ( 'NONE',  ( 20.94999999999999929, 76.00000000001213607, -136.5231074845243313 ) ) ;
#121126=DIRECTION ( 'NONE',  ( 0.000000000000000000, 6.982962677686266711E-15, -1.000000000000000000 ) ) ;
#121137=FACE_OUTER_BOUND ( 'NONE', #89700, .T. ) ;
#121183=DIRECTION ( 'NONE',  ( 0.000000000000000000, -6.467318590049456648E-15, 1.000000000000000000 ) ) ;
#121190=CARTESIAN_POINT ( 'NONE',  ( -20.54999999999999716, 71.65000000001225544, -153.2731074845243882 ) ) ;
#121192=SPHERICAL_SURFACE ( 'NONE', #28068, 0.1000000000000000056 ) ;
#121211=DIRECTION ( 'NONE',  ( 0.000000000000000000, 0.000000000000000000, -1.000000000000000000 ) ) ;
#121230=DIRECTION ( 'NONE',  ( 0.000000000000000000, -0.4930308989874980785, -0.8700118002898462599 ) ) ;
#121240=EDGE_CURVE ( 'NONE', #80321, #257571, #251110, .T. ) ;
#121243=DIRECTION ( 'NONE',  ( 0.000000000000000000, 0.000000000000000000, 1.000000000000000000 ) ) ;
#121259=AXIS2_PLACEMENT_3D ( 'NONE', #120428, #1710, #179116 ) ;
#121260=ORIENTED_EDGE ( 'NONE', *, *, #79273, .F. ) ;
#121289=CARTESIAN_POINT ( 'NONE',  ( 18.58222699835054570, 65.66799936921553638, -130.9299399888601272 ) ) ;
#121348=CIRCLE ( 'NONE', #216952, 0.09999999999999939493 ) ;
#121388=EDGE_LOOP ( 'NONE', ( #137241, #133519, #84246, #70677 ) ) ;
#121404=CARTESIAN_POINT ( 'NONE',  ( -18.59999999999999787, 76.00000000001237765, -170.0231074845243597 ) ) ;
#121406=ORIENTED_EDGE ( 'NONE', *, *, #227403, .F. ) ;
#121446=CARTESIAN_POINT ( 'NONE',  ( 21.13507111622889667, 65.28231661301390432, -157.7739388981636353 ) ) ;
#121453=AXIS2_PLACEMENT_3D ( 'NONE', #146410, #63032, #123029 ) ;
#121463=CARTESIAN_POINT ( 'NONE',  ( 20.95512820512820440, 67.12384868372420499, -161.4644784893834810 ) ) ;
#121473=ORIENTED_EDGE ( 'NONE', *, *, #186340, .T. ) ;
#121484=CARTESIAN_POINT ( 'NONE',  ( -21.05000000000000071, 77.83534155023670564, -158.4679561919613491 ) ) ;
#121492=LINE ( 'NONE', #61488, #133104 ) ;
#121501=DIRECTION ( 'NONE',  ( 0.000000000000000000, 0.9908441862701791170, -0.1350103645450472789 ) ) ;
#121503=ORIENTED_EDGE ( 'NONE', *, *, #154463, .T. ) ;
#121514=CARTESIAN_POINT ( 'NONE',  ( 20.22894356738409627, 66.72150177717459485, -161.7545845782749154 ) ) ;
#121522=DIRECTION ( 'NONE',  ( 0.000000000000000000, 0.4999999999999608646, 0.8660254037844612451 ) ) ;
#121606=DIRECTION ( 'NONE',  ( 0.000000000000000000, 6.769652589177795712E-15, -1.000000000000000000 ) ) ;
#121607=EDGE_LOOP ( 'NONE', ( #17834, #220643, #83003, #136247, #219491, #164469 ) ) ;
#121633=ORIENTED_EDGE ( 'NONE', *, *, #164804, .T. ) ;
#121635=CARTESIAN_POINT ( 'NONE',  ( -21.05000000000000071, 87.29603075034744109, -139.5710066441881452 ) ) ;
#121639=DIRECTION ( 'NONE',  ( -0.000000000000000000, 6.982962677686266711E-15, -1.000000000000000000 ) ) ;
#121650=DIRECTION ( 'NONE',  ( 0.000000000000000000, -0.1575844902526687130, -0.9875055080513762684 ) ) ;
#121672=VERTEX_POINT ( 'NONE', #235404 ) ;
#121701=FACE_OUTER_BOUND ( 'NONE', #141249, .T. ) ;
#121714=ORIENTED_EDGE ( 'NONE', *, *, #16147, .F. ) ;
#121727=CARTESIAN_POINT ( 'NONE',  ( 21.05000000000000071, 65.49746832288732890, -162.4642776674505171 ) ) ;
#121728=CYLINDRICAL_SURFACE ( 'NONE', #131828, 0.09999999999999939493 ) ;
#121736=CARTESIAN_POINT ( 'NONE',  ( -20.94999999999999929, 87.48912529308842068, -167.0231074845242745 ) ) ;
#121784=ORIENTED_EDGE ( 'NONE', *, *, #150347, .F. ) ;
#121841=ADVANCED_FACE ( 'NONE', ( #244400 ), #181873, .F. ) ;
#121843=ORIENTED_EDGE ( 'NONE', *, *, #139163, .T. ) ;
#121849=CARTESIAN_POINT ( 'NONE',  ( 21.05000000000000071, 76.08559286337477090, -176.4367702193935656 ) ) ;
#121851=DIRECTION ( 'NONE',  ( 0.000000000000000000, 0.9893560106964510714, -0.1455152366551481502 ) ) ;
#121863=VERTEX_POINT ( 'NONE', #124476 ) ;
#121877=ORIENTED_EDGE ( 'NONE', *, *, #44358, .F. ) ;
#121887=ORIENTED_EDGE ( 'NONE', *, *, #31842, .F. ) ;
#121895=ORIENTED_EDGE ( 'NONE', *, *, #130199, .F. ) ;
#121897=DIRECTION ( 'NONE',  ( 0.000000000000000000, 6.982962677686266711E-15, -1.000000000000000000 ) ) ;
#121905=ORIENTED_EDGE ( 'NONE', *, *, #37964, .T. ) ;
#121906=CARTESIAN_POINT ( 'NONE',  ( -20.54999999999999716, 85.00000000001222134, -146.4170766071767389 ) ) ;
#121911=ADVANCED_FACE ( 'NONE', ( #149186 ), #91759, .F. ) ;
#121929=VERTEX_POINT ( 'NONE', #207883 ) ;
#121945=FACE_OUTER_BOUND ( 'NONE', #80172, .T. ) ;
#121983=ORIENTED_EDGE ( 'NONE', *, *, #89531, .F. ) ;
#121994=DIRECTION ( 'NONE',  ( -0.000000000000000000, 1.000000000000000000, 6.982962677686266711E-15 ) ) ;
#122009=EDGE_CURVE ( 'NONE', #225207, #125758, #226352, .T. ) ;
#122022=FACE_OUTER_BOUND ( 'NONE', #42152, .T. ) ;
#122069=DIRECTION ( 'NONE',  ( 0.7071067811865127117, 0.7071067811865821007, 0.000000000000000000 ) ) ;
#122079=EDGE_LOOP ( 'NONE', ( #45642, #107207, #80241, #60930 ) ) ;
#122087=EDGE_CURVE ( 'NONE', #251940, #219844, #130693, .T. ) ;
#122090=VECTOR ( 'NONE', #106474, 1000.000000000000000 ) ;
#122115=DIRECTION ( 'NONE',  ( 0.000000000000000000, 6.982962677686266711E-15, -1.000000000000000000 ) ) ;
#122136=ORIENTED_EDGE ( 'NONE', *, *, #29547, .F. ) ;
#122153=EDGE_CURVE ( 'NONE', #151457, #152968, #43402, .T. ) ;
#122172=DIRECTION ( 'NONE',  ( 8.673617379884087537E-15, 6.982962677686266711E-15, -1.000000000000000000 ) ) ;
#122181=LINE ( 'NONE', #25641, #39194 ) ;
#122207=CARTESIAN_POINT ( 'NONE',  ( 20.94999999999999574, 74.16465844978787914, -158.4679561919613775 ) ) ;
#122213=ORIENTED_EDGE ( 'NONE', *, *, #29979, .F. ) ;
#122222=DIRECTION ( 'NONE',  ( 0.000000000000000000, 0.000000000000000000, 1.000000000000000000 ) ) ;
#122226=AXIS2_PLACEMENT_3D ( 'NONE', #57550, #171147, #54974 ) ;
#122269=CARTESIAN_POINT ( 'NONE',  ( -23.15000000000000213, 74.00000000001223555, -149.7477294072864709 ) ) ;
#122282=EDGE_CURVE ( 'NONE', #113546, #115854, #210129, .T. ) ;
#122310=CARTESIAN_POINT ( 'NONE',  ( 22.49999999999999645, 64.25043287652299284, -170.1239658536231616 ) ) ;
#122358=VERTEX_POINT ( 'NONE', #177440 ) ;
#122381=ORIENTED_EDGE ( 'NONE', *, *, #98490, .T. ) ;
#122403=EDGE_LOOP ( 'NONE', ( #45976, #105822, #61090, #10464, #68787 ) ) ;
#122406=AXIS2_PLACEMENT_3D ( 'NONE', #42846, #126221, #67537 ) ;
#122408=DIRECTION ( 'NONE',  ( 0.000000000000000000, 0.000000000000000000, 1.000000000000000000 ) ) ;
#122432=ORIENTED_EDGE ( 'NONE', *, *, #202771, .F. ) ;
#122450=AXIS2_PLACEMENT_3D ( 'NONE', #251857, #215304, #155369 ) ;
#122457=ORIENTED_EDGE ( 'NONE', *, *, #133347, .T. ) ;
#122470=DIRECTION ( 'NONE',  ( 0.000000000000000000, -0.8660254037844420383, 0.4999999999999942824 ) ) ;
#122514=DIRECTION ( 'NONE',  ( 0.000000000000000000, 6.982962677686267499E-15, -1.000000000000000000 ) ) ;
#122541=AXIS2_PLACEMENT_3D ( 'NONE', #193305, #35540, #231161 ) ;
#122542=AXIS2_PLACEMENT_3D ( 'NONE', #63182, #26665, #7070 ) ;
#122550=CARTESIAN_POINT ( 'NONE',  ( 21.05000000000000071, 85.00000000001232081, -160.1291383618718385 ) ) ;
#122636=CARTESIAN_POINT ( 'NONE',  ( 23.14999999999999858, 79.90000000001214175, -136.5231074845243029 ) ) ;
#122653=ORIENTED_EDGE ( 'NONE', *, *, #100993, .F. ) ;
#122655=CARTESIAN_POINT ( 'NONE',  ( -1.739115166359751801E-14, 64.35000000001221565, -145.1731074845244507 ) ) ;
#122657=CARTESIAN_POINT ( 'NONE',  ( 20.94999999999999574, 77.26178616857734482, -161.9366085209788650 ) ) ;
#122697=FACE_OUTER_BOUND ( 'NONE', #17597, .T. ) ;
#122700=TOROIDAL_SURFACE ( 'NONE', #126769, 0.4000000000000005773, 0.1000000000000000056 ) ;
#122780=EDGE_CURVE ( 'NONE', #105518, #200975, #94981, .T. ) ;
#122793=VECTOR ( 'NONE', #37096, 1000.000000000000114 ) ;
#122796=EDGE_CURVE ( 'NONE', #218186, #99277, #88782, .T. ) ;
#122799=DIRECTION ( 'NONE',  ( 2.952720810173289112E-16, 1.000000000000000000, 6.982962677686266711E-15 ) ) ;
#122802=CARTESIAN_POINT ( 'NONE',  ( -20.64999999999999858, 74.00000000001223555, -149.2477294072864709 ) ) ;
#122888=CARTESIAN_POINT ( 'NONE',  ( 23.14999999999999503, 69.45000000001222418, -148.8731074845244109 ) ) ;
#122906=CARTESIAN_POINT ( 'NONE',  ( -18.41418431465368144, 85.50000000001233502, -129.9229180933028829 ) ) ;
#122923=FACE_OUTER_BOUND ( 'NONE', #402, .T. ) ;
#122942=ORIENTED_EDGE ( 'NONE', *, *, #16658, .T. ) ;
#122965=CARTESIAN_POINT ( 'NONE',  ( -18.50596464788227635, 65.69367753730678317, -131.0189238066348594 ) ) ;
#122972=CIRCLE ( 'NONE', #248229, 11.75000000000001066 ) ;
#123000=ORIENTED_EDGE ( 'NONE', *, *, #246110, .F. ) ;
#123029=DIRECTION ( 'NONE',  ( 0.000000000000000000, 0.000000000000000000, 1.000000000000000000 ) ) ;
#123044=CARTESIAN_POINT ( 'NONE',  ( -23.15000000000000213, 84.59626168225530307, -160.5729799673740104 ) ) ;
#123053=CARTESIAN_POINT ( 'NONE',  ( 20.94999999999999574, 74.83729825007431202, -162.1231074845243540 ) ) ;
#123056=FACE_OUTER_BOUND ( 'NONE', #49078, .T. ) ;
#123115=EDGE_CURVE ( 'NONE', #176041, #229965, #10972, .T. ) ;
#123174=AXIS2_PLACEMENT_3D ( 'NONE', #53904, #212977, #115163 ) ;
#123183=DIRECTION ( 'NONE',  ( 0.000000000000000000, -7.109473446599835262E-15, 1.000000000000000000 ) ) ;
#123219=ORIENTED_EDGE ( 'NONE', *, *, #156734, .F. ) ;
#123262=ORIENTED_EDGE ( 'NONE', *, *, #95303, .F. ) ;
#123275=CARTESIAN_POINT ( 'NONE',  ( -21.14999999999999858, 76.10085836911117951, -181.7726746080137445 ) ) ;
#123286=ADVANCED_FACE ( 'NONE', ( #122923 ), #164613, .T. ) ;
#123290=ADVANCED_FACE ( 'NONE', ( #23838 ), #27704, .T. ) ;
#123319=EDGE_LOOP ( 'NONE', ( #193215, #247719, #113164, #154487 ) ) ;
#123354=CONICAL_SURFACE ( 'NONE', #189987, 4.049999999999998046, 0.7853981633974604915 ) ;
#123357=CIRCLE ( 'NONE', #31809, 0.09999999999999971412 ) ;
#123398=VERTEX_POINT ( 'NONE', #229718 ) ;
#123435=DIRECTION ( 'NONE',  ( 0.000000000000000000, -0.9908441862701791170, 0.1350103645450472789 ) ) ;
#123497=AXIS2_PLACEMENT_3D ( 'NONE', #70797, #111182, #129458 ) ;
#123509=EDGE_LOOP ( 'NONE', ( #153939, #199366, #236135, #243633 ) ) ;
#123510=ORIENTED_EDGE ( 'NONE', *, *, #75459, .T. ) ;
#123544=LINE ( 'NONE', #204349, #93714 ) ;
#123568=FACE_OUTER_BOUND ( 'NONE', #72960, .T. ) ;
#123571=CARTESIAN_POINT ( 'NONE',  ( 23.14999999999999858, 78.10000000001214460, -136.5231074845243029 ) ) ;
#123576=FACE_OUTER_BOUND ( 'NONE', #245284, .T. ) ;
#123594=AXIS2_PLACEMENT_3D ( 'NONE', #128140, #188108, #47282 ) ;
#123602=B_SPLINE_CURVE_WITH_KNOTS ( 'NONE', 3,
 ( #116540, #132242, #211792, #100772, #163373, #219468, #139927, #82510, #198631, #218172, #2989, #180366, #122965, #43418, #202493, #4272, #40880, #162101, #179113 ),
 .UNSPECIFIED., .F., .F.,
 ( 4, 3, 3, 3, 3, 3, 4 ),
 ( 0.000000000000000000, 2.646747978908353324E-05, 5.271166642128909460E-05, 9.008788829885495768E-05, 0.0001426648776561096547, 0.0001897378458659754511, 0.0001917382627806486133 ),
 .UNSPECIFIED. ) ;
#123623=EDGE_CURVE ( 'NONE', #78078, #180142, #68439, .T. ) ;
#123631=EDGE_LOOP ( 'NONE', ( #68402, #254173, #197663, #187132 ) ) ;
#123639=CIRCLE ( 'NONE', #198462, 1.900000000000012790 ) ;
#123649=CYLINDRICAL_SURFACE ( 'NONE', #19970, 0.09999999999998898659 ) ;
#123662=VECTOR ( 'NONE', #30333, 1000.000000000000000 ) ;
#123666=CARTESIAN_POINT ( 'NONE',  ( -18.59999999999999787, 77.83585931145570669, -124.9186683157258244 ) ) ;
#123687=VECTOR ( 'NONE', #221726, 1000.000000000000000 ) ;
#123691=ORIENTED_EDGE ( 'NONE', *, *, #208940, .F. ) ;
#123699=CARTESIAN_POINT ( 'NONE',  ( 18.59999999999999432, 77.83585931145570669, -125.0186683157258045 ) ) ;
#123712=CARTESIAN_POINT ( 'NONE',  ( 18.59999999999999076, 65.79142135624952914, -148.6731074845244223 ) ) ;
#123719=CARTESIAN_POINT ( 'NONE',  ( 21.05000000000000071, 69.35000000001228670, -157.8731074845244109 ) ) ;
#123721=CARTESIAN_POINT ( 'NONE',  ( -23.25000000000000000, 85.00000000001223555, -145.8170766071767446 ) ) ;
#123722=DIRECTION ( 'NONE',  ( -0.000000000000000000, 1.000000000000000000, 8.717686153663073805E-15 ) ) ;
#123730=CARTESIAN_POINT ( 'NONE',  ( -18.59999999999999787, 64.35000000001214460, -136.5231074845244166 ) ) ;
#123750=FACE_OUTER_BOUND ( 'NONE', #181880, .T. ) ;
#123780=DIRECTION ( 'NONE',  ( 0.000000000000000000, 0.4999999999999088507, -0.8660254037844913322 ) ) ;
#123841=CARTESIAN_POINT ( 'NONE',  ( 23.24999999999999289, 64.25000000001244871, -181.7731074845244450 ) ) ;
#123863=VERTEX_POINT ( 'NONE', #10378 ) ;
#123864=CIRCLE ( 'NONE', #7321, 0.2000000000000057288 ) ;
#123881=DIRECTION ( 'NONE',  ( 0.000000000000000000, 0.4999999999999088507, -0.8660254037844913322 ) ) ;
#123909=EDGE_CURVE ( 'NONE', #206936, #161742, #15522, .T. ) ;
#123913=AXIS2_PLACEMENT_3D ( 'NONE', #123730, #63745, #104137 ) ;
#123915=EDGE_LOOP ( 'NONE', ( #245458, #97165, #224529, #61788 ) ) ;
#123934=EDGE_CURVE ( 'NONE', #108723, #15940, #176858, .T. ) ;
#123950=CARTESIAN_POINT ( 'NONE',  ( -18.50000000000000000, 69.15387683765952431, -132.7853812176745407 ) ) ;
#123952=AXIS2_PLACEMENT_3D ( 'NONE', #159289, #56300, #141007 ) ;
#123954=VERTEX_POINT ( 'NONE', #37647 ) ;
#123969=ORIENTED_EDGE ( 'NONE', *, *, #9279, .F. ) ;
#123973=DIRECTION ( 'NONE',  ( 0.000000000000000000, 7.056502275159890832E-15, -1.000000000000000000 ) ) ;
#123976=AXIS2_PLACEMENT_3D ( 'NONE', #116496, #34416, #193473 ) ;
#124003=EDGE_LOOP ( 'NONE', ( #172559, #83028, #183727, #17782 ) ) ;
#124029=ORIENTED_EDGE ( 'NONE', *, *, #137848, .T. ) ;
#124073=CIRCLE ( 'NONE', #19843, 0.09999999999999939493 ) ;
#124093=CARTESIAN_POINT ( 'NONE',  ( 22.60000000000000142, 64.25043287652299284, -170.1239658536231616 ) ) ;
#124110=EDGE_CURVE ( 'NONE', #118231, #18113, #85217, .T. ) ;
#124137=ADVANCED_FACE ( 'NONE', ( #90859 ), #158335, .T. ) ;
#124140=DIRECTION ( 'NONE',  ( 0.000000000000000000, -7.147358527629766941E-15, 1.000000000000000000 ) ) ;
#124158=CARTESIAN_POINT ( 'NONE',  ( -20.94999999999999929, 76.00000000001213607, -136.5231074845243313 ) ) ;
#124171=CARTESIAN_POINT ( 'NONE',  ( 21.05000000000000071, 76.03753606329811987, -176.3553797584600318 ) ) ;
#124182=CARTESIAN_POINT ( 'NONE',  ( -23.15000000000000213, 64.25000000001227818, -157.8731074845244393 ) ) ;
#124183=ORIENTED_EDGE ( 'NONE', *, *, #194535, .F. ) ;
#124193=CARTESIAN_POINT ( 'NONE',  ( -18.42637059832564006, 85.49694546190180233, -129.9140301747244450 ) ) ;
#124197=CARTESIAN_POINT ( 'NONE',  ( 21.05000000000000071, 76.00000000001237765, -170.0231074845243597 ) ) ;
#124218=DIRECTION ( 'NONE',  ( 3.265361837132813093E-16, 1.000000000000000000, 6.982962677686266711E-15 ) ) ;
#124224=ORIENTED_EDGE ( 'NONE', *, *, #217770, .T. ) ;
#124230=DIRECTION ( 'NONE',  ( 0.000000000000000000, 6.982962677686266711E-15, -1.000000000000000000 ) ) ;
#124255=ORIENTED_EDGE ( 'NONE', *, *, #91718, .T. ) ;
#124280=ORIENTED_EDGE ( 'NONE', *, *, #79648, .T. ) ;
#124289=CARTESIAN_POINT ( 'NONE',  ( -22.39999999999999858, 68.20922040163897293, -170.1231074845244109 ) ) ;
#124304=DIRECTION ( 'NONE',  ( 1.000000000000000000, 0.000000000000000000, 0.000000000000000000 ) ) ;
#124338=ORIENTED_EDGE ( 'NONE', *, *, #246686, .T. ) ;
#124378=DIRECTION ( 'NONE',  ( 0.000000000000000000, -0.1495327102803283015, -0.9887567792719397231 ) ) ;
#124391=VECTOR ( 'NONE', #16791, 1000.000000000000000 ) ;
#124410=CARTESIAN_POINT ( 'NONE',  ( -20.94999999999999929, 77.16412189325330928, -128.8082593989527425 ) ) ;
#124476=CARTESIAN_POINT ( 'NONE',  ( 21.05000000000000071, 87.48912529308842068, -167.1231074845242688 ) ) ;
#124496=DIRECTION ( 'NONE',  ( -0.000000000000000000, -0.8660254037844420383, 0.4999999999999943379 ) ) ;
#124498=DIRECTION ( 'NONE',  ( 1.734723475976817507E-14, -6.982962677686266711E-15, 1.000000000000000000 ) ) ;
#124512=TOROIDAL_SURFACE ( 'NONE', #103629, 4.149999999999999467, 0.1000000000000000056 ) ;
#124608=CARTESIAN_POINT ( 'NONE',  ( 20.94983749550516450, 65.70233904877032671, -131.0487410911968880 ) ) ;
#124629=ORIENTED_EDGE ( 'NONE', *, *, #116792, .T. ) ;
#124665=CARTESIAN_POINT ( 'NONE',  ( 18.52928932188133970, 65.72071067813085676, -145.3731074845244109 ) ) ;
#124667=DIRECTION ( 'NONE',  ( 0.000000000000000000, -6.982962677686266711E-15, 1.000000000000000000 ) ) ;
#124687=FACE_OUTER_BOUND ( 'NONE', #225686, .T. ) ;
#124688=ADVANCED_FACE ( 'NONE', ( #178809 ), #68902, .T. ) ;
#124692=AXIS2_PLACEMENT_3D ( 'NONE', #10781, #249398, #91600 ) ;
#124698=CARTESIAN_POINT ( 'NONE',  ( -23.15000000000000213, 76.00000000001213607, -136.5231074845243313 ) ) ;
#124720=DIRECTION ( 'NONE',  ( 0.000000000000000000, 0.1350103645451807555, 0.9908441862701609093 ) ) ;
#124725=ORIENTED_EDGE ( 'NONE', *, *, #54510, .F. ) ;
#124816=ORIENTED_EDGE ( 'NONE', *, *, #138957, .T. ) ;
#124833=ORIENTED_EDGE ( 'NONE', *, *, #200606, .T. ) ;
#124855=ORIENTED_EDGE ( 'NONE', *, *, #52182, .T. ) ;
#124869=AXIS2_PLACEMENT_3D ( 'NONE', #40164, #200493, #180933 ) ;
#124870=ADVANCED_FACE ( 'NONE', ( #5233 ), #206428, .T. ) ;
#124887=EDGE_CURVE ( 'NONE', #4792, #95398, #221717, .T. ) ;
#124904=DIRECTION ( 'NONE',  ( 0.000000000000000000, 0.000000000000000000, -1.000000000000000000 ) ) ;
#124912=DIRECTION ( 'NONE',  ( -2.915501640297152804E-16, -1.000000000000000000, -6.997203936713167125E-15 ) ) ;
#124939=CARTESIAN_POINT ( 'NONE',  ( -20.64999999999999858, 76.00000000001237765, -170.0231074845243597 ) ) ;
#124967=ADVANCED_FACE ( 'NONE', ( #49532 ), #177426, .T. ) ;
#124984=DIRECTION ( 'NONE',  ( 1.000000000000000000, 0.000000000000000000, 0.000000000000000000 ) ) ;
#125012=CARTESIAN_POINT ( 'NONE',  ( 20.04142135623730070, 64.35000000001222986, -148.6731074845244507 ) ) ;
#125031=DIRECTION ( 'NONE',  ( 1.000000000000000000, 0.000000000000000000, 0.000000000000000000 ) ) ;
#125053=EDGE_CURVE ( 'NONE', #250411, #120222, #218530, .T. ) ;
#125062=CARTESIAN_POINT ( 'NONE',  ( -23.25000000000000000, 77.73670573947964613, -125.0056848969006182 ) ) ;
#125088=DIRECTION ( 'NONE',  ( -0.000000000000000000, 0.1298341882519953583, 0.9915357197604862671 ) ) ;
#125121=CARTESIAN_POINT ( 'NONE',  ( 21.14999999999999858, 76.00000000001242029, -176.5637644362255969 ) ) ;
#125161=ORIENTED_EDGE ( 'NONE', *, *, #143036, .F. ) ;
#125163=ORIENTED_EDGE ( 'NONE', *, *, #67009, .T. ) ;
#125189=VECTOR ( 'NONE', #229836, 1000.000000000000000 ) ;
#125206=ORIENTED_EDGE ( 'NONE', *, *, #86463, .T. ) ;
#125287=CARTESIAN_POINT ( 'NONE',  ( 21.04999999999999716, 67.10527618163473562, -161.5360231613763915 ) ) ;
#125324=EDGE_CURVE ( 'NONE', #99053, #109724, #35941, .T. ) ;
#125341=ORIENTED_EDGE ( 'NONE', *, *, #19240, .T. ) ;
#125368=VECTOR ( 'NONE', #170904, 1000.000000000000000 ) ;
#125390=ADVANCED_FACE ( 'NONE', ( #142351 ), #202514, .T. ) ;
#125411=LINE ( 'NONE', #44589, #254859 ) ;
#125435=DIRECTION ( 'NONE',  ( 0.000000000000000000, 6.982962677686266711E-15, -1.000000000000000000 ) ) ;
#125460=CIRCLE ( 'NONE', #217007, 0.1000000000000028644 ) ;
#125477=CARTESIAN_POINT ( 'NONE',  ( -20.85000000000000142, 68.97833521811203639, -132.6895420826271277 ) ) ;
#125512=EDGE_CURVE ( 'NONE', #258015, #182460, #199636, .T. ) ;
#125516=( BOUNDED_SURFACE ( )  B_SPLINE_SURFACE ( 3, 2, ( 
 ( #201028, #170620, #71488 ),
 ( #106715, #147137, #89727 ),
 ( #29808, #186287, #28534 ),
 ( #7643, #121514, #101892 ),
 ( #87155, #181478, #161920 ),
 ( #247535, #130140, #169323 ),
 ( #2803, #68918, #62798 ),
 ( #31092, #82325, #241446 ),
 ( #149742, #126289, #108028 ),
 ( #187583, #142321, #221839 ),
 ( #190137, #229266, #50593 ),
 ( #70207, #209691, #166748 ) ),
 .UNSPECIFIED., .F., .F., .F. ) 
 B_SPLINE_SURFACE_WITH_KNOTS ( ( 4, 2, 2, 2, 2, 4 ),
 ( 3, 3 ),
 ( 3.174653483277205090, 3.943930578431714018, 4.713207673586222946, 5.482484768740731873, 5.867123316317986337, 6.251761863895240801 ),
 ( 0.000000000000000000, 1.000000000000000000 ),
 .UNSPECIFIED. ) 
 GEOMETRIC_REPRESENTATION_ITEM ( )  RATIONAL_B_SPLINE_SURFACE ( (
 ( 1.000000000000000000, 0.8659465255642114778, 1.000000000000000000),
 ( 1.000000000000000000, 0.8648614068487411322, 1.000000000000000000),
 ( 1.000000000000000000, 0.8489031841324523597, 1.000000000000000000),
 ( 1.000000000000000000, 0.7927507630160768315, 1.000000000000000000),
 ( 1.000000000000000000, 0.7523013859006951742, 1.000000000000000000),
 ( 1.000000000000000000, 0.6616226951198839190, 1.000000000000000000),
 ( 1.000000000000000000, 0.6112214368721479163, 1.000000000000000000),
 ( 1.000000000000000000, 0.5507684314500016498, 1.000000000000000000),
 ( 1.000000000000000000, 0.5333267243152196579, 1.000000000000000000),
 ( 1.000000000000000000, 0.5084565446481067452, 1.000000000000000000),
 ( 1.000000000000000000, 0.5010722703450574134, 1.000000000000000000),
 ( 1.000000000000000000, 0.5001234037138888588, 1.000000000000000000) ) ) 
 REPRESENTATION_ITEM ( '' )  SURFACE ( )  );
#125521=ADVANCED_FACE ( 'NONE', ( #69260 ), #194161, .F. ) ;
#125544=AXIS2_PLACEMENT_3D ( 'NONE', #122207, #162623, #43943 ) ;
#125545=ORIENTED_EDGE ( 'NONE', *, *, #82829, .T. ) ;
#125553=ORIENTED_EDGE ( 'NONE', *, *, #210911, .F. ) ;
#125555=DIRECTION ( 'NONE',  ( 1.000000000000000000, 1.110223024625155531E-13, 0.000000000000000000 ) ) ;
#125556=DIRECTION ( 'NONE',  ( 1.000000000000000000, 0.000000000000000000, 0.000000000000000000 ) ) ;
#125558=DIRECTION ( 'NONE',  ( 0.000000000000000000, -6.982962677686266711E-15, 1.000000000000000000 ) ) ;
#125668=DIRECTION ( 'NONE',  ( 1.000000000000000000, 0.000000000000000000, 0.000000000000000000 ) ) ;
#125708=VERTEX_POINT ( 'NONE', #241172 ) ;
#125716=DIRECTION ( 'NONE',  ( -0.000000000000000000, 0.2605042016806385363, 0.9654727137038795481 ) ) ;
#125758=VERTEX_POINT ( 'NONE', #24706 ) ;
#125768=DIRECTION ( 'NONE',  ( -1.000000000000000000, -0.000000000000000000, -0.000000000000000000 ) ) ;
#125787=CIRCLE ( 'NONE', #871, 0.09999999999998898659 ) ;
#125794=EDGE_LOOP ( 'NONE', ( #95291, #186850, #68966 ) ) ;
#125850=DIRECTION ( 'NONE',  ( 0.000000000000000000, -6.982962677686266711E-15, 1.000000000000000000 ) ) ;
#125865=CARTESIAN_POINT ( 'NONE',  ( -20.87155475150660777, 64.25000000001220712, -143.4275209553668162 ) ) ;
#125870=CARTESIAN_POINT ( 'NONE',  ( -21.05000000000000071, 69.72991413632323088, -170.0579754875375329 ) ) ;
#125883=DIRECTION ( 'NONE',  ( 0.000000000000000000, -7.116814260417693756E-15, 1.000000000000000000 ) ) ;
#125901=CARTESIAN_POINT ( 'NONE',  ( -20.15000000000000568, 66.70857864377498458, -157.6731074845244223 ) ) ;
#125921=DIRECTION ( 'NONE',  ( -0.1538461538461484146, -0.9880948137434723000, 0.000000000000000000 ) ) ;
#125924=CARTESIAN_POINT ( 'NONE',  ( -18.59999999999999787, 68.97833521811203639, -132.6895420826271277 ) ) ;
#125930=ORIENTED_EDGE ( 'NONE', *, *, #58259, .F. ) ;
#125940=AXIS2_PLACEMENT_3D ( 'NONE', #119728, #143106, #83107 ) ;
#125941=AXIS2_PLACEMENT_3D ( 'NONE', #96476, #220312, #121243 ) ;
#125964=CIRCLE ( 'NONE', #159323, 0.09999999999998898659 ) ;
#125992=EDGE_CURVE ( 'NONE', #133057, #58091, #37206, .T. ) ;
#125999=DIRECTION ( 'NONE',  ( 1.000000000000000000, 0.000000000000000000, 0.000000000000000000 ) ) ;
#126033=ADVANCED_FACE ( 'NONE', ( #198821 ), #197534, .F. ) ;
#126040=ORIENTED_EDGE ( 'NONE', *, *, #16673, .T. ) ;
#126050=CARTESIAN_POINT ( 'NONE',  ( -23.25000000000000000, 76.10085836911117951, -181.7726746080137445 ) ) ;
#126092=FACE_OUTER_BOUND ( 'NONE', #50032, .T. ) ;
#126108=CARTESIAN_POINT ( 'NONE',  ( 21.00000000000000000, 66.25000000001223555, -148.7731074845244450 ) ) ;
#126162=AXIS2_PLACEMENT_3D ( 'NONE', #199252, #4851, #84364 ) ;
#126173=ORIENTED_EDGE ( 'NONE', *, *, #124887, .F. ) ;
#126183=ORIENTED_EDGE ( 'NONE', *, *, #200033, .T. ) ;
#126217=EDGE_CURVE ( 'NONE', #109454, #182460, #256995, .T. ) ;
#126221=DIRECTION ( 'NONE',  ( 0.000000000000000000, -6.982962677686266711E-15, 1.000000000000000000 ) ) ;
#126226=EDGE_CURVE ( 'NONE', #82525, #39426, #195978, .T. ) ;
#126249=ORIENTED_EDGE ( 'NONE', *, *, #11019, .F. ) ;
#126276=DIRECTION ( 'NONE',  ( -1.000000000000000000, 0.000000000000000000, 0.000000000000000000 ) ) ;
#126289=CARTESIAN_POINT ( 'NONE',  ( 20.50589344625199217, 65.51681206853677963, -162.4501125058534399 ) ) ;
#126313=DIRECTION ( 'NONE',  ( 0.000000000000000000, -1.000000000000000000, -6.982962677686265922E-15 ) ) ;
#126346=CARTESIAN_POINT ( 'NONE',  ( -18.59999999999999787, 77.14957036958777792, -128.7071950000224092 ) ) ;
#126408=DIRECTION ( 'NONE',  ( 1.000000000000000000, 0.000000000000000000, 0.000000000000000000 ) ) ;
#126416=EDGE_CURVE ( 'NONE', #136655, #200182, #132155, .T. ) ;
#126432=CARTESIAN_POINT ( 'NONE',  ( -21.44999999999999929, 68.65000000001222702, -148.7731074845244166 ) ) ;
#126458=DIRECTION ( 'NONE',  ( 0.000000000000000000, -0.9998779222360097974, 0.01562500000000363945 ) ) ;
#126488=EDGE_LOOP ( 'NONE', ( #257176, #64737, #56141, #240781 ) ) ;
#126496=ORIENTED_EDGE ( 'NONE', *, *, #53523, .F. ) ;
#126510=EDGE_CURVE ( 'NONE', #218493, #38619, #69805, .T. ) ;
#126545=ORIENTED_EDGE ( 'NONE', *, *, #143595, .F. ) ;
#126552=DIRECTION ( 'NONE',  ( 0.000000000000000000, -1.000000000000000000, -6.982962677686265922E-15 ) ) ;
#126562=ORIENTED_EDGE ( 'NONE', *, *, #227403, .T. ) ;
#126585=DIRECTION ( 'NONE',  ( -1.000000000000000000, 0.000000000000000000, -0.000000000000000000 ) ) ;
#126636=EDGE_LOOP ( 'NONE', ( #189068, #86645, #197057, #88386 ) ) ;
#126671=EDGE_CURVE ( 'NONE', #12740, #9341, #153208, .T. ) ;
#126685=DIRECTION ( 'NONE',  ( 1.000000000000000000, 0.000000000000000000, 0.000000000000000000 ) ) ;
#126689=PLANE ( 'NONE',  #245696 ) ;
#126769=AXIS2_PLACEMENT_3D ( 'NONE', #209652, #89687, #127550 ) ;
#126839=CARTESIAN_POINT ( 'NONE',  ( -21.51976009735018991, 69.08954155835317579, -170.0231074845243882 ) ) ;
#126845=DIRECTION ( 'NONE',  ( -1.000000000000000000, -0.000000000000000000, -0.000000000000000000 ) ) ;
#126848=DIRECTION ( 'NONE',  ( 0.000000000000000000, -6.938893903907222067E-15, 1.000000000000000000 ) ) ;
#126850=CARTESIAN_POINT ( 'NONE',  ( 22.49999999999999645, 75.89914163091373212, -181.7726746080137445 ) ) ;
#126871=AXIS2_PLACEMENT_3D ( 'NONE', #117699, #65426, #184089 ) ;
#126888=DIRECTION ( 'NONE',  ( 0.000000000000000000, 1.000000000000000000, 6.352154140967427193E-15 ) ) ;
#126901=DIRECTION ( 'NONE',  ( 0.000000000000000000, 0.000000000000000000, 1.000000000000000000 ) ) ;
#126925=FACE_OUTER_BOUND ( 'NONE', #60762, .T. ) ;
#126932=ORIENTED_EDGE ( 'NONE', *, *, #4434, .F. ) ;
#126942=DIRECTION ( 'NONE',  ( -1.000000000000000000, 3.265361837132813093E-16, 2.280189983783949500E-30 ) ) ;
#126961=VERTEX_POINT ( 'NONE', #230630 ) ;
#127003=FACE_OUTER_BOUND ( 'NONE', #222227, .T. ) ;
#127058=VERTEX_POINT ( 'NONE', #256535 ) ;
#127075=CARTESIAN_POINT ( 'NONE',  ( -20.54999999999999716, 74.00000000001223555, -149.7477294072864709 ) ) ;
#127081=ORIENTED_EDGE ( 'NONE', *, *, #10714, .T. ) ;
#127101=DIRECTION ( 'NONE',  ( -0.000000000000000000, -6.982962677686266711E-15, 1.000000000000000000 ) ) ;
#127148=CARTESIAN_POINT ( 'NONE',  ( -20.94999999999999929, 87.48912529308842068, -166.9231074845242802 ) ) ;
#127167=EDGE_CURVE ( 'NONE', #238290, #195092, #233156, .T. ) ;
#127214=VECTOR ( 'NONE', #23515, 1000.000000000000000 ) ;
#127225=CIRCLE ( 'NONE', #64674, 11.80000000000000426 ) ;
#127283=CARTESIAN_POINT ( 'NONE',  ( -23.25000000000000000, 85.00000000001232081, -160.1291383618718385 ) ) ;
#127294=DIRECTION ( 'NONE',  ( -0.000000000000000000, -6.982962677686266711E-15, 1.000000000000000000 ) ) ;
#127299=AXIS2_PLACEMENT_3D ( 'NONE', #103383, #202510, #23906 ) ;
#127304=VERTEX_POINT ( 'NONE', #73832 ) ;
#127322=VECTOR ( 'NONE', #14075, 1000.000000000000000 ) ;
#127337=VERTEX_POINT ( 'NONE', #69971 ) ;
#127349=AXIS2_PLACEMENT_3D ( 'NONE', #172302, #35350, #114844 ) ;
#127359=ORIENTED_EDGE ( 'NONE', *, *, #217770, .F. ) ;
#127363=DIRECTION ( 'NONE',  ( -1.000000000000000000, 2.952720810173289112E-16, 2.061873921506763405E-30 ) ) ;
#127366=ORIENTED_EDGE ( 'NONE', *, *, #155616, .T. ) ;
#127393=EDGE_CURVE ( 'NONE', #69711, #226308, #83258, .T. ) ;
#127421=DIRECTION ( 'NONE',  ( 0.000000000000000000, -6.982962677686267499E-15, 1.000000000000000000 ) ) ;
#127422=LINE ( 'NONE', #110416, #41009 ) ;
#127426=EDGE_LOOP ( 'NONE', ( #131501, #141848, #217045, #231269 ) ) ;
#127438=CARTESIAN_POINT ( 'NONE',  ( 18.60000000000000142, 85.32100840337361092, -162.7871692354463846 ) ) ;
#127440=ORIENTED_EDGE ( 'NONE', *, *, #36647, .F. ) ;
#127500=CARTESIAN_POINT ( 'NONE',  ( 20.94999999999999574, 87.65000000001234071, -166.9231074845242802 ) ) ;
#127550=DIRECTION ( 'NONE',  ( 0.000000000000000000, 0.000000000000000000, 1.000000000000000000 ) ) ;
#127624=DIRECTION ( 'NONE',  ( 0.000000000000000000, 0.1298341882519953583, 0.9915357197604862671 ) ) ;
#127639=VECTOR ( 'NONE', #124496, 999.9999999999998863 ) ;
#127646=CARTESIAN_POINT ( 'NONE',  ( -21.44999999999999929, 68.85000000001222986, -148.8731074845244109 ) ) ;
#127667=EDGE_CURVE ( 'NONE', #9341, #219647, #251807, .T. ) ;
#127714=ORIENTED_EDGE ( 'NONE', *, *, #111307, .T. ) ;
#127757=EDGE_CURVE ( 'NONE', #200243, #60057, #128022, .T. ) ;
#127762=VERTEX_POINT ( 'NONE', #179993 ) ;
#127786=VERTEX_POINT ( 'NONE', #181286 ) ;
#127830=ORIENTED_EDGE ( 'NONE', *, *, #216867, .T. ) ;
#127847=CIRCLE ( 'NONE', #48713, 2.000000000000001776 ) ;
#127849=AXIS2_PLACEMENT_3D ( 'NONE', #109423, #169457, #106857 ) ;
#127859=DIRECTION ( 'NONE',  ( 1.000000000000000000, 0.000000000000000000, 0.000000000000000000 ) ) ;
#127875=FACE_OUTER_BOUND ( 'NONE', #72138, .T. ) ;
#127895=CIRCLE ( 'NONE', #19566, 0.1000000000000070832 ) ;
#127910=VECTOR ( 'NONE', #244104, 1000.000000000000000 ) ;
#127955=DIRECTION ( 'NONE',  ( -0.000000000000000000, 1.000000000000000000, 6.982962677686266711E-15 ) ) ;
#127958=ORIENTED_EDGE ( 'NONE', *, *, #12329, .T. ) ;
#128018=DIRECTION ( 'NONE',  ( -1.000000000000000000, 0.000000000000000000, -0.000000000000000000 ) ) ;
#128022=CIRCLE ( 'NONE', #157257, 0.09999999999999939493 ) ;
#128027=EDGE_LOOP ( 'NONE', ( #106027, #235810, #90171 ) ) ;
#128043=DIRECTION ( 'NONE',  ( 1.000000000000000000, -0.000000000000000000, 0.000000000000000000 ) ) ;
#128082=AXIS2_PLACEMENT_3D ( 'NONE', #110622, #71523, #127624 ) ;
#128090=DIRECTION ( 'NONE',  ( 1.000000000000000000, 0.000000000000000000, 0.000000000000000000 ) ) ;
#128123=VECTOR ( 'NONE', #34314, 1000.000000000000000 ) ;
#128140=CARTESIAN_POINT ( 'NONE',  ( 18.59999999999996945, 68.97833521811203639, -132.6895420826271277 ) ) ;
#128142=DIRECTION ( 'NONE',  ( -1.000000000000000000, 0.000000000000000000, 0.000000000000000000 ) ) ;
#128145=FACE_OUTER_BOUND ( 'NONE', #2066, .T. ) ;
#128170=ORIENTED_EDGE ( 'NONE', *, *, #239377, .F. ) ;
#128185=AXIS2_PLACEMENT_3D ( 'NONE', #160950, #185635, #224740 ) ;
#128189=ORIENTED_EDGE ( 'NONE', *, *, #245508, .F. ) ;
#128250=ORIENTED_EDGE ( 'NONE', *, *, #19713, .F. ) ;
#128309=DIRECTION ( 'NONE',  ( -1.000000000000000000, 0.000000000000000000, -0.000000000000000000 ) ) ;
#128335=EDGE_CURVE ( 'NONE', #26629, #103428, #211592, .T. ) ;
#128440=AXIS2_PLACEMENT_3D ( 'NONE', #52259, #191827, #73164 ) ;
#128453=CARTESIAN_POINT ( 'NONE',  ( -20.85000000106584750, 64.25000000001220712, -143.3676028280510764 ) ) ;
#128454=CARTESIAN_POINT ( 'NONE',  ( 20.95496329884391784, 65.43256679391929254, -162.4487975522395971 ) ) ;
#128475=CARTESIAN_POINT ( 'NONE',  ( 20.99551997958397465, 64.25000000001217870, -143.3714483468355638 ) ) ;
#128506=VERTEX_POINT ( 'NONE', #206490 ) ;
#128528=ADVANCED_FACE ( 'NONE', ( #5690 ), #108674, .F. ) ;
#128529=DIRECTION ( 'NONE',  ( -0.000000000000000000, -6.982962677686266711E-15, 1.000000000000000000 ) ) ;
#128544=AXIS2_PLACEMENT_3D ( 'NONE', #41699, #217727, #59935 ) ;
#128575=ORIENTED_EDGE ( 'NONE', *, *, #35503, .T. ) ;
#128608=CIRCLE ( 'NONE', #149292, 0.09999999999998898659 ) ;
#128626=VERTEX_POINT ( 'NONE', #133384 ) ;
#128632=EDGE_CURVE ( 'NONE', #9791, #45573, #215834, .T. ) ;
#128639=AXIS2_PLACEMENT_3D ( 'NONE', #162143, #104675, #43460 ) ;
#128640=DIRECTION ( 'NONE',  ( 0.000000000000000000, -6.982962677686266711E-15, 1.000000000000000000 ) ) ;
#128650=DIRECTION ( 'NONE',  ( 0.000000000000000000, -6.853228547068871147E-15, 1.000000000000000000 ) ) ;
#128659=VERTEX_POINT ( 'NONE', #90384 ) ;
#128683=DIRECTION ( 'NONE',  ( 1.000000000000000000, -2.952720810173289112E-16, -2.061873921506763405E-30 ) ) ;
#128736=DIRECTION ( 'NONE',  ( 0.000000000000000000, -6.982962677686266711E-15, 1.000000000000000000 ) ) ;
#128748=VECTOR ( 'NONE', #174757, 1000.000000000000000 ) ;
#128751=TOROIDAL_SURFACE ( 'NONE', #178861, 0.2000000000000000111, 0.1000000000000000056 ) ;
#128760=ORIENTED_EDGE ( 'NONE', *, *, #138957, .F. ) ;
#128766=VERTEX_POINT ( 'NONE', #253460 ) ;
#128785=ORIENTED_EDGE ( 'NONE', *, *, #3775, .F. ) ;
#128797=CARTESIAN_POINT ( 'NONE',  ( -21.05000000000000071, 74.83729825007431202, -162.0231074845243597 ) ) ;
#128807=ORIENTED_EDGE ( 'NONE', *, *, #4987, .T. ) ;
#128819=CARTESIAN_POINT ( 'NONE',  ( 20.94999999999999929, 65.27628289530470340, -148.7731074845244450 ) ) ;
#128843=FACE_OUTER_BOUND ( 'NONE', #154847, .T. ) ;
#128845=EDGE_CURVE ( 'NONE', #104106, #117472, #123602, .T. ) ;
#128847=CYLINDRICAL_SURFACE ( 'NONE', #145692, 0.09999999999999939493 ) ;
#128889=CARTESIAN_POINT ( 'NONE',  ( 22.49436431346199683, 75.93309647029019516, -181.6730584321778110 ) ) ;
#128918=DIRECTION ( 'NONE',  ( 0.000000000000000000, 0.000000000000000000, 1.000000000000000000 ) ) ;
#128945=EDGE_CURVE ( 'NONE', #42435, #50990, #61926, .T. ) ;
#128947=VERTEX_POINT ( 'NONE', #185497 ) ;
#128984=DIRECTION ( 'NONE',  ( 0.000000000000000000, -7.272083257015735086E-15, 1.000000000000000000 ) ) ;
#129087=ORIENTED_EDGE ( 'NONE', *, *, #167454, .F. ) ;
#129127=EDGE_CURVE ( 'NONE', #67356, #52417, #57988, .T. ) ;
#129150=FACE_OUTER_BOUND ( 'NONE', #46196, .T. ) ;
#129153=ORIENTED_EDGE ( 'NONE', *, *, #1617, .F. ) ;
#129155=CARTESIAN_POINT ( 'NONE',  ( -20.54999999999999716, 74.00000000001229239, -156.7984855617622770 ) ) ;
#129185=CARTESIAN_POINT ( 'NONE',  ( 20.85000000000000142, 76.00000000001213607, -136.5231074845243313 ) ) ;
#129196=CARTESIAN_POINT ( 'NONE',  ( 21.14999999999999858, 69.45934304831114048, -170.0231074845243882 ) ) ;
#129222=CARTESIAN_POINT ( 'NONE',  ( -21.13498764882296044, 75.99834360528109301, -176.5187256279983217 ) ) ;
#129223=EDGE_CURVE ( 'NONE', #165825, #137060, #62111, .T. ) ;
#129228=ORIENTED_EDGE ( 'NONE', *, *, #184007, .T. ) ;
#129229=CARTESIAN_POINT ( 'NONE',  ( 21.07933241753356768, 69.67135405163263329, -170.1164870749437057 ) ) ;
#129250=TOROIDAL_SURFACE ( 'NONE', #62617, 11.70000000000000639, 0.1000000000000000056 ) ;
#129321=ORIENTED_EDGE ( 'NONE', *, *, #109624, .T. ) ;
#129364=ORIENTED_EDGE ( 'NONE', *, *, #28637, .F. ) ;
#129386=DIRECTION ( 'NONE',  ( 1.000000000000000000, -3.265361837132813093E-16, -2.280189983783949500E-30 ) ) ;
#129399=CARTESIAN_POINT ( 'NONE',  ( 23.15000000000000213, 84.59626168225520360, -145.9732350016745954 ) ) ;
#129417=CARTESIAN_POINT ( 'NONE',  ( 22.50046968637550648, 75.95483015286804118, -181.7731526389976295 ) ) ;
#129446=CARTESIAN_POINT ( 'NONE',  ( 21.30000000000002558, 76.00000000001240608, -174.0731074845243711 ) ) ;
#129458=DIRECTION ( 'NONE',  ( 2.952720810173289112E-16, 1.000000000000000000, 6.982962677686266711E-15 ) ) ;
#129477=ORIENTED_EDGE ( 'NONE', *, *, #155947, .F. ) ;
#129504=CARTESIAN_POINT ( 'NONE',  ( 20.95512820512820440, 65.37615131630035137, -148.7731074845244450 ) ) ;
#129537=CARTESIAN_POINT ( 'NONE',  ( 21.53752568617687402, 69.21319212550855582, -170.1220819458087874 ) ) ;
#129545=CARTESIAN_POINT ( 'NONE',  ( -20.64999999999999858, 74.00000000001229239, -157.2984855617622770 ) ) ;
#129550=CARTESIAN_POINT ( 'NONE',  ( 20.94999999999999929, 76.00000000001212186, -134.5231074845243313 ) ) ;
#129573=EDGE_CURVE ( 'NONE', #59304, #66247, #132455, .T. ) ;
#129630=DIRECTION ( 'NONE',  ( 0.000000000000000000, -0.7397360091702802620, 0.6728971962616779878 ) ) ;
#129641=VERTEX_POINT ( 'NONE', #119456 ) ;
#129695=CARTESIAN_POINT ( 'NONE',  ( 20.94999999999999574, 74.73821383144729680, -161.9366085209788935 ) ) ;
#129729=ADVANCED_FACE ( 'NONE', ( #130998 ), #140839, .F. ) ;
#129754=CARTESIAN_POINT ( 'NONE',  ( 21.04386569057582079, 64.25000000001217870, -143.3802701327438172 ) ) ;
#129766=EDGE_LOOP ( 'NONE', ( #152281, #185467, #108603, #164426 ) ) ;
#129768=EDGE_LOOP ( 'NONE', ( #17852, #133207 ) ) ;
#129773=ORIENTED_EDGE ( 'NONE', *, *, #85953, .F. ) ;
#129780=ORIENTED_EDGE ( 'NONE', *, *, #179673, .T. ) ;
#129789=DIRECTION ( 'NONE',  ( 2.557131231893037478E-16, 0.8660254037844420383, -0.4999999999999943379 ) ) ;
#129798=DIRECTION ( 'NONE',  ( 1.000000000000000000, 0.000000000000000000, 0.000000000000000000 ) ) ;
#129827=CYLINDRICAL_SURFACE ( 'NONE', #83806, 0.1000000000000028644 ) ;
#129848=TOROIDAL_SURFACE ( 'NONE', #9064, 7.800000000000000711, 0.1000000000000000056 ) ;
#129920=CARTESIAN_POINT ( 'NONE',  ( -21.29999999999995808, 76.00000000001234923, -165.9731074845243768 ) ) ;
#129932=LINE ( 'NONE', #191241, #184396 ) ;
#129947=ORIENTED_EDGE ( 'NONE', *, *, #87536, .T. ) ;
#129975=EDGE_CURVE ( 'NONE', #165339, #38619, #13624, .T. ) ;
#129987=CARTESIAN_POINT ( 'NONE',  ( -20.64999999999999858, 71.75000000001229239, -157.7731074845243882 ) ) ;
#129998=CARTESIAN_POINT ( 'NONE',  ( -20.94999999999999929, 64.25000000001232081, -163.0083017138704236 ) ) ;
#130003=DIRECTION ( 'NONE',  ( 0.000000000000000000, -6.982962677686266711E-15, 1.000000000000000000 ) ) ;
#130007=FACE_OUTER_BOUND ( 'NONE', #127426, .T. ) ;
#130022=AXIS2_PLACEMENT_3D ( 'NONE', #250433, #71820, #140762 ) ;
#130045=ADVANCED_FACE ( 'NONE', ( #163411 ), #209327, .F. ) ;
#130069=ORIENTED_EDGE ( 'NONE', *, *, #206612, .T. ) ;
#130105=DIRECTION ( 'NONE',  ( 0.000000000000000000, 6.982962677686266711E-15, -1.000000000000000000 ) ) ;
#130120=LINE ( 'NONE', #34919, #187913 ) ;
#130130=DIRECTION ( 'NONE',  ( -1.000000000000000000, 2.952720810173289112E-16, 2.061873921506763405E-30 ) ) ;
#130139=DIRECTION ( 'NONE',  ( 1.000000000000000000, 0.000000000000000000, 0.000000000000000000 ) ) ;
#130140=CARTESIAN_POINT ( 'NONE',  ( 20.11144452914042802, 66.06638914889235537, -162.1328140305747070 ) ) ;
#130145=DIRECTION ( 'NONE',  ( 4.408576920032446739E-17, 0.1350103645451945777, -0.9908441862701590219 ) ) ;
#130156=CARTESIAN_POINT ( 'NONE',  ( -21.53699400380208928, 69.21228820681662341, -170.0231074845244166 ) ) ;
#130166=AXIS2_PLACEMENT_3D ( 'NONE', #247642, #162994, #9032 ) ;
#130168=DIRECTION ( 'NONE',  ( 0.000000000000000000, 0.000000000000000000, 1.000000000000000000 ) ) ;
#130174=EDGE_CURVE ( 'NONE', #5643, #18809, #257650, .T. ) ;
#130194=EDGE_CURVE ( 'NONE', #69695, #76100, #211944, .T. ) ;
#130199=EDGE_CURVE ( 'NONE', #179596, #64893, #137103, .T. ) ;
#130220=ORIENTED_EDGE ( 'NONE', *, *, #202512, .F. ) ;
#130257=EDGE_LOOP ( 'NONE', ( #117294, #50409, #203170, #211347 ) ) ;
#130271=EDGE_CURVE ( 'NONE', #120146, #51370, #153727, .T. ) ;
#130303=B_SPLINE_CURVE_WITH_KNOTS ( 'NONE', 3,
 ( #111926, #255208, #74100, #175754, #192739, #75376, #154915, #135302, #117047, #216127 ),
 .UNSPECIFIED., .F., .F.,
 ( 4, 3, 3, 4 ),
 ( 0.000000000000000000, 0.0002000000000008733344, 0.001000000000082982470, 0.001967863649483324578 ),
 .UNSPECIFIED. ) ;
#130314=CYLINDRICAL_SURFACE ( 'NONE', #72031, 0.09999999999999939493 ) ;
#130327=ORIENTED_EDGE ( 'NONE', *, *, #178468, .T. ) ;
#130346=ORIENTED_EDGE ( 'NONE', *, *, #194738, .F. ) ;
#130364=VECTOR ( 'NONE', #207200, 1000.000000000000000 ) ;
#130386=CARTESIAN_POINT ( 'NONE',  ( -18.59999999999999787, 74.16465844978787914, -158.4679561919613775 ) ) ;
#130400=EDGE_CURVE ( 'NONE', #61299, #184336, #107391, .T. ) ;
#130415=AXIS2_PLACEMENT_3D ( 'NONE', #182343, #44102, #119810 ) ;
#130429=DIRECTION ( 'NONE',  ( 1.713247197920696616E-14, -0.9876197685951263461, 0.1568667991644794590 ) ) ;
#130497=CARTESIAN_POINT ( 'NONE',  ( 21.12757541349815682, 69.52661942876092382, -170.0282687003341664 ) ) ;
#130500=DIRECTION ( 'NONE',  ( 1.000000000000000000, -0.000000000000000000, 0.000000000000000000 ) ) ;
#130522=EDGE_CURVE ( 'NONE', #62499, #204905, #245269, .T. ) ;
#130523=ORIENTED_EDGE ( 'NONE', *, *, #87036, .T. ) ;
#130524=DIRECTION ( 'NONE',  ( 1.000000000000000000, 0.000000000000000000, 0.000000000000000000 ) ) ;
#130533=ADVANCED_FACE ( 'NONE', ( #105668 ), #143529, .T. ) ;
#130562=CARTESIAN_POINT ( 'NONE',  ( -22.39999999999999858, 76.10085836911117951, -181.7726746080137445 ) ) ;
#130570=CIRCLE ( 'NONE', #188847, 0.1000000000000072220 ) ;
#130643=FACE_OUTER_BOUND ( 'NONE', #92251, .T. ) ;
#130660=ORIENTED_EDGE ( 'NONE', *, *, #197992, .T. ) ;
#130667=DIRECTION ( 'NONE',  ( 1.000000000000000000, -0.000000000000000000, 0.000000000000000000 ) ) ;
#130675=VECTOR ( 'NONE', #74834, 1000.000000000000000 ) ;
#130681=EDGE_CURVE ( 'NONE', #127304, #104858, #120554, .T. ) ;
#130693=CIRCLE ( 'NONE', #168163, 7.900000000000003908 ) ;
#130699=CIRCLE ( 'NONE', #197329, 0.09999999999998898659 ) ;
#130704=FACE_OUTER_BOUND ( 'NONE', #91504, .T. ) ;
#130709=B_SPLINE_CURVE_WITH_KNOTS ( 'NONE', 3,
 ( #18285, #216485, #17022, #37876, #45555, #183784, #26000, #245038 ),
 .UNSPECIFIED., .F., .F.,
 ( 4, 2, 2, 4 ),
 ( 0.000000000000000000, 0.0001049670497869849457, 0.0002099340995739698915, 0.0004198681991479773505 ),
 .UNSPECIFIED. ) ;
#130712=AXIS2_PLACEMENT_3D ( 'NONE', #27114, #46618, #166625 ) ;
#130732=LINE ( 'NONE', #246820, #145919 ) ;
#130734=TOROIDAL_SURFACE ( 'NONE', #97385, 11.65000000000000036, 0.1000000000000000056 ) ;
#130763=ORIENTED_EDGE ( 'NONE', *, *, #130681, .T. ) ;
#130809=FACE_OUTER_BOUND ( 'NONE', #148280, .T. ) ;
#130821=DIRECTION ( 'NONE',  ( 0.000000000000000000, -0.1350103645451974088, 0.9908441862701587999 ) ) ;
#130837=( BOUNDED_CURVE ( )  B_SPLINE_CURVE ( 3, ( #198041, #141919, #83203, #216322 ),
 .UNSPECIFIED., .F., .F. ) 
 B_SPLINE_CURVE_WITH_KNOTS ( ( 4, 4 ),
 ( 1.570796326794901665, 3.141592653589802886 ),
 .UNSPECIFIED. ) 
 CURVE ( )  GEOMETRIC_REPRESENTATION_ITEM ( )  RATIONAL_B_SPLINE_CURVE ( ( 1.000000000000000000, 0.8047378541243639383, 0.8047378541243639383, 1.000000000000000000 ) ) 
 REPRESENTATION_ITEM ( '' )  );
#130838=CARTESIAN_POINT ( 'NONE',  ( -20.64999999999999858, 71.65000000001222702, -148.8731074845244109 ) ) ;
#130855=LINE ( 'NONE', #51289, #51791 ) ;
#130856=DIRECTION ( 'NONE',  ( 1.000000000000000000, 0.000000000000000000, 0.000000000000000000 ) ) ;
#130879=CIRCLE ( 'NONE', #68354, 0.09999999999998898659 ) ;
#130892=CARTESIAN_POINT ( 'NONE',  ( -21.45000000000000284, 68.29142135624952914, -148.7731074845244166 ) ) ;
#130893=DIRECTION ( 'NONE',  ( -1.000000000000000000, 3.265361837132813093E-16, 2.280189983783949500E-30 ) ) ;
#130894=FACE_BOUND ( 'NONE', #91929, .T. ) ;
#130898=CARTESIAN_POINT ( 'NONE',  ( -18.59999999999999787, 77.73670573947964613, -125.0056848969006182 ) ) ;
#130903=FACE_OUTER_BOUND ( 'NONE', #71104, .T. ) ;
#130906=EDGE_CURVE ( 'NONE', #191184, #141149, #239771, .T. ) ;
#130924=ADVANCED_FACE ( 'NONE', ( #131035 ), #179637, .T. ) ;
#130954=CARTESIAN_POINT ( 'NONE',  ( 18.59999999999999787, 74.14897176987143723, -158.3691942151018850 ) ) ;
#130967=CARTESIAN_POINT ( 'NONE',  ( 22.39999999999999858, 68.20922040163900135, -170.1231074845244109 ) ) ;
#130986=AXIS2_PLACEMENT_3D ( 'NONE', #155739, #94441, #157015 ) ;
#130998=FACE_OUTER_BOUND ( 'NONE', #135792, .T. ) ;
#130999=DIRECTION ( 'NONE',  ( 0.000000000000000000, -7.304098846218085561E-15, 1.000000000000000000 ) ) ;
#131001=CARTESIAN_POINT ( 'NONE',  ( 19.92426406871192412, 64.25000000001220712, -145.1731074845244507 ) ) ;
#131003=FACE_OUTER_BOUND ( 'NONE', #101173, .T. ) ;
#131010=VECTOR ( 'NONE', #75683, 1000.000000000000000 ) ;
#131031=EDGE_CURVE ( 'NONE', #112125, #57514, #115319, .T. ) ;
#131035=FACE_OUTER_BOUND ( 'NONE', #208679, .T. ) ;
#131067=CARTESIAN_POINT ( 'NONE',  ( -18.59999999999999787, 74.16465844978787914, -158.3679561919613832 ) ) ;
#131076=EDGE_LOOP ( 'NONE', ( #149596, #251184, #233053 ) ) ;
#131084=AXIS2_PLACEMENT_3D ( 'NONE', #239596, #38833, #139175 ) ;
#131102=CARTESIAN_POINT ( 'NONE',  ( 21.05000000000000071, 65.27628289530485972, -170.0231074845244166 ) ) ;
#131106=ORIENTED_EDGE ( 'NONE', *, *, #228730, .F. ) ;
#131120=CIRCLE ( 'NONE', #118679, 0.09999999999998898659 ) ;
#131122=CARTESIAN_POINT ( 'NONE',  ( -20.85000000000000142, 64.35000000001214460, -136.5231074845244166 ) ) ;
#131127=AXIS2_PLACEMENT_3D ( 'NONE', #168799, #205284, #85323 ) ;
#131188=CARTESIAN_POINT ( 'NONE',  ( 18.59999999999999787, 77.25000000001209344, -128.7226267301092548 ) ) ;
#131191=CARTESIAN_POINT ( 'NONE',  ( -20.94999027547553894, 65.70673848566998743, -131.0638252334829588 ) ) ;
#131195=SPHERICAL_SURFACE ( 'NONE', #142727, 0.1000000000000000056 ) ;
#131223=ORIENTED_EDGE ( 'NONE', *, *, #51546, .F. ) ;
#131253=CIRCLE ( 'NONE', #102003, 12.77500000000000924 ) ;
#131258=FACE_OUTER_BOUND ( 'NONE', #162033, .T. ) ;
#131269=ORIENTED_EDGE ( 'NONE', *, *, #227642, .T. ) ;
#131285=EDGE_CURVE ( 'NONE', #163114, #76314, #190745, .T. ) ;
#131309=ORIENTED_EDGE ( 'NONE', *, *, #95989, .F. ) ;
#131313=CIRCLE ( 'NONE', #106348, 0.09999999999998898659 ) ;
#131326=ORIENTED_EDGE ( 'NONE', *, *, #116503, .T. ) ;
#131330=ORIENTED_EDGE ( 'NONE', *, *, #13951, .T. ) ;
#131347=EDGE_CURVE ( 'NONE', #182252, #56847, #227260, .T. ) ;
#131355=DIRECTION ( 'NONE',  ( 0.000000000000000000, 6.982962677686266711E-15, -1.000000000000000000 ) ) ;
#131360=CARTESIAN_POINT ( 'NONE',  ( 18.49999999999999645, 77.16270174995034381, -161.9231074845243370 ) ) ;
#131364=CARTESIAN_POINT ( 'NONE',  ( -22.39999999999999858, 68.20922040163897293, -170.0231074845243882 ) ) ;
#131393=DIRECTION ( 'NONE',  ( 0.000000000000000000, 6.982962677686266711E-15, -1.000000000000000000 ) ) ;
#131419=ORIENTED_EDGE ( 'NONE', *, *, #144102, .F. ) ;
#131451=CYLINDRICAL_SURFACE ( 'NONE', #134670, 4.049999999999998046 ) ;
#131463=ORIENTED_EDGE ( 'NONE', *, *, #256841, .F. ) ;
#131470=AXIS2_PLACEMENT_3D ( 'NONE', #235989, #135599, #62181 ) ;
#131484=FACE_OUTER_BOUND ( 'NONE', #93342, .T. ) ;
#131485=DIRECTION ( 'NONE',  ( -1.000000000000000000, -0.000000000000000000, -0.000000000000000000 ) ) ;
#131486=DIRECTION ( 'NONE',  ( 1.000000000000000000, 0.000000000000000000, 0.000000000000000000 ) ) ;
#131501=ORIENTED_EDGE ( 'NONE', *, *, #185782, .F. ) ;
#131516=EDGE_LOOP ( 'NONE', ( #213860, #171286, #28548, #181376 ) ) ;
#131536=PLANE ( 'NONE',  #2032 ) ;
#131552=ORIENTED_EDGE ( 'NONE', *, *, #166072, .F. ) ;
#131567=CARTESIAN_POINT ( 'NONE',  ( 20.95289811251229750, 67.10683199555371914, -161.5212979906058877 ) ) ;
#131601=DIRECTION ( 'NONE',  ( -0.000000000000000000, -6.982962677686266711E-15, 1.000000000000000000 ) ) ;
#131627=FACE_OUTER_BOUND ( 'NONE', #82207, .T. ) ;
#131640=ORIENTED_EDGE ( 'NONE', *, *, #165972, .T. ) ;
#131750=FACE_OUTER_BOUND ( 'NONE', #184476, .T. ) ;
#131780=CARTESIAN_POINT ( 'NONE',  ( -21.08035267497491816, 75.91731137523639461, -176.3548143243073980 ) ) ;
#131801=EDGE_CURVE ( 'NONE', #59416, #44364, #146017, .T. ) ;
#131802=CYLINDRICAL_SURFACE ( 'NONE', #138544, 0.09999999999998898659 ) ;
#131807=AXIS2_PLACEMENT_3D ( 'NONE', #153108, #17404, #132215 ) ;
#131814=AXIS2_PLACEMENT_3D ( 'NONE', #132293, #252233, #95723 ) ;
#131828=AXIS2_PLACEMENT_3D ( 'NONE', #162140, #125558, #103400 ) ;
#131847=DIRECTION ( 'NONE',  ( 1.000000000000000000, -3.469446951953718318E-14, 2.003086131649645455E-14 ) ) ;
#131848=EDGE_CURVE ( 'NONE', #200243, #31922, #213825, .T. ) ;
#131852=EDGE_CURVE ( 'NONE', #94754, #79539, #194292, .T. ) ;
#131857=DIRECTION ( 'NONE',  ( 1.000000000000000000, 0.000000000000000000, 0.000000000000000000 ) ) ;
#131859=TOROIDAL_SURFACE ( 'NONE', #31927, 12.77500000000000036, 0.1000000000000000056 ) ;
#131888=EDGE_CURVE ( 'NONE', #108252, #226867, #83622, .T. ) ;
#131897=AXIS2_PLACEMENT_3D ( 'NONE', #118163, #79001, #197683 ) ;
#131907=DIRECTION ( 'NONE',  ( 0.000000000000000000, -1.000000000000000000, 0.000000000000000000 ) ) ;
#131918=ORIENTED_EDGE ( 'NONE', *, *, #177473, .F. ) ;
#131924=TOROIDAL_SURFACE ( 'NONE', #198555, 0.2000000000000000111, 0.1000000000000000056 ) ;
#131925=CARTESIAN_POINT ( 'NONE',  ( -20.94999999999999929, 76.00000000001237765, -170.0231074845243597 ) ) ;
#131931=DIRECTION ( 'NONE',  ( -0.000000000000000000, -6.982962677686266711E-15, 1.000000000000000000 ) ) ;
#131990=CIRCLE ( 'NONE', #27977, 0.09999999999998802902 ) ;
#132000=CARTESIAN_POINT ( 'NONE',  ( -18.59999999999999787, 64.35000000001222986, -148.6731074845244507 ) ) ;
#132009=VERTEX_POINT ( 'NONE', #168015 ) ;
#132017=CARTESIAN_POINT ( 'NONE',  ( -20.94999999999999929, 74.63912941282028157, -161.9501095574334215 ) ) ;
#132041=DIRECTION ( 'NONE',  ( 0.000000000000000000, 0.000000000000000000, -1.000000000000000000 ) ) ;
#132086=CARTESIAN_POINT ( 'NONE',  ( 21.05000000000000071, 76.00000000001213607, -136.5231074845243313 ) ) ;
#132089=CARTESIAN_POINT ( 'NONE',  ( -21.52071067811865746, 68.22071067813094203, -157.6731074845243938 ) ) ;
#132125=AXIS2_PLACEMENT_3D ( 'NONE', #58062, #119355, #240579 ) ;
#132133=LINE ( 'NONE', #35637, #95593 ) ;
#132149=ORIENTED_EDGE ( 'NONE', *, *, #131285, .T. ) ;
#132155=CIRCLE ( 'NONE', #7227, 11.64999999999999325 ) ;
#132173=EDGE_CURVE ( 'NONE', #206325, #46365, #130120, .T. ) ;
#132176=VERTEX_POINT ( 'NONE', #253913 ) ;
#132185=CYLINDRICAL_SURFACE ( 'NONE', #244949, 0.09999999999999939493 ) ;
#132194=DIRECTION ( 'NONE',  ( -1.000000000000000000, 2.952720810173289112E-16, 2.061873921506763405E-30 ) ) ;
#132199=CARTESIAN_POINT ( 'NONE',  ( 21.14999999999999858, 64.35000000001245724, -181.7731074845244450 ) ) ;
#132210=VERTEX_POINT ( 'NONE', #114420 ) ;
#132215=DIRECTION ( 'NONE',  ( 0.7071067811865127117, 0.7071067811865821007, 0.000000000000000000 ) ) ;
#132228=ORIENTED_EDGE ( 'NONE', *, *, #210180, .F. ) ;
#132236=CIRCLE ( 'NONE', #223802, 11.80000000000000426 ) ;
#132242=CARTESIAN_POINT ( 'NONE',  ( -18.59117750673697245, 65.66751761918692409, -130.9282609406112670 ) ) ;
#132257=ORIENTED_EDGE ( 'NONE', *, *, #16329, .F. ) ;
#132287=DIRECTION ( 'NONE',  ( 0.000000000000000000, 0.000000000000000000, -1.000000000000000000 ) ) ;
#132292=EDGE_CURVE ( 'NONE', #168738, #136655, #158886, .T. ) ;
#132293=CARTESIAN_POINT ( 'NONE',  ( -20.64999999999999858, 68.85000000001222986, -148.8731074845244109 ) ) ;
#132308=DIRECTION ( 'NONE',  ( -4.448008912761042820E-16, -1.000000000000000000, -7.116814260417668513E-15 ) ) ;
#132342=AXIS2_PLACEMENT_3D ( 'NONE', #179000, #218059, #19901 ) ;
#132364=AXIS2_PLACEMENT_3D ( 'NONE', #75165, #12619, #17707 ) ;
#132365=EDGE_CURVE ( 'NONE', #248967, #73243, #29719, .T. ) ;
#132370=CARTESIAN_POINT ( 'NONE',  ( -21.14999999999999858, 69.74218538953626023, -170.1208977758331855 ) ) ;
#132371=LINE ( 'NONE', #154541, #104001 ) ;
#132398=EDGE_CURVE ( 'NONE', #23721, #141610, #146196, .T. ) ;
#132401=AXIS2_PLACEMENT_3D ( 'NONE', #82548, #85113, #143827 ) ;
#132410=EDGE_CURVE ( 'NONE', #70695, #227218, #167092, .T. ) ;
#132415=LINE ( 'NONE', #167712, #175890 ) ;
#132421=TOROIDAL_SURFACE ( 'NONE', #86592, 0.2000000000000000111, 0.1000000000000000056 ) ;
#132428=ORIENTED_EDGE ( 'NONE', *, *, #235735, .F. ) ;
#132439=EDGE_LOOP ( 'NONE', ( #43799, #58853, #215919, #206974 ) ) ;
#132440=DIRECTION ( 'NONE',  ( 1.000000000000000000, -2.952720810173289112E-16, -2.061873921506763405E-30 ) ) ;
#132451=CARTESIAN_POINT ( 'NONE',  ( 18.49999999999999289, 65.79142135624951493, -145.3731074845244109 ) ) ;
#132455=CIRCLE ( 'NONE', #20046, 4.049999999999998046 ) ;
#132498=VERTEX_POINT ( 'NONE', #240264 ) ;
#132508=AXIS2_PLACEMENT_3D ( 'NONE', #158140, #18587, #159389 ) ;
#132512=EDGE_CURVE ( 'NONE', #248708, #121929, #163164, .T. ) ;
#132535=ORIENTED_EDGE ( 'NONE', *, *, #52880, .F. ) ;
#132564=ORIENTED_EDGE ( 'NONE', *, *, #250532, .T. ) ;
#132565=CARTESIAN_POINT ( 'NONE',  ( 21.05000000000000071, 76.00000000001210765, -132.4231074845243370 ) ) ;
#132569=DIRECTION ( 'NONE',  ( 0.000000000000000000, 6.467318590049456648E-15, -1.000000000000000000 ) ) ;
#132572=ORIENTED_EDGE ( 'NONE', *, *, #237473, .F. ) ;
#132581=CARTESIAN_POINT ( 'NONE',  ( -21.29999999999995808, 76.00000000001240608, -174.0731074845243711 ) ) ;
#132582=VECTOR ( 'NONE', #65396, 1000.000000000000000 ) ;
#132588=CARTESIAN_POINT ( 'NONE',  ( 18.59999999999999076, 65.79142135624952914, -148.6731074845244223 ) ) ;
#132603=CARTESIAN_POINT ( 'NONE',  ( -20.54999999999999716, 73.50000000001223555, -149.7477294072864709 ) ) ;
#132631=ADVANCED_FACE ( 'NONE', ( #180281 ), #229777, .F. ) ;
#132636=EDGE_LOOP ( 'NONE', ( #39671, #160525, #256346, #125161 ) ) ;
#132640=ORIENTED_EDGE ( 'NONE', *, *, #164508, .T. ) ;
#132646=DIRECTION ( 'NONE',  ( 0.000000000000000000, 0.000000000000000000, 1.000000000000000000 ) ) ;
#132671=AXIS2_PLACEMENT_3D ( 'NONE', #237181, #215042, #234601 ) ;
#132686=ORIENTED_EDGE ( 'NONE', *, *, #20835, .F. ) ;
#132702=ORIENTED_EDGE ( 'NONE', *, *, #140015, .T. ) ;
#132706=FACE_OUTER_BOUND ( 'NONE', #88230, .T. ) ;
#132727=DIRECTION ( 'NONE',  ( 0.000000000000000000, 0.000000000000000000, 1.000000000000000000 ) ) ;
#132743=ADVANCED_FACE ( 'NONE', ( #43343 ), #165865, .T. ) ;
#132747=TOROIDAL_SURFACE ( 'NONE', #153628, 0.2000000000000000111, 0.1000000000000000056 ) ;
#132806=EDGE_LOOP ( 'NONE', ( #232035, #58409, #95901, #221959 ) ) ;
#132807=CARTESIAN_POINT ( 'NONE',  ( -20.85000000000000142, 87.65000000001214175, -136.5231074845242745 ) ) ;
#132818=DIRECTION ( 'NONE',  ( 1.000000000000000000, 0.000000000000000000, 0.000000000000000000 ) ) ;
#132829=DIRECTION ( 'NONE',  ( 0.000000000000000000, 1.000000000000000000, 6.982962677686266711E-15 ) ) ;
#132833=EDGE_CURVE ( 'NONE', #200975, #95684, #192366, .T. ) ;
#132837=AXIS2_PLACEMENT_3D ( 'NONE', #24901, #67847, #66580 ) ;
#132851=DIRECTION ( 'NONE',  ( 2.952720810173289112E-16, 1.000000000000000000, 6.982962677686266711E-15 ) ) ;
#132867=VERTEX_POINT ( 'NONE', #1309 ) ;
#132869=DIRECTION ( 'NONE',  ( -1.000000000000000000, 2.952720810173289112E-16, 2.061873921506763405E-30 ) ) ;
#132872=DIRECTION ( 'NONE',  ( 0.000000000000000000, 0.000000000000000000, 1.000000000000000000 ) ) ;
#132876=CARTESIAN_POINT ( 'NONE',  ( 20.85000000000000142, 87.75000000001215028, -139.5231074845243029 ) ) ;
#132908=CARTESIAN_POINT ( 'NONE',  ( -21.14999999999999858, 87.65000000001238334, -170.0231074845242745 ) ) ;
#132974=DIRECTION ( 'NONE',  ( 0.000000000000000000, 1.000000000000000000, 6.982962677686266711E-15 ) ) ;
#133042=DIRECTION ( 'NONE',  ( 1.000000000000000000, 0.000000000000000000, 0.000000000000000000 ) ) ;
#133045=EDGE_CURVE ( 'NONE', #95398, #176651, #30087, .T. ) ;
#133047=CIRCLE ( 'NONE', #20623, 0.1000000000000043771 ) ;
#133057=VERTEX_POINT ( 'NONE', #46851 ) ;
#133064=LINE ( 'NONE', #195620, #196116 ) ;
#133075=CARTESIAN_POINT ( 'NONE',  ( -21.07933241753356413, 75.90662040959315959, -176.3517534329041041 ) ) ;
#133078=VECTOR ( 'NONE', #2844, 1000.000000000000000 ) ;
#133104=VECTOR ( 'NONE', #182732, 1000.000000000000000 ) ;
#133145=FACE_OUTER_BOUND ( 'NONE', #167798, .T. ) ;
#133155=CARTESIAN_POINT ( 'NONE',  ( 21.05000000000000071, 76.00000000001229239, -157.8731074845243540 ) ) ;
#133169=DIRECTION ( 'NONE',  ( 0.000000000000000000, 6.982962677686266711E-15, -1.000000000000000000 ) ) ;
#133183=VERTEX_POINT ( 'NONE', #109396 ) ;
#133207=ORIENTED_EDGE ( 'NONE', *, *, #228975, .T. ) ;
#133251=DIRECTION ( 'NONE',  ( 0.000000000000000000, 0.6728971962617862346, -0.7397360091701815632 ) ) ;
#133262=CARTESIAN_POINT ( 'NONE',  ( 18.41789779300671981, 85.50000000001233502, -162.9910378181636474 ) ) ;
#133266=CIRCLE ( 'NONE', #83347, 0.4000000000000114575 ) ;
#133271=LINE ( 'NONE', #188107, #194071 ) ;
#133329=VERTEX_POINT ( 'NONE', #98791 ) ;
#133335=ORIENTED_EDGE ( 'NONE', *, *, #131285, .F. ) ;
#133347=EDGE_CURVE ( 'NONE', #75413, #133057, #238524, .T. ) ;
#133375=DIRECTION ( 'NONE',  ( -0.000000000000000000, 0.8660254037844377084, 0.5000000000000016653 ) ) ;
#133382=AXIS2_PLACEMENT_3D ( 'NONE', #178250, #257693, #79095 ) ;
#133384=CARTESIAN_POINT ( 'NONE',  ( -21.59142135623730852, 68.15000000001228386, -157.7731074845244166 ) ) ;
#133399=DIRECTION ( 'NONE',  ( 1.000000000000000000, 7.304098846218105085E-16, 4.217023435051676515E-16 ) ) ;
#133400=CARTESIAN_POINT ( 'NONE',  ( -23.25000000000000000, 64.35000000001222986, -148.6731074845244507 ) ) ;
#133409=ORIENTED_EDGE ( 'NONE', *, *, #48112, .F. ) ;
#133414=DIRECTION ( 'NONE',  ( 1.000000000000000000, 0.000000000000000000, 0.000000000000000000 ) ) ;
#133419=DIRECTION ( 'NONE',  ( -0.7071067811865389130, -5.024295867788141276E-15, 0.7071067811865561215 ) ) ;
#133424=CARTESIAN_POINT ( 'NONE',  ( -18.31331870001040940, 85.53629471919306582, -129.6545287935387307 ) ) ;
#133433=ORIENTED_EDGE ( 'NONE', *, *, #154463, .F. ) ;
#133441=CARTESIAN_POINT ( 'NONE',  ( -20.94999999999999929, 87.65000000001235492, -167.1231074845242688 ) ) ;
#133452=TOROIDAL_SURFACE ( 'NONE', #229324, 11.90000000000000391, 0.1000000000000000056 ) ;
#133466=CYLINDRICAL_SURFACE ( 'NONE', #74933, 0.09999999999998898659 ) ;
#133487=AXIS2_PLACEMENT_3D ( 'NONE', #240002, #219125, #40551 ) ;
#133513=EDGE_CURVE ( 'NONE', #163114, #49440, #19114, .T. ) ;
#133516=VERTEX_POINT ( 'NONE', #242183 ) ;
#133518=AXIS2_PLACEMENT_3D ( 'NONE', #197698, #242925, #116892 ) ;
#133519=ORIENTED_EDGE ( 'NONE', *, *, #9904, .T. ) ;
#133548=DIRECTION ( 'NONE',  ( 0.000000000000000000, -6.982962677686266711E-15, 1.000000000000000000 ) ) ;
#133559=EDGE_CURVE ( 'NONE', #251678, #160550, #224552, .T. ) ;
#133561=DIRECTION ( 'NONE',  ( 0.000000000000000000, -0.1575844902526687130, -0.9875055080513762684 ) ) ;
#133569=DIRECTION ( 'NONE',  ( 0.000000000000000000, -1.000000000000000000, -8.717686153663073805E-15 ) ) ;
#133574=DIRECTION ( 'NONE',  ( 0.000000000000000000, 0.000000000000000000, -1.000000000000000000 ) ) ;
#133619=AXIS2_PLACEMENT_3D ( 'NONE', #1210, #138156, #97733 ) ;
#133629=EDGE_CURVE ( 'NONE', #16708, #182252, #186076, .T. ) ;
#133672=CARTESIAN_POINT ( 'NONE',  ( 18.59999999999999432, 77.16270174995034381, -161.9231074845243370 ) ) ;
#133680=CARTESIAN_POINT ( 'NONE',  ( -21.07928932188134041, 69.67148334361908724, -170.1220026301787982 ) ) ;
#133689=DIRECTION ( 'NONE',  ( 0.000000000000000000, 0.000000000000000000, 1.000000000000000000 ) ) ;
#133713=CARTESIAN_POINT ( 'NONE',  ( 18.49999999999999645, 74.26374286841490857, -158.4544551555068779 ) ) ;
#133729=CARTESIAN_POINT ( 'NONE',  ( 22.50000000000000000, 75.90000000001245439, -181.6726782920691505 ) ) ;
#133741=AXIS2_PLACEMENT_3D ( 'NONE', #143312, #162913, #62508 ) ;
#133760=CARTESIAN_POINT ( 'NONE',  ( -20.85000000000000142, 65.66751761918692409, -130.9282609406112670 ) ) ;
#133785=EDGE_CURVE ( 'NONE', #161742, #173882, #184522, .T. ) ;
#133839=ORIENTED_EDGE ( 'NONE', *, *, #206039, .F. ) ;
#133840=FACE_OUTER_BOUND ( 'NONE', #19316, .T. ) ;
#133849=EDGE_CURVE ( 'NONE', #251542, #140576, #213567, .T. ) ;
#133870=CARTESIAN_POINT ( 'NONE',  ( -22.47886152344871036, 75.96249906115076556, -181.6730961275722507 ) ) ;
#133872=DIRECTION ( 'NONE',  ( 0.000000000000000000, 0.4999999999999088507, -0.8660254037844913322 ) ) ;
#133886=ORIENTED_EDGE ( 'NONE', *, *, #24101, .T. ) ;
#133932=FACE_OUTER_BOUND ( 'NONE', #84266, .T. ) ;
#133956=AXIS2_PLACEMENT_3D ( 'NONE', #164925, #183212, #145350 ) ;
#133961=ORIENTED_EDGE ( 'NONE', *, *, #62543, .F. ) ;
#133965=DIRECTION ( 'NONE',  ( 1.000000000000000000, -0.000000000000000000, 0.000000000000000000 ) ) ;
#134001=CIRCLE ( 'NONE', #159161, 0.09999999999998898659 ) ;
#134016=CARTESIAN_POINT ( 'NONE',  ( 20.94999999999999929, 70.50000000001230660, -157.6178414656113205 ) ) ;
#134021=EDGE_LOOP ( 'NONE', ( #132640, #156933, #34028, #112819 ) ) ;
#134029=DIRECTION ( 'NONE',  ( 1.000000000000000000, -2.952720810173289112E-16, -2.061873921506763405E-30 ) ) ;
#134099=CARTESIAN_POINT ( 'NONE',  ( -23.25000000000000000, 71.65000000001228386, -157.6731074845243938 ) ) ;
#134102=VERTEX_POINT ( 'NONE', #139571 ) ;
#134141=EDGE_CURVE ( 'NONE', #248967, #200038, #199598, .T. ) ;
#134153=DIRECTION ( 'NONE',  ( 0.000000000000000000, 6.608470384673536035E-15, -1.000000000000000000 ) ) ;
#134187=EDGE_CURVE ( 'NONE', #217454, #51561, #250788, .T. ) ;
#134207=DIRECTION ( 'NONE',  ( 0.000000000000000000, 0.000000000000000000, 1.000000000000000000 ) ) ;
#134226=ORIENTED_EDGE ( 'NONE', *, *, #117301, .F. ) ;
#134261=FACE_OUTER_BOUND ( 'NONE', #129766, .T. ) ;
#134283=EDGE_CURVE ( 'NONE', #171719, #53585, #222099, .T. ) ;
#134290=EDGE_CURVE ( 'NONE', #75413, #176760, #104988, .T. ) ;
#134328=DIRECTION ( 'NONE',  ( -1.000000000000000000, -0.000000000000000000, -0.000000000000000000 ) ) ;
#134342=AXIS2_PLACEMENT_3D ( 'NONE', #87816, #209078, #70883 ) ;
#134344=DIRECTION ( 'NONE',  ( 1.000000000000000000, 0.000000000000000000, 0.000000000000000000 ) ) ;
#134375=DIRECTION ( 'NONE',  ( -1.000000000000000000, 0.000000000000000000, -0.000000000000000000 ) ) ;
#134415=ORIENTED_EDGE ( 'NONE', *, *, #28494, .F. ) ;
#134454=ORIENTED_EDGE ( 'NONE', *, *, #76117, .T. ) ;
#134460=CARTESIAN_POINT ( 'NONE',  ( -23.25000000000000000, 65.66751761918692409, -130.9282609406112670 ) ) ;
#134473=PLANE ( 'NONE',  #75886 ) ;
#134475=CIRCLE ( 'NONE', #226048, 0.2000000000000057288 ) ;
#134491=ORIENTED_EDGE ( 'NONE', *, *, #194535, .T. ) ;
#134520=ORIENTED_EDGE ( 'NONE', *, *, #121240, .T. ) ;
#134523=CARTESIAN_POINT ( 'NONE',  ( 18.45036689428336629, 85.49018414334112492, -163.0104116570379915 ) ) ;
#134531=CARTESIAN_POINT ( 'NONE',  ( 21.05933563467872105, 65.27547528793097342, -157.8294597355684630 ) ) ;
#134542=VERTEX_POINT ( 'NONE', #40216 ) ;
#134557=CARTESIAN_POINT ( 'NONE',  ( -21.05000000000000071, 75.90220970870363715, -176.2809220950004487 ) ) ;
#134558=AXIS2_PLACEMENT_3D ( 'NONE', #102270, #82708, #226078 ) ;
#134566=ORIENTED_EDGE ( 'NONE', *, *, #10949, .F. ) ;
#134612=FACE_OUTER_BOUND ( 'NONE', #224005, .T. ) ;
#134622=AXIS2_PLACEMENT_3D ( 'NONE', #29188, #89105, #49984 ) ;
#134663=CYLINDRICAL_SURFACE ( 'NONE', #229200, 0.5000000000000004441 ) ;
#134668=ADVANCED_FACE ( 'NONE', ( #123576 ), #203105, .F. ) ;
#134670=AXIS2_PLACEMENT_3D ( 'NONE', #34961, #37504, #233152 ) ;
#134682=CARTESIAN_POINT ( 'NONE',  ( -18.39999999999999858, 85.68240343348850274, -129.8662641071115047 ) ) ;
#134685=VERTEX_POINT ( 'NONE', #103979 ) ;
#134744=EDGE_LOOP ( 'NONE', ( #135506, #179959, #140318, #96334 ) ) ;
#134765=ORIENTED_EDGE ( 'NONE', *, *, #350, .T. ) ;
#134820=FACE_OUTER_BOUND ( 'NONE', #216716, .T. ) ;
#134862=CARTESIAN_POINT ( 'NONE',  ( 21.97500000000000497, 66.25000000001229239, -157.7731074845244166 ) ) ;
#134867=CARTESIAN_POINT ( 'NONE',  ( -21.03571358705754335, 64.25000000001233502, -163.1980006624665123 ) ) ;
#134969=EDGE_CURVE ( 'NONE', #253904, #6455, #116845, .T. ) ;
#134986=DIRECTION ( 'NONE',  ( 1.000000000000000000, 0.000000000000000000, 0.000000000000000000 ) ) ;
#134993=CARTESIAN_POINT ( 'NONE',  ( 18.49999999999999289, 65.50857864377491069, -145.2731074845243882 ) ) ;
#135013=( BOUNDED_CURVE ( )  B_SPLINE_CURVE ( 3, ( #11056, #48892, #131001, #9765 ),
 .UNSPECIFIED., .F., .T. ) 
 B_SPLINE_CURVE_WITH_KNOTS ( ( 4, 4 ),
 ( 0.000000000000000000, 1.570796326794908992 ),
 .UNSPECIFIED. ) 
 CURVE ( )  GEOMETRIC_REPRESENTATION_ITEM ( )  RATIONAL_B_SPLINE_CURVE ( ( 1.000000000000000000, 0.8047378541243619399, 0.8047378541243619399, 1.000000000000000000 ) ) 
 REPRESENTATION_ITEM ( '' )  );
#135042=AXIS2_PLACEMENT_3D ( 'NONE', #93421, #255005, #76426 ) ;
#135049=EDGE_CURVE ( 'NONE', #200243, #134542, #72112, .T. ) ;
#135131=DIRECTION ( 'NONE',  ( 0.000000000000000000, -6.982962677686266711E-15, 1.000000000000000000 ) ) ;
#135148=CIRCLE ( 'NONE', #81168, 4.000000000000003553 ) ;
#135155=AXIS2_PLACEMENT_3D ( 'NONE', #111309, #209111, #69623 ) ;
#135160=DIRECTION ( 'NONE',  ( 0.000000000000000000, 0.000000000000000000, 1.000000000000000000 ) ) ;
#135163=EDGE_LOOP ( 'NONE', ( #23454, #187840, #188375, #144394 ) ) ;
#135165=ORIENTED_EDGE ( 'NONE', *, *, #106627, .T. ) ;
#135227=EDGE_LOOP ( 'NONE', ( #208705, #179295, #221434, #33284 ) ) ;
#135236=PLANE ( 'NONE',  #84063 ) ;
#135275=ORIENTED_EDGE ( 'NONE', *, *, #22430, .T. ) ;
#135295=ORIENTED_EDGE ( 'NONE', *, *, #21267, .F. ) ;
#135302=CARTESIAN_POINT ( 'NONE',  ( 22.01447462590973814, 75.90096299995289542, -177.2869076857542723 ) ) ;
#135306=FACE_OUTER_BOUND ( 'NONE', #142459, .T. ) ;
#135308=DIRECTION ( 'NONE',  ( 0.000000000000000000, 0.000000000000000000, 1.000000000000000000 ) ) ;
#135341=CIRCLE ( 'NONE', #173005, 0.09999999999999080458 ) ;
#135369=ADVANCED_FACE ( 'NONE', ( #121701 ), #184207, .T. ) ;
#135385=DIRECTION ( 'NONE',  ( 0.000000000000000000, 0.000000000000000000, -1.000000000000000000 ) ) ;
#135413=CIRCLE ( 'NONE', #173257, 2.000000000000001776 ) ;
#135440=ORIENTED_EDGE ( 'NONE', *, *, #48112, .T. ) ;
#135474=ORIENTED_EDGE ( 'NONE', *, *, #103954, .F. ) ;
#135478=VERTEX_POINT ( 'NONE', #26442 ) ;
#135506=ORIENTED_EDGE ( 'NONE', *, *, #166314, .T. ) ;
#135508=ORIENTED_EDGE ( 'NONE', *, *, #52376, .F. ) ;
#135517=AXIS2_PLACEMENT_3D ( 'NONE', #28365, #109127, #184821 ) ;
#135567=CARTESIAN_POINT ( 'NONE',  ( -18.50000000000000000, 64.35000000001247145, -181.7731074845244450 ) ) ;
#135595=ORIENTED_EDGE ( 'NONE', *, *, #232260, .T. ) ;
#135599=DIRECTION ( 'NONE',  ( 1.000000000000000000, -2.952720810173289112E-16, -2.061873921506763405E-30 ) ) ;
#135610=ORIENTED_EDGE ( 'NONE', *, *, #71758, .F. ) ;
#135616=EDGE_CURVE ( 'NONE', #151457, #56292, #79331, .T. ) ;
#135647=AXIS2_PLACEMENT_3D ( 'NONE', #257786, #139146, #97453 ) ;
#135673=DIRECTION ( 'NONE',  ( 0.000000000000000000, -6.938893903907222067E-15, 1.000000000000000000 ) ) ;
#135681=ORIENTED_EDGE ( 'NONE', *, *, #227957, .F. ) ;
#135702=LINE ( 'NONE', #17078, #73091 ) ;
#135727=EDGE_CURVE ( 'NONE', #141149, #206737, #72474, .T. ) ;
#135734=DIRECTION ( 'NONE',  ( 0.000000000000000000, 6.982962677686266711E-15, -1.000000000000000000 ) ) ;
#135741=VERTEX_POINT ( 'NONE', #222692 ) ;
#135758=DIRECTION ( 'NONE',  ( 0.000000000000000000, 0.000000000000000000, 1.000000000000000000 ) ) ;
#135770=DIRECTION ( 'NONE',  ( -1.836970198721029934E-16, -1.000000000000000000, -6.982962677686266711E-15 ) ) ;
#135789=ORIENTED_EDGE ( 'NONE', *, *, #40839, .T. ) ;
#135790=LINE ( 'NONE', #173705, #46636 ) ;
#135792=EDGE_LOOP ( 'NONE', ( #207271, #78607, #241336, #135610 ) ) ;
#135809=CARTESIAN_POINT ( 'NONE',  ( 18.54147908293606406, 85.46326165794057772, -162.9741585877686987 ) ) ;
#135810=ORIENTED_EDGE ( 'NONE', *, *, #74370, .T. ) ;
#135811=DIRECTION ( 'NONE',  ( -1.000000000000000000, 0.000000000000000000, -0.000000000000000000 ) ) ;
#135827=ORIENTED_EDGE ( 'NONE', *, *, #28942, .F. ) ;
#135875=DIRECTION ( 'NONE',  ( 0.000000000000000000, 0.000000000000000000, 1.000000000000000000 ) ) ;
#135906=CIRCLE ( 'NONE', #173392, 0.09999999999999939493 ) ;
#135918=DIRECTION ( 'NONE',  ( 3.265361837132813093E-16, 1.000000000000000000, 6.982962677686266711E-15 ) ) ;
#135934=ADVANCED_FACE ( 'NONE', ( #4494 ), #146565, .T. ) ;
#135938=DIRECTION ( 'NONE',  ( 2.952720810173289112E-16, 1.000000000000000000, 6.938893903907222067E-15 ) ) ;
#135946=ORIENTED_EDGE ( 'NONE', *, *, #168727, .T. ) ;
#135949=AXIS2_PLACEMENT_3D ( 'NONE', #69500, #210285, #73361 ) ;
#135968=CARTESIAN_POINT ( 'NONE',  ( -18.31572283045112570, 85.54843783089792453, -129.6724818334656675 ) ) ;
#135977=AXIS2_PLACEMENT_3D ( 'NONE', #251235, #72638, #75210 ) ;
#136003=CIRCLE ( 'NONE', #219225, 0.5000000000000004441 ) ;
#136009=DIRECTION ( 'NONE',  ( 1.000000000000000000, 0.000000000000000000, 0.000000000000000000 ) ) ;
#136038=LINE ( 'NONE', #215591, #71377 ) ;
#136057=ORIENTED_EDGE ( 'NONE', *, *, #75615, .F. ) ;
#136075=EDGE_LOOP ( 'NONE', ( #190514, #108714, #111051, #26460 ) ) ;
#136109=DIRECTION ( 'NONE',  ( 0.000000000000000000, -7.086529944415894657E-15, 1.000000000000000000 ) ) ;
#136110=FACE_OUTER_BOUND ( 'NONE', #92878, .T. ) ;
#136166=ORIENTED_EDGE ( 'NONE', *, *, #55966, .T. ) ;
#136167=DIRECTION ( 'NONE',  ( 0.000000000000000000, -0.1298341882519953583, -0.9915357197604862671 ) ) ;
#136183=DIRECTION ( 'NONE',  ( 0.000000000000000000, -1.000000000000000000, -7.109473446599835262E-15 ) ) ;
#136224=CARTESIAN_POINT ( 'NONE',  ( 22.48970261584622321, 64.35000000001238618, -170.0784769727418393 ) ) ;
#136247=ORIENTED_EDGE ( 'NONE', *, *, #53661, .T. ) ;
#136265=CARTESIAN_POINT ( 'NONE',  ( -20.64999999999999858, 76.00000000001213607, -136.5231074845243313 ) ) ;
#136291=VECTOR ( 'NONE', #168964, 1000.000000000000000 ) ;
#136297=FACE_OUTER_BOUND ( 'NONE', #141207, .T. ) ;
#136303=CARTESIAN_POINT ( 'NONE',  ( -18.59999999999999787, 64.35000000001230092, -157.8731074845244393 ) ) ;
#136333=DIRECTION ( 'NONE',  ( 0.000000000000000000, -6.938893903907222067E-15, 1.000000000000000000 ) ) ;
#136345=ORIENTED_EDGE ( 'NONE', *, *, #178468, .F. ) ;
#136347=EDGE_CURVE ( 'NONE', #245009, #173882, #172834, .T. ) ;
#136355=ORIENTED_EDGE ( 'NONE', *, *, #49283, .T. ) ;
#136383=ORIENTED_EDGE ( 'NONE', *, *, #3775, .T. ) ;
#136408=EDGE_CURVE ( 'NONE', #218618, #132210, #190208, .T. ) ;
#136412=CARTESIAN_POINT ( 'NONE',  ( 20.85000000000000142, 77.83585931145570669, -125.0186683157258329 ) ) ;
#136461=ORIENTED_EDGE ( 'NONE', *, *, #147242, .F. ) ;
#136478=CARTESIAN_POINT ( 'NONE',  ( -21.07094088545368393, 75.90110629746020265, -176.3432747064415196 ) ) ;
#136501=CARTESIAN_POINT ( 'NONE',  ( 18.59999999999998721, 69.15387683765952431, -132.7853812176745407 ) ) ;
#136519=EDGE_CURVE ( 'NONE', #141640, #206438, #85259, .T. ) ;
#136544=DIRECTION ( 'NONE',  ( 0.000000000000000000, -6.982962677686266711E-15, 1.000000000000000000 ) ) ;
#136571=DIRECTION ( 'NONE',  ( 1.000000000000000000, 0.000000000000000000, 0.000000000000000000 ) ) ;
#136606=( BOUNDED_SURFACE ( )  B_SPLINE_SURFACE ( 3, 2, ( 
 ( #28095, #65910, #64613 ),
 ( #204118, #88009, #128453 ),
 ( #103717, #145430, #125865 ),
 ( #185850, #46328, #167598 ),
 ( #247093, #224956, #68483 ),
 ( #86728, #108881, #205394 ) ),
 .UNSPECIFIED., .F., .F., .F. ) 
 B_SPLINE_SURFACE_WITH_KNOTS ( ( 4, 2, 4 ),
 ( 3, 3 ),
 ( 1.570796326794897668, 2.356194490192346169, 3.141592653589794448 ),
 ( 0.000000000000000000, 1.000000000000000000 ),
 .UNSPECIFIED. ) 
 GEOMETRIC_REPRESENTATION_ITEM ( )  RATIONAL_B_SPLINE_SURFACE ( (
 ( 1.000000000000000000, 0.7071067811865597852, 1.000000000000000000),
 ( 1.000000000000000000, 0.6611148371781027100, 1.000000000000000000),
 ( 1.000000000000000000, 0.6092287576693442563, 1.000000000000000000),
 ( 1.000000000000000000, 0.5278258667060597986, 1.000000000000000000),
 ( 1.000000000000000000, 0.4993418825332296973, 1.000000000000000000),
 ( 1.000000000000000000, 0.5000000000000456302, 1.000000000000000000) ) ) 
 REPRESENTATION_ITEM ( '' )  SURFACE ( )  );
#136655=VERTEX_POINT ( 'NONE', #223853 ) ;
#136719=VECTOR ( 'NONE', #38331, 1000.000000000000000 ) ;
#136787=AXIS2_PLACEMENT_3D ( 'NONE', #123044, #85153, #202574 ) ;
#136795=DIRECTION ( 'NONE',  ( -1.000000000000000000, 0.000000000000000000, 0.000000000000000000 ) ) ;
#136816=CIRCLE ( 'NONE', #70218, 0.09999999999999939493 ) ;
#136822=DIRECTION ( 'NONE',  ( 0.000000000000000000, 0.000000000000000000, -1.000000000000000000 ) ) ;
#136835=EDGE_CURVE ( 'NONE', #225207, #40351, #49077, .T. ) ;
#136857=DIRECTION ( 'NONE',  ( 0.000000000000000000, -6.982962677686266711E-15, 1.000000000000000000 ) ) ;
#136873=AXIS2_PLACEMENT_3D ( 'NONE', #36536, #157785, #74384 ) ;
#136876=AXIS2_PLACEMENT_3D ( 'NONE', #62002, #63264, #142784 ) ;
#136911=LINE ( 'NONE', #57356, #40978 ) ;
#136928=AXIS2_PLACEMENT_3D ( 'NONE', #193625, #150646, #52810 ) ;
#136929=CYLINDRICAL_SURFACE ( 'NONE', #222634, 0.09999999999998898659 ) ;
#136934=ORIENTED_EDGE ( 'NONE', *, *, #32141, .F. ) ;
#136953=CARTESIAN_POINT ( 'NONE',  ( 18.49999999999999289, 65.70729864261026876, -131.0657455973724836 ) ) ;
#136990=CIRCLE ( 'NONE', #99540, 0.09999999999998898659 ) ;
#137033=CARTESIAN_POINT ( 'NONE',  ( -20.85000000000000142, 77.83585931145570669, -125.0186683157258329 ) ) ;
#137057=VECTOR ( 'NONE', #39102, 1000.000000000000000 ) ;
#137060=VERTEX_POINT ( 'NONE', #6775 ) ;
#137072=DIRECTION ( 'NONE',  ( 0.000000000000000000, -1.000000000000000000, -6.982962677686266711E-15 ) ) ;
#137087=EDGE_LOOP ( 'NONE', ( #234138, #208103, #140818, #94344, #68674, #116550, #127714, #29856, #64173, #56898 ) ) ;
#137101=AXIS2_PLACEMENT_3D ( 'NONE', #230599, #251433, #11558 ) ;
#137103=CIRCLE ( 'NONE', #182905, 0.09999999999998898659 ) ;
#137115=ORIENTED_EDGE ( 'NONE', *, *, #12869, .T. ) ;
#137116=ADVANCED_FACE ( 'NONE', ( #133145 ), #233543, .T. ) ;
#137143=CARTESIAN_POINT ( 'NONE',  ( -23.25000000000000000, 77.83585931145570669, -125.0186683157258329 ) ) ;
#137167=EDGE_CURVE ( 'NONE', #103428, #114980, #91455, .T. ) ;
#137175=CARTESIAN_POINT ( 'NONE',  ( 23.15000000000000213, 88.41227409416185878, -139.6231074845242688 ) ) ;
#137192=CIRCLE ( 'NONE', #149879, 0.09999999999999134581 ) ;
#137238=CARTESIAN_POINT ( 'NONE',  ( -21.05000000000000071, 74.63912941282028157, -161.9501095574334215 ) ) ;
#137241=ORIENTED_EDGE ( 'NONE', *, *, #26272, .F. ) ;
#137262=CARTESIAN_POINT ( 'NONE',  ( -18.50000000000001066, 85.48068669529106955, -129.5819923157664562 ) ) ;
#137364=ADVANCED_FACE ( 'NONE', ( #101679 ), #58712, .F. ) ;
#137416=ORIENTED_EDGE ( 'NONE', *, *, #119131, .T. ) ;
#137424=CIRCLE ( 'NONE', #91661, 2.100000000000004530 ) ;
#137445=CARTESIAN_POINT ( 'NONE',  ( -22.50000000000000000, 64.35000000001238618, -170.0231074845244166 ) ) ;
#137452=EDGE_CURVE ( 'NONE', #22920, #206325, #196869, .T. ) ;
#137496=CARTESIAN_POINT ( 'NONE',  ( -21.14999999999999858, 76.00000000001237765, -170.0231074845243597 ) ) ;
#137499=EDGE_CURVE ( 'NONE', #228568, #208658, #59272, .T. ) ;
#137520=DIRECTION ( 'NONE',  ( 0.000000000000000000, 0.000000000000000000, -1.000000000000000000 ) ) ;
#137526=ORIENTED_EDGE ( 'NONE', *, *, #139117, .T. ) ;
#137546=ORIENTED_EDGE ( 'NONE', *, *, #127757, .T. ) ;
#137552=CARTESIAN_POINT ( 'NONE',  ( -23.15000000000000213, 76.00000000001230660, -157.1481074845243882 ) ) ;
#137573=DIRECTION ( 'NONE',  ( 0.000000000000000000, 0.1455152366551700771, 0.9893560106964479628 ) ) ;
#137628=DIRECTION ( 'NONE',  ( -1.000000000000000000, 0.000000000000000000, 0.000000000000000000 ) ) ;
#137629=CARTESIAN_POINT ( 'NONE',  ( 21.07094088545367327, 75.90110629746020265, -176.3432747064415196 ) ) ;
#137630=AXIS2_PLACEMENT_3D ( 'NONE', #193665, #12474, #110261 ) ;
#137640=FACE_OUTER_BOUND ( 'NONE', #236131, .T. ) ;
#137646=DIRECTION ( 'NONE',  ( -4.336808689942052446E-15, 0.8660254037844445918, 0.4999999999999896194 ) ) ;
#137690=ORIENTED_EDGE ( 'NONE', *, *, #133785, .F. ) ;
#137704=CARTESIAN_POINT ( 'NONE',  ( -21.05000000000000071, 64.35000000001218723, -143.5379132551784096 ) ) ;
#137707=VECTOR ( 'NONE', #157450, 1000.000000000000000 ) ;
#137708=CARTESIAN_POINT ( 'NONE',  ( -20.64999999999999858, 76.00000000001213607, -136.5231074845243313 ) ) ;
#137734=LINE ( 'NONE', #37390, #63432 ) ;
#137792=CARTESIAN_POINT ( 'NONE',  ( 18.59999999999999076, 69.45000000001222418, -148.7731074845244166 ) ) ;
#137816=AXIS2_PLACEMENT_3D ( 'NONE', #236361, #79830, #96817 ) ;
#137819=CIRCLE ( 'NONE', #29537, 0.09999999999998898659 ) ;
#137846=CARTESIAN_POINT ( 'NONE',  ( -23.15000000000000213, 64.25000000001237765, -170.0231074845244166 ) ) ;
#137848=EDGE_CURVE ( 'NONE', #203407, #193751, #13714, .T. ) ;
#137853=AXIS2_PLACEMENT_3D ( 'NONE', #87805, #125668, #246894 ) ;
#137856=FACE_OUTER_BOUND ( 'NONE', #186115, .T. ) ;
#137861=AXIS2_PLACEMENT_3D ( 'NONE', #6650, #86166, #230868 ) ;
#137877=DIRECTION ( 'NONE',  ( -0.000000000000000000, 1.000000000000000000, 6.982962677686266711E-15 ) ) ;
#137903=ORIENTED_EDGE ( 'NONE', *, *, #252897, .F. ) ;
#137943=EDGE_CURVE ( 'NONE', #73802, #11381, #129932, .T. ) ;
#137967=ORIENTED_EDGE ( 'NONE', *, *, #225652, .T. ) ;
#137985=DIRECTION ( 'NONE',  ( 0.000000000000000000, 0.000000000000000000, 1.000000000000000000 ) ) ;
#138005=EDGE_LOOP ( 'NONE', ( #96324, #179310, #243249, #143228 ) ) ;
#138018=LINE ( 'NONE', #141882, #72350 ) ;
#138048=CIRCLE ( 'NONE', #163041, 12.87499999999999822 ) ;
#138056=FACE_OUTER_BOUND ( 'NONE', #138615, .T. ) ;
#138073=ADVANCED_FACE ( 'NONE', ( #239327 ), #58090, .T. ) ;
#138075=EDGE_LOOP ( 'NONE', ( #55368, #131106, #108367, #111399 ) ) ;
#138102=ORIENTED_EDGE ( 'NONE', *, *, #160261, .T. ) ;
#138133=ORIENTED_EDGE ( 'NONE', *, *, #34503, .T. ) ;
#138143=EDGE_CURVE ( 'NONE', #149556, #16833, #176235, .T. ) ;
#138153=CARTESIAN_POINT ( 'NONE',  ( -21.05000000000000071, 87.48912529308842068, -166.9231074845242802 ) ) ;
#138156=DIRECTION ( 'NONE',  ( 1.000000000000000000, 0.000000000000000000, 0.000000000000000000 ) ) ;
#138157=VERTEX_POINT ( 'NONE', #102340 ) ;
#138165=CARTESIAN_POINT ( 'NONE',  ( 20.94999999999999929, 68.97833521811203639, -132.6895420826271277 ) ) ;
#138179=TOROIDAL_SURFACE ( 'NONE', #79900, 11.65000000000000036, 0.1000000000000000056 ) ;
#138205=CIRCLE ( 'NONE', #826, 7.800000000000001599 ) ;
#138234=VECTOR ( 'NONE', #226678, 1000.000000000000000 ) ;
#138236=DIRECTION ( 'NONE',  ( -0.000000000000000000, -1.000000000000000000, -6.982962677686266711E-15 ) ) ;
#138242=AXIS2_PLACEMENT_3D ( 'NONE', #94508, #32004, #111520 ) ;
#138256=EDGE_CURVE ( 'NONE', #23498, #147377, #243024, .T. ) ;
#138310=ORIENTED_EDGE ( 'NONE', *, *, #225997, .F. ) ;
#138313=VERTEX_POINT ( 'NONE', #55206 ) ;
#138335=CIRCLE ( 'NONE', #184148, 0.09999999999998898659 ) ;
#138337=VERTEX_POINT ( 'NONE', #159494 ) ;
#138349=ORIENTED_EDGE ( 'NONE', *, *, #136835, .T. ) ;
#138351=FACE_OUTER_BOUND ( 'NONE', #240507, .T. ) ;
#138362=CARTESIAN_POINT ( 'NONE',  ( -20.54999999999999716, 68.75000000001230660, -157.7731074845244166 ) ) ;
#138372=ORIENTED_EDGE ( 'NONE', *, *, #118889, .F. ) ;
#138408=LINE ( 'NONE', #115026, #144495 ) ;
#138416=FACE_OUTER_BOUND ( 'NONE', #63335, .T. ) ;
#138429=AXIS2_PLACEMENT_3D ( 'NONE', #68591, #90703, #133689 ) ;
#138435=DIRECTION ( 'NONE',  ( 1.000000000000000000, 0.000000000000000000, 0.000000000000000000 ) ) ;
#138454=EDGE_CURVE ( 'NONE', #23498, #4036, #10377, .T. ) ;
#138463=ORIENTED_EDGE ( 'NONE', *, *, #139749, .T. ) ;
#138497=EDGE_LOOP ( 'NONE', ( #41203, #221214 ) ) ;
#138504=ORIENTED_EDGE ( 'NONE', *, *, #155348, .F. ) ;
#138544=AXIS2_PLACEMENT_3D ( 'NONE', #71854, #211351, #230930 ) ;
#138568=CARTESIAN_POINT ( 'NONE',  ( 23.15000000000000213, 85.60000000001220144, -146.4170766071767389 ) ) ;
#138584=VERTEX_POINT ( 'NONE', #172042 ) ;
#138590=VERTEX_POINT ( 'NONE', #151167 ) ;
#138593=TOROIDAL_SURFACE ( 'NONE', #134342, 11.65000000000000036, 0.1000000000000000056 ) ;
#138613=CARTESIAN_POINT ( 'NONE',  ( 20.94999999999999574, 77.85102823015316176, -158.3691942151018566 ) ) ;
#138615=EDGE_LOOP ( 'NONE', ( #144109, #133886, #163568, #209963, #209535, #226745, #163740, #178429, #131326, #215178, #207636, #132564 ) ) ;
#138638=ORIENTED_EDGE ( 'NONE', *, *, #140386, .T. ) ;
#138641=ORIENTED_EDGE ( 'NONE', *, *, #106157, .T. ) ;
#138660=LINE ( 'NONE', #43452, #76222 ) ;
#138662=CARTESIAN_POINT ( 'NONE',  ( 20.95595012432474391, 65.39582078693598532, -162.4273381543061703 ) ) ;
#138715=ORIENTED_EDGE ( 'NONE', *, *, #184007, .F. ) ;
#138718=CARTESIAN_POINT ( 'NONE',  ( 23.15000000000000213, 85.00000000001222134, -146.4170766071767389 ) ) ;
#138730=DIRECTION ( 'NONE',  ( 1.000000000000000000, 0.000000000000000000, 0.000000000000000000 ) ) ;
#138737=CARTESIAN_POINT ( 'NONE',  ( 21.05000000000000071, 87.48912529308822172, -139.4231074845242802 ) ) ;
#138746=ORIENTED_EDGE ( 'NONE', *, *, #232307, .T. ) ;
#138757=EDGE_CURVE ( 'NONE', #116513, #48521, #180679, .T. ) ;
#138785=CARTESIAN_POINT ( 'NONE',  ( 21.09107601085592520, 75.96069283529527638, -176.3869854598848974 ) ) ;
#138796=EDGE_CURVE ( 'NONE', #86021, #133057, #168248, .T. ) ;
#138808=FACE_OUTER_BOUND ( 'NONE', #132806, .T. ) ;
#138817=AXIS2_PLACEMENT_3D ( 'NONE', #45883, #125435, #204940 ) ;
#138836=ORIENTED_EDGE ( 'NONE', *, *, #253820, .T. ) ;
#138882=AXIS2_PLACEMENT_3D ( 'NONE', #41399, #103891, #81749 ) ;
#138884=AXIS2_PLACEMENT_3D ( 'NONE', #12180, #171283, #72146 ) ;
#138891=DIRECTION ( 'NONE',  ( -1.000000000000000000, 0.000000000000000000, -0.000000000000000000 ) ) ;
#138927=CARTESIAN_POINT ( 'NONE',  ( -21.05000000000000071, 62.00000000001218581, -141.9502000149069261 ) ) ;
#138931=PLANE ( 'NONE',  #96890 ) ;
#138936=FACE_OUTER_BOUND ( 'NONE', #183010, .T. ) ;
#138951=VERTEX_POINT ( 'NONE', #223945 ) ;
#138957=EDGE_CURVE ( 'NONE', #94515, #238290, #10044, .T. ) ;
#138972=CARTESIAN_POINT ( 'NONE',  ( -22.49510344025093644, 75.93287232181820912, -181.6730775896386376 ) ) ;
#139006=VERTEX_POINT ( 'NONE', #251206 ) ;
#139029=ADVANCED_FACE ( 'NONE', ( #72610 ), #156000, .T. ) ;
#139044=LINE ( 'NONE', #255125, #161290 ) ;
#139085=DIRECTION ( 'NONE',  ( 1.000000000000000000, 0.000000000000000000, 0.000000000000000000 ) ) ;
#139090=DIRECTION ( 'NONE',  ( 0.000000000000000000, 0.000000000000000000, -1.000000000000000000 ) ) ;
#139108=DIRECTION ( 'NONE',  ( 1.000000000000000000, 0.000000000000000000, 0.000000000000000000 ) ) ;
#139117=EDGE_CURVE ( 'NONE', #92778, #230733, #134475, .T. ) ;
#139126=ADVANCED_FACE ( 'NONE', ( #133840 ), #205801, .T. ) ;
#139146=DIRECTION ( 'NONE',  ( 1.000000000000000000, 0.000000000000000000, 0.000000000000000000 ) ) ;
#139163=EDGE_CURVE ( 'NONE', #220534, #12740, #119427, .T. ) ;
#139175=DIRECTION ( 'NONE',  ( 0.000000000000000000, 0.000000000000000000, -1.000000000000000000 ) ) ;
#139215=ORIENTED_EDGE ( 'NONE', *, *, #237296, .T. ) ;
#139221=DIRECTION ( 'NONE',  ( 1.000000000000000000, 0.000000000000000000, 0.000000000000000000 ) ) ;
#139243=CARTESIAN_POINT ( 'NONE',  ( 18.37172112093866971, 85.57096165225503626, -129.7063730310401297 ) ) ;
#139244=LINE ( 'NONE', #140542, #207212 ) ;
#139252=ORIENTED_EDGE ( 'NONE', *, *, #6370, .T. ) ;
#139274=CARTESIAN_POINT ( 'NONE',  ( 20.94999999999999929, 69.45000000001229523, -157.8731074845244109 ) ) ;
#139280=CYLINDRICAL_SURFACE ( 'NONE', #237557, 0.09999999999999939493 ) ;
#139286=EDGE_LOOP ( 'NONE', ( #39433, #96040, #168916, #110083 ) ) ;
#139315=AXIS2_PLACEMENT_3D ( 'NONE', #248539, #228988, #86873 ) ;
#139427=DIRECTION ( 'NONE',  ( 1.000000000000000000, 0.000000000000000000, 0.000000000000000000 ) ) ;
#139434=CYLINDRICAL_SURFACE ( 'NONE', #212132, 0.09999999999998898659 ) ;
#139439=CARTESIAN_POINT ( 'NONE',  ( -22.24259225415828567, 68.50806212944695517, -170.1221733679772115 ) ) ;
#139458=( GEOMETRIC_REPRESENTATION_CONTEXT ( 3 ) GLOBAL_UNCERTAINTY_ASSIGNED_CONTEXT ( ( #11258 ) ) GLOBAL_UNIT_ASSIGNED_CONTEXT ( ( #33384, #150728, #111602 ) ) REPRESENTATION_CONTEXT ( 'NONE', 'WORKASPACE' ) );
#139474=CARTESIAN_POINT ( 'NONE',  ( -23.15000000000000213, 64.35000000001245724, -181.7731074845244450 ) ) ;
#139478=EDGE_CURVE ( 'NONE', #151389, #236311, #34474, .T. ) ;
#139482=CARTESIAN_POINT ( 'NONE',  ( -18.59999999999999787, 77.83534155023670564, -158.4679561919613491 ) ) ;
#139483=DIRECTION ( 'NONE',  ( 0.000000000000000000, 0.000000000000000000, 1.000000000000000000 ) ) ;
#139503=ORIENTED_EDGE ( 'NONE', *, *, #91118, .F. ) ;
#139560=DIRECTION ( 'NONE',  ( 0.000000000000000000, -6.982962677686266711E-15, 1.000000000000000000 ) ) ;
#139571=CARTESIAN_POINT ( 'NONE',  ( -23.15000000000000213, 74.07476635515247665, -157.2928639513982318 ) ) ;
#139573=DIRECTION ( 'NONE',  ( 0.000000000000000000, 0.8660254037844377084, 0.5000000000000016653 ) ) ;
#139579=DIRECTION ( 'NONE',  ( 0.000000000000000000, 0.000000000000000000, 1.000000000000000000 ) ) ;
#139584=AXIS2_PLACEMENT_3D ( 'NONE', #117930, #136183, #215741 ) ;
#139591=CARTESIAN_POINT ( 'NONE',  ( 20.94999999999999929, 70.50000000001223555, -148.9283735034374843 ) ) ;
#139612=DIRECTION ( 'NONE',  ( 0.000000000000000000, -6.530723674265620862E-15, 1.000000000000000000 ) ) ;
#139632=ORIENTED_EDGE ( 'NONE', *, *, #167685, .T. ) ;
#139663=LINE ( 'NONE', #184911, #66287 ) ;
#139701=CIRCLE ( 'NONE', #27342, 0.1000000000000009492 ) ;
#139710=DIRECTION ( 'NONE',  ( 0.000000000000000000, 0.1568667991644355497, -0.9876197685951332295 ) ) ;
#139717=B_SPLINE_CURVE_WITH_KNOTS ( 'NONE', 3,
 ( #27773, #12053, #51125, #111129, #126839, #246774, #168588 ),
 .UNSPECIFIED., .F., .F.,
 ( 4, 3, 4 ),
 ( 0.000000000000000000, 0.0009834301579440022593, 0.001767853679402679300 ),
 .UNSPECIFIED. ) ;
#139719=AXIS2_PLACEMENT_3D ( 'NONE', #99255, #19756, #79690 ) ;
#139745=CARTESIAN_POINT ( 'NONE',  ( -23.15000000000000213, 76.00000000001237765, -170.0231074845243597 ) ) ;
#139749=EDGE_CURVE ( 'NONE', #223792, #54460, #72340, .T. ) ;
#139767=VECTOR ( 'NONE', #43116, 1000.000000000000000 ) ;
#139856=AXIS2_PLACEMENT_3D ( 'NONE', #73025, #74305, #234623 ) ;
#139871=CARTESIAN_POINT ( 'NONE',  ( 23.24999999999999289, 80.15000000001238334, -170.0231074845243313 ) ) ;
#139880=ORIENTED_EDGE ( 'NONE', *, *, #89531, .T. ) ;
#139888=AXIS2_PLACEMENT_3D ( 'NONE', #824, #159958, #101195 ) ;
#139902=CARTESIAN_POINT ( 'NONE',  ( 21.05000000000000071, 65.27628289530480288, -162.3581939154368285 ) ) ;
#139927=CARTESIAN_POINT ( 'NONE',  ( -18.55121869061588669, 65.67252876774553272, -130.9457041994994881 ) ) ;
#139929=ORIENTED_EDGE ( 'NONE', *, *, #248474, .F. ) ;
#139938=CIRCLE ( 'NONE', #127299, 0.09999999999998898659 ) ;
#139951=AXIS2_PLACEMENT_3D ( 'NONE', #78520, #215470, #116390 ) ;
#139976=EDGE_CURVE ( 'NONE', #250411, #66273, #48470, .T. ) ;
#139984=DIRECTION ( 'NONE',  ( 0.000000000000000000, 0.000000000000000000, 1.000000000000000000 ) ) ;
#140015=EDGE_CURVE ( 'NONE', #157651, #218493, #168477, .T. ) ;
#140024=CIRCLE ( 'NONE', #235902, 0.5000000000000004441 ) ;
#140040=DIRECTION ( 'NONE',  ( 0.000000000000000000, 0.000000000000000000, 1.000000000000000000 ) ) ;
#140065=DIRECTION ( 'NONE',  ( 0.000000000000000000, 0.000000000000000000, 1.000000000000000000 ) ) ;
#140071=CIRCLE ( 'NONE', #210831, 0.09999999999999230338 ) ;
#140086=CARTESIAN_POINT ( 'NONE',  ( -21.05000000000000071, 64.25000000001219291, -143.5379132551784096 ) ) ;
#140098=AXIS2_PLACEMENT_3D ( 'NONE', #212711, #116187, #195732 ) ;
#140108=DIRECTION ( 'NONE',  ( -2.940209281316621016E-16, -1.000000000000000000, -7.056502275159890832E-15 ) ) ;
#140162=VERTEX_POINT ( 'NONE', #238669 ) ;
#140179=AXIS2_PLACEMENT_3D ( 'NONE', #99543, #214385, #235232 ) ;
#140189=DIRECTION ( 'NONE',  ( 0.000000000000000000, 0.000000000000000000, 1.000000000000000000 ) ) ;
#140192=DIRECTION ( 'NONE',  ( 0.000000000000000000, 7.147358527629766941E-15, -1.000000000000000000 ) ) ;
#140199=DIRECTION ( 'NONE',  ( 1.000000000000000000, 0.000000000000000000, 0.000000000000000000 ) ) ;
#140221=CARTESIAN_POINT ( 'NONE',  ( -21.05000000000000071, 87.48912529308822172, -139.6231074845242688 ) ) ;
#140225=CARTESIAN_POINT ( 'NONE',  ( -20.64999999999999858, 68.85000000001228670, -157.6731074845243938 ) ) ;
#140236=ORIENTED_EDGE ( 'NONE', *, *, #220196, .F. ) ;
#140269=DIRECTION ( 'NONE',  ( -1.000000000000000000, 0.000000000000000000, 0.000000000000000000 ) ) ;
#140270=DIRECTION ( 'NONE',  ( 0.000000000000000000, 0.000000000000000000, 1.000000000000000000 ) ) ;
#140272=AXIS2_PLACEMENT_3D ( 'NONE', #126432, #66465, #69052 ) ;
#140293=EDGE_LOOP ( 'NONE', ( #111825, #202346, #152696, #164051 ) ) ;
#140301=ORIENTED_EDGE ( 'NONE', *, *, #12656, .T. ) ;
#140316=DIRECTION ( 'NONE',  ( 0.000000000000000000, -1.000000000000000000, -6.352154140967427193E-15 ) ) ;
#140318=ORIENTED_EDGE ( 'NONE', *, *, #167430, .F. ) ;
#140386=EDGE_CURVE ( 'NONE', #91302, #88568, #155914, .T. ) ;
#140394=DIRECTION ( 'NONE',  ( -0.000000000000000000, -0.9876197685951290106, 0.1568667991644625281 ) ) ;
#140436=CARTESIAN_POINT ( 'NONE',  ( 21.05000000000000071, 69.69548367074834516, -170.0020041764652774 ) ) ;
#140441=CARTESIAN_POINT ( 'NONE',  ( 21.05000000000000071, 67.22371710471985295, -161.4644784893834810 ) ) ;
#140442=CARTESIAN_POINT ( 'NONE',  ( -22.50000000000000000, 76.00000000001242029, -176.2731074845243597 ) ) ;
#140444=ADVANCED_FACE ( 'NONE', ( #195085 ), #76964, .T. ) ;
#140489=ORIENTED_EDGE ( 'NONE', *, *, #188098, .T. ) ;
#140515=ADVANCED_FACE ( 'NONE', ( #121945 ), #74577, .F. ) ;
#140519=FACE_OUTER_BOUND ( 'NONE', #225993, .T. ) ;
#140520=VERTEX_POINT ( 'NONE', #218452 ) ;
#140538=CARTESIAN_POINT ( 'NONE',  ( 18.50000000000000355, 85.40000000001209912, -129.6410656363516125 ) ) ;
#140542=CARTESIAN_POINT ( 'NONE',  ( -23.25000000000000000, 85.68240343348850274, -129.8662641071115047 ) ) ;
#140553=TOROIDAL_SURFACE ( 'NONE', #73957, 11.65000000000000036, 0.1000000000000000056 ) ;
#140557=ORIENTED_EDGE ( 'NONE', *, *, #133849, .F. ) ;
#140565=CARTESIAN_POINT ( 'NONE',  ( 21.05000000000000071, 71.00000000001230660, -157.6178414656113205 ) ) ;
#140576=VERTEX_POINT ( 'NONE', #119382 ) ;
#140625=FACE_OUTER_BOUND ( 'NONE', #119276, .T. ) ;
#140638=EDGE_CURVE ( 'NONE', #46071, #85130, #26932, .T. ) ;
#140644=ADVANCED_FACE ( 'NONE', ( #248307 ), #143606, .T. ) ;
#140656=DIRECTION ( 'NONE',  ( 1.000000000000000000, 0.000000000000000000, 0.000000000000000000 ) ) ;
#140668=ORIENTED_EDGE ( 'NONE', *, *, #252765, .F. ) ;
#140702=DIRECTION ( 'NONE',  ( 0.000000000000000000, 0.000000000000000000, 1.000000000000000000 ) ) ;
#140731=AXIS2_PLACEMENT_3D ( 'NONE', #6868, #129386, #29047 ) ;
#140735=AXIS2_PLACEMENT_3D ( 'NONE', #12021, #91540, #189360 ) ;
#140743=DIRECTION ( 'NONE',  ( 1.000000000000000000, 0.000000000000000000, 0.000000000000000000 ) ) ;
#140749=DIRECTION ( 'NONE',  ( 0.000000000000000000, -0.8700118002898357128, 0.4930308989875170633 ) ) ;
#140756=AXIS2_PLACEMENT_3D ( 'NONE', #94225, #209048, #173827 ) ;
#140762=DIRECTION ( 'NONE',  ( 0.000000000000000000, -6.454785026890489601E-15, 1.000000000000000000 ) ) ;
#140797=AXIS2_PLACEMENT_3D ( 'NONE', #95181, #193008, #70518 ) ;
#140807=CARTESIAN_POINT ( 'NONE',  ( -21.14999999999999858, 76.10000000001241460, -176.2731074845243597 ) ) ;
#140814=CARTESIAN_POINT ( 'NONE',  ( 18.55121869061587958, 65.67252876774553272, -130.9457041994994881 ) ) ;
#140818=ORIENTED_EDGE ( 'NONE', *, *, #160418, .F. ) ;
#140839=TOROIDAL_SURFACE ( 'NONE', #182550, 0.2000000000000000111, 0.1000000000000000056 ) ;
#140874=EDGE_LOOP ( 'NONE', ( #184351, #217840, #208944, #40596 ) ) ;
#140905=AXIS2_PLACEMENT_3D ( 'NONE', #235140, #136009, #254658 ) ;
#140907=ORIENTED_EDGE ( 'NONE', *, *, #112456, .F. ) ;
#140925=AXIS2_PLACEMENT_3D ( 'NONE', #132000, #210268, #231125 ) ;
#141007=DIRECTION ( 'NONE',  ( -2.952720810173289605E-16, -1.000000000000000000, -7.086529944415894657E-15 ) ) ;
#141010=ORIENTED_EDGE ( 'NONE', *, *, #238713, .T. ) ;
#141029=LINE ( 'NONE', #204826, #145353 ) ;
#141102=DIRECTION ( 'NONE',  ( -1.000000000000000000, 2.952720810173289112E-16, 2.061873921506763405E-30 ) ) ;
#141148=CIRCLE ( 'NONE', #195325, 0.1000000000000028644 ) ;
#141149=VERTEX_POINT ( 'NONE', #231030 ) ;
#141178=DIRECTION ( 'NONE',  ( 1.000000000000000000, 0.000000000000000000, 0.000000000000000000 ) ) ;
#141181=EDGE_CURVE ( 'NONE', #61384, #168421, #210446, .T. ) ;
#141185=CARTESIAN_POINT ( 'NONE',  ( 20.97462148592287079, 67.12526242356170769, -157.7684631527933732 ) ) ;
#141207=EDGE_LOOP ( 'NONE', ( #209085, #199925, #92823, #132228 ) ) ;
#141237=EDGE_LOOP ( 'NONE', ( #175673, #145895 ) ) ;
#141248=EDGE_LOOP ( 'NONE', ( #134226, #36443, #19387, #40151 ) ) ;
#141249=EDGE_LOOP ( 'NONE', ( #108383, #94142, #179922, #40567 ) ) ;
#141267=EDGE_CURVE ( 'NONE', #177752, #9341, #77322, .T. ) ;
#141269=CARTESIAN_POINT ( 'NONE',  ( 21.05000000000000071, 65.27628289530478867, -162.3581939154368285 ) ) ;
#141278=CARTESIAN_POINT ( 'NONE',  ( 18.59999999999999076, 69.55000000001230376, -160.0060803140843859 ) ) ;
#141282=AXIS2_PLACEMENT_3D ( 'NONE', #188885, #10257, #111934 ) ;
#141284=VECTOR ( 'NONE', #42834, 1000.000000000000000 ) ;
#141328=ORIENTED_EDGE ( 'NONE', *, *, #136408, .F. ) ;
#141337=EDGE_LOOP ( 'NONE', ( #136383, #24344, #152485, #148621 ) ) ;
#141338=DIRECTION ( 'NONE',  ( -0.7071067811865127117, -0.7071067811865821007, 0.000000000000000000 ) ) ;
#141345=CARTESIAN_POINT ( 'NONE',  ( -21.14999999999999858, 64.35000000001238618, -169.9231074845244507 ) ) ;
#141363=CARTESIAN_POINT ( 'NONE',  ( -21.05000000000000071, 76.00000000001213607, -136.5231074845243313 ) ) ;
#141401=EDGE_LOOP ( 'NONE', ( #85299, #229813, #183345, #13773, #20622 ) ) ;
#141424=CARTESIAN_POINT ( 'NONE',  ( 21.12230431290518951, 75.99479014832341761, -176.4806741378173740 ) ) ;
#141441=DIRECTION ( 'NONE',  ( 2.840903330521631775E-16, 0.8700118002898354908, -0.4930308989875170078 ) ) ;
#141499=DIRECTION ( 'NONE',  ( 1.000000000000000000, 0.000000000000000000, 0.000000000000000000 ) ) ;
#141511=DIRECTION ( 'NONE',  ( 1.000000000000000000, 0.000000000000000000, 0.000000000000000000 ) ) ;
#141524=DIRECTION ( 'NONE',  ( -1.000000000000000000, -7.304098846218164250E-16, 4.217023435051628197E-16 ) ) ;
#141534=DIRECTION ( 'NONE',  ( 0.000000000000000000, -7.034366652768095332E-15, 1.000000000000000000 ) ) ;
#141552=VECTOR ( 'NONE', #215690, 1000.000000000000000 ) ;
#141569=AXIS2_PLACEMENT_3D ( 'NONE', #65996, #185947, #67281 ) ;
#141589=CARTESIAN_POINT ( 'NONE',  ( -23.15000000000000213, 85.00000000001222134, -146.4170766071767389 ) ) ;
#141610=VERTEX_POINT ( 'NONE', #139274 ) ;
#141619=AXIS2_PLACEMENT_3D ( 'NONE', #100346, #80784, #139483 ) ;
#141624=VERTEX_POINT ( 'NONE', #213698 ) ;
#141628=ORIENTED_EDGE ( 'NONE', *, *, #245758, .F. ) ;
#141640=VERTEX_POINT ( 'NONE', #20657 ) ;
#141643=ORIENTED_EDGE ( 'NONE', *, *, #30688, .F. ) ;
#141658=CARTESIAN_POINT ( 'NONE',  ( 20.95512820512820440, 67.12384868372420499, -161.4644784893834810 ) ) ;
#141665=VERTEX_POINT ( 'NONE', #37657 ) ;
#141698=CARTESIAN_POINT ( 'NONE',  ( -21.14999999999999858, 76.00000000001242029, -176.5637644362255969 ) ) ;
#141715=CARTESIAN_POINT ( 'NONE',  ( 20.94999999999999929, 76.00000000001216449, -140.5231074845243597 ) ) ;
#141764=CARTESIAN_POINT ( 'NONE',  ( 20.94999999999999574, 67.07338541492521244, -161.5514244653012952 ) ) ;
#141783=EDGE_CURVE ( 'NONE', #121863, #138313, #98317, .T. ) ;
#141827=AXIS2_PLACEMENT_3D ( 'NONE', #125012, #184973, #141983 ) ;
#141830=CARTESIAN_POINT ( 'NONE',  ( 18.44208962362720428, 85.55234049692090537, -129.6809344290617219 ) ) ;
#141836=CIRCLE ( 'NONE', #50250, 0.2000000000000057288 ) ;
#141842=DIRECTION ( 'NONE',  ( 0.000000000000000000, -0.1350103645451807555, -0.9908441862701609093 ) ) ;
#141848=ORIENTED_EDGE ( 'NONE', *, *, #109624, .F. ) ;
#141879=CIRCLE ( 'NONE', #121077, 0.6000000000000033085 ) ;
#141880=CARTESIAN_POINT ( 'NONE',  ( -18.59999999999999787, 66.85000000001228670, -157.6731074845244223 ) ) ;
#141882=CARTESIAN_POINT ( 'NONE',  ( -20.94999999999999929, 64.40000000001219860, -143.4513107147999449 ) ) ;
#141897=VERTEX_POINT ( 'NONE', #132581 ) ;
#141907=DIRECTION ( 'NONE',  ( 0.000000000000000000, 0.000000000000000000, 1.000000000000000000 ) ) ;
#141915=DIRECTION ( 'NONE',  ( -0.000000000000000000, -6.982962677686266711E-15, 1.000000000000000000 ) ) ;
#141919=CARTESIAN_POINT ( 'NONE',  ( 18.49999999999999289, 65.67426406872414191, -145.1731074845244223 ) ) ;
#141931=EDGE_LOOP ( 'NONE', ( #149912, #97536, #243798, #205169 ) ) ;
#141949=ORIENTED_EDGE ( 'NONE', *, *, #52182, .F. ) ;
#141951=EDGE_LOOP ( 'NONE', ( #84980, #192694, #121025, #115228 ) ) ;
#141958=DIRECTION ( 'NONE',  ( 1.000000000000000000, -0.000000000000000000, 0.000000000000000000 ) ) ;
#141965=ORIENTED_EDGE ( 'NONE', *, *, #60650, .T. ) ;
#141983=DIRECTION ( 'NONE',  ( 1.000000000000000000, 0.000000000000000000, 0.000000000000000000 ) ) ;
#141988=EDGE_CURVE ( 'NONE', #138590, #109794, #194651, .T. ) ;
#142053=DIRECTION ( 'NONE',  ( 1.836970198721029934E-16, 1.000000000000000000, 6.982962677686266711E-15 ) ) ;
#142057=DIRECTION ( 'NONE',  ( 0.000000000000000000, 0.000000000000000000, -1.000000000000000000 ) ) ;
#142066=VECTOR ( 'NONE', #176907, 1000.000000000000000 ) ;
#142082=CARTESIAN_POINT ( 'NONE',  ( 21.14999999999999858, 69.45000000001229523, -157.6731074845243938 ) ) ;
#142087=ORIENTED_EDGE ( 'NONE', *, *, #228610, .F. ) ;
#142146=ADVANCED_FACE ( 'NONE', ( #228498 ), #9427, .T. ) ;
#142175=VECTOR ( 'NONE', #43043, 1000.000000000000000 ) ;
#142176=EDGE_LOOP ( 'NONE', ( #242893, #10666, #63252, #226961, #112066, #36294, #225575 ) ) ;
#142190=EDGE_LOOP ( 'NONE', ( #231586, #217775, #172765, #215308 ) ) ;
#142194=VECTOR ( 'NONE', #41713, 1000.000000000000000 ) ;
#142227=CIRCLE ( 'NONE', #8955, 0.09999999999999971412 ) ;
#142253=CARTESIAN_POINT ( 'NONE',  ( -18.50000000000000000, 66.75000000001223555, -148.7731074845244166 ) ) ;
#142281=CARTESIAN_POINT ( 'NONE',  ( -21.05000000000000071, 87.65000000001215597, -139.4231074845242802 ) ) ;
#142305=EDGE_CURVE ( 'NONE', #94754, #38206, #150249, .T. ) ;
#142308=DIRECTION ( 'NONE',  ( 0.000000000000000000, 0.000000000000000000, 1.000000000000000000 ) ) ;
#142321=CARTESIAN_POINT ( 'NONE',  ( 20.72390388899090041, 65.41003688158824048, -162.5117591887780577 ) ) ;
#142335=CARTESIAN_POINT ( 'NONE',  ( -23.25000000000000000, 76.00000000001213607, -136.5231074845243313 ) ) ;
#142351=FACE_OUTER_BOUND ( 'NONE', #25938, .T. ) ;
#142394=DIRECTION ( 'NONE',  ( -1.000000000000000000, -0.000000000000000000, 0.000000000000000000 ) ) ;
#142398=TOROIDAL_SURFACE ( 'NONE', #154907, 0.2000000000000000111, 0.1000000000000000056 ) ;
#142430=DIRECTION ( 'NONE',  ( -0.000000000000000000, -1.000000000000000000, -6.982962677686266711E-15 ) ) ;
#142432=EDGE_CURVE ( 'NONE', #127762, #68761, #216616, .T. ) ;
#142459=EDGE_LOOP ( 'NONE', ( #155053, #209805, #20339, #215925 ) ) ;
#142487=EDGE_CURVE ( 'NONE', #94999, #109724, #9132, .T. ) ;
#142497=DIRECTION ( 'NONE',  ( 0.000000000000000000, 6.982962677686266711E-15, -1.000000000000000000 ) ) ;
#142526=CIRCLE ( 'NONE', #105084, 0.09999999999999939493 ) ;
#142557=EDGE_CURVE ( 'NONE', #4792, #93776, #245175, .T. ) ;
#142605=CARTESIAN_POINT ( 'NONE',  ( -21.05000000000000071, 87.65000000001235492, -167.0231074845242460 ) ) ;
#142608=AXIS2_PLACEMENT_3D ( 'NONE', #248778, #29755, #87108 ) ;
#142621=ORIENTED_EDGE ( 'NONE', *, *, #132512, .T. ) ;
#142693=EDGE_CURVE ( 'NONE', #78383, #109454, #234789, .T. ) ;
#142705=ORIENTED_EDGE ( 'NONE', *, *, #250941, .T. ) ;
#142711=CIRCLE ( 'NONE', #30314, 0.1000000000000118433 ) ;
#142721=DIRECTION ( 'NONE',  ( -1.000000000000000000, -0.000000000000000000, -0.000000000000000000 ) ) ;
#142727=AXIS2_PLACEMENT_3D ( 'NONE', #68671, #148197, #210741 ) ;
#142781=AXIS2_PLACEMENT_3D ( 'NONE', #158684, #217315, #154827 ) ;
#142784=DIRECTION ( 'NONE',  ( 0.000000000000000000, -1.000000000000000000, 0.000000000000000000 ) ) ;
#142786=CARTESIAN_POINT ( 'NONE',  ( 22.39999999999999858, 75.90000000001242597, -177.8138870828977360 ) ) ;
#142792=FACE_OUTER_BOUND ( 'NONE', #35715, .T. ) ;
#142821=DIRECTION ( 'NONE',  ( -1.000000000000000000, 0.000000000000000000, -0.000000000000000000 ) ) ;
#142856=CARTESIAN_POINT ( 'NONE',  ( 20.94999999999999929, 71.18691588786276725, -158.0815897280005800 ) ) ;
#142880=DIRECTION ( 'NONE',  ( -0.7071067811865475727, 0.7071067811865475727, 4.937700262164531476E-15 ) ) ;
#142892=LINE ( 'NONE', #161212, #102646 ) ;
#142895=ORIENTED_EDGE ( 'NONE', *, *, #132512, .F. ) ;
#142910=CARTESIAN_POINT ( 'NONE',  ( -2.995603634470891112E-16, 87.75000000001220712, -145.2731074845242745 ) ) ;
#142943=DIRECTION ( 'NONE',  ( -1.000000000000000000, -0.000000000000000000, -0.000000000000000000 ) ) ;
#142978=EDGE_CURVE ( 'NONE', #133329, #76888, #201883, .T. ) ;
#142980=DIRECTION ( 'NONE',  ( 1.000000000000000000, 0.000000000000000000, 0.000000000000000000 ) ) ;
#143016=CARTESIAN_POINT ( 'NONE',  ( 21.05281448260627641, 67.22398984147466194, -157.8495495727129878 ) ) ;
#143022=CIRCLE ( 'NONE', #97205, 0.09999999999998898659 ) ;
#143036=EDGE_CURVE ( 'NONE', #103428, #7914, #132236, .T. ) ;
#143037=CARTESIAN_POINT ( 'NONE',  ( -21.05000000000000071, 69.74218538953626023, -170.1208977758331855 ) ) ;
#143050=EDGE_LOOP ( 'NONE', ( #74759, #146627, #102215 ) ) ;
#143081=DIRECTION ( 'NONE',  ( 0.000000000000000000, -1.000000000000000000, 0.000000000000000000 ) ) ;
#143106=DIRECTION ( 'NONE',  ( -1.000000000000000000, -0.000000000000000000, 0.000000000000000000 ) ) ;
#143129=VERTEX_POINT ( 'NONE', #249996 ) ;
#143176=DIRECTION ( 'NONE',  ( 1.000000000000000000, 0.000000000000000000, 0.000000000000000000 ) ) ;
#143187=ORIENTED_EDGE ( 'NONE', *, *, #245827, .F. ) ;
#143201=CARTESIAN_POINT ( 'NONE',  ( 22.14074124539698829, 68.60992214896863572, -170.1221603803684843 ) ) ;
#143228=ORIENTED_EDGE ( 'NONE', *, *, #58044, .T. ) ;
#143300=ORIENTED_EDGE ( 'NONE', *, *, #238083, .T. ) ;
#143312=CARTESIAN_POINT ( 'NONE',  ( 21.00000000000000000, 66.25000000001223555, -148.7731074845244450 ) ) ;
#143343=EDGE_CURVE ( 'NONE', #94754, #183270, #252742, .T. ) ;
#143371=CIRCLE ( 'NONE', #185067, 0.1000000000000028644 ) ;
#143374=ADVANCED_FACE ( 'NONE', ( #165010 ), #44935, .T. ) ;
#143375=ORIENTED_EDGE ( 'NONE', *, *, #148111, .T. ) ;
#143388=CYLINDRICAL_SURFACE ( 'NONE', #42228, 0.09999999999998898659 ) ;
#143397=LINE ( 'NONE', #22189, #26903 ) ;
#143408=EDGE_CURVE ( 'NONE', #240571, #145384, #165973, .T. ) ;
#143419=CARTESIAN_POINT ( 'NONE',  ( -22.32929514600008503, 75.90092432189851479, -177.6017550499008735 ) ) ;
#143432=DIRECTION ( 'NONE',  ( -3.265361837132813093E-16, -1.000000000000000000, -6.982962677686266711E-15 ) ) ;
#143457=AXIS2_PLACEMENT_3D ( 'NONE', #104031, #164039, #4921 ) ;
#143473=ORIENTED_EDGE ( 'NONE', *, *, #144102, .T. ) ;
#143484=ORIENTED_EDGE ( 'NONE', *, *, #177340, .F. ) ;
#143509=ORIENTED_EDGE ( 'NONE', *, *, #238350, .T. ) ;
#143528=CARTESIAN_POINT ( 'NONE',  ( 19.96984138294286026, 64.25000000001220712, -145.2985354133239753 ) ) ;
#143529=CYLINDRICAL_SURFACE ( 'NONE', #112190, 0.09999999999998898659 ) ;
#143532=CARTESIAN_POINT ( 'NONE',  ( 23.25000000000000000, 87.65000000001215597, -139.6231074845242688 ) ) ;
#143553=CARTESIAN_POINT ( 'NONE',  ( 21.05000000000000071, 67.12791932463460398, -161.5020600656926035 ) ) ;
#143569=AXIS2_PLACEMENT_3D ( 'NONE', #102688, #145680, #223929 ) ;
#143593=VERTEX_POINT ( 'NONE', #49521 ) ;
#143595=EDGE_CURVE ( 'NONE', #258015, #55258, #20187, .T. ) ;
#143606=TOROIDAL_SURFACE ( 'NONE', #6038, 0.6000000000000013101, 0.1000000000000000056 ) ;
#143642=EDGE_LOOP ( 'NONE', ( #91245, #82077, #198755 ) ) ;
#143673=LINE ( 'NONE', #180251, #28541 ) ;
#143722=CARTESIAN_POINT ( 'NONE',  ( -21.13435531349785634, 69.50627893642028710, -170.0231074845243882 ) ) ;
#143741=CARTESIAN_POINT ( 'NONE',  ( -20.85000000000000142, 87.75000000001215028, -136.5231074845242745 ) ) ;
#143755=ORIENTED_EDGE ( 'NONE', *, *, #125053, .T. ) ;
#143763=CARTESIAN_POINT ( 'NONE',  ( 20.94999999999999929, 64.35000000001218723, -143.3647081744214802 ) ) ;
#143772=ORIENTED_EDGE ( 'NONE', *, *, #137167, .F. ) ;
#143820=CARTESIAN_POINT ( 'NONE',  ( 21.05000000000000071, 65.31570632562512913, -162.4964335458869016 ) ) ;
#143827=DIRECTION ( 'NONE',  ( 1.000000000000000000, 0.000000000000000000, 0.000000000000000000 ) ) ;
#143884=ORIENTED_EDGE ( 'NONE', *, *, #92641, .F. ) ;
#143939=ADVANCED_FACE ( 'NONE', ( #164026 ), #198664, .F. ) ;
#143944=CARTESIAN_POINT ( 'NONE',  ( 20.94999999999999574, 74.26374286841490857, -158.4544551555068779 ) ) ;
#143986=LINE ( 'NONE', #244372, #20788 ) ;
#143989=DIRECTION ( 'NONE',  ( 0.000000000000000000, 0.000000000000000000, 1.000000000000000000 ) ) ;
#144003=ORIENTED_EDGE ( 'NONE', *, *, #100388, .T. ) ;
#144009=CARTESIAN_POINT ( 'NONE',  ( 22.60000000000000142, 75.95218160930768647, -181.7731299035715438 ) ) ;
#144045=AXIS2_PLACEMENT_3D ( 'NONE', #118084, #12590, #197608 ) ;
#144053=DIRECTION ( 'NONE',  ( -0.000000000000000000, 1.000000000000000000, 6.982962677686266711E-15 ) ) ;
#144071=AXIS2_PLACEMENT_3D ( 'NONE', #233519, #134375, #213935 ) ;
#144076=AXIS2_PLACEMENT_3D ( 'NONE', #60967, #80501, #62261 ) ;
#144087=CARTESIAN_POINT ( 'NONE',  ( -18.50000000000000000, 66.65000000001222702, -148.8731074845244393 ) ) ;
#144090=ORIENTED_EDGE ( 'NONE', *, *, #59876, .F. ) ;
#144099=ADVANCED_FACE ( 'NONE', ( #113031 ), #75213, .T. ) ;
#144102=EDGE_CURVE ( 'NONE', #238448, #77760, #23912, .T. ) ;
#144109=ORIENTED_EDGE ( 'NONE', *, *, #8659, .T. ) ;
#144130=VERTEX_POINT ( 'NONE', #156032 ) ;
#144171=VECTOR ( 'NONE', #237369, 1000.000000000000000 ) ;
#144174=ADVANCED_FACE ( 'NONE', ( #115591 ), #34808, .T. ) ;
#144185=EDGE_CURVE ( 'NONE', #21932, #121672, #161273, .T. ) ;
#144205=ORIENTED_EDGE ( 'NONE', *, *, #214990, .T. ) ;
#144218=FACE_OUTER_BOUND ( 'NONE', #49691, .T. ) ;
#144227=CARTESIAN_POINT ( 'NONE',  ( 23.14999999999998437, 76.00000000001237765, -170.0231074845243597 ) ) ;
#144230=DIRECTION ( 'NONE',  ( 1.000000000000000000, 7.304098846218133681E-16, 5.311601492717083645E-30 ) ) ;
#144234=CIRCLE ( 'NONE', #81674, 0.09999999999998898659 ) ;
#144244=CARTESIAN_POINT ( 'NONE',  ( -18.59999999999999787, 70.05000000001236060, -159.7174051794895320 ) ) ;
#144250=DIRECTION ( 'NONE',  ( 0.000000000000000000, 0.000000000000000000, 1.000000000000000000 ) ) ;
#144280=EDGE_CURVE ( 'NONE', #210220, #5518, #36382, .T. ) ;
#144283=FACE_OUTER_BOUND ( 'NONE', #36142, .T. ) ;
#144332=DIRECTION ( 'NONE',  ( -1.000000000000000000, -0.000000000000000000, -0.000000000000000000 ) ) ;
#144354=CARTESIAN_POINT ( 'NONE',  ( 23.14999999999999858, 73.90000000001214175, -136.5231074845243597 ) ) ;
#144373=PLANE ( 'NONE',  #72216 ) ;
#144380=DIRECTION ( 'NONE',  ( 0.000000000000000000, -1.000000000000000000, 0.000000000000000000 ) ) ;
#144389=DIRECTION ( 'NONE',  ( -1.000000000000000000, 0.000000000000000000, -0.000000000000000000 ) ) ;
#144394=ORIENTED_EDGE ( 'NONE', *, *, #133629, .T. ) ;
#144464=DIRECTION ( 'NONE',  ( 1.000000000000000000, 0.000000000000000000, 0.000000000000000000 ) ) ;
#144474=VERTEX_POINT ( 'NONE', #12368 ) ;
#144495=VECTOR ( 'NONE', #55025, 1000.000000000000000 ) ;
#144501=VECTOR ( 'NONE', #80940, 1000.000000000000000 ) ;
#144546=CARTESIAN_POINT ( 'NONE',  ( -23.15000000000000213, 85.60000000001231513, -160.1291383618718385 ) ) ;
#144548=CARTESIAN_POINT ( 'NONE',  ( 21.30000000000002558, 76.00000000001234923, -165.9731074845243768 ) ) ;
#144555=TOROIDAL_SURFACE ( 'NONE', #11289, 0.6000000000000006439, 0.1000000000000000056 ) ;
#144560=ORIENTED_EDGE ( 'NONE', *, *, #30688, .T. ) ;
#144561=DIRECTION ( 'NONE',  ( 0.000000000000000000, 0.000000000000000000, 1.000000000000000000 ) ) ;
#144572=CARTESIAN_POINT ( 'NONE',  ( 22.49999999999999645, 75.91119002362552237, -181.6728704025562706 ) ) ;
#144577=CARTESIAN_POINT ( 'NONE',  ( -23.15000000000000213, 70.05000000001221849, -146.8288097895591875 ) ) ;
#144594=CARTESIAN_POINT ( 'NONE',  ( -20.94999999999999929, 77.83585931145570669, -125.0186683157258045 ) ) ;
#144625=DIRECTION ( 'NONE',  ( 1.000000000000000000, 0.000000000000000000, 0.000000000000000000 ) ) ;
#144651=CARTESIAN_POINT ( 'NONE',  ( 21.98333005346336222, 76.00000000001243450, -177.3971828135810256 ) ) ;
#144691=EDGE_LOOP ( 'NONE', ( #79408, #3639, #256824, #91964 ) ) ;
#144699=CARTESIAN_POINT ( 'NONE',  ( -21.05000000000000071, 74.83729825007431202, -162.1231074845243540 ) ) ;
#144712=ORIENTED_EDGE ( 'NONE', *, *, #188114, .F. ) ;
#144729=ORIENTED_EDGE ( 'NONE', *, *, #26437, .T. ) ;
#144735=EDGE_CURVE ( 'NONE', #128659, #248708, #215766, .T. ) ;
#144742=ADVANCED_FACE ( 'NONE', ( #184248 ), #242934, .T. ) ;
#144747=AXIS2_PLACEMENT_3D ( 'NONE', #35692, #170084, #233863 ) ;
#144767=ORIENTED_EDGE ( 'NONE', *, *, #188599, .T. ) ;
#144806=CARTESIAN_POINT ( 'NONE',  ( 21.14999999999999858, 65.28660755661240955, -157.7731074845244450 ) ) ;
#144873=DIRECTION ( 'NONE',  ( 0.000000000000000000, 1.000000000000000000, 6.982962677686266711E-15 ) ) ;
#144892=ORIENTED_EDGE ( 'NONE', *, *, #112252, .F. ) ;
#144925=CYLINDRICAL_SURFACE ( 'NONE', #41001, 4.049999999999998046 ) ;
#144931=CARTESIAN_POINT ( 'NONE',  ( 23.15000000000000213, 87.65000000001245439, -181.7731074845242745 ) ) ;
#144967=FACE_OUTER_BOUND ( 'NONE', #135227, .T. ) ;
#145011=DIRECTION ( 'NONE',  ( 0.000000000000000000, -6.467318590049456648E-15, 1.000000000000000000 ) ) ;
#145013=CARTESIAN_POINT ( 'NONE',  ( 21.11345278033211414, 67.11787792664067354, -157.7770853137656104 ) ) ;
#145019=EDGE_CURVE ( 'NONE', #60353, #76100, #177472, .T. ) ;
#145027=CARTESIAN_POINT ( 'NONE',  ( -23.25000000000000000, 76.00000000001237765, -170.0231074845243597 ) ) ;
#145067=DIRECTION ( 'NONE',  ( 0.000000000000000000, -6.938893903907222067E-15, 1.000000000000000000 ) ) ;
#145086=ORIENTED_EDGE ( 'NONE', *, *, #251161, .T. ) ;
#145121=LINE ( 'NONE', #240394, #199239 ) ;
#145126=FACE_OUTER_BOUND ( 'NONE', #226503, .T. ) ;
#145174=VERTEX_POINT ( 'NONE', #28783 ) ;
#145183=AXIS2_PLACEMENT_3D ( 'NONE', #44012, #103959, #166558 ) ;
#145195=LINE ( 'NONE', #3107, #75028 ) ;
#145292=DIRECTION ( 'NONE',  ( 0.000000000000000000, -1.000000000000000000, 0.000000000000000000 ) ) ;
#145330=CARTESIAN_POINT ( 'NONE',  ( -22.50000000000000000, 76.00000000001237765, -170.0231074845243597 ) ) ;
#145350=DIRECTION ( 'NONE',  ( 0.000000000000000000, -0.9915357197604982575, 0.1298341882519033486 ) ) ;
#145353=VECTOR ( 'NONE', #79733, 1000.000000000000000 ) ;
#145373=DIRECTION ( 'NONE',  ( 0.000000000000000000, -6.530723674265620862E-15, 1.000000000000000000 ) ) ;
#145384=VERTEX_POINT ( 'NONE', #65940 ) ;
#145387=ORIENTED_EDGE ( 'NONE', *, *, #128845, .T. ) ;
#145392=LINE ( 'NONE', #85387, #7256 ) ;
#145419=CYLINDRICAL_SURFACE ( 'NONE', #24421, 0.09999999999999939493 ) ;
#145430=CARTESIAN_POINT ( 'NONE',  ( -20.99551997958407412, 64.25000000001219291, -143.3714483468355922 ) ) ;
#145433=CARTESIAN_POINT ( 'NONE',  ( 20.94999675878240808, 65.70692517833255408, -131.0644653378303985 ) ) ;
#145447=VERTEX_POINT ( 'NONE', #69809 ) ;
#145473=ORIENTED_EDGE ( 'NONE', *, *, #153415, .F. ) ;
#145504=DIRECTION ( 'NONE',  ( 0.000000000000000000, 0.000000000000000000, 1.000000000000000000 ) ) ;
#145540=DIRECTION ( 'NONE',  ( 0.000000000000000000, -0.4999999999999088507, 0.8660254037844913322 ) ) ;
#145559=ADVANCED_FACE ( 'NONE', ( #253545 ), #194891, .F. ) ;
#145610=CARTESIAN_POINT ( 'NONE',  ( -21.05000000000000071, 87.29603075034764004, -166.9752083248604038 ) ) ;
#145611=EDGE_CURVE ( 'NONE', #74964, #40351, #237010, .T. ) ;
#145612=CARTESIAN_POINT ( 'NONE',  ( -23.15000000000000213, 64.25000000001219291, -143.5379132551784096 ) ) ;
#145629=EDGE_CURVE ( 'NONE', #160806, #93811, #82837, .T. ) ;
#145667=CARTESIAN_POINT ( 'NONE',  ( -23.25000000000000000, 74.08971962618051066, -157.3917396293254285 ) ) ;
#145680=DIRECTION ( 'NONE',  ( -0.000000000000000000, 0.9908441862701591329, 0.1350103645451946055 ) ) ;
#145692=AXIS2_PLACEMENT_3D ( 'NONE', #169286, #131393, #27203 ) ;
#145703=CARTESIAN_POINT ( 'NONE',  ( 22.48660254037843842, 64.25000000001237765, -170.0731074845244279 ) ) ;
#145704=EDGE_CURVE ( 'NONE', #35313, #108264, #218262, .T. ) ;
#145753=ORIENTED_EDGE ( 'NONE', *, *, #93076, .T. ) ;
#145779=ORIENTED_EDGE ( 'NONE', *, *, #35491, .T. ) ;
#145781=ORIENTED_EDGE ( 'NONE', *, *, #116202, .F. ) ;
#145782=DIRECTION ( 'NONE',  ( 1.000000000000000000, -1.836970198721029934E-16, -1.282749433769087582E-30 ) ) ;
#145786=DIRECTION ( 'NONE',  ( 0.000000000000000000, 0.000000000000000000, 1.000000000000000000 ) ) ;
#145788=ORIENTED_EDGE ( 'NONE', *, *, #142487, .F. ) ;
#145802=EDGE_CURVE ( 'NONE', #87344, #235293, #207811, .T. ) ;
#145841=EDGE_LOOP ( 'NONE', ( #46076, #204494, #142895, #227552 ) ) ;
#145857=CARTESIAN_POINT ( 'NONE',  ( -21.10257677756356998, 69.60161825747967157, -170.0480582340924514 ) ) ;
#145858=CARTESIAN_POINT ( 'NONE',  ( 22.48508240969612615, 75.95372358549553837, -181.6731182160979188 ) ) ;
#145864=DIRECTION ( 'NONE',  ( 0.000000000000000000, 0.5000000000000128786, 0.8660254037844311581 ) ) ;
#145884=DIRECTION ( 'NONE',  ( 0.000000000000000000, 0.000000000000000000, 1.000000000000000000 ) ) ;
#145895=ORIENTED_EDGE ( 'NONE', *, *, #174213, .T. ) ;
#145897=CARTESIAN_POINT ( 'NONE',  ( -20.15000000000000568, 66.70857864377498458, -157.7731074845244166 ) ) ;
#145912=ADVANCED_FACE ( 'NONE', ( #166044 ), #49916, .F. ) ;
#145913=CARTESIAN_POINT ( 'NONE',  ( 23.25000000000000000, 87.75000000001216449, -139.6231074845242688 ) ) ;
#145918=VECTOR ( 'NONE', #136857, 1000.000000000000000 ) ;
#145919=VECTOR ( 'NONE', #147738, 1000.000000000000000 ) ;
#145950=DIRECTION ( 'NONE',  ( 0.000000000000000000, -6.938893903907222067E-15, 1.000000000000000000 ) ) ;
#145955=ORIENTED_EDGE ( 'NONE', *, *, #7854, .F. ) ;
#145956=EDGE_LOOP ( 'NONE', ( #108501, #19075, #96911, #69050 ) ) ;
#145965=AXIS2_PLACEMENT_3D ( 'NONE', #200658, #161546, #241084 ) ;
#145993=ORIENTED_EDGE ( 'NONE', *, *, #204991, .T. ) ;
#146017=CIRCLE ( 'NONE', #25417, 7.720710678118663850 ) ;
#146054=ORIENTED_EDGE ( 'NONE', *, *, #125324, .T. ) ;
#146058=DIRECTION ( 'NONE',  ( -0.000000000000000000, -0.8660254037844420383, 0.4999999999999943379 ) ) ;
#146075=EDGE_CURVE ( 'NONE', #588, #42521, #19806, .T. ) ;
#146095=CARTESIAN_POINT ( 'NONE',  ( 19.97071067811865674, 64.27928932189354327, -145.3731074845244109 ) ) ;
#146102=LINE ( 'NONE', #204781, #119053 ) ;
#146110=VECTOR ( 'NONE', #168484, 1000.000000000000000 ) ;
#146122=CARTESIAN_POINT ( 'NONE',  ( 21.05000000000000071, 67.07338541492521244, -161.5514244653012952 ) ) ;
#146138=CARTESIAN_POINT ( 'NONE',  ( 20.85000000000000142, 77.14957036958777792, -128.7071950000224092 ) ) ;
#146147=FACE_OUTER_BOUND ( 'NONE', #94086, .T. ) ;
#146162=ORIENTED_EDGE ( 'NONE', *, *, #118274, .T. ) ;
#146190=ORIENTED_EDGE ( 'NONE', *, *, #4350, .T. ) ;
#146196=CIRCLE ( 'NONE', #221205, 0.2000000000000057288 ) ;
#146269=EDGE_CURVE ( 'NONE', #128506, #178267, #62769, .T. ) ;
#146289=CARTESIAN_POINT ( 'NONE',  ( -21.05000000000000071, 69.74115727647316021, -170.0551211777118112 ) ) ;
#146355=AXIS2_PLACEMENT_3D ( 'NONE', #54490, #55741, #173215 ) ;
#146375=EDGE_CURVE ( 'NONE', #1901, #158699, #187312, .T. ) ;
#146385=CARTESIAN_POINT ( 'NONE',  ( 20.04142135623730070, 64.35000000001220144, -145.3731074845244109 ) ) ;
#146392=EDGE_CURVE ( 'NONE', #164553, #65207, #92585, .T. ) ;
#146394=ORIENTED_EDGE ( 'NONE', *, *, #218500, .F. ) ;
#146405=FACE_OUTER_BOUND ( 'NONE', #226720, .T. ) ;
#146410=CARTESIAN_POINT ( 'NONE',  ( 20.94999999999999929, 85.00000000001232081, -160.1291383618718385 ) ) ;
#146423=CIRCLE ( 'NONE', #75564, 11.70000000000001528 ) ;
#146450=DIRECTION ( 'NONE',  ( 0.000000000000000000, 0.4930308989874980785, 0.8700118002898462599 ) ) ;
#146481=EDGE_CURVE ( 'NONE', #86183, #588, #100275, .T. ) ;
#146523=ORIENTED_EDGE ( 'NONE', *, *, #21953, .T. ) ;
#146541=ORIENTED_EDGE ( 'NONE', *, *, #4283, .T. ) ;
#146559=AXIS2_PLACEMENT_3D ( 'NONE', #17578, #153293, #137520 ) ;
#146565=CYLINDRICAL_SURFACE ( 'NONE', #122542, 0.1000000000000070832 ) ;
#146578=AXIS2_PLACEMENT_3D ( 'NONE', #170814, #247724, #191643 ) ;
#146599=CYLINDRICAL_SURFACE ( 'NONE', #114146, 0.09999999999999939493 ) ;
#146627=ORIENTED_EDGE ( 'NONE', *, *, #225781, .T. ) ;
#146654=DIRECTION ( 'NONE',  ( 1.000000000000000000, 7.304098846218133681E-16, 5.100424963727255128E-30 ) ) ;
#146697=LINE ( 'NONE', #7198, #256661 ) ;
#146706=EDGE_LOOP ( 'NONE', ( #215713, #57194, #195684 ) ) ;
#146731=VERTEX_POINT ( 'NONE', #144548 ) ;
#146736=DIRECTION ( 'NONE',  ( 0.000000000000000000, 0.000000000000000000, -1.000000000000000000 ) ) ;
#146749=LINE ( 'NONE', #148074, #67057 ) ;
#146814=AXIS2_PLACEMENT_3D ( 'NONE', #201568, #205412, #159906 ) ;
#146815=DIRECTION ( 'NONE',  ( 1.875376730785737719E-16, 1.000000000000000000, 6.982962677686266711E-15 ) ) ;
#146820=ORIENTED_EDGE ( 'NONE', *, *, #26193, .T. ) ;
#146846=DIRECTION ( 'NONE',  ( -0.000000000000000000, -1.000000000000000000, -6.982962677686266711E-15 ) ) ;
#146869=DIRECTION ( 'NONE',  ( 0.000000000000000000, 0.000000000000000000, 1.000000000000000000 ) ) ;
#146889=AXIS2_PLACEMENT_3D ( 'NONE', #81275, #61744, #201242 ) ;
#146898=CARTESIAN_POINT ( 'NONE',  ( -23.25000000000000000, 73.40000000001228386, -156.7984855617622770 ) ) ;
#146904=CARTESIAN_POINT ( 'NONE',  ( 18.59999999999998721, 56.14960075277880946, -167.7428044267231257 ) ) ;
#146933=VERTEX_POINT ( 'NONE', #183237 ) ;
#146942=ORIENTED_EDGE ( 'NONE', *, *, #14946, .F. ) ;
#146953=DIRECTION ( 'NONE',  ( 0.000000000000000000, -6.652207440891584540E-15, 1.000000000000000000 ) ) ;
#146954=CYLINDRICAL_SURFACE ( 'NONE', #92998, 0.09999999999999939493 ) ;
#146998=ADVANCED_FACE ( 'NONE', ( #142792 ), #25454, .F. ) ;
#147034=EDGE_LOOP ( 'NONE', ( #112040, #63676, #32811, #141949 ) ) ;
#147041=VERTEX_POINT ( 'NONE', #89254 ) ;
#147101=ADVANCED_FACE ( 'NONE', ( #34467 ), #228793, .T. ) ;
#147110=FACE_OUTER_BOUND ( 'NONE', #45194, .T. ) ;
#147126=DIRECTION ( 'NONE',  ( 0.000000000000000000, 6.982962677686267499E-15, -1.000000000000000000 ) ) ;
#147137=CARTESIAN_POINT ( 'NONE',  ( 20.75572585718182239, 67.11768327161492209, -161.5258490858113873 ) ) ;
#147140=DIRECTION ( 'NONE',  ( 0.000000000000000000, 0.000000000000000000, 1.000000000000000000 ) ) ;
#147145=LINE ( 'NONE', #152318, #138234 ) ;
#147148=CARTESIAN_POINT ( 'NONE',  ( 22.43288208788031568, 75.99510014512706846, -181.6727593282434157 ) ) ;
#147161=TOROIDAL_SURFACE ( 'NONE', #251397, 0.2000000000000000111, 0.1000000000000000056 ) ;
#147184=AXIS2_PLACEMENT_3D ( 'NONE', #46274, #207957, #226172 ) ;
#147236=VECTOR ( 'NONE', #22495, 999.9999999999998863 ) ;
#147242=EDGE_CURVE ( 'NONE', #86886, #182252, #200318, .T. ) ;
#147245=CARTESIAN_POINT ( 'NONE',  ( 20.12500000000000000, 66.25000000001232081, -161.9113362024101548 ) ) ;
#147272=AXIS2_PLACEMENT_3D ( 'NONE', #210971, #152307, #70204 ) ;
#147313=CARTESIAN_POINT ( 'NONE',  ( -21.05000000000000071, 87.48912529308842068, -166.9231074845242802 ) ) ;
#147328=CARTESIAN_POINT ( 'NONE',  ( -21.07928932188134041, 76.00000000001237765, -170.0231074845243597 ) ) ;
#147335=CYLINDRICAL_SURFACE ( 'NONE', #257995, 0.09999999999999939493 ) ;
#147355=ORIENTED_EDGE ( 'NONE', *, *, #162199, .F. ) ;
#147370=DIRECTION ( 'NONE',  ( -0.000000000000000000, 6.982962677686266711E-15, -1.000000000000000000 ) ) ;
#147373=ORIENTED_EDGE ( 'NONE', *, *, #54045, .F. ) ;
#147377=VERTEX_POINT ( 'NONE', #43039 ) ;
#147389=ORIENTED_EDGE ( 'NONE', *, *, #19240, .F. ) ;
#147390=DIRECTION ( 'NONE',  ( 1.000000000000000000, 0.000000000000000000, 0.000000000000000000 ) ) ;
#147396=SPHERICAL_SURFACE ( 'NONE', #240547, 0.1000000000000000056 ) ;
#147413=EDGE_LOOP ( 'NONE', ( #245456, #114581, #129228, #243567, #224758, #58036, #186332, #34647, #105964, #64502, #193097, #126183, #225645, #52611 ) ) ;
#147430=FACE_OUTER_BOUND ( 'NONE', #210238, .T. ) ;
#147435=SPHERICAL_SURFACE ( 'NONE', #67317, 0.1000000000000000056 ) ;
#147448=AXIS2_PLACEMENT_3D ( 'NONE', #106991, #70489, #247799 ) ;
#147463=EDGE_LOOP ( 'NONE', ( #78063, #119939, #255956, #187575 ) ) ;
#147492=CARTESIAN_POINT ( 'NONE',  ( 20.94999999999999929, 71.00000000001223555, -148.9283735034374843 ) ) ;
#147506=CARTESIAN_POINT ( 'NONE',  ( -23.15000000000000213, 64.35000000001222986, -148.6731074845244507 ) ) ;
#147512=DIRECTION ( 'NONE',  ( 0.000000000000000000, -7.116814260417668513E-15, 1.000000000000000000 ) ) ;
#147535=DIRECTION ( 'NONE',  ( 0.000000000000000000, -6.982962677686266711E-15, 1.000000000000000000 ) ) ;
#147539=AXIS2_PLACEMENT_3D ( 'NONE', #214737, #174386, #235577 ) ;
#147542=CARTESIAN_POINT ( 'NONE',  ( -18.59999999999999787, 77.73625713160970463, -158.4544551555068495 ) ) ;
#147568=DIRECTION ( 'NONE',  ( -1.000000000000000000, -0.000000000000000000, 0.000000000000000000 ) ) ;
#147589=AXIS2_PLACEMENT_3D ( 'NONE', #115729, #94869, #93596 ) ;
#147602=CARTESIAN_POINT ( 'NONE',  ( 21.14999999999999503, 87.65000000001235492, -167.1231074845242688 ) ) ;
#147642=AXIS2_PLACEMENT_3D ( 'NONE', #59414, #99828, #41204 ) ;
#147648=DIRECTION ( 'NONE',  ( 3.616040088954490704E-32, 7.105427357601001859E-15, -1.000000000000000000 ) ) ;
#147669=ORIENTED_EDGE ( 'NONE', *, *, #119131, .F. ) ;
#147670=EDGE_LOOP ( 'NONE', ( #241003, #187654, #255924, #112287 ) ) ;
#147694=CARTESIAN_POINT ( 'NONE',  ( 20.94999999999999929, 64.35000000001218723, -143.3069731475025037 ) ) ;
#147700=LINE ( 'NONE', #228531, #12144 ) ;
#147738=DIRECTION ( 'NONE',  ( 1.000000000000000000, -0.000000000000000000, 0.000000000000000000 ) ) ;
#147748=DIRECTION ( 'NONE',  ( -1.000000000000000000, 0.000000000000000000, -0.000000000000000000 ) ) ;
#147775=DIRECTION ( 'NONE',  ( -1.000000000000000000, 0.000000000000000000, -0.000000000000000000 ) ) ;
#147792=ADVANCED_FACE ( 'NONE', ( #221328 ), #60879, .F. ) ;
#147797=CIRCLE ( 'NONE', #118765, 0.09999999999999971412 ) ;
#147823=DIRECTION ( 'NONE',  ( 0.000000000000000000, 0.000000000000000000, 1.000000000000000000 ) ) ;
#147824=( GEOMETRIC_REPRESENTATION_CONTEXT ( 3 ) GLOBAL_UNCERTAINTY_ASSIGNED_CONTEXT ( ( #6098 ) ) GLOBAL_UNIT_ASSIGNED_CONTEXT ( ( #35512, #193272, #13349 ) ) REPRESENTATION_CONTEXT ( 'NONE', 'WORKASPACE' ) );
#147842=CARTESIAN_POINT ( 'NONE',  ( -21.14999999999999858, 64.35000000001238618, -169.9231074845244507 ) ) ;
#147854=AXIS2_PLACEMENT_3D ( 'NONE', #207581, #9349, #188007 ) ;
#147874=CARTESIAN_POINT ( 'NONE',  ( 23.14999999999999503, 64.35000000001222986, -148.6731074845244507 ) ) ;
#147953=EDGE_CURVE ( 'NONE', #12740, #77748, #7428, .T. ) ;
#148025=ORIENTED_EDGE ( 'NONE', *, *, #46542, .T. ) ;
#148026=ORIENTED_EDGE ( 'NONE', *, *, #23842, .T. ) ;
#148036=DIRECTION ( 'NONE',  ( 0.000000000000000000, 6.982962677686266711E-15, -1.000000000000000000 ) ) ;
#148066=CARTESIAN_POINT ( 'NONE',  ( -23.25000000000000000, 77.25000000001209344, -128.7226267301092548 ) ) ;
#148074=CARTESIAN_POINT ( 'NONE',  ( 20.94999999999999929, 70.15000000001221281, -146.6556047088023149 ) ) ;
#148087=ORIENTED_EDGE ( 'NONE', *, *, #164449, .F. ) ;
#148104=DIRECTION ( 'NONE',  ( 1.000000000000000000, 0.000000000000000000, 0.000000000000000000 ) ) ;
#148111=EDGE_CURVE ( 'NONE', #145447, #216520, #190073, .T. ) ;
#148125=CARTESIAN_POINT ( 'NONE',  ( -21.05000000000000071, 77.16270174995034381, -162.1231074845243540 ) ) ;
#148144=AXIS2_PLACEMENT_3D ( 'NONE', #169981, #31744, #248191 ) ;
#148147=ORIENTED_EDGE ( 'NONE', *, *, #236614, .F. ) ;
#148164=ORIENTED_EDGE ( 'NONE', *, *, #57942, .T. ) ;
#148183=EDGE_CURVE ( 'NONE', #90961, #22950, #31878, .T. ) ;
#148197=DIRECTION ( 'NONE',  ( 0.000000000000000000, -1.000000000000000000, -6.982962677686265922E-15 ) ) ;
#148244=FACE_OUTER_BOUND ( 'NONE', #209030, .T. ) ;
#148248=ORIENTED_EDGE ( 'NONE', *, *, #36860, .F. ) ;
#148280=EDGE_LOOP ( 'NONE', ( #20032, #123691, #138310, #188227 ) ) ;
#148290=LINE ( 'NONE', #129987, #69889 ) ;
#148295=AXIS2_PLACEMENT_3D ( 'NONE', #110836, #151269, #52132 ) ;
#148301=EDGE_CURVE ( 'NONE', #94706, #3474, #15303, .T. ) ;
#148315=ORIENTED_EDGE ( 'NONE', *, *, #247298, .T. ) ;
#148332=ORIENTED_EDGE ( 'NONE', *, *, #197164, .T. ) ;
#148345=DIRECTION ( 'NONE',  ( -1.000000000000000000, -0.000000000000000000, -0.000000000000000000 ) ) ;
#148346=VERTEX_POINT ( 'NONE', #111369 ) ;
#148347=CARTESIAN_POINT ( 'NONE',  ( 22.37643362114956247, 68.37421000605401389, -170.1221888582057886 ) ) ;
#148367=PLANE ( 'NONE',  #26935 ) ;
#148455=ORIENTED_EDGE ( 'NONE', *, *, #93623, .F. ) ;
#148466=EDGE_LOOP ( 'NONE', ( #149853, #146541, #92181, #243869 ) ) ;
#148471=ORIENTED_EDGE ( 'NONE', *, *, #96738, .F. ) ;
#148525=DIRECTION ( 'NONE',  ( -0.000000000000000000, 1.000000000000000000, 6.982962677686266711E-15 ) ) ;
#148553=DIRECTION ( 'NONE',  ( 1.000000000000000000, -0.000000000000000000, 0.000000000000000000 ) ) ;
#148588=FACE_OUTER_BOUND ( 'NONE', #83388, .T. ) ;
#148599=AXIS2_PLACEMENT_3D ( 'NONE', #189457, #10816, #193309 ) ;
#148621=ORIENTED_EDGE ( 'NONE', *, *, #211949, .F. ) ;
#148638=ORIENTED_EDGE ( 'NONE', *, *, #95341, .F. ) ;
#148655=ORIENTED_EDGE ( 'NONE', *, *, #191678, .T. ) ;
#148666=CARTESIAN_POINT ( 'NONE',  ( -23.15000000000000213, 85.00000000001222134, -146.4170766071767389 ) ) ;
#148676=VECTOR ( 'NONE', #55044, 1000.000000000000000 ) ;
#148698=DIRECTION ( 'NONE',  ( -1.000000000000000000, -0.000000000000000000, -0.000000000000000000 ) ) ;
#148736=DIRECTION ( 'NONE',  ( -1.000000000000000000, 7.304098846218134667E-16, 5.100424963727256530E-30 ) ) ;
#148739=AXIS2_PLACEMENT_3D ( 'NONE', #116434, #190859, #154317 ) ;
#148753=DIRECTION ( 'NONE',  ( 0.000000000000000000, 0.000000000000000000, 1.000000000000000000 ) ) ;
#148758=AXIS2_PLACEMENT_3D ( 'NONE', #114281, #154723, #54296 ) ;
#148761=VECTOR ( 'NONE', #243959, 1000.000000000000114 ) ;
#148775=CARTESIAN_POINT ( 'NONE',  ( -18.59999999999999787, 77.83585931145570669, -125.0186683157258329 ) ) ;
#148804=ORIENTED_EDGE ( 'NONE', *, *, #165081, .T. ) ;
#148832=AXIS2_PLACEMENT_3D ( 'NONE', #169358, #228006, #12832 ) ;
#148846=FACE_OUTER_BOUND ( 'NONE', #6724, .T. ) ;
#148854=CARTESIAN_POINT ( 'NONE',  ( 21.05000000000000071, 76.10000000001238618, -170.0231074845243313 ) ) ;
#148858=EDGE_CURVE ( 'NONE', #134685, #167063, #194565, .T. ) ;
#148904=EDGE_CURVE ( 'NONE', #164268, #113546, #197660, .T. ) ;
#148915=CIRCLE ( 'NONE', #103090, 0.2000000000000057288 ) ;
#148925=DIRECTION ( 'NONE',  ( 0.000000000000000000, -0.8660254037844377084, -0.5000000000000016653 ) ) ;
#148943=AXIS2_PLACEMENT_3D ( 'NONE', #90554, #190981, #48865 ) ;
#148945=CIRCLE ( 'NONE', #36539, 0.1000000000000028783 ) ;
#148948=DIRECTION ( 'NONE',  ( 0.000000000000000000, -0.4930308989874980785, -0.8700118002898462599 ) ) ;
#148954=ADVANCED_FACE ( 'NONE', ( #193830 ), #73907, .F. ) ;
#148969=EDGE_LOOP ( 'NONE', ( #117213, #13595, #52067, #113788 ) ) ;
#148975=CARTESIAN_POINT ( 'NONE',  ( -21.05000000000000071, 87.65000000001215597, -139.6231074845242688 ) ) ;
#148976=VERTEX_POINT ( 'NONE', #123275 ) ;
#148996=VECTOR ( 'NONE', #210830, 1000.000000000000000 ) ;
#149004=CARTESIAN_POINT ( 'NONE',  ( 22.49999999999999645, 75.90000000001245439, -181.6726782920691505 ) ) ;
#149044=DIRECTION ( 'NONE',  ( 0.7071067811865474617, -0.7071067811865474617, -4.937700262164531476E-15 ) ) ;
#149058=FACE_OUTER_BOUND ( 'NONE', #232427, .T. ) ;
#149068=VECTOR ( 'NONE', #147370, 1000.000000000000000 ) ;
#149070=CARTESIAN_POINT ( 'NONE',  ( -18.59999999999999787, 76.00000000001213607, -136.5231074845243313 ) ) ;
#149082=FACE_OUTER_BOUND ( 'NONE', #178521, .T. ) ;
#149099=CYLINDRICAL_SURFACE ( 'NONE', #186822, 0.09999999999998898659 ) ;
#149101=CARTESIAN_POINT ( 'NONE',  ( 23.24999999999999645, 76.00000000001237765, -170.0231074845243597 ) ) ;
#149103=AXIS2_PLACEMENT_3D ( 'NONE', #165914, #5503, #28991 ) ;
#149128=EDGE_CURVE ( 'NONE', #236311, #173065, #145392, .T. ) ;
#149152=ORIENTED_EDGE ( 'NONE', *, *, #8659, .F. ) ;
#149159=DIRECTION ( 'NONE',  ( 1.000000000000000000, -7.304098846218134667E-16, -5.100424963727256530E-30 ) ) ;
#149186=FACE_OUTER_BOUND ( 'NONE', #18249, .T. ) ;
#149231=EDGE_CURVE ( 'NONE', #204085, #65207, #107224, .T. ) ;
#149245=CIRCLE ( 'NONE', #224229, 0.2000000000000057288 ) ;
#149275=VECTOR ( 'NONE', #228004, 1000.000000000000000 ) ;
#149292=AXIS2_PLACEMENT_3D ( 'NONE', #82163, #99165, #178771 ) ;
#149296=CARTESIAN_POINT ( 'NONE',  ( 18.59999999999999787, 85.40000000001208491, -129.6410656363516125 ) ) ;
#149311=EDGE_CURVE ( 'NONE', #75851, #61384, #24048, .T. ) ;
#149341=DIRECTION ( 'NONE',  ( 0.000000000000000000, -1.000000000000000000, -6.982962677686266711E-15 ) ) ;
#149351=DIRECTION ( 'NONE',  ( 0.000000000000000000, 0.8660254037844419273, -0.4999999999999942824 ) ) ;
#149374=ORIENTED_EDGE ( 'NONE', *, *, #127393, .T. ) ;
#149377=ADVANCED_FACE ( 'NONE', ( #94409 ), #33207, .F. ) ;
#149398=VERTEX_POINT ( 'NONE', #233929 ) ;
#149462=LINE ( 'NONE', #210693, #166027 ) ;
#149492=VECTOR ( 'NONE', #66405, 1000.000000000000000 ) ;
#149537=CARTESIAN_POINT ( 'NONE',  ( 20.12500000000000355, 65.75804927292965374, -162.1629037574383290 ) ) ;
#149556=VERTEX_POINT ( 'NONE', #162116 ) ;
#149562=AXIS2_PLACEMENT_3D ( 'NONE', #202429, #66776, #69354 ) ;
#149563=ADVANCED_FACE ( 'NONE', ( #47258 ), #36712, .T. ) ;
#149591=ORIENTED_EDGE ( 'NONE', *, *, #183081, .T. ) ;
#149596=ORIENTED_EDGE ( 'NONE', *, *, #102553, .T. ) ;
#149597=CIRCLE ( 'NONE', #249552, 0.09999999999998898659 ) ;
#149668=DIRECTION ( 'NONE',  ( -1.000000000000000000, 0.000000000000000000, -0.000000000000000000 ) ) ;
#149715=CARTESIAN_POINT ( 'NONE',  ( -21.05000000000000071, 87.39257802171783851, -139.5970570643562212 ) ) ;
#149742=CARTESIAN_POINT ( 'NONE',  ( 20.59588692710267921, 65.63127657884321309, -162.3840263900140144 ) ) ;
#149746=DIRECTION ( 'NONE',  ( 0.000000000000000000, 1.000000000000000000, 0.000000000000000000 ) ) ;
#149801=ORIENTED_EDGE ( 'NONE', *, *, #243078, .F. ) ;
#149817=CARTESIAN_POINT ( 'NONE',  ( 23.14999999999999858, 70.40000000001222702, -148.9283735034374843 ) ) ;
#149853=ORIENTED_EDGE ( 'NONE', *, *, #89774, .F. ) ;
#149869=DIRECTION ( 'NONE',  ( 2.952720810173289112E-16, 1.000000000000000000, 6.530723674265620862E-15 ) ) ;
#149879=AXIS2_PLACEMENT_3D ( 'NONE', #109211, #73986, #251287 ) ;
#149912=ORIENTED_EDGE ( 'NONE', *, *, #119032, .F. ) ;
#149918=CIRCLE ( 'NONE', #178988, 12.77499999999999503 ) ;
#149937=EDGE_LOOP ( 'NONE', ( #126545, #41511, #84039, #21621 ) ) ;
#149974=CIRCLE ( 'NONE', #66754, 0.09999999999999939493 ) ;
#150007=ORIENTED_EDGE ( 'NONE', *, *, #195527, .F. ) ;
#150152=DIRECTION ( 'NONE',  ( 1.000000000000000000, 0.000000000000000000, 0.000000000000000000 ) ) ;
#150157=CARTESIAN_POINT ( 'NONE',  ( 21.05000000000000071, 76.10000000001241460, -176.5637644362255969 ) ) ;
#150177=ORIENTED_EDGE ( 'NONE', *, *, #227532, .T. ) ;
#150188=LINE ( 'NONE', #28987, #255940 ) ;
#150249=LINE ( 'NONE', #189366, #36022 ) ;
#150260=AXIS2_PLACEMENT_3D ( 'NONE', #122636, #104306, #5200 ) ;
#150275=DIRECTION ( 'NONE',  ( 0.000000000000000000, 0.000000000000000000, 1.000000000000000000 ) ) ;
#150292=ORIENTED_EDGE ( 'NONE', *, *, #97469, .F. ) ;
#150317=CARTESIAN_POINT ( 'NONE',  ( 22.39999999999999503, 76.00000000001246292, -181.6726782920691505 ) ) ;
#150336=EDGE_LOOP ( 'NONE', ( #239948, #67440, #93028, #37397 ) ) ;
#150347=EDGE_CURVE ( 'NONE', #2383, #222373, #219626, .T. ) ;
#150373=CARTESIAN_POINT ( 'NONE',  ( -21.00857864376268935, 64.40000000001234071, -163.0949042542488883 ) ) ;
#150382=LINE ( 'NONE', #112536, #209173 ) ;
#150398=CONICAL_SURFACE ( 'NONE', #133619, 6.250000000000005329, 0.7853981633974431720 ) ;
#150433=DIRECTION ( 'NONE',  ( 0.000000000000000000, 0.000000000000000000, -1.000000000000000000 ) ) ;
#150441=DIRECTION ( 'NONE',  ( 0.000000000000000000, 6.982962677686266711E-15, -1.000000000000000000 ) ) ;
#150452=CARTESIAN_POINT ( 'NONE',  ( 18.52928932188133970, 65.72071067813085676, -145.3731074845244109 ) ) ;
#150462=DIRECTION ( 'NONE',  ( -0.000000000000000000, -1.000000000000000000, -6.982962677686266711E-15 ) ) ;
#150470=AXIS2_PLACEMENT_3D ( 'NONE', #254457, #36766, #255728 ) ;
#150497=DIRECTION ( 'NONE',  ( 0.000000000000000000, 1.000000000000000000, 6.982962677686266711E-15 ) ) ;
#150521=LINE ( 'NONE', #34450, #173047 ) ;
#150527=CARTESIAN_POINT ( 'NONE',  ( -20.85000000000000142, 77.14957036958777792, -128.7071950000224092 ) ) ;
#150533=AXIS2_PLACEMENT_3D ( 'NONE', #22373, #40675, #139710 ) ;
#150538=DIRECTION ( 'NONE',  ( 0.000000000000000000, 0.4930308989874980785, 0.8700118002898462599 ) ) ;
#150548=AXIS2_PLACEMENT_3D ( 'NONE', #129185, #172209, #167052 ) ;
#150559=ORIENTED_EDGE ( 'NONE', *, *, #246110, .T. ) ;
#150568=ORIENTED_EDGE ( 'NONE', *, *, #145629, .T. ) ;
#150569=DIRECTION ( 'NONE',  ( 0.000000000000000000, 0.000000000000000000, 1.000000000000000000 ) ) ;
#150581=AXIS2_PLACEMENT_3D ( 'NONE', #65062, #140749, #121230 ) ;
#150596=ORIENTED_EDGE ( 'NONE', *, *, #97412, .F. ) ;
#150605=EDGE_LOOP ( 'NONE', ( #120810, #79452, #137967, #57576 ) ) ;
#150624=CARTESIAN_POINT ( 'NONE',  ( -23.15000000000000213, 76.00000000001237765, -170.0231074845243597 ) ) ;
#150646=DIRECTION ( 'NONE',  ( 0.000000000000000000, -0.5000000000000016653, 0.8660254037844377084 ) ) ;
#150662=CARTESIAN_POINT ( 'NONE',  ( -23.15000000000000213, 87.75000000001237765, -170.0231074845242745 ) ) ;
#150722=LINE ( 'NONE', #230247, #27643 ) ;
#150726=CARTESIAN_POINT ( 'NONE',  ( 21.14999999999999858, 87.75000000001229239, -157.7731074845242745 ) ) ;
#150728=( NAMED_UNIT ( * ) PLANE_ANGLE_UNIT ( ) SI_UNIT ( $, .RADIAN. ) );
#150803=EDGE_LOOP ( 'NONE', ( #185473, #106300, #12685, #87627 ) ) ;
#150818=DIRECTION ( 'NONE',  ( -1.000000000000000000, -0.000000000000000000, -0.000000000000000000 ) ) ;
#150824=DIRECTION ( 'NONE',  ( -6.938893903907222856E-15, -1.000000000000000000, -6.982962677686266711E-15 ) ) ;
#150853=EDGE_LOOP ( 'NONE', ( #160607, #193283, #182548, #186014, #224152 ) ) ;
#150898=ORIENTED_EDGE ( 'NONE', *, *, #242989, .F. ) ;
#150904=VERTEX_POINT ( 'NONE', #19859 ) ;
#150932=DIRECTION ( 'NONE',  ( -2.561896900575096011E-15, 0.5907332058517336115, -0.8068669527896984439 ) ) ;
#150933=EDGE_LOOP ( 'NONE', ( #36336, #216787, #230442, #236926 ) ) ;
#150961=ORIENTED_EDGE ( 'NONE', *, *, #10558, .T. ) ;
#150966=CARTESIAN_POINT ( 'NONE',  ( -20.54999999999999716, 76.00000000001215028, -138.5231074845243313 ) ) ;
#150967=DIRECTION ( 'NONE',  ( 0.000000000000000000, -7.056502275159890043E-15, 1.000000000000000000 ) ) ;
#150975=AXIS2_PLACEMENT_3D ( 'NONE', #88789, #172253, #91392 ) ;
#150978=ORIENTED_EDGE ( 'NONE', *, *, #105516, .F. ) ;
#150985=CARTESIAN_POINT ( 'NONE',  ( 21.13461538461538325, 65.38541703798675542, -157.7731074845244166 ) ) ;
#150994=CARTESIAN_POINT ( 'NONE',  ( -18.59999999999999787, 76.00000000001213607, -136.5231074845243313 ) ) ;
#151043=CARTESIAN_POINT ( 'NONE',  ( -20.85000000000000142, 77.85161776048096272, -124.9199177649206689 ) ) ;
#151053=CARTESIAN_POINT ( 'NONE',  ( -18.59999999999999787, 66.75000000001223555, -148.8731074845244393 ) ) ;
#151086=DIRECTION ( 'NONE',  ( 2.952720810173289112E-16, 1.000000000000000000, -6.088138035986627436E-46 ) ) ;
#151099=CIRCLE ( 'NONE', #225880, 0.09999999999998898659 ) ;
#151115=DIRECTION ( 'NONE',  ( 0.000000000000000000, 0.000000000000000000, 1.000000000000000000 ) ) ;
#151131=EDGE_CURVE ( 'NONE', #164268, #174107, #169989, .T. ) ;
#151167=CARTESIAN_POINT ( 'NONE',  ( 18.60000000000000142, 85.32100840337361092, -162.7871692354463846 ) ) ;
#151181=LINE ( 'NONE', #155055, #220792 ) ;
#151265=CARTESIAN_POINT ( 'NONE',  ( 20.04142135623730070, 64.25000000001246292, -181.7731074845244450 ) ) ;
#151269=DIRECTION ( 'NONE',  ( 0.000000000000000000, 1.000000000000000000, 7.272083257015735086E-15 ) ) ;
#151292=DIRECTION ( 'NONE',  ( 0.000000000000000000, 6.938893903907222067E-15, -1.000000000000000000 ) ) ;
#151303=DIRECTION ( 'NONE',  ( -1.040834085586090694E-13, 0.1568667991644355497, 0.9876197685951332295 ) ) ;
#151311=CARTESIAN_POINT ( 'NONE',  ( -18.43707690579159930, 85.68240343348850274, -129.8662641071114763 ) ) ;
#151316=EDGE_CURVE ( 'NONE', #122358, #238290, #74491, .T. ) ;
#151318=CARTESIAN_POINT ( 'NONE',  ( -20.94999999999999929, 87.65000000001214175, -136.5231074845242745 ) ) ;
#151324=AXIS2_PLACEMENT_3D ( 'NONE', #256459, #157469, #97420 ) ;
#151360=ORIENTED_EDGE ( 'NONE', *, *, #206039, .T. ) ;
#151369=CARTESIAN_POINT ( 'NONE',  ( -21.09813707148783735, 75.96864850048297058, -176.4081695902610250 ) ) ;
#151389=VERTEX_POINT ( 'NONE', #61230 ) ;
#151432=EDGE_CURVE ( 'NONE', #150904, #94999, #236736, .T. ) ;
#151457=VERTEX_POINT ( 'NONE', #82039 ) ;
#151495=B_SPLINE_CURVE_WITH_KNOTS ( 'NONE', 3,
 ( #20820, #173512, #252980, #118636, #99019, #16964, #153941, #174787, #139439, #237286 ),
 .UNSPECIFIED., .F., .F.,
 ( 4, 3, 3, 4 ),
 ( 0.000000000000000000, 0.0002000000000008537104, 0.001000000000082977483, 0.001967863649483329782 ),
 .UNSPECIFIED. ) ;
#151541=ORIENTED_EDGE ( 'NONE', *, *, #183739, .F. ) ;
#151555=CARTESIAN_POINT ( 'NONE',  ( -20.85000000000000142, 76.00000000001213607, -136.5231074845243313 ) ) ;
#151571=CARTESIAN_POINT ( 'NONE',  ( 18.51565452909435905, 85.35285933884642873, -162.8281981632931377 ) ) ;
#151573=CARTESIAN_POINT ( 'NONE',  ( -20.94999999999999929, 76.00000000001213607, -136.5231074845243313 ) ) ;
#151577=DIRECTION ( 'NONE',  ( 1.000000000000000000, 0.000000000000000000, -0.000000000000000000 ) ) ;
#151583=AXIS2_PLACEMENT_3D ( 'NONE', #83995, #123183, #145292 ) ;
#151598=CIRCLE ( 'NONE', #30788, 0.1000000000000072220 ) ;
#151600=DIRECTION ( 'NONE',  ( 1.000000000000000000, -7.304098846218135653E-16, -5.100424963727256530E-30 ) ) ;
#151644=FACE_OUTER_BOUND ( 'NONE', #222893, .T. ) ;
#151652=AXIS2_PLACEMENT_3D ( 'NONE', #181091, #175965, #36458 ) ;
#151662=DIRECTION ( 'NONE',  ( -0.000000000000000000, 6.982962677686266711E-15, -1.000000000000000000 ) ) ;
#151664=AXIS2_PLACEMENT_3D ( 'NONE', #152223, #230446, #195197 ) ;
#151670=CARTESIAN_POINT ( 'NONE',  ( 23.24999999999999289, 71.85000000001237197, -170.0231074845243882 ) ) ;
#151677=ORIENTED_EDGE ( 'NONE', *, *, #25541, .F. ) ;
#151689=CARTESIAN_POINT ( 'NONE',  ( 20.94999999999999929, 76.00000000001237765, -170.0231074845243597 ) ) ;
#151698=CARTESIAN_POINT ( 'NONE',  ( 21.07094088545303734, 69.67983277809588571, -170.1220011870766200 ) ) ;
#151699=CARTESIAN_POINT ( 'NONE',  ( 18.50000000000000000, 85.50000000001209344, -129.9229180933022576 ) ) ;
#151705=DIRECTION ( 'NONE',  ( 1.000000000000000000, -3.265361837132813093E-16, -2.280189983783949500E-30 ) ) ;
#151710=ORIENTED_EDGE ( 'NONE', *, *, #159900, .T. ) ;
#151723=DIRECTION ( 'NONE',  ( 0.000000000000000000, -1.000000000000000000, -6.982962677686265922E-15 ) ) ;
#151752=CIRCLE ( 'NONE', #93437, 0.09999999999999939493 ) ;
#151753=CIRCLE ( 'NONE', #1845, 0.09999999999998898659 ) ;
#151755=DIRECTION ( 'NONE',  ( 0.000000000000000000, 0.000000000000000000, 1.000000000000000000 ) ) ;
#151774=CYLINDRICAL_SURFACE ( 'NONE', #140905, 0.09999999999998898659 ) ;
#151778=DIRECTION ( 'NONE',  ( 1.000000000000000000, -3.265361837132813093E-16, -2.280189983783949500E-30 ) ) ;
#151780=FACE_OUTER_BOUND ( 'NONE', #85792, .T. ) ;
#151786=CARTESIAN_POINT ( 'NONE',  ( -20.94999999999999929, 87.65000000001235492, -166.9231074845242802 ) ) ;
#151806=DIRECTION ( 'NONE',  ( 0.000000000000000000, -0.8660254037844420383, 0.4999999999999943379 ) ) ;
#151834=EDGE_CURVE ( 'NONE', #47890, #187756, #232864, .T. ) ;
#151844=ORIENTED_EDGE ( 'NONE', *, *, #224122, .F. ) ;
#151852=ORIENTED_EDGE ( 'NONE', *, *, #182096, .T. ) ;
#151862=CIRCLE ( 'NONE', #130986, 0.09999999999999939493 ) ;
#151867=VERTEX_POINT ( 'NONE', #154315 ) ;
#151873=CARTESIAN_POINT ( 'NONE',  ( 18.39999999999999858, 85.68240343348850274, -129.8662641071115047 ) ) ;
#151887=CARTESIAN_POINT ( 'NONE',  ( -20.64999999999999858, 68.85000000001228670, -157.6731074845243938 ) ) ;
#151889=AXIS2_PLACEMENT_3D ( 'NONE', #219321, #223169, #1552 ) ;
#151902=CARTESIAN_POINT ( 'NONE',  ( -18.59999999999999787, 76.00000000001213607, -136.5231074845243313 ) ) ;
#151913=CARTESIAN_POINT ( 'NONE',  ( 21.05315837477641949, 64.25000000001217870, -143.3647514783578742 ) ) ;
#151952=CARTESIAN_POINT ( 'NONE',  ( 18.49999999999999289, 64.35000000001245724, -181.7731074845244450 ) ) ;
#151953=LINE ( 'NONE', #72410, #174394 ) ;
#151989=EDGE_LOOP ( 'NONE', ( #207113, #124833, #192326, #42496 ) ) ;
#152039=DIRECTION ( 'NONE',  ( 0.000000000000000000, 6.982962677686266711E-15, -1.000000000000000000 ) ) ;
#152074=DIRECTION ( 'NONE',  ( 1.000000000000000000, 0.000000000000000000, 0.000000000000000000 ) ) ;
#152111=COLOUR_RGB ( '', 0.08235294, 0.09019608, 0.10196078) ;
#152146=ORIENTED_EDGE ( 'NONE', *, *, #128945, .T. ) ;
#152183=AXIS2_PLACEMENT_3D ( 'NONE', #61993, #137646, #36020 ) ;
#152223=CARTESIAN_POINT ( 'NONE',  ( 20.94999999999999574, 77.36087058720436005, -161.9501095574333931 ) ) ;
#152253=ADVANCED_FACE ( 'NONE', ( #232231 ), #49857, .T. ) ;
#152266=EDGE_LOOP ( 'NONE', ( #217455, #36459, #35470, #163928 ) ) ;
#152281=ORIENTED_EDGE ( 'NONE', *, *, #215831, .F. ) ;
#152285=CARTESIAN_POINT ( 'NONE',  ( 20.94999999999999929, 76.00000000001213607, -136.5231074845243313 ) ) ;
#152307=DIRECTION ( 'NONE',  ( 0.000000000000000000, -0.4999999999999943379, -0.8660254037844420383 ) ) ;
#152318=CARTESIAN_POINT ( 'NONE',  ( -23.25000000000000000, 77.85161776048096272, -124.9199177649206689 ) ) ;
#152321=CARTESIAN_POINT ( 'NONE',  ( -18.50000000000000000, 77.13501884592227498, -128.8061306010920362 ) ) ;
#152337=CARTESIAN_POINT ( 'NONE',  ( 21.05000000000000071, 76.00000000001237765, -170.0231074845243597 ) ) ;
#152339=DIRECTION ( 'NONE',  ( 1.000000000000000000, 0.000000000000000000, 0.000000000000000000 ) ) ;
#152389=ADVANCED_FACE ( 'NONE', ( #193093 ), #53951, .T. ) ;
#152417=DIRECTION ( 'NONE',  ( -1.000000000000000000, 0.000000000000000000, -0.000000000000000000 ) ) ;
#152420=VERTEX_POINT ( 'NONE', #219046 ) ;
#152431=CARTESIAN_POINT ( 'NONE',  ( -20.94999999999999929, 76.00000000001213607, -136.5231074845243313 ) ) ;
#152478=AXIS2_PLACEMENT_3D ( 'NONE', #66205, #244825, #221396 ) ;
#152485=ORIENTED_EDGE ( 'NONE', *, *, #117136, .F. ) ;
#152489=ORIENTED_EDGE ( 'NONE', *, *, #35201, .T. ) ;
#152500=CARTESIAN_POINT ( 'NONE',  ( -18.50000000000000000, 76.00000000001213607, -136.5231074845243313 ) ) ;
#152585=DIRECTION ( 'NONE',  ( 0.000000000000000000, -1.000000000000000000, -6.860497997771531562E-15 ) ) ;
#152621=FACE_OUTER_BOUND ( 'NONE', #173388, .T. ) ;
#152640=ADVANCED_FACE ( 'NONE', ( #12878 ), #228053, .T. ) ;
#152664=CARTESIAN_POINT ( 'NONE',  ( -21.08134388332232589, 75.92418108250545572, -176.3577880650423140 ) ) ;
#152672=ORIENTED_EDGE ( 'NONE', *, *, #34128, .T. ) ;
#152696=ORIENTED_EDGE ( 'NONE', *, *, #236392, .F. ) ;
#152710=EDGE_LOOP ( 'NONE', ( #22312, #10367, #12627, #80628 ) ) ;
#152737=EDGE_CURVE ( 'NONE', #26629, #18391, #248907, .T. ) ;
#152750=ORIENTED_EDGE ( 'NONE', *, *, #108172, .T. ) ;
#152784=FACE_OUTER_BOUND ( 'NONE', #79379, .T. ) ;
#152835=EDGE_LOOP ( 'NONE', ( #35444, #60191, #7193, #229054 ) ) ;
#152884=LINE ( 'NONE', #211543, #169468 ) ;
#152890=( LENGTH_UNIT ( ) NAMED_UNIT ( * ) SI_UNIT ( .MILLI., .METRE. ) );
#152924=DIRECTION ( 'NONE',  ( 0.000000000000000000, 0.000000000000000000, 1.000000000000000000 ) ) ;
#152928=CIRCLE ( 'NONE', #240379, 0.09999999999998898659 ) ;
#152968=VERTEX_POINT ( 'NONE', #182201 ) ;
#152978=AXIS2_PLACEMENT_3D ( 'NONE', #68058, #128043, #48491 ) ;
#152985=CARTESIAN_POINT ( 'NONE',  ( 22.00411653962159164, 68.74655713164219151, -170.1221455902930302 ) ) ;
#152996=CARTESIAN_POINT ( 'NONE',  ( 21.04999999999999716, 65.31569084252720359, -162.4964106941976070 ) ) ;
#153005=ORIENTED_EDGE ( 'NONE', *, *, #206007, .T. ) ;
#153041=EDGE_CURVE ( 'NONE', #206239, #86183, #204150, .T. ) ;
#153061=AXIS2_PLACEMENT_3D ( 'NONE', #206774, #188485, #145504 ) ;
#153108=CARTESIAN_POINT ( 'NONE',  ( 18.59999999999999076, 65.79142135624952914, -148.6731074845244223 ) ) ;
#153110=ORIENTED_EDGE ( 'NONE', *, *, #208866, .T. ) ;
#153120=ORIENTED_EDGE ( 'NONE', *, *, #113904, .T. ) ;
#153135=CARTESIAN_POINT ( 'NONE',  ( 20.95512820512820440, 67.12384868372417657, -157.8731074845244109 ) ) ;
#153147=AXIS2_PLACEMENT_3D ( 'NONE', #225776, #86262, #64165 ) ;
#153160=ORIENTED_EDGE ( 'NONE', *, *, #39474, .T. ) ;
#153165=AXIS2_PLACEMENT_3D ( 'NONE', #110571, #130130, #195273 ) ;
#153171=CARTESIAN_POINT ( 'NONE',  ( 21.00000000000000000, 66.25000000001229239, -157.6731074845244223 ) ) ;
#153181=DIRECTION ( 'NONE',  ( -0.000000000000000000, 6.982962677686266711E-15, -1.000000000000000000 ) ) ;
#153190=ORIENTED_EDGE ( 'NONE', *, *, #157964, .F. ) ;
#153208=CIRCLE ( 'NONE', #111481, 0.1000000000000028644 ) ;
#153216=AXIS2_PLACEMENT_3D ( 'NONE', #90615, #167627, #250973 ) ;
#153234=ORIENTED_EDGE ( 'NONE', *, *, #199001, .T. ) ;
#153263=VECTOR ( 'NONE', #90919, 1000.000000000000227 ) ;
#153293=DIRECTION ( 'NONE',  ( -1.000000000000000000, 0.000000000000000000, -0.000000000000000000 ) ) ;
#153312=EDGE_CURVE ( 'NONE', #133183, #145174, #220996, .T. ) ;
#153318=AXIS2_PLACEMENT_3D ( 'NONE', #118696, #79524, #198206 ) ;
#153344=CARTESIAN_POINT ( 'NONE',  ( 18.52928932304156717, 65.72071067697063995, -145.3468540517212944 ) ) ;
#153346=CARTESIAN_POINT ( 'NONE',  ( -18.49346865148307018, 85.44307379853742646, -162.8379112292089985 ) ) ;
#153378=CARTESIAN_POINT ( 'NONE',  ( -20.89878130938411616, 65.67252876774553272, -130.9457041994994881 ) ) ;
#153415=EDGE_CURVE ( 'NONE', #50939, #209214, #226119, .T. ) ;
#153438=AXIS2_PLACEMENT_3D ( 'NONE', #130386, #190393, #249081 ) ;
#153488=AXIS2_PLACEMENT_3D ( 'NONE', #141363, #22731, #102202 ) ;
#153513=CARTESIAN_POINT ( 'NONE',  ( 0.000000000000000000, 0.000000000000000000, 0.000000000000000000 ) ) ;
#153521=CARTESIAN_POINT ( 'NONE',  ( -18.50000000000000000, 102.4393534156131977, -151.8815988770167280 ) ) ;
#153522=DIRECTION ( 'NONE',  ( -4.408576920032448588E-17, -0.1350103645451807555, -0.9908441862701609093 ) ) ;
#153536=CIRCLE ( 'NONE', #128544, 0.1000000000000028644 ) ;
#153556=CIRCLE ( 'NONE', #107710, 0.09999999999998898659 ) ;
#153563=ORIENTED_EDGE ( 'NONE', *, *, #161878, .T. ) ;
#153570=ADVANCED_FACE ( 'NONE', ( #56157 ), #60009, .T. ) ;
#153586=VECTOR ( 'NONE', #146846, 1000.000000000000000 ) ;
#153611=VERTEX_POINT ( 'NONE', #117441 ) ;
#153627=CARTESIAN_POINT ( 'NONE',  ( 21.05000000000000071, 67.12338541492522381, -161.6380270056797599 ) ) ;
#153628=AXIS2_PLACEMENT_3D ( 'NONE', #40653, #236234, #120185 ) ;
#153632=ORIENTED_EDGE ( 'NONE', *, *, #37964, .F. ) ;
#153636=DIRECTION ( 'NONE',  ( 0.000000000000000000, 0.000000000000000000, 1.000000000000000000 ) ) ;
#153664=CARTESIAN_POINT ( 'NONE',  ( 20.94999999999999929, 76.00000000001213607, -136.5231074845243313 ) ) ;
#153670=EDGE_CURVE ( 'NONE', #200730, #62499, #46865, .T. ) ;
#153672=CIRCLE ( 'NONE', #257592, 4.300000000000025580 ) ;
#153694=EDGE_CURVE ( 'NONE', #106082, #86886, #17295, .T. ) ;
#153711=FACE_OUTER_BOUND ( 'NONE', #161793, .T. ) ;
#153712=FACE_OUTER_BOUND ( 'NONE', #223498, .T. ) ;
#153725=ORIENTED_EDGE ( 'NONE', *, *, #237385, .F. ) ;
#153727=CIRCLE ( 'NONE', #74601, 0.09999999999998898659 ) ;
#153772=AXIS2_PLACEMENT_3D ( 'NONE', #179942, #160395, #239917 ) ;
#153830=EDGE_LOOP ( 'NONE', ( #79912, #123262, #234529, #191529 ) ) ;
#153833=ORIENTED_EDGE ( 'NONE', *, *, #24142, .F. ) ;
#153842=DIRECTION ( 'NONE',  ( 2.952720810173289112E-16, 1.000000000000000000, 6.982962677686266711E-15 ) ) ;
#153850=ORIENTED_EDGE ( 'NONE', *, *, #46487, .T. ) ;
#153885=CARTESIAN_POINT ( 'NONE',  ( -18.50000000000000000, 77.68707439010402993, -182.8376804510660065 ) ) ;
#153890=DIRECTION ( 'NONE',  ( 0.000000000000000000, 0.000000000000000000, -1.000000000000000000 ) ) ;
#153901=CARTESIAN_POINT ( 'NONE',  ( -20.54999999999999716, 76.00000000001213607, -136.5231074845243313 ) ) ;
#153903=DIRECTION ( 'NONE',  ( 0.000000000000000000, 0.000000000000000000, -1.000000000000000000 ) ) ;
#153925=EDGE_CURVE ( 'NONE', #95684, #90874, #238024, .T. ) ;
#153939=ORIENTED_EDGE ( 'NONE', *, *, #210439, .T. ) ;
#153941=CARTESIAN_POINT ( 'NONE',  ( -21.78635804494510708, 68.96433851485919320, -170.1221125500320852 ) ) ;
#153970=CARTESIAN_POINT ( 'NONE',  ( -21.45000000000000284, 68.29142135624960019, -157.6731074845243938 ) ) ;
#154010=DIRECTION ( 'NONE',  ( 0.000000000000000000, -7.026728003956695223E-15, 1.000000000000000000 ) ) ;
#154019=ORIENTED_EDGE ( 'NONE', *, *, #256033, .F. ) ;
#154029=CIRCLE ( 'NONE', #104057, 0.2000000000000057288 ) ;
#154048=DIRECTION ( 'NONE',  ( 1.000000000000000000, -7.304098846218134667E-16, -4.639676173203993355E-30 ) ) ;
#154088=CARTESIAN_POINT ( 'NONE',  ( 18.59999999999999787, 77.83534155023670564, -158.4679561919613491 ) ) ;
#154111=ADVANCED_BREP_SHAPE_REPRESENTATION ( '', ( #196328, #2425 ), #81157 ) ;
#154146=ADVANCED_FACE ( 'NONE', ( #126092 ), #81808, .F. ) ;
#154152=CARTESIAN_POINT ( 'NONE',  ( 18.43473516226089259, 85.49494228277045238, -162.9772088011748110 ) ) ;
#154186=FILL_AREA_STYLE_COLOUR ( '', #152111 ) ;
#154222=ORIENTED_EDGE ( 'NONE', *, *, #111554, .T. ) ;
#154231=TOROIDAL_SURFACE ( 'NONE', #66707, 0.2000000000000000111, 0.1000000000000000056 ) ;
#154238=CARTESIAN_POINT ( 'NONE',  ( 21.14999999999999858, 76.10000000001241460, -176.5637644362255969 ) ) ;
#154302=ADVANCED_FACE ( 'NONE', ( #137640 ), #256251, .F. ) ;
#154315=CARTESIAN_POINT ( 'NONE',  ( 18.59999999999999076, 69.35000000001222986, -148.7731074845244166 ) ) ;
#154317=DIRECTION ( 'NONE',  ( -1.000000000000000000, 0.000000000000000000, 0.000000000000000000 ) ) ;
#154325=LINE ( 'NONE', #69616, #96620 ) ;
#154339=FACE_OUTER_BOUND ( 'NONE', #47944, .T. ) ;
#154368=DIRECTION ( 'NONE',  ( 2.952720810173289112E-16, 1.000000000000000000, -6.088138035986627436E-46 ) ) ;
#154369=CYLINDRICAL_SURFACE ( 'NONE', #144747, 0.09999999999998898659 ) ;
#154378=CIRCLE ( 'NONE', #133487, 4.299999999999970512 ) ;
#154395=ORIENTED_EDGE ( 'NONE', *, *, #146269, .F. ) ;
#154407=EDGE_CURVE ( 'NONE', #40931, #113635, #59296, .T. ) ;
#154445=ORIENTED_EDGE ( 'NONE', *, *, #249011, .F. ) ;
#154446=TOROIDAL_SURFACE ( 'NONE', #171214, 0.6000000000000009770, 0.1000000000000000056 ) ;
#154461=FACE_OUTER_BOUND ( 'NONE', #144691, .T. ) ;
#154463=EDGE_CURVE ( 'NONE', #229965, #84708, #150382, .T. ) ;
#154478=LINE ( 'NONE', #119172, #207909 ) ;
#154484=CIRCLE ( 'NONE', #162857, 0.09999999999998898659 ) ;
#154487=ORIENTED_EDGE ( 'NONE', *, *, #12403, .T. ) ;
#154498=CARTESIAN_POINT ( 'NONE',  ( -21.05000000000000071, 64.36312671090826143, -163.2013482711997199 ) ) ;
#154502=VECTOR ( 'NONE', #99753, 1000.000000000000000 ) ;
#154541=CARTESIAN_POINT ( 'NONE',  ( -21.05000000000000071, 77.85102823015316176, -158.3691942151018566 ) ) ;
#154613=EDGE_LOOP ( 'NONE', ( #68675, #129087, #230362, #94828 ) ) ;
#154616=LINE ( 'NONE', #16377, #192452 ) ;
#154619=DIRECTION ( 'NONE',  ( 4.026293107431335996E-15, 0.8700118002898393765, -0.4930308989875104575 ) ) ;
#154620=CARTESIAN_POINT ( 'NONE',  ( -18.50000000000001066, 85.42130820975189920, -162.7807442704735479 ) ) ;
#154644=UNCERTAINTY_MEASURE_WITH_UNIT (LENGTH_MEASURE( 1.000000000000000082E-05 ), #152890, 'distance_accuracy_value', 'NONE');
#154690=DIRECTION ( 'NONE',  ( 0.000000000000000000, 0.000000000000000000, 1.000000000000000000 ) ) ;
#154723=DIRECTION ( 'NONE',  ( 1.000000000000000000, 0.000000000000000000, 0.000000000000000000 ) ) ;
#154740=FACE_OUTER_BOUND ( 'NONE', #6958, .T. ) ;
#154747=DIRECTION ( 'NONE',  ( -1.000000000000000000, 0.000000000000000000, 0.000000000000000000 ) ) ;
#154750=CARTESIAN_POINT ( 'NONE',  ( 18.57071067811864040, 65.82071067813089371, -148.7731074845244450 ) ) ;
#154807=ORIENTED_EDGE ( 'NONE', *, *, #77197, .F. ) ;
#154822=ORIENTED_EDGE ( 'NONE', *, *, #94695, .F. ) ;
#154827=DIRECTION ( 'NONE',  ( 0.000000000000000000, -1.000000000000000000, 0.000000000000000000 ) ) ;
#154836=ORIENTED_EDGE ( 'NONE', *, *, #128945, .F. ) ;
#154847=EDGE_LOOP ( 'NONE', ( #154822, #10999, #225837, #161839 ) ) ;
#154850=CARTESIAN_POINT ( 'NONE',  ( -18.59999999999999787, 74.36282728704190959, -158.4409541190523498 ) ) ;
#154854=DIRECTION ( 'NONE',  ( 0.000000000000000000, 1.000000000000000000, 6.982962677686266711E-15 ) ) ;
#154869=ADVANCED_FACE ( 'NONE', ( #184317 ), #162226, .F. ) ;
#154907=AXIS2_PLACEMENT_3D ( 'NONE', #26197, #207407, #109554 ) ;
#154915=CARTESIAN_POINT ( 'NONE',  ( 21.78635804494511419, 75.90099493450475165, -177.0587689696775442 ) ) ;
#154935=CARTESIAN_POINT ( 'NONE',  ( -20.64999999999999858, 71.75000000001223555, -148.8731074845244109 ) ) ;
#154944=AXIS2_PLACEMENT_3D ( 'NONE', #172207, #52188, #148753 ) ;
#154963=DIRECTION ( 'NONE',  ( -1.000000000000000000, 0.000000000000000000, 0.000000000000000000 ) ) ;
#154973=CYLINDRICAL_SURFACE ( 'NONE', #52510, 0.09999999999998898659 ) ;
#155037=EDGE_CURVE ( 'NONE', #33291, #238448, #255810, .T. ) ;
#155047=CIRCLE ( 'NONE', #109209, 0.09999999999999939493 ) ;
#155053=ORIENTED_EDGE ( 'NONE', *, *, #91503, .F. ) ;
#155055=CARTESIAN_POINT ( 'NONE',  ( -21.05000000000000071, 77.26178616857734482, -161.9366085209788650 ) ) ;
#155062=ORIENTED_EDGE ( 'NONE', *, *, #218642, .F. ) ;
#155064=CARTESIAN_POINT ( 'NONE',  ( 20.94999999999999929, 87.65000000001214175, -136.5231074845242745 ) ) ;
#155113=ADVANCED_FACE ( 'NONE', ( #112511 ), #58748, .F. ) ;
#155138=EDGE_CURVE ( 'NONE', #128766, #86886, #82323, .T. ) ;
#155149=DIRECTION ( 'NONE',  ( -1.000000000000000000, 0.000000000000000000, 0.000000000000000000 ) ) ;
#155157=ORIENTED_EDGE ( 'NONE', *, *, #201218, .F. ) ;
#155240=DIRECTION ( 'NONE',  ( -0.000000000000000000, 7.272083257015735086E-15, -1.000000000000000000 ) ) ;
#155276=CARTESIAN_POINT ( 'NONE',  ( -23.15000000000000213, 76.00000000001213607, -136.5231074845243313 ) ) ;
#155293=DIRECTION ( 'NONE',  ( -1.000000000000000000, 0.000000000000000000, -0.000000000000000000 ) ) ;
#155301=TOROIDAL_SURFACE ( 'NONE', #92711, 0.2000000000000000111, 0.1000000000000000056 ) ;
#155348=EDGE_CURVE ( 'NONE', #159949, #70015, #179772, .T. ) ;
#155359=DIRECTION ( 'NONE',  ( -1.000000000000000000, 0.000000000000000000, 0.000000000000000000 ) ) ;
#155369=DIRECTION ( 'NONE',  ( 0.000000000000000000, 7.056502275159890043E-15, -1.000000000000000000 ) ) ;
#155384=CARTESIAN_POINT ( 'NONE',  ( 18.49999999999998934, 69.45000000001230944, -160.0060803140843859 ) ) ;
#155389=ORIENTED_EDGE ( 'NONE', *, *, #31842, .T. ) ;
#155425=CIRCLE ( 'NONE', #101164, 0.09999999999999939493 ) ;
#155428=AXIS2_PLACEMENT_3D ( 'NONE', #91664, #126942, #248173 ) ;
#155431=ORIENTED_EDGE ( 'NONE', *, *, #155037, .F. ) ;
#155434=CARTESIAN_POINT ( 'NONE',  ( 18.49999999999997868, 85.32100840337365355, -162.7871692354464130 ) ) ;
#155472=CARTESIAN_POINT ( 'NONE',  ( -20.54999999999999716, 73.50000000001223555, -149.7477294072864709 ) ) ;
#155484=DIRECTION ( 'NONE',  ( 0.000000000000000000, 0.000000000000000000, 1.000000000000000000 ) ) ;
#155507=CARTESIAN_POINT ( 'NONE',  ( 18.59999999999996945, 65.66751761918692409, -130.9282609406112670 ) ) ;
#155511=ORIENTED_EDGE ( 'NONE', *, *, #76829, .T. ) ;
#155533=AXIS2_PLACEMENT_3D ( 'NONE', #192154, #73499, #146869 ) ;
#155534=CIRCLE ( 'NONE', #209477, 0.09999999999998898659 ) ;
#155559=LINE ( 'NONE', #195953, #226092 ) ;
#155579=EDGE_LOOP ( 'NONE', ( #247297, #61694, #16160, #126496 ) ) ;
#155594=DIRECTION ( 'NONE',  ( 0.000000000000000000, -0.008583690987162452199, 0.9999631594459053030 ) ) ;
#155611=CIRCLE ( 'NONE', #147184, 0.5000000000000004441 ) ;
#155616=EDGE_CURVE ( 'NONE', #64893, #5474, #200799, .T. ) ;
#155626=AXIS2_PLACEMENT_3D ( 'NONE', #176769, #197586, #77620 ) ;
#155631=EDGE_LOOP ( 'NONE', ( #188242, #256012, #191116, #134566 ) ) ;
#155639=FACE_OUTER_BOUND ( 'NONE', #155579, .T. ) ;
#155642=EDGE_CURVE ( 'NONE', #237787, #56976, #159130, .T. ) ;
#155643=DIRECTION ( 'NONE',  ( -1.000000000000000000, 2.952720810173289112E-16, 2.061873921506763405E-30 ) ) ;
#155668=ADVANCED_FACE ( 'NONE', ( #20819 ), #57332, .T. ) ;
#155712=EDGE_LOOP ( 'NONE', ( #223217, #174882, #35006 ) ) ;
#155739=CARTESIAN_POINT ( 'NONE',  ( 21.14999999999999858, 76.10000000001245724, -181.6726782920691505 ) ) ;
#155745=AXIS2_PLACEMENT_3D ( 'NONE', #230942, #50968, #130524 ) ;
#155746=EDGE_CURVE ( 'NONE', #22920, #18391, #209155, .T. ) ;
#155751=CIRCLE ( 'NONE', #51626, 0.1000000000000072220 ) ;
#155778=CARTESIAN_POINT ( 'NONE',  ( -21.05000000000000071, 64.35000000001234355, -163.2392418215462726 ) ) ;
#155793=TOROIDAL_SURFACE ( 'NONE', #247340, 0.2000000000000000111, 0.1000000000000000056 ) ;
#155800=CARTESIAN_POINT ( 'NONE',  ( 21.05000000000000071, 85.50000000001222134, -146.4170766071767389 ) ) ;
#155822=CARTESIAN_POINT ( 'NONE',  ( -20.64999999999999858, 71.65000000001228386, -157.6731074845243938 ) ) ;
#155841=DIRECTION ( 'NONE',  ( 0.000000000000000000, 6.982962677686266711E-15, -1.000000000000000000 ) ) ;
#155855=EDGE_CURVE ( 'NONE', #78078, #23345, #221615, .T. ) ;
#155884=CARTESIAN_POINT ( 'NONE',  ( 21.07928932188134397, 75.90110485435802445, -176.3516241409176644 ) ) ;
#155900=CARTESIAN_POINT ( 'NONE',  ( -18.45037301276615693, 85.49020044755471304, -163.0104333481092453 ) ) ;
#155910=CIRCLE ( 'NONE', #43463, 11.75000000000001066 ) ;
#155914=CIRCLE ( 'NONE', #218222, 4.150000000000001243 ) ;
#155917=CARTESIAN_POINT ( 'NONE',  ( 20.94999999999999574, 69.65000000001231228, -160.1792853948412869 ) ) ;
#155934=ORIENTED_EDGE ( 'NONE', *, *, #249011, .T. ) ;
#155947=EDGE_CURVE ( 'NONE', #113546, #149556, #151099, .T. ) ;
#155959=AXIS2_PLACEMENT_3D ( 'NONE', #15583, #191661, #37711 ) ;
#156000=CYLINDRICAL_SURFACE ( 'NONE', #93366, 12.87499999999999822 ) ;
#156031=CARTESIAN_POINT ( 'NONE',  ( -22.48479450179659977, 75.95300841882557563, -181.6731059307759608 ) ) ;
#156032=CARTESIAN_POINT ( 'NONE',  ( 22.48660254037844197, 64.35000000001237197, -170.0731074845244279 ) ) ;
#156044=AXIS2_PLACEMENT_3D ( 'NONE', #139482, #42977, #181213 ) ;
#156062=VERTEX_POINT ( 'NONE', #86853 ) ;
#156082=ORIENTED_EDGE ( 'NONE', *, *, #21750, .F. ) ;
#156125=ORIENTED_EDGE ( 'NONE', *, *, #102492, .F. ) ;
#156164=CARTESIAN_POINT ( 'NONE',  ( -23.15000000000000213, 87.41227409416185878, -139.5231074845243029 ) ) ;
#156189=AXIS2_PLACEMENT_3D ( 'NONE', #81175, #197289, #158214 ) ;
#156248=EDGE_LOOP ( 'NONE', ( #247405, #6982, #136057, #187293 ) ) ;
#156288=AXIS2_PLACEMENT_3D ( 'NONE', #124182, #246667, #25095 ) ;
#156322=CARTESIAN_POINT ( 'NONE',  ( -18.50000000000000000, 64.35000000001230092, -157.8731074845244393 ) ) ;
#156326=ORIENTED_EDGE ( 'NONE', *, *, #80074, .F. ) ;
#156331=CARTESIAN_POINT ( 'NONE',  ( -21.05000000000000071, 76.00000000001213607, -136.5231074845243313 ) ) ;
#156345=ORIENTED_EDGE ( 'NONE', *, *, #89850, .T. ) ;
#156434=CYLINDRICAL_SURFACE ( 'NONE', #61927, 11.80000000000000426 ) ;
#156444=ORIENTED_EDGE ( 'NONE', *, *, #198683, .T. ) ;
#156501=CIRCLE ( 'NONE', #119056, 0.09999999999999939493 ) ;
#156514=CARTESIAN_POINT ( 'NONE',  ( -20.54999999999999716, 68.75000000001223555, -148.7731074845244166 ) ) ;
#156525=AXIS2_PLACEMENT_3D ( 'NONE', #142910, #2125, #200347 ) ;
#156546=VECTOR ( 'NONE', #223827, 1000.000000000000000 ) ;
#156552=DIRECTION ( 'NONE',  ( 0.000000000000000000, 6.982962677686266711E-15, -1.000000000000000000 ) ) ;
#156618=DIRECTION ( 'NONE',  ( 1.000000000000000000, -0.000000000000000000, -0.000000000000000000 ) ) ;
#156623=ADVANCED_FACE ( 'NONE', ( #32741 ), #136929, .F. ) ;
#156657=AXIS2_PLACEMENT_3D ( 'NONE', #254063, #38894, #118429 ) ;
#156704=EDGE_CURVE ( 'NONE', #194806, #167959, #10290, .T. ) ;
#156734=EDGE_CURVE ( 'NONE', #196891, #40351, #6162, .T. ) ;
#156838=CARTESIAN_POINT ( 'NONE',  ( 23.14999999999999503, 64.25000000001244871, -181.7731074845244450 ) ) ;
#156858=EDGE_CURVE ( 'NONE', #218618, #218857, #135148, .T. ) ;
#156909=DIRECTION ( 'NONE',  ( 0.000000000000000000, -0.9908441862701791170, 0.1350103645450472789 ) ) ;
#156933=ORIENTED_EDGE ( 'NONE', *, *, #223728, .F. ) ;
#156956=DIRECTION ( 'NONE',  ( 0.000000000000000000, -6.982962677686266711E-15, 1.000000000000000000 ) ) ;
#156975=DIRECTION ( 'NONE',  ( 1.000000000000000000, 0.000000000000000000, 0.000000000000000000 ) ) ;
#156985=EDGE_LOOP ( 'NONE', ( #170553, #94764, #184470, #154395 ) ) ;
#156994=AXIS2_PLACEMENT_3D ( 'NONE', #210547, #48894, #110153 ) ;
#157015=DIRECTION ( 'NONE',  ( 1.000000000000000000, 0.000000000000000000, 0.000000000000000000 ) ) ;
#157043=DIRECTION ( 'NONE',  ( 1.000000000000000000, 0.000000000000000000, 0.000000000000000000 ) ) ;
#157061=EDGE_CURVE ( 'NONE', #241247, #153611, #131253, .T. ) ;
#157071=VECTOR ( 'NONE', #253706, 1000.000000000000000 ) ;
#157101=CARTESIAN_POINT ( 'NONE',  ( 20.94999999999999574, 74.16465844978787914, -158.3679561919613832 ) ) ;
#157108=AXIS2_PLACEMENT_3D ( 'NONE', #599, #159710, #18899 ) ;
#157127=CARTESIAN_POINT ( 'NONE',  ( 18.59999999999999432, 77.16270174995034381, -161.9231074845243370 ) ) ;
#157139=TOROIDAL_SURFACE ( 'NONE', #61259, 0.2000000000000000111, 0.1000000000000000056 ) ;
#157146=DIRECTION ( 'NONE',  ( -1.000000000000000000, -0.000000000000000000, -0.000000000000000000 ) ) ;
#157166=ADVANCED_FACE ( 'NONE', ( #60919 ), #41394, .T. ) ;
#157167=ORIENTED_EDGE ( 'NONE', *, *, #35057, .T. ) ;
#157172=SPHERICAL_SURFACE ( 'NONE', #36609, 0.1000000000000000056 ) ;
#157193=EDGE_CURVE ( 'NONE', #29646, #199802, #202000, .T. ) ;
#157200=VECTOR ( 'NONE', #17840, 1000.000000000000000 ) ;
#157215=EDGE_CURVE ( 'NONE', #176760, #101907, #207729, .T. ) ;
#157237=VERTEX_POINT ( 'NONE', #247254 ) ;
#157252=DIRECTION ( 'NONE',  ( 0.000000000000000000, -7.086529944415886769E-15, 1.000000000000000000 ) ) ;
#157257=AXIS2_PLACEMENT_3D ( 'NONE', #43045, #47, #196958 ) ;
#157266=CIRCLE ( 'NONE', #15630, 11.74999999999999645 ) ;
#157275=FACE_OUTER_BOUND ( 'NONE', #79468, .T. ) ;
#157282=CARTESIAN_POINT ( 'NONE',  ( -22.39999999999999858, 76.00000000001237765, -170.0231074845243597 ) ) ;
#157305=EDGE_LOOP ( 'NONE', ( #4384, #253298, #57707, #225919 ) ) ;
#157324=CYLINDRICAL_SURFACE ( 'NONE', #54948, 0.09999999999998898659 ) ;
#157350=AXIS2_PLACEMENT_3D ( 'NONE', #155822, #97061, #254836 ) ;
#157363=CARTESIAN_POINT ( 'NONE',  ( 21.05000000000000071, 71.00000000001223555, -148.9283735034374843 ) ) ;
#157379=ORIENTED_EDGE ( 'NONE', *, *, #132833, .F. ) ;
#157388=CARTESIAN_POINT ( 'NONE',  ( 21.30000000000002558, 76.00000000001237765, -170.0231074845243597 ) ) ;
#157412=DIRECTION ( 'NONE',  ( 1.000000000000000000, -2.952720810173289112E-16, -2.061873921506763405E-30 ) ) ;
#157450=DIRECTION ( 'NONE',  ( 0.000000000000000000, 1.000000000000000000, 6.982962677686266711E-15 ) ) ;
#157469=DIRECTION ( 'NONE',  ( 0.000000000000000000, 6.982962677686266711E-15, -1.000000000000000000 ) ) ;
#157494=CARTESIAN_POINT ( 'NONE',  ( -20.94999999999999929, 68.96868720525692709, -132.9139565462971007 ) ) ;
#157519=CIRCLE ( 'NONE', #190841, 0.09999999999999939493 ) ;
#157531=ORIENTED_EDGE ( 'NONE', *, *, #116792, .F. ) ;
#157534=DIRECTION ( 'NONE',  ( 1.000000000000000000, 0.000000000000000000, 0.000000000000000000 ) ) ;
#157553=AXIS2_PLACEMENT_3D ( 'NONE', #195432, #251523, #32525 ) ;
#157556=LINE ( 'NONE', #97502, #73408 ) ;
#157563=EDGE_CURVE ( 'NONE', #159849, #997, #158472, .T. ) ;
#157651=VERTEX_POINT ( 'NONE', #103579 ) ;
#157671=EDGE_LOOP ( 'NONE', ( #80299, #108549, #165077, #50819 ) ) ;
#157693=ORIENTED_EDGE ( 'NONE', *, *, #114540, .T. ) ;
#157703=CARTESIAN_POINT ( 'NONE',  ( -18.59999999999999787, 64.35000000001230092, -157.8731074845244393 ) ) ;
#157707=VERTEX_POINT ( 'NONE', #107459 ) ;
#157708=DIRECTION ( 'NONE',  ( 1.000000000000000000, 0.000000000000000000, 0.000000000000000000 ) ) ;
#157710=CYLINDRICAL_SURFACE ( 'NONE', #65549, 0.1000000000000026007 ) ;
#157728=CARTESIAN_POINT ( 'NONE',  ( -20.94999999999999929, 76.00000000001213607, -136.5231074845243313 ) ) ;
#157752=EDGE_CURVE ( 'NONE', #252845, #174960, #185520, .T. ) ;
#157780=ORIENTED_EDGE ( 'NONE', *, *, #170074, .T. ) ;
#157782=FACE_OUTER_BOUND ( 'NONE', #131516, .T. ) ;
#157785=DIRECTION ( 'NONE',  ( -0.000000000000000000, 1.000000000000000000, 6.982962677686267499E-15 ) ) ;
#157792=LINE ( 'NONE', #40402, #137057 ) ;
#157845=PLANE ( 'NONE',  #232839 ) ;
#157847=FACE_OUTER_BOUND ( 'NONE', #97057, .T. ) ;
#157857=DIRECTION ( 'NONE',  ( 0.000000000000000000, 0.000000000000000000, 1.000000000000000000 ) ) ;
#157868=EDGE_LOOP ( 'NONE', ( #140907, #171959, #73758, #207966 ) ) ;
#157869=CARTESIAN_POINT ( 'NONE',  ( -18.59999999999999787, 66.65000000001229807, -157.8731074845244393 ) ) ;
#157955=ORIENTED_EDGE ( 'NONE', *, *, #227642, .F. ) ;
#157960=AXIS2_PLACEMENT_3D ( 'NONE', #200623, #46331, #220188 ) ;
#157964=EDGE_CURVE ( 'NONE', #227218, #223792, #56202, .T. ) ;
#157967=ORIENTED_EDGE ( 'NONE', *, *, #51546, .T. ) ;
#158007=SPHERICAL_SURFACE ( 'NONE', #159632, 0.1000000000000000056 ) ;
#158008=CARTESIAN_POINT ( 'NONE',  ( -20.94999999999999929, 87.41227409416185878, -139.4231074845242802 ) ) ;
#158019=CARTESIAN_POINT ( 'NONE',  ( 21.08750232978087524, 65.27513661400213607, -157.7942493115248510 ) ) ;
#158025=AXIS2_PLACEMENT_3D ( 'NONE', #49902, #166031, #47316 ) ;
#158028=ORIENTED_EDGE ( 'NONE', *, *, #115614, .T. ) ;
#158065=DIRECTION ( 'NONE',  ( 1.000000000000000000, 0.000000000000000000, 0.000000000000000000 ) ) ;
#158070=ADVANCED_FACE ( 'NONE', ( #134261 ), #31373, .F. ) ;
#158111=CIRCLE ( 'NONE', #257971, 0.09999999999998898659 ) ;
#158127=DIRECTION ( 'NONE',  ( 0.000000000000000000, -7.487053152578127080E-15, 1.000000000000000000 ) ) ;
#158140=CARTESIAN_POINT ( 'NONE',  ( -2.995603634470891112E-16, 87.75000000001229239, -157.7731074845242745 ) ) ;
#158185=FACE_OUTER_BOUND ( 'NONE', #24607, .T. ) ;
#158214=DIRECTION ( 'NONE',  ( 1.000000000000000000, 0.000000000000000000, 0.000000000000000000 ) ) ;
#158246=LINE ( 'NONE', #100751, #235908 ) ;
#158256=CYLINDRICAL_SURFACE ( 'NONE', #119038, 0.09999999999999939493 ) ;
#158278=ORIENTED_EDGE ( 'NONE', *, *, #235289, .F. ) ;
#158288=ADVANCED_FACE ( 'NONE', ( #180049 ), #45666, .T. ) ;
#158335=( BOUNDED_SURFACE ( )  B_SPLINE_SURFACE ( 3, 2, ( 
 ( #247364, #191284, #110426 ),
 ( #169157, #27077, #248657 ),
 ( #246103, #210816, #109133 ),
 ( #92148, #67446, #170458 ) ),
 .UNSPECIFIED., .F., .F., .F. ) 
 B_SPLINE_SURFACE_WITH_KNOTS ( ( 4, 4 ),
 ( 3, 3 ),
 ( -5.692061405548898279E-19, 0.0003124336117481331431 ),
 ( 0.000000000000000000, 1.000000000000000000 ),
 .UNSPECIFIED. ) 
 GEOMETRIC_REPRESENTATION_ITEM ( )  RATIONAL_B_SPLINE_SURFACE ( (
 ( 1.000000000000000000, 0.7040654476015839602, 1.000000000000000000),
 ( 1.000000000000000000, 0.7039193538781509663, 1.000000000000000000),
 ( 1.000000000000000000, 0.7089171279144148574, 1.000000000000000000),
 ( 1.000000000000000000, 0.7071067811866490471, 1.000000000000000000) ) ) 
 REPRESENTATION_ITEM ( '' )  SURFACE ( )  );
#158354=CARTESIAN_POINT ( 'NONE',  ( -20.54999999999999716, 87.75000000001229239, -157.6731074845242517 ) ) ;
#158366=CARTESIAN_POINT ( 'NONE',  ( -20.85000000000000142, 76.00000000001213607, -136.5231074845243313 ) ) ;
#158413=CARTESIAN_POINT ( 'NONE',  ( -18.46856557590793457, 85.47421590779882195, -162.9211212436420055 ) ) ;
#158430=CARTESIAN_POINT ( 'NONE',  ( 21.04999999999999716, 76.01759718702130897, -176.4638783781849440 ) ) ;
#158452=ORIENTED_EDGE ( 'NONE', *, *, #215547, .T. ) ;
#158470=CARTESIAN_POINT ( 'NONE',  ( -18.43599941264930209, 85.51932742860702774, -163.0501306950028777 ) ) ;
#158472=LINE ( 'NONE', #21520, #14554 ) ;
#158521=ORIENTED_EDGE ( 'NONE', *, *, #87392, .F. ) ;
#158571=DIRECTION ( 'NONE',  ( 0.000000000000000000, 0.000000000000000000, 1.000000000000000000 ) ) ;
#158586=VECTOR ( 'NONE', #211403, 1000.000000000000000 ) ;
#158587=ORIENTED_EDGE ( 'NONE', *, *, #44973, .F. ) ;
#158588=ORIENTED_EDGE ( 'NONE', *, *, #190099, .T. ) ;
#158594=CARTESIAN_POINT ( 'NONE',  ( 20.85000000000000142, 64.35000000001214460, -136.5231074845244166 ) ) ;
#158617=EDGE_CURVE ( 'NONE', #238448, #164498, #173349, .T. ) ;
#158646=FACE_OUTER_BOUND ( 'NONE', #141401, .T. ) ;
#158665=EDGE_CURVE ( 'NONE', #588, #141897, #160847, .T. ) ;
#158684=CARTESIAN_POINT ( 'NONE',  ( 18.59999999999999076, 74.16465844978787914, -158.4679561919613775 ) ) ;
#158693=ADVANCED_FACE ( 'NONE', ( #80599 ), #160196, .T. ) ;
#158695=ORIENTED_EDGE ( 'NONE', *, *, #27689, .T. ) ;
#158699=VERTEX_POINT ( 'NONE', #201858 ) ;
#158729=CARTESIAN_POINT ( 'NONE',  ( 23.24999999999999289, 69.35000000001222986, -148.6731074845243938 ) ) ;
#158741=EDGE_LOOP ( 'NONE', ( #62514, #236180, #134454, #191763, #195236 ) ) ;
#158758=CIRCLE ( 'NONE', #150548, 7.899999999999990585 ) ;
#158760=CARTESIAN_POINT ( 'NONE',  ( 21.05000000000000071, 69.45934304831114048, -169.9231074845244223 ) ) ;
#158843=EDGE_CURVE ( 'NONE', #9710, #61341, #186148, .T. ) ;
#158844=CARTESIAN_POINT ( 'NONE',  ( 20.94999999999999574, 74.75000000001232081, -162.1231074845243540 ) ) ;
#158860=CARTESIAN_POINT ( 'NONE',  ( 18.47135592147661853, 85.47108861327768636, -129.8395125446803320 ) ) ;
#158886=CIRCLE ( 'NONE', #25599, 0.09999999999999939493 ) ;
#158934=EDGE_LOOP ( 'NONE', ( #182022, #147669, #241863, #2393 ) ) ;
#158954=ORIENTED_EDGE ( 'NONE', *, *, #181821, .T. ) ;
#159007=DIRECTION ( 'NONE',  ( 1.000000000000000000, 0.000000000000000000, 0.000000000000000000 ) ) ;
#159014=ORIENTED_EDGE ( 'NONE', *, *, #122282, .T. ) ;
#159041=AXIS2_PLACEMENT_3D ( 'NONE', #215132, #213847, #133042 ) ;
#159047=DIRECTION ( 'NONE',  ( -1.000000000000000000, -7.304098846218135653E-16, -5.100424963727256530E-30 ) ) ;
#159070=LINE ( 'NONE', #57353, #186047 ) ;
#159115=CARTESIAN_POINT ( 'NONE',  ( 18.51697539158856998, 65.68434038414380893, -130.9866880726065688 ) ) ;
#159120=AXIS2_PLACEMENT_3D ( 'NONE', #194524, #57536, #176242 ) ;
#159130=CIRCLE ( 'NONE', #84203, 0.09999999999999939493 ) ;
#159136=FACE_OUTER_BOUND ( 'NONE', #147413, .T. ) ;
#159151=CIRCLE ( 'NONE', #242315, 0.09999999999998898659 ) ;
#159161=AXIS2_PLACEMENT_3D ( 'NONE', #106156, #185726, #7073 ) ;
#159163=DIRECTION ( 'NONE',  ( 0.000000000000000000, -0.4930308989875170078, -0.8700118002898356018 ) ) ;
#159209=ORIENTED_EDGE ( 'NONE', *, *, #255682, .F. ) ;
#159217=DIRECTION ( 'NONE',  ( 1.000000000000000000, 0.000000000000000000, 0.000000000000000000 ) ) ;
#159221=CIRCLE ( 'NONE', #142781, 0.1000000000000028644 ) ;
#159282=ORIENTED_EDGE ( 'NONE', *, *, #238083, .F. ) ;
#159289=CARTESIAN_POINT ( 'NONE',  ( 18.59999999999998366, 76.00000000001213607, -136.5231074845243313 ) ) ;
#159305=DIRECTION ( 'NONE',  ( -1.000000000000000000, 0.000000000000000000, 0.000000000000000000 ) ) ;
#159323=AXIS2_PLACEMENT_3D ( 'NONE', #157703, #102782, #177251 ) ;
#159333=CIRCLE ( 'NONE', #146814, 0.09999999999998898659 ) ;
#159334=CYLINDRICAL_SURFACE ( 'NONE', #225980, 0.09999999999999939493 ) ;
#159347=DIRECTION ( 'NONE',  ( 0.000000000000000000, 0.000000000000000000, 1.000000000000000000 ) ) ;
#159358=AXIS2_PLACEMENT_3D ( 'NONE', #120808, #21691, #240736 ) ;
#159378=DIRECTION ( 'NONE',  ( 0.000000000000000000, 0.000000000000000000, 1.000000000000000000 ) ) ;
#159389=DIRECTION ( 'NONE',  ( 1.000000000000000000, 0.000000000000000000, 0.000000000000000000 ) ) ;
#159393=EDGE_LOOP ( 'NONE', ( #219272, #173062, #176219, #36067 ) ) ;
#159418=CARTESIAN_POINT ( 'NONE',  ( -21.05000000000000071, 74.16465844978787914, -158.4679561919613775 ) ) ;
#159458=EDGE_CURVE ( 'NONE', #244808, #127337, #256812, .T. ) ;
#159494=CARTESIAN_POINT ( 'NONE',  ( 21.05000000000000071, 71.18691588786276725, -158.0815897280005800 ) ) ;
#159515=AXIS2_PLACEMENT_3D ( 'NONE', #181300, #2626, #60031 ) ;
#159523=ORIENTED_EDGE ( 'NONE', *, *, #84618, .F. ) ;
#159568=EDGE_LOOP ( 'NONE', ( #60179, #64779, #58365, #211345 ) ) ;
#159591=ORIENTED_EDGE ( 'NONE', *, *, #156858, .T. ) ;
#159592=EDGE_CURVE ( 'NONE', #200182, #26287, #206982, .T. ) ;
#159628=DIRECTION ( 'NONE',  ( 0.000000000000000000, -6.982962677686266711E-15, 1.000000000000000000 ) ) ;
#159632=AXIS2_PLACEMENT_3D ( 'NONE', #61431, #181401, #152 ) ;
#159676=CARTESIAN_POINT ( 'NONE',  ( 20.94999999999999929, 70.60000000001222986, -148.9283735034374843 ) ) ;
#159710=DIRECTION ( 'NONE',  ( 0.000000000000000000, 6.982962677686266711E-15, -1.000000000000000000 ) ) ;
#159791=ORIENTED_EDGE ( 'NONE', *, *, #246872, .F. ) ;
#159792=DIRECTION ( 'NONE',  ( 6.484947573744954877E-15, -0.9274965247785555977, 0.3738317757009190223 ) ) ;
#159801=ORIENTED_EDGE ( 'NONE', *, *, #206007, .F. ) ;
#159822=ORIENTED_EDGE ( 'NONE', *, *, #24691, .T. ) ;
#159844=( BOUNDED_SURFACE ( )  B_SPLINE_SURFACE ( 3, 2, ( 
 ( #160146, #117150, #196666 ),
 ( #18037, #161422, #97543 ),
 ( #177145, #81825, #179697 ),
 ( #257881, #59709, #256596 ),
 ( #78003, #237093, #58424 ),
 ( #200527, #79276, #217503 ),
 ( #158860, #139243, #40203 ),
 ( #119722, #141830, #21897 ),
 ( #199258, #20629, #61008 ),
 ( #140538, #220096, #31864 ) ),
 .UNSPECIFIED., .F., .F., .F. ) 
 B_SPLINE_SURFACE_WITH_KNOTS ( ( 4, 2, 2, 2, 4 ),
 ( 3, 3 ),
 ( 0.0001701955120502350236, 0.0002247052511886071975, 0.0002792149903269793444, 0.0003882344686037236380, 0.0006062734251572122254 ),
 ( 0.000000000000000000, 1.000000000000000000 ),
 .UNSPECIFIED. ) 
 GEOMETRIC_REPRESENTATION_ITEM ( )  RATIONAL_B_SPLINE_SURFACE ( (
 ( 1.000000000000000000, 0.2966190024561151661, 1.000000000000000000),
 ( 1.000000000000000000, 0.2964522492709388279, 1.000000000000000000),
 ( 1.000000000000000000, 0.3059923531885315184, 1.000000000000000000),
 ( 1.000000000000000000, 0.3355751146943017904, 1.000000000000000000),
 ( 1.000000000000000000, 0.3550672384958052930, 1.000000000000000000),
 ( 1.000000000000000000, 0.4157034672192139180, 1.000000000000000000),
 ( 1.000000000000000000, 0.4588031877657839930, 1.000000000000000000),
 ( 1.000000000000000000, 0.5771441759654667436, 1.000000000000000000),
 ( 1.000000000000000000, 0.6469377121776090922, 1.000000000000000000),
 ( 1.000000000000000000, 0.7071067811865870967, 1.000000000000000000) ) ) 
 REPRESENTATION_ITEM ( '' )  SURFACE ( )  );
#159849=VERTEX_POINT ( 'NONE', #51795 ) ;
#159887=TOROIDAL_SURFACE ( 'NONE', #226480, 11.65000000000000036, 0.1000000000000000056 ) ;
#159900=EDGE_CURVE ( 'NONE', #128506, #231943, #148915, .T. ) ;
#159906=DIRECTION ( 'NONE',  ( 0.000000000000000000, 0.000000000000000000, 1.000000000000000000 ) ) ;
#159949=VERTEX_POINT ( 'NONE', #235575 ) ;
#159958=DIRECTION ( 'NONE',  ( -1.000000000000000000, -0.000000000000000000, -0.000000000000000000 ) ) ;
#159991=CIRCLE ( 'NONE', #35105, 0.09999999999999939493 ) ;
#160003=FACE_OUTER_BOUND ( 'NONE', #132439, .T. ) ;
#160006=DIRECTION ( 'NONE',  ( 0.000000000000000000, 0.9915357197604982575, -0.1298341882519033486 ) ) ;
#160021=DIRECTION ( 'NONE',  ( 0.000000000000000000, -1.000000000000000000, -6.982962677686266711E-15 ) ) ;
#160022=DIRECTION ( 'NONE',  ( 0.000000000000000000, 0.000000000000000000, 1.000000000000000000 ) ) ;
#160057=CARTESIAN_POINT ( 'NONE',  ( -18.39999999999999858, 85.68240343348850274, -129.8662641071115047 ) ) ;
#160088=CARTESIAN_POINT ( 'NONE',  ( 23.25000000000000000, 69.45000000001229523, -157.6731074845243938 ) ) ;
#160090=ORIENTED_EDGE ( 'NONE', *, *, #256443, .F. ) ;
#160104=CARTESIAN_POINT ( 'NONE',  ( 23.25000000000000000, 87.75000000001229239, -157.8731074845242688 ) ) ;
#160129=EDGE_CURVE ( 'NONE', #67500, #51561, #178147, .T. ) ;
#160146=CARTESIAN_POINT ( 'NONE',  ( 18.39999999999999858, 85.50000000001209344, -129.9229180933022576 ) ) ;
#160166=AXIS2_PLACEMENT_3D ( 'NONE', #246092, #83110, #144380 ) ;
#160196=PLANE ( 'NONE',  #252382 ) ;
#160226=ORIENTED_EDGE ( 'NONE', *, *, #180054, .T. ) ;
#160235=CARTESIAN_POINT ( 'NONE',  ( 21.05000000000000071, 67.22371710471989559, -170.0231074845244166 ) ) ;
#160243=CARTESIAN_POINT ( 'NONE',  ( -23.15000000000000213, 64.35000000001238618, -170.0231074845244166 ) ) ;
#160257=DIRECTION ( 'NONE',  ( 0.000000000000000000, 0.000000000000000000, 1.000000000000000000 ) ) ;
#160261=EDGE_CURVE ( 'NONE', #47267, #240428, #257185, .T. ) ;
#160265=EDGE_CURVE ( 'NONE', #167384, #195708, #112768, .T. ) ;
#160271=ORIENTED_EDGE ( 'NONE', *, *, #188638, .T. ) ;
#160300=DIRECTION ( 'NONE',  ( 1.000000000000000000, 0.000000000000000000, 0.000000000000000000 ) ) ;
#160348=ORIENTED_EDGE ( 'NONE', *, *, #167685, .F. ) ;
#160391=CIRCLE ( 'NONE', #60390, 11.75000000000001066 ) ;
#160395=DIRECTION ( 'NONE',  ( -1.000000000000000000, 2.952720810173289112E-16, 2.061873921506763405E-30 ) ) ;
#160403=CARTESIAN_POINT ( 'NONE',  ( 18.50596464788227280, 65.69367753730676895, -131.0189238066348310 ) ) ;
#160409=CARTESIAN_POINT ( 'NONE',  ( 21.00000000000000000, 66.25000000001223555, -148.7731074845244450 ) ) ;
#160418=EDGE_CURVE ( 'NONE', #143129, #240241, #82585, .T. ) ;
#160451=CARTESIAN_POINT ( 'NONE',  ( -21.53551880898957904, 75.90103026544076670, -176.8079052459406739 ) ) ;
#160460=EDGE_CURVE ( 'NONE', #153611, #70242, #174254, .T. ) ;
#160465=PLANE ( 'NONE',  #207016 ) ;
#160484=CARTESIAN_POINT ( 'NONE',  ( -18.59999999999999787, 77.83585931145570669, -125.0186683157258329 ) ) ;
#160491=ORIENTED_EDGE ( 'NONE', *, *, #120150, .T. ) ;
#160525=ORIENTED_EDGE ( 'NONE', *, *, #184789, .F. ) ;
#160550=VERTEX_POINT ( 'NONE', #27824 ) ;
#160557=DIRECTION ( 'NONE',  ( 0.000000000000000000, 0.000000000000000000, 1.000000000000000000 ) ) ;
#160558=CARTESIAN_POINT ( 'NONE',  ( 18.54286124688534798, 85.62391757880992316, -129.7819051526616079 ) ) ;
#160565=CARTESIAN_POINT ( 'NONE',  ( 21.05563370358598263, 65.27576964416579131, -157.8400166685613328 ) ) ;
#160575=ORIENTED_EDGE ( 'NONE', *, *, #160644, .F. ) ;
#160577=AXIS2_PLACEMENT_3D ( 'NONE', #96421, #50867, #172180 ) ;
#160585=CIRCLE ( 'NONE', #198534, 0.1999999999999987899 ) ;
#160607=ORIENTED_EDGE ( 'NONE', *, *, #64741, .T. ) ;
#160610=CARTESIAN_POINT ( 'NONE',  ( 23.14999999999998437, 76.00000000001234923, -165.9731074845243768 ) ) ;
#160615=DIRECTION ( 'NONE',  ( 0.000000000000000000, 0.000000000000000000, -1.000000000000000000 ) ) ;
#160620=CIRCLE ( 'NONE', #139719, 0.09999999999999134581 ) ;
#160644=EDGE_CURVE ( 'NONE', #209999, #244761, #236731, .T. ) ;
#160653=DIRECTION ( 'NONE',  ( 0.000000000000000000, 8.783410004945868831E-15, -1.000000000000000000 ) ) ;
#160654=DIRECTION ( 'NONE',  ( 0.000000000000000000, -6.938893903907222067E-15, 1.000000000000000000 ) ) ;
#160664=DIRECTION ( 'NONE',  ( 1.000000000000000000, 0.000000000000000000, 0.000000000000000000 ) ) ;
#160691=DIRECTION ( 'NONE',  ( 0.000000000000000000, 1.000000000000000000, 6.688090509790097607E-15 ) ) ;
#160717=DIRECTION ( 'NONE',  ( 0.000000000000000000, 0.000000000000000000, -1.000000000000000000 ) ) ;
#160746=ORIENTED_EDGE ( 'NONE', *, *, #23705, .T. ) ;
#160768=CARTESIAN_POINT ( 'NONE',  ( -18.50000000000000000, 85.40000000001209912, -129.6410656363516125 ) ) ;
#160769=FACE_OUTER_BOUND ( 'NONE', #100028, .T. ) ;
#160773=CYLINDRICAL_SURFACE ( 'NONE', #163972, 0.1000000000000028644 ) ;
#160806=VERTEX_POINT ( 'NONE', #198419 ) ;
#160821=VERTEX_POINT ( 'NONE', #22376 ) ;
#160829=ORIENTED_EDGE ( 'NONE', *, *, #198667, .F. ) ;
#160847=CIRCLE ( 'NONE', #152478, 4.049999999999998046 ) ;
#160863=VECTOR ( 'NONE', #67409, 1000.000000000000000 ) ;
#160866=ORIENTED_EDGE ( 'NONE', *, *, #113262, .F. ) ;
#160882=DIRECTION ( 'NONE',  ( 0.000000000000000000, -0.5000000000000016653, 0.8660254037844377084 ) ) ;
#160903=CARTESIAN_POINT ( 'NONE',  ( -20.94999999999999929, 64.40000000001234071, -163.0949042542488883 ) ) ;
#160939=AXIS2_PLACEMENT_3D ( 'NONE', #226029, #85233, #68286 ) ;
#160950=CARTESIAN_POINT ( 'NONE',  ( -21.05000000000000071, 77.16270174995034381, -161.9231074845243370 ) ) ;
#160959=AXIS2_PLACEMENT_3D ( 'NONE', #189468, #9526, #69533 ) ;
#160962=CARTESIAN_POINT ( 'NONE',  ( -18.45068461519106862, 85.48650652910143322, -162.9543303156196146 ) ) ;
#161000=ORIENTED_EDGE ( 'NONE', *, *, #144280, .T. ) ;
#161003=CARTESIAN_POINT ( 'NONE',  ( 21.08479644141223375, 75.94144555744830427, -176.3681461422563075 ) ) ;
#161043=ORIENTED_EDGE ( 'NONE', *, *, #248971, .T. ) ;
#161066=CARTESIAN_POINT ( 'NONE',  ( 23.14999999999999503, 64.35000000001222986, -148.7731074845244450 ) ) ;
#161080=CARTESIAN_POINT ( 'NONE',  ( 22.00356870069842330, 76.00000000001244871, -177.2773498462712496 ) ) ;
#161091=EDGE_CURVE ( 'NONE', #81561, #213031, #3441, .T. ) ;
#161094=AXIS2_PLACEMENT_3D ( 'NONE', #196790, #42867, #122408 ) ;
#161096=FACE_OUTER_BOUND ( 'NONE', #123319, .T. ) ;
#161167=CARTESIAN_POINT ( 'NONE',  ( -21.05000000000000426, 69.52295361822253028, -169.9231074845244507 ) ) ;
#161200=CARTESIAN_POINT ( 'NONE',  ( -18.59999999999999787, 74.14897176987143723, -158.3691942151018850 ) ) ;
#161212=CARTESIAN_POINT ( 'NONE',  ( -20.94999999999999929, 64.35000000001214460, -136.5231074845244166 ) ) ;
#161270=EDGE_CURVE ( 'NONE', #78078, #240241, #252304, .T. ) ;
#161273=CIRCLE ( 'NONE', #190513, 0.09999999999998712696 ) ;
#161280=CYLINDRICAL_SURFACE ( 'NONE', #217104, 11.80000000000000426 ) ;
#161290=VECTOR ( 'NONE', #216042, 1000.000000000000000 ) ;
#161310=PLANE ( 'NONE',  #162062 ) ;
#161332=CIRCLE ( 'NONE', #123913, 0.09999999999999939493 ) ;
#161342=CARTESIAN_POINT ( 'NONE',  ( -23.15000000000000213, 73.50000000001223555, -149.7477294072864709 ) ) ;
#161384=EDGE_LOOP ( 'NONE', ( #37684, #167975, #155934 ) ) ;
#161422=CARTESIAN_POINT ( 'NONE',  ( 18.36493879433253440, 85.50000080620210952, -129.6009588241725226 ) ) ;
#161482=DIRECTION ( 'NONE',  ( 0.000000000000000000, 0.000000000000000000, -1.000000000000000000 ) ) ;
#161510=B_SPLINE_CURVE_WITH_KNOTS ( 'NONE', 3,
 ( #65122, #144651, #224192, #125121 ),
 .UNSPECIFIED., .F., .F.,
 ( 4, 4 ),
 ( 0.000000000000000000, 0.001767853679387121216 ),
 .UNSPECIFIED. ) ;
#161521=CARTESIAN_POINT ( 'NONE',  ( 20.94999999999999929, 70.60000000001221565, -146.4170766071768526 ) ) ;
#161528=VERTEX_POINT ( 'NONE', #1828 ) ;
#161530=CARTESIAN_POINT ( 'NONE',  ( -18.59999999999999787, 66.65000000001222702, -148.7731074845244166 ) ) ;
#161546=DIRECTION ( 'NONE',  ( -1.000000000000000000, -0.000000000000000000, -0.000000000000000000 ) ) ;
#161603=ORIENTED_EDGE ( 'NONE', *, *, #116442, .T. ) ;
#161609=CARTESIAN_POINT ( 'NONE',  ( -23.15000000000000213, 80.83132476063518368, -153.0534105423255653 ) ) ;
#161624=EDGE_LOOP ( 'NONE', ( #255963, #6355, #188492, #250113, #72751 ) ) ;
#161644=ADVANCED_FACE ( 'NONE', ( #241161 ), #48075, .F. ) ;
#161653=DIRECTION ( 'NONE',  ( -1.000000000000000000, 0.000000000000000000, 0.000000000000000000 ) ) ;
#161682=DIRECTION ( 'NONE',  ( -3.469446951953515108E-14, 1.000000000000000000, 0.000000000000000000 ) ) ;
#161694=CARTESIAN_POINT ( 'NONE',  ( 20.94999999999999929, 76.00000000001213607, -136.5231074845243313 ) ) ;
#161742=VERTEX_POINT ( 'NONE', #144594 ) ;
#161748=CARTESIAN_POINT ( 'NONE',  ( -23.25000000000000000, 76.00000000001212186, -134.4231074845243370 ) ) ;
#161774=DIRECTION ( 'NONE',  ( 0.000000000000000000, -1.000000000000000000, -6.982962677686266711E-15 ) ) ;
#161784=EDGE_CURVE ( 'NONE', #55132, #54225, #91059, .T. ) ;
#161793=EDGE_LOOP ( 'NONE', ( #158954, #24495, #117234, #252931 ) ) ;
#161807=CARTESIAN_POINT ( 'NONE',  ( -18.50000000000000000, 74.16465844978787914, -158.4679561919613775 ) ) ;
#161839=ORIENTED_EDGE ( 'NONE', *, *, #98082, .T. ) ;
#161843=DIRECTION ( 'NONE',  ( 1.000000000000000000, 0.000000000000000000, 0.000000000000000000 ) ) ;
#161856=ORIENTED_EDGE ( 'NONE', *, *, #72842, .T. ) ;
#161878=EDGE_CURVE ( 'NONE', #2383, #109875, #80434, .T. ) ;
#161885=ORIENTED_EDGE ( 'NONE', *, *, #192417, .T. ) ;
#161908=AXIS2_PLACEMENT_3D ( 'NONE', #173269, #154963, #190220 ) ;
#161920=CARTESIAN_POINT ( 'NONE',  ( 20.12481660106788439, 66.47365600773738947, -161.7969658154282229 ) ) ;
#161936=VECTOR ( 'NONE', #88797, 1000.000000000000000 ) ;
#161983=AXIS2_PLACEMENT_3D ( 'NONE', #230784, #168269, #172120 ) ;
#161984=DIRECTION ( 'NONE',  ( 1.000000000000000000, 0.000000000000000000, -0.000000000000000000 ) ) ;
#161998=ORIENTED_EDGE ( 'NONE', *, *, #243685, .T. ) ;
#161999=VERTEX_POINT ( 'NONE', #37517 ) ;
#162033=EDGE_LOOP ( 'NONE', ( #124338, #217252, #218084, #190223, #155062, #157780, #250425 ) ) ;
#162034=CARTESIAN_POINT ( 'NONE',  ( -20.00857864376270001, 66.75000000001223555, -148.7731074845244166 ) ) ;
#162052=ORIENTED_EDGE ( 'NONE', *, *, #32872, .T. ) ;
#162062=AXIS2_PLACEMENT_3D ( 'NONE', #102562, #101260, #257767 ) ;
#162081=CIRCLE ( 'NONE', #41291, 0.09999999999998898659 ) ;
#162101=CARTESIAN_POINT ( 'NONE',  ( -18.50000000000000000, 65.70711192142388768, -131.0651054685122574 ) ) ;
#162104=ORIENTED_EDGE ( 'NONE', *, *, #165937, .F. ) ;
#162109=DIRECTION ( 'NONE',  ( 1.000000000000000000, 0.000000000000000000, 0.000000000000000000 ) ) ;
#162116=CARTESIAN_POINT ( 'NONE',  ( -20.54999999999999716, 71.65000000001228386, -157.6731074845243938 ) ) ;
#162118=CARTESIAN_POINT ( 'NONE',  ( 21.00000000000000000, 66.25000000001229239, -157.6731074845244223 ) ) ;
#162138=CARTESIAN_POINT ( 'NONE',  ( 20.95262331984766746, 65.49584273722238947, -162.4622191549311481 ) ) ;
#162140=CARTESIAN_POINT ( 'NONE',  ( -23.15000000000000213, 73.40000000001245439, -181.7731074845243882 ) ) ;
#162143=CARTESIAN_POINT ( 'NONE',  ( -20.64999999999999858, 68.75000000001230660, -157.6731074845243938 ) ) ;
#162145=CARTESIAN_POINT ( 'NONE',  ( -20.54999999999999716, 73.60000000001221565, -146.4170766071768242 ) ) ;
#162188=DIRECTION ( 'NONE',  ( 0.000000000000000000, 6.997203936713175802E-15, -1.000000000000000000 ) ) ;
#162189=EDGE_CURVE ( 'NONE', #206663, #35927, #149462, .T. ) ;
#162199=EDGE_CURVE ( 'NONE', #76100, #106358, #112881, .T. ) ;
#162226=CYLINDRICAL_SURFACE ( 'NONE', #83846, 0.09999999999998898659 ) ;
#162227=CARTESIAN_POINT ( 'NONE',  ( -18.59999999999999787, 74.26374286841490857, -158.4544551555068779 ) ) ;
#162267=DIRECTION ( 'NONE',  ( 0.000000000000000000, 8.896017825522085641E-15, -1.000000000000000000 ) ) ;
#162310=VECTOR ( 'NONE', #22452, 1000.000000000000000 ) ;
#162346=CARTESIAN_POINT ( 'NONE',  ( -21.05000000000000071, 76.25610579210459150, -170.0580039261966192 ) ) ;
#162353=DIRECTION ( 'NONE',  ( 1.000000000000000000, 0.000000000000000000, 0.000000000000000000 ) ) ;
#162414=ADVANCED_FACE ( 'NONE', ( #247907 ), #207906, .F. ) ;
#162423=ORIENTED_EDGE ( 'NONE', *, *, #201371, .F. ) ;
#162443=LINE ( 'NONE', #102409, #19214 ) ;
#162460=CARTESIAN_POINT ( 'NONE',  ( 20.89192007715127986, 65.67101464000523947, -130.9404391622479977 ) ) ;
#162491=LINE ( 'NONE', #3378, #214357 ) ;
#162496=EDGE_LOOP ( 'NONE', ( #247690, #54716, #219326, #47290 ) ) ;
#162507=VECTOR ( 'NONE', #108009, 1000.000000000000000 ) ;
#162518=AXIS2_PLACEMENT_3D ( 'NONE', #103442, #21389, #163446 ) ;
#162532=DIRECTION ( 'NONE',  ( 3.265361837132813093E-16, 1.000000000000000000, 6.982962677686266711E-15 ) ) ;
#162550=DIRECTION ( 'NONE',  ( -0.000000000000000000, -0.1350103645451807555, -0.9908441862701610203 ) ) ;
#162568=CARTESIAN_POINT ( 'NONE',  ( 22.47071067811865319, 68.27992525551434255, -170.1221999392270163 ) ) ;
#162593=EDGE_LOOP ( 'NONE', ( #101945, #30968, #229954, #135810, #148655, #137416, #227698, #46759 ) ) ;
#162623=DIRECTION ( 'NONE',  ( -2.578261006436899437E-14, -0.1350103645451973811, 0.9908441862701586889 ) ) ;
#162682=ORIENTED_EDGE ( 'NONE', *, *, #206567, .T. ) ;
#162701=ADVANCED_FACE ( 'NONE', ( #219041 ), #157845, .F. ) ;
#162703=ADVANCED_FACE ( 'NONE', ( #256840 ), #80804, .T. ) ;
#162716=ADVANCED_FACE ( 'NONE', ( #58674 ), #7984, .T. ) ;
#162719=DIRECTION ( 'NONE',  ( 6.938893903907991995E-14, 0.000000000000000000, -1.000000000000000000 ) ) ;
#162743=EDGE_CURVE ( 'NONE', #170736, #58594, #130709, .T. ) ;
#162751=DIRECTION ( 'NONE',  ( 0.000000000000000000, 6.982962677686266711E-15, -1.000000000000000000 ) ) ;
#162786=DIRECTION ( 'NONE',  ( 0.000000000000000000, 0.8660254037844378194, 0.5000000000000016653 ) ) ;
#162793=CIRCLE ( 'NONE', #195743, 0.09999999999998898659 ) ;
#162815=CARTESIAN_POINT ( 'NONE',  ( 20.96077737575347300, 64.37609936600742344, -143.3823155274180294 ) ) ;
#162820=DIRECTION ( 'NONE',  ( 1.000000000000000000, 0.000000000000000000, 0.000000000000000000 ) ) ;
#162841=EDGE_LOOP ( 'NONE', ( #163045, #249846, #206607, #105874 ) ) ;
#162855=EDGE_LOOP ( 'NONE', ( #32024, #44086, #219528, #159791 ) ) ;
#162856=VERTEX_POINT ( 'NONE', #65111 ) ;
#162857=AXIS2_PLACEMENT_3D ( 'NONE', #220578, #144873, #142308 ) ;
#162913=DIRECTION ( 'NONE',  ( -0.000000000000000000, -6.982962677686266711E-15, 1.000000000000000000 ) ) ;
#162923=FACE_OUTER_BOUND ( 'NONE', #13512, .T. ) ;
#162986=EDGE_CURVE ( 'NONE', #61696, #49587, #78855, .T. ) ;
#162994=DIRECTION ( 'NONE',  ( 0.000000000000000000, -1.000000000000000000, -6.982962677686265922E-15 ) ) ;
#162995=DIRECTION ( 'NONE',  ( 0.000000000000000000, -6.982962677686266711E-15, 1.000000000000000000 ) ) ;
#162999=ORIENTED_EDGE ( 'NONE', *, *, #153415, .T. ) ;
#163008=CARTESIAN_POINT ( 'NONE',  ( -20.54999999999999716, 84.66355140188136374, -146.0472086025916099 ) ) ;
#163041=AXIS2_PLACEMENT_3D ( 'NONE', #23387, #102863, #5042 ) ;
#163045=ORIENTED_EDGE ( 'NONE', *, *, #165140, .F. ) ;
#163046=CARTESIAN_POINT ( 'NONE',  ( 21.14999999999999858, 65.28660755661240955, -157.7731074845244450 ) ) ;
#163058=FACE_OUTER_BOUND ( 'NONE', #88770, .T. ) ;
#163097=ORIENTED_EDGE ( 'NONE', *, *, #112237, .F. ) ;
#163108=ORIENTED_EDGE ( 'NONE', *, *, #250532, .F. ) ;
#163114=VERTEX_POINT ( 'NONE', #199186 ) ;
#163120=CARTESIAN_POINT ( 'NONE',  ( 19.99999999738052026, 64.25000000001219291, -145.3359355348916040 ) ) ;
#163144=DIRECTION ( 'NONE',  ( 0.000000000000000000, 1.000000000000000000, 0.000000000000000000 ) ) ;
#163164=CIRCLE ( 'NONE', #75676, 0.09999999999999939493 ) ;
#163177=CIRCLE ( 'NONE', #246540, 0.1000000000000028644 ) ;
#163184=FACE_OUTER_BOUND ( 'NONE', #165933, .T. ) ;
#163192=ADVANCED_FACE ( 'NONE', ( #105162 ), #26989, .F. ) ;
#163201=VECTOR ( 'NONE', #44547, 1000.000000000000000 ) ;
#163202=CARTESIAN_POINT ( 'NONE',  ( 23.15000000000000213, 87.75000000001229239, -157.7731074845242745 ) ) ;
#163203=CARTESIAN_POINT ( 'NONE',  ( 23.15000000000000213, 85.00000000001232081, -160.1291383618718385 ) ) ;
#163300=CARTESIAN_POINT ( 'NONE',  ( -21.45000000000000284, 68.29142135624952914, -148.7731074845244166 ) ) ;
#163305=CARTESIAN_POINT ( 'NONE',  ( -21.14999999999999858, 69.45934304831114048, -170.0231074845243882 ) ) ;
#163306=CARTESIAN_POINT ( 'NONE',  ( -20.85000000000000142, 68.97833521811203639, -132.6895420826271277 ) ) ;
#163320=CARTESIAN_POINT ( 'NONE',  ( 21.09546886439534674, 67.12144688699737571, -157.7860136339689916 ) ) ;
#163331=ORIENTED_EDGE ( 'NONE', *, *, #97295, .F. ) ;
#163346=ORIENTED_EDGE ( 'NONE', *, *, #88699, .F. ) ;
#163368=DIRECTION ( 'NONE',  ( 1.000000000000000000, 0.000000000000000000, 0.000000000000000000 ) ) ;
#163373=CARTESIAN_POINT ( 'NONE',  ( -18.56579813702275672, 65.66974365629688748, -130.9360145562605169 ) ) ;
#163411=FACE_OUTER_BOUND ( 'NONE', #32011, .T. ) ;
#163433=CARTESIAN_POINT ( 'NONE',  ( -22.57320508075687115, 64.35000000001238618, -170.0231074845243882 ) ) ;
#163446=DIRECTION ( 'NONE',  ( 0.000000000000000000, -6.547589603894034005E-15, 1.000000000000000000 ) ) ;
#163463=EDGE_CURVE ( 'NONE', #28696, #38071, #187408, .T. ) ;
#163478=CARTESIAN_POINT ( 'NONE',  ( 21.05000000000000071, 64.40000000001218439, -143.4513107147999449 ) ) ;
#163541=ORIENTED_EDGE ( 'NONE', *, *, #75946, .F. ) ;
#163568=ORIENTED_EDGE ( 'NONE', *, *, #84867, .T. ) ;
#163569=CARTESIAN_POINT ( 'NONE',  ( -18.59999999999999787, 77.36242903720540198, -128.6342262366031548 ) ) ;
#163664=ORIENTED_EDGE ( 'NONE', *, *, #1653, .F. ) ;
#163714=AXIS2_PLACEMENT_3D ( 'NONE', #86242, #161984, #26306 ) ;
#163735=CARTESIAN_POINT ( 'NONE',  ( 20.85882249326303040, 65.66751761918692409, -130.9282609406112670 ) ) ;
#163740=ORIENTED_EDGE ( 'NONE', *, *, #214990, .F. ) ;
#163741=EDGE_LOOP ( 'NONE', ( #244656, #58150, #191908, #22298, #65215, #27009, #8893, #61770, #200232, #31714, #215871, #103236, #179568, #155389, #55601, #254959 ) ) ;
#163751=ORIENTED_EDGE ( 'NONE', *, *, #83939, .T. ) ;
#163775=ORIENTED_EDGE ( 'NONE', *, *, #164804, .F. ) ;
#163831=AXIS2_PLACEMENT_3D ( 'NONE', #92211, #12716, #70124 ) ;
#163928=ORIENTED_EDGE ( 'NONE', *, *, #232307, .F. ) ;
#163936=LINE ( 'NONE', #160104, #39791 ) ;
#163968=ORIENTED_EDGE ( 'NONE', *, *, #195071, .T. ) ;
#163972=AXIS2_PLACEMENT_3D ( 'NONE', #62924, #43370, #120369 ) ;
#163977=ADVANCED_FACE ( 'NONE', ( #105866 ), #219402, .F. ) ;
#164003=CARTESIAN_POINT ( 'NONE',  ( -20.00857864376270001, 66.85000000001228670, -157.6731074845244223 ) ) ;
#164015=DIRECTION ( 'NONE',  ( -0.7071067811865475727, 0.7071067811865475727, 4.937700262164531476E-15 ) ) ;
#164026=FACE_OUTER_BOUND ( 'NONE', #233031, .T. ) ;
#164033=ORIENTED_EDGE ( 'NONE', *, *, #97102, .T. ) ;
#164039=DIRECTION ( 'NONE',  ( -1.000000000000000000, -0.000000000000000000, -0.000000000000000000 ) ) ;
#164051=ORIENTED_EDGE ( 'NONE', *, *, #197105, .T. ) ;
#164075=CARTESIAN_POINT ( 'NONE',  ( 18.59999999999999076, 68.87972903831452243, -132.8635444426850825 ) ) ;
#164079=DIRECTION ( 'NONE',  ( -0.7070776581708965169, 0.7071359030027827286, 4.937903618720407826E-15 ) ) ;
#164118=CIRCLE ( 'NONE', #151664, 0.1000000000000033362 ) ;
#164125=DIRECTION ( 'NONE',  ( 1.000000000000000000, 0.000000000000000000, 0.000000000000000000 ) ) ;
#164146=CIRCLE ( 'NONE', #51666, 0.09999999999999938105 ) ;
#164160=CIRCLE ( 'NONE', #51687, 0.09999999999998898659 ) ;
#164162=CARTESIAN_POINT ( 'NONE',  ( 22.50000000000000000, 75.90000000001245439, -181.6726782920691505 ) ) ;
#164163=ADVANCED_FACE ( 'NONE', ( #140519 ), #80527, .F. ) ;
#164165=EDGE_LOOP ( 'NONE', ( #25409, #112264, #156444, #239699 ) ) ;
#164239=CIRCLE ( 'NONE', #1884, 0.09999999999999939493 ) ;
#164255=CARTESIAN_POINT ( 'NONE',  ( 18.49999999999998934, 69.35000000001228670, -157.6731074845243938 ) ) ;
#164268=VERTEX_POINT ( 'NONE', #86946 ) ;
#164271=SPHERICAL_SURFACE ( 'NONE', #130166, 0.1000000000000000056 ) ;
#164311=ORIENTED_EDGE ( 'NONE', *, *, #3323, .F. ) ;
#164359=CARTESIAN_POINT ( 'NONE',  ( -23.25000000000000000, 77.14957036958777792, -128.7071950000224092 ) ) ;
#164393=CARTESIAN_POINT ( 'NONE',  ( 19.86930884467584590, 64.31308993304128307, -145.2838848455857317 ) ) ;
#164396=CARTESIAN_POINT ( 'NONE',  ( 23.14999999999999503, 64.35000000001245724, -181.7731074845244450 ) ) ;
#164411=CARTESIAN_POINT ( 'NONE',  ( -18.59999999999999787, 76.00000000001213607, -136.5231074845243313 ) ) ;
#164416=CARTESIAN_POINT ( 'NONE',  ( 20.95429402530550433, 67.12380584891013768, -161.5000207865867026 ) ) ;
#164425=VECTOR ( 'NONE', #207435, 1000.000000000000000 ) ;
#164426=ORIENTED_EDGE ( 'NONE', *, *, #9600, .T. ) ;
#164434=VECTOR ( 'NONE', #21805, 1000.000000000000000 ) ;
#164439=CARTESIAN_POINT ( 'NONE',  ( 21.97500000000000497, 66.25000000001223555, -148.7731074845244450 ) ) ;
#164449=EDGE_CURVE ( 'NONE', #24875, #134102, #171419, .T. ) ;
#164469=ORIENTED_EDGE ( 'NONE', *, *, #228610, .T. ) ;
#164482=DIRECTION ( 'NONE',  ( 1.000000000000000000, 0.000000000000000000, 0.000000000000000000 ) ) ;
#164498=VERTEX_POINT ( 'NONE', #179374 ) ;
#164508=EDGE_CURVE ( 'NONE', #184497, #18470, #167137, .T. ) ;
#164553=VERTEX_POINT ( 'NONE', #17695 ) ;
#164565=CARTESIAN_POINT ( 'NONE',  ( 21.05000000000000071, 71.14953271029267512, -157.9888400755227167 ) ) ;
#164567=CARTESIAN_POINT ( 'NONE',  ( -22.59999999999999787, 76.00000000001237765, -170.0231074845243597 ) ) ;
#164574=CARTESIAN_POINT ( 'NONE',  ( -20.64999999999999858, 85.00000000001222134, -146.4170766071767389 ) ) ;
#164575=EDGE_LOOP ( 'NONE', ( #89757, #48606, #75220, #63369 ) ) ;
#164579=ADVANCED_FACE ( 'NONE', ( #78936 ), #1981, .T. ) ;
#164613=CYLINDRICAL_SURFACE ( 'NONE', #188952, 0.09999999999998898659 ) ;
#164673=AXIS2_PLACEMENT_3D ( 'NONE', #36395, #196715, #115912 ) ;
#164681=ADVANCED_FACE ( 'NONE', ( #103640 ), #184475, .T. ) ;
#164715=CARTESIAN_POINT ( 'NONE',  ( 21.05000000000000071, 85.00000000001232081, -160.1291383618718385 ) ) ;
#164717=ORIENTED_EDGE ( 'NONE', *, *, #247730, .F. ) ;
#164753=ORIENTED_EDGE ( 'NONE', *, *, #222955, .T. ) ;
#164801=CARTESIAN_POINT ( 'NONE',  ( 20.94999999999999929, 76.00000000001237765, -170.0231074845243597 ) ) ;
#164804=EDGE_CURVE ( 'NONE', #230504, #994, #84024, .T. ) ;
#164854=DIRECTION ( 'NONE',  ( 1.000000000000000000, 0.000000000000000000, 0.000000000000000000 ) ) ;
#164881=AXIS2_PLACEMENT_3D ( 'NONE', #43212, #186587, #203566 ) ;
#164884=ORIENTED_EDGE ( 'NONE', *, *, #236932, .T. ) ;
#164910=ORIENTED_EDGE ( 'NONE', *, *, #186226, .F. ) ;
#164913=EDGE_CURVE ( 'NONE', #77760, #75529, #221859, .T. ) ;
#164925=CARTESIAN_POINT ( 'NONE',  ( 18.59999999999999432, 70.30054753569086756, -182.5653814410942459 ) ) ;
#164930=CARTESIAN_POINT ( 'NONE',  ( 20.94999999999999574, 65.52661458509942349, -162.4444530202758870 ) ) ;
#164943=FACE_OUTER_BOUND ( 'NONE', #195734, .T. ) ;
#164957=CARTESIAN_POINT ( 'NONE',  ( -20.54999999999999361, 64.35000000001222986, -148.6731074845244507 ) ) ;
#164977=EDGE_LOOP ( 'NONE', ( #220494, #193312, #131463, #106131 ) ) ;
#164983=ORIENTED_EDGE ( 'NONE', *, *, #196914, .F. ) ;
#165005=FACE_OUTER_BOUND ( 'NONE', #93327, .T. ) ;
#165010=FACE_OUTER_BOUND ( 'NONE', #27726, .T. ) ;
#165056=CIRCLE ( 'NONE', #85718, 11.74999999999999645 ) ;
#165063=CARTESIAN_POINT ( 'NONE',  ( -18.50000000000000000, 74.83729825007431202, -161.9231074845243654 ) ) ;
#165065=VECTOR ( 'NONE', #113874, 1000.000000000000000 ) ;
#165077=ORIENTED_EDGE ( 'NONE', *, *, #73665, .T. ) ;
#165081=EDGE_CURVE ( 'NONE', #110495, #42521, #34224, .T. ) ;
#165108=EDGE_CURVE ( 'NONE', #99384, #127304, #38470, .T. ) ;
#165140=EDGE_CURVE ( 'NONE', #55132, #128766, #246567, .T. ) ;
#165168=CARTESIAN_POINT ( 'NONE',  ( 18.41416235934317669, 85.50000000001209344, -129.9229180933022860 ) ) ;
#165217=ORIENTED_EDGE ( 'NONE', *, *, #12872, .F. ) ;
#165225=CARTESIAN_POINT ( 'NONE',  ( -23.15000000000000213, 87.65000000001215597, -139.6231074845242688 ) ) ;
#165258=ADVANCED_FACE ( 'NONE', ( #130643 ), #134473, .F. ) ;
#165260=DIRECTION ( 'NONE',  ( 1.000000000000000000, 0.000000000000000000, 0.000000000000000000 ) ) ;
#165328=ORIENTED_EDGE ( 'NONE', *, *, #231874, .F. ) ;
#165335=EDGE_CURVE ( 'NONE', #66273, #141610, #109180, .T. ) ;
#165339=VERTEX_POINT ( 'NONE', #199634 ) ;
#165342=FACE_OUTER_BOUND ( 'NONE', #43949, .T. ) ;
#165373=DIRECTION ( 'NONE',  ( -1.000000000000000000, -0.000000000000000000, -0.000000000000000000 ) ) ;
#165411=ORIENTED_EDGE ( 'NONE', *, *, #10517, .T. ) ;
#165428=TOROIDAL_SURFACE ( 'NONE', #219557, 0.2000000000000000111, 0.1000000000000000056 ) ;
#165535=AXIS2_PLACEMENT_3D ( 'NONE', #180225, #257126, #158127 ) ;
#165559=EDGE_LOOP ( 'NONE', ( #115852, #145781, #167894, #79907 ) ) ;
#165566=CARTESIAN_POINT ( 'NONE',  ( -18.59999999999999787, 74.13328508995498112, -158.2704322382423641 ) ) ;
#165571=CARTESIAN_POINT ( 'NONE',  ( -20.64999999999999858, 85.00000000001232081, -160.6291383618718385 ) ) ;
#165645=EDGE_LOOP ( 'NONE', ( #109107, #93116, #136355 ) ) ;
#165659=ORIENTED_EDGE ( 'NONE', *, *, #222109, .T. ) ;
#165711=FACE_OUTER_BOUND ( 'NONE', #233346, .T. ) ;
#165715=CARTESIAN_POINT ( 'NONE',  ( 21.05000000000000071, 67.12338541492520960, -161.6380270056797599 ) ) ;
#165732=DIRECTION ( 'NONE',  ( -1.000000000000000000, -0.000000000000000000, -0.000000000000000000 ) ) ;
#165746=CIRCLE ( 'NONE', #182293, 0.4000000000000114575 ) ;
#165764=CARTESIAN_POINT ( 'NONE',  ( -20.85000000000000142, 76.00000000001213607, -136.5231074845243313 ) ) ;
#165779=DIRECTION ( 'NONE',  ( -3.890533409366484652E-14, 0.1298341882520054891, 0.9915357197604850459 ) ) ;
#165817=DIRECTION ( 'NONE',  ( 0.000000000000000000, 0.000000000000000000, 1.000000000000000000 ) ) ;
#165825=VERTEX_POINT ( 'NONE', #87985 ) ;
#165858=DIRECTION ( 'NONE',  ( 1.000000000000000000, 0.000000000000000000, 0.000000000000000000 ) ) ;
#165865=PLANE ( 'NONE',  #42345 ) ;
#165884=VECTOR ( 'NONE', #186856, 1000.000000000000000 ) ;
#165901=CARTESIAN_POINT ( 'NONE',  ( 19.97071067811865319, 64.27928932189354327, -145.3145288407617386 ) ) ;
#165914=CARTESIAN_POINT ( 'NONE',  ( 20.85000000000000142, 76.00000000001213607, -136.5231074845243313 ) ) ;
#165918=AXIS2_PLACEMENT_3D ( 'NONE', #53125, #234324, #115675 ) ;
#165933=EDGE_LOOP ( 'NONE', ( #9063, #137690, #17517, #28108 ) ) ;
#165934=CIRCLE ( 'NONE', #232583, 0.09999999999998898659 ) ;
#165937=EDGE_CURVE ( 'NONE', #120222, #58764, #176229, .T. ) ;
#165972=EDGE_CURVE ( 'NONE', #15940, #108252, #242844, .T. ) ;
#165973=B_SPLINE_CURVE_WITH_KNOTS ( 'NONE', 3,
 ( #42486, #43782, #125870, #102430, #185854, #7202, #161167, #3344 ),
 .UNSPECIFIED., .F., .F.,
 ( 4, 2, 2, 4 ),
 ( 0.000000000000000000, 9.550056980125360177E-05, 0.0001910011396025072035, 0.0003820022792049716353 ),
 .UNSPECIFIED. ) ;
#166007=CARTESIAN_POINT ( 'NONE',  ( -23.15000000000000213, 64.25000000001222134, -148.6731074845244507 ) ) ;
#166013=B_SPLINE_CURVE_WITH_KNOTS ( 'NONE', 3,
 ( #230915, #87509, #32736, #130497, #170972, #186646, #228334, #107083, #225729, #71838, #28892, #30146, #191797, #112247, #67964, #31446, #168404, #129229, #9274 ),
 .UNSPECIFIED., .F., .F.,
 ( 4, 3, 3, 3, 3, 3, 4 ),
 ( 0.000000000000000000, 7.110282409889357531E-05, 0.0001508797727291297914, 0.0002027344179858282824, 0.0002343294522349063957, 0.0002454816334821210652, 0.0002619873080085486088 ),
 .UNSPECIFIED. ) ;
#166020=FACE_OUTER_BOUND ( 'NONE', #183692, .T. ) ;
#166025=VERTEX_POINT ( 'NONE', #63001 ) ;
#166027=VECTOR ( 'NONE', #191157, 1000.000000000000000 ) ;
#166031=DIRECTION ( 'NONE',  ( 0.000000000000000000, 0.8660254037844377084, 0.5000000000000016653 ) ) ;
#166044=FACE_OUTER_BOUND ( 'NONE', #12769, .T. ) ;
#166046=CARTESIAN_POINT ( 'NONE',  ( -20.97625342178412566, 64.39999999919187701, -163.0949042547225645 ) ) ;
#166053=TOROIDAL_SURFACE ( 'NONE', #12115, 0.2000000000000000111, 0.1000000000000000056 ) ;
#166072=EDGE_CURVE ( 'NONE', #146933, #167205, #113849, .T. ) ;
#166107=CARTESIAN_POINT ( 'NONE',  ( 21.05000000000000071, 76.10000000001241460, -176.5637644362255969 ) ) ;
#166124=AXIS2_PLACEMENT_3D ( 'NONE', #40963, #98295, #162188 ) ;
#166200=AXIS2_PLACEMENT_3D ( 'NONE', #39173, #118704, #198213 ) ;
#166204=ORIENTED_EDGE ( 'NONE', *, *, #16147, .T. ) ;
#166218=ORIENTED_EDGE ( 'NONE', *, *, #28442, .F. ) ;
#166221=AXIS2_PLACEMENT_3D ( 'NONE', #140807, #156552, #79522 ) ;
#166232=ADVANCED_FACE ( 'NONE', ( #206379 ), #27770, .T. ) ;
#166289=DIRECTION ( 'NONE',  ( 0.000000000000000000, -0.9654727137038715545, 0.2605042016806676242 ) ) ;
#166304=AXIS2_PLACEMENT_3D ( 'NONE', #193593, #114035, #170230 ) ;
#166314=EDGE_CURVE ( 'NONE', #23846, #128626, #117562, .T. ) ;
#166321=EDGE_CURVE ( 'NONE', #148976, #65207, #71794, .T. ) ;
#166343=CYLINDRICAL_SURFACE ( 'NONE', #31054, 0.5000000000000004441 ) ;
#166352=CIRCLE ( 'NONE', #37341, 0.09999999999999971412 ) ;
#166365=EDGE_LOOP ( 'NONE', ( #38531, #32567, #97887 ) ) ;
#166387=CARTESIAN_POINT ( 'NONE',  ( 18.55857864376268296, 65.63284271248683410, -145.2731074845244450 ) ) ;
#166396=DIRECTION ( 'NONE',  ( -0.000000000000000000, 1.000000000000000000, 6.352154140967427193E-15 ) ) ;
#166404=CARTESIAN_POINT ( 'NONE',  ( 20.85000000000000142, 77.26327546522934142, -128.6212428177779543 ) ) ;
#166409=ORIENTED_EDGE ( 'NONE', *, *, #203595, .T. ) ;
#166450=AXIS2_PLACEMENT_3D ( 'NONE', #19096, #98593, #79047 ) ;
#166518=DIRECTION ( 'NONE',  ( 2.952720810173289112E-16, 1.000000000000000000, 7.086529944415894657E-15 ) ) ;
#166544=CARTESIAN_POINT ( 'NONE',  ( 21.14999999999999503, 64.25000000001237765, -170.0231074845244166 ) ) ;
#166558=DIRECTION ( 'NONE',  ( 0.000000000000000000, 0.000000000000000000, 1.000000000000000000 ) ) ;
#166592=DIRECTION ( 'NONE',  ( 0.000000000000000000, -7.272083257015735086E-15, 1.000000000000000000 ) ) ;
#166595=CARTESIAN_POINT ( 'NONE',  ( 18.43565242384934066, 85.51932773110476660, -163.0501311079649724 ) ) ;
#166600=AXIS2_PLACEMENT_3D ( 'NONE', #173262, #50666, #209774 ) ;
#166604=CARTESIAN_POINT ( 'NONE',  ( -21.59142135623730852, 68.15000000001222702, -148.8731074845244393 ) ) ;
#166625=DIRECTION ( 'NONE',  ( 0.000000000000000000, 0.000000000000000000, -1.000000000000000000 ) ) ;
#166629=AXIS2_PLACEMENT_3D ( 'NONE', #187869, #112183, #13084 ) ;
#166735=AXIS2_PLACEMENT_3D ( 'NONE', #157363, #175624, #79043 ) ;
#166748=CARTESIAN_POINT ( 'NONE',  ( 20.97250901189795513, 65.37543196631044395, -162.3585617675574326 ) ) ;
#166758=CARTESIAN_POINT ( 'NONE',  ( 22.39999999999999503, 76.00000000001246292, -181.6726782920691505 ) ) ;
#166770=ORIENTED_EDGE ( 'NONE', *, *, #122796, .T. ) ;
#166787=DIRECTION ( 'NONE',  ( -0.000000000000000000, 0.4791956752371485107, 0.8777080977375185666 ) ) ;
#166809=ORIENTED_EDGE ( 'NONE', *, *, #98752, .F. ) ;
#166812=CIRCLE ( 'NONE', #233439, 0.4000000000000114575 ) ;
#166813=VECTOR ( 'NONE', #190814, 1000.000000000000000 ) ;
#166820=VERTEX_POINT ( 'NONE', #251618 ) ;
#166839=ORIENTED_EDGE ( 'NONE', *, *, #201949, .F. ) ;
#166856=DIRECTION ( 'NONE',  ( 0.000000000000000000, -1.000000000000000000, -7.272083257015735086E-15 ) ) ;
#166889=CARTESIAN_POINT ( 'NONE',  ( -23.25000000000000000, 76.00000000001240608, -174.1731074845243654 ) ) ;
#166909=EDGE_CURVE ( 'NONE', #55547, #165825, #237195, .T. ) ;
#166919=ORIENTED_EDGE ( 'NONE', *, *, #192417, .F. ) ;
#166941=FACE_OUTER_BOUND ( 'NONE', #157868, .T. ) ;
#166985=ORIENTED_EDGE ( 'NONE', *, *, #74370, .F. ) ;
#166993=CARTESIAN_POINT ( 'NONE',  ( 19.75857864376269291, 64.35000000001220144, -145.2731074845244166 ) ) ;
#167009=ORIENTED_EDGE ( 'NONE', *, *, #171731, .F. ) ;
#167013=CARTESIAN_POINT ( 'NONE',  ( -20.64999999999999858, 74.00000000001229239, -156.7984855617622770 ) ) ;
#167034=DIRECTION ( 'NONE',  ( -1.000000000000000000, 0.000000000000000000, -0.000000000000000000 ) ) ;
#167041=DIRECTION ( 'NONE',  ( 1.000000000000000000, 0.000000000000000000, 0.000000000000000000 ) ) ;
#167052=DIRECTION ( 'NONE',  ( 0.000000000000000000, -1.756682000989173806E-15, 1.000000000000000000 ) ) ;
#167055=ORIENTED_EDGE ( 'NONE', *, *, #92457, .F. ) ;
#167063=VERTEX_POINT ( 'NONE', #123666 ) ;
#167067=CARTESIAN_POINT ( 'NONE',  ( 21.14999999999999503, 76.10000000001245724, -181.6726782920691505 ) ) ;
#167090=AXIS2_PLACEMENT_3D ( 'NONE', #37251, #97152, #183179 ) ;
#167092=CIRCLE ( 'NONE', #33830, 12.97499999999998721 ) ;
#167098=DIRECTION ( 'NONE',  ( -1.000000000000000000, 2.952720810173289112E-16, 2.061873921506763405E-30 ) ) ;
#167125=ORIENTED_EDGE ( 'NONE', *, *, #240476, .T. ) ;
#167137=CIRCLE ( 'NONE', #13172, 0.09999999999998898659 ) ;
#167185=CARTESIAN_POINT ( 'NONE',  ( 21.14999999999999858, 64.35000000001228670, -157.8731074845244393 ) ) ;
#167194=CARTESIAN_POINT ( 'NONE',  ( -20.64999999999999858, 84.73084112150753811, -146.1211822035086243 ) ) ;
#167197=ORIENTED_EDGE ( 'NONE', *, *, #42809, .T. ) ;
#167205=VERTEX_POINT ( 'NONE', #191366 ) ;
#167212=EDGE_CURVE ( 'NONE', #138584, #203751, #151753, .T. ) ;
#167222=EDGE_CURVE ( 'NONE', #46071, #52417, #222416, .T. ) ;
#167286=CARTESIAN_POINT ( 'NONE',  ( 21.14999999999999858, 65.28660755661240955, -157.6731074845244223 ) ) ;
#167298=ORIENTED_EDGE ( 'NONE', *, *, #247209, .T. ) ;
#167326=CIRCLE ( 'NONE', #138242, 11.89999999999999325 ) ;
#167360=DIRECTION ( 'NONE',  ( 1.000000000000000000, 0.000000000000000000, 0.000000000000000000 ) ) ;
#167369=FACE_OUTER_BOUND ( 'NONE', #78430, .T. ) ;
#167371=ADVANCED_FACE ( 'NONE', ( #238148 ), #59483, .F. ) ;
#167372=CARTESIAN_POINT ( 'NONE',  ( 21.05000000000000071, 69.35000000001231513, -160.1792853948412869 ) ) ;
#167384=VERTEX_POINT ( 'NONE', #214742 ) ;
#167399=CARTESIAN_POINT ( 'NONE',  ( 22.39999999999999147, 68.20922040163900135, -170.0231074845244166 ) ) ;
#167404=ORIENTED_EDGE ( 'NONE', *, *, #205034, .F. ) ;
#167430=EDGE_CURVE ( 'NONE', #253904, #71080, #184269, .T. ) ;
#167454=EDGE_CURVE ( 'NONE', #223317, #140520, #202878, .T. ) ;
#167455=ORIENTED_EDGE ( 'NONE', *, *, #222109, .F. ) ;
#167498=AXIS2_PLACEMENT_3D ( 'NONE', #138153, #1207, #237284 ) ;
#167524=EDGE_LOOP ( 'NONE', ( #43364, #6795 ) ) ;
#167533=AXIS2_PLACEMENT_3D ( 'NONE', #226694, #126313, #32393 ) ;
#167567=EDGE_CURVE ( 'NONE', #35976, #150904, #193599, .T. ) ;
#167598=CARTESIAN_POINT ( 'NONE',  ( -20.94560253601877164, 64.25000000001220712, -143.5130239720093925 ) ) ;
#167622=CARTESIAN_POINT ( 'NONE',  ( 21.05000000000000071, 64.40000000001218439, -143.4513107147999165 ) ) ;
#167627=DIRECTION ( 'NONE',  ( 0.000000000000000000, -1.000000000000000000, -6.982962677686266711E-15 ) ) ;
#167670=AXIS2_PLACEMENT_3D ( 'NONE', #144227, #29474, #67276 ) ;
#167679=CARTESIAN_POINT ( 'NONE',  ( -21.44999999999999929, 68.65000000001222702, -148.8731074845244109 ) ) ;
#167685=EDGE_CURVE ( 'NONE', #178841, #99053, #5369, .T. ) ;
#167686=ORIENTED_EDGE ( 'NONE', *, *, #146269, .T. ) ;
#167709=VECTOR ( 'NONE', #248410, 1000.000000000000000 ) ;
#167711=FACE_OUTER_BOUND ( 'NONE', #240871, .T. ) ;
#167712=CARTESIAN_POINT ( 'NONE',  ( -20.85000000000000142, 87.75000000001215028, -136.5231074845242745 ) ) ;
#167733=EDGE_CURVE ( 'NONE', #56292, #62202, #38176, .T. ) ;
#167751=ORIENTED_EDGE ( 'NONE', *, *, #89371, .F. ) ;
#167775=CARTESIAN_POINT ( 'NONE',  ( -21.64999999999999858, 68.75000000001230660, -157.7731074845244166 ) ) ;
#167781=CIRCLE ( 'NONE', #51200, 0.09999999999998898659 ) ;
#167798=EDGE_LOOP ( 'NONE', ( #212425, #210777, #131419, #155431 ) ) ;
#167800=DIRECTION ( 'NONE',  ( 1.000000000000000000, 0.000000000000000000, 0.000000000000000000 ) ) ;
#167816=AXIS2_PLACEMENT_3D ( 'NONE', #217585, #74286, #153842 ) ;
#167846=DIRECTION ( 'NONE',  ( -1.000000000000000000, -0.000000000000000000, -0.000000000000000000 ) ) ;
#167858=CIRCLE ( 'NONE', #130415, 0.09999999999998712696 ) ;
#167881=DIRECTION ( 'NONE',  ( 0.000000000000000000, -6.982962677686266711E-15, 1.000000000000000000 ) ) ;
#167894=ORIENTED_EDGE ( 'NONE', *, *, #189723, .F. ) ;
#167912=DIRECTION ( 'NONE',  ( -1.000000000000000000, -0.000000000000000000, -0.000000000000000000 ) ) ;
#167937=CYLINDRICAL_SURFACE ( 'NONE', #5855, 0.5000000000000004441 ) ;
#167938=EDGE_LOOP ( 'NONE', ( #195319, #214327, #163097 ) ) ;
#167942=CARTESIAN_POINT ( 'NONE',  ( 21.76363531954645936, 68.98706345214066005, -170.1221093588238489 ) ) ;
#167943=DIRECTION ( 'NONE',  ( -1.000000000000000000, -0.000000000000000000, -0.000000000000000000 ) ) ;
#167959=VERTEX_POINT ( 'NONE', #212551 ) ;
#167975=ORIENTED_EDGE ( 'NONE', *, *, #85638, .F. ) ;
#168004=VERTEX_POINT ( 'NONE', #255458 ) ;
#168015=CARTESIAN_POINT ( 'NONE',  ( 18.39999999999999858, 85.50000000001233502, -162.9910380878246201 ) ) ;
#168019=DIRECTION ( 'NONE',  ( 0.000000000000000000, 0.000000000000000000, -1.000000000000000000 ) ) ;
#168046=CARTESIAN_POINT ( 'NONE',  ( 22.47809213839789066, 75.96246293238394287, -181.6730808193121618 ) ) ;
#168050=DIRECTION ( 'NONE',  ( 1.000000000000000000, 0.000000000000000000, 0.000000000000000000 ) ) ;
#168088=ORIENTED_EDGE ( 'NONE', *, *, #102492, .T. ) ;
#168089=ORIENTED_EDGE ( 'NONE', *, *, #236088, .T. ) ;
#168109=AXIS2_PLACEMENT_3D ( 'NONE', #257246, #78645, #198605 ) ;
#168139=FACE_OUTER_BOUND ( 'NONE', #23952, .T. ) ;
#168161=DIRECTION ( 'NONE',  ( 0.000000000000000000, 0.000000000000000000, -1.000000000000000000 ) ) ;
#168163=AXIS2_PLACEMENT_3D ( 'NONE', #242812, #240269, #101993 ) ;
#168211=ORIENTED_EDGE ( 'NONE', *, *, #245827, .T. ) ;
#168221=VERTEX_POINT ( 'NONE', #27205 ) ;
#168233=VERTEX_POINT ( 'NONE', #87126 ) ;
#168248=CIRCLE ( 'NONE', #89088, 0.09999999999998898659 ) ;
#168249=EDGE_LOOP ( 'NONE', ( #230279, #193565, #36289, #199557 ) ) ;
#168255=ORIENTED_EDGE ( 'NONE', *, *, #240476, .F. ) ;
#168267=CIRCLE ( 'NONE', #238970, 0.09999999999999939493 ) ;
#168269=DIRECTION ( 'NONE',  ( -1.000000000000000000, 2.952720810173289112E-16, 2.061873921506763405E-30 ) ) ;
#168286=DIRECTION ( 'NONE',  ( 1.000000000000000000, 0.000000000000000000, 0.000000000000000000 ) ) ;
#168308=ORIENTED_EDGE ( 'NONE', *, *, #234533, .F. ) ;
#168329=EDGE_CURVE ( 'NONE', #3474, #140520, #229873, .T. ) ;
#168332=FACE_OUTER_BOUND ( 'NONE', #150853, .T. ) ;
#168363=EDGE_LOOP ( 'NONE', ( #102508, #64618, #184430, #236980 ) ) ;
#168369=ADVANCED_FACE ( 'NONE', ( #31059 ), #135236, .F. ) ;
#168376=ORIENTED_EDGE ( 'NONE', *, *, #182057, .F. ) ;
#168404=CARTESIAN_POINT ( 'NONE',  ( 21.07971444708685738, 69.67020791838582738, -170.1109309208423213 ) ) ;
#168421=VERTEX_POINT ( 'NONE', #233098 ) ;
#168451=EDGE_LOOP ( 'NONE', ( #79578, #153120, #38291, #188099, #172964 ) ) ;
#168458=DIRECTION ( 'NONE',  ( 1.000000000000000000, -3.265361837132813093E-16, -2.280189983783949500E-30 ) ) ;
#168466=ORIENTED_EDGE ( 'NONE', *, *, #167212, .F. ) ;
#168468=CIRCLE ( 'NONE', #197613, 0.1000000000000026007 ) ;
#168477=LINE ( 'NONE', #207569, #34952 ) ;
#168483=CARTESIAN_POINT ( 'NONE',  ( -21.07954640115405809, 69.67071230398747161, -170.0891151916640922 ) ) ;
#168484=DIRECTION ( 'NONE',  ( 0.000000000000000000, -0.8660254037844377084, -0.5000000000000016653 ) ) ;
#168514=VECTOR ( 'NONE', #247495, 1000.000000000000000 ) ;
#168517=ORIENTED_EDGE ( 'NONE', *, *, #217126, .F. ) ;
#168523=VERTEX_POINT ( 'NONE', #102507 ) ;
#168525=ORIENTED_EDGE ( 'NONE', *, *, #155855, .F. ) ;
#168529=DIRECTION ( 'NONE',  ( -1.000000000000000000, 0.000000000000000000, 0.000000000000000000 ) ) ;
#168533=EDGE_LOOP ( 'NONE', ( #88011, #150898, #114924, #176160 ) ) ;
#168565=AXIS2_PLACEMENT_3D ( 'NONE', #16651, #257756, #153636 ) ;
#168588=CARTESIAN_POINT ( 'NONE',  ( -21.14999999999999858, 69.45934304831114048, -170.0231074845243882 ) ) ;
#168592=DIRECTION ( 'NONE',  ( -0.9880948137434723000, -0.1538461538461483591, -1.074301950413233512E-15 ) ) ;
#168595=LINE ( 'NONE', #69462, #199396 ) ;
#168623=ORIENTED_EDGE ( 'NONE', *, *, #105570, .F. ) ;
#168646=CARTESIAN_POINT ( 'NONE',  ( -22.39999999999999858, 76.10085836911117951, -181.7726746080137445 ) ) ;
#168668=CARTESIAN_POINT ( 'NONE',  ( 22.39999999999999503, 75.90000000001242597, -177.8138870828977360 ) ) ;
#168686=CIRCLE ( 'NONE', #31298, 12.87499999999999822 ) ;
#168702=DIRECTION ( 'NONE',  ( 0.000000000000000000, 6.982962677686266711E-15, -1.000000000000000000 ) ) ;
#168706=AXIS2_PLACEMENT_3D ( 'NONE', #59526, #58263, #217330 ) ;
#168709=ORIENTED_EDGE ( 'NONE', *, *, #194738, .T. ) ;
#168712=CARTESIAN_POINT ( 'NONE',  ( 20.94999999999999574, 70.10000000001235776, -159.8040077198679683 ) ) ;
#168727=EDGE_CURVE ( 'NONE', #187756, #243905, #59314, .T. ) ;
#168729=AXIS2_PLACEMENT_3D ( 'NONE', #202145, #139573, #238697 ) ;
#168731=VECTOR ( 'NONE', #103064, 1000.000000000000000 ) ;
#168738=VERTEX_POINT ( 'NONE', #150662 ) ;
#168754=ORIENTED_EDGE ( 'NONE', *, *, #195527, .T. ) ;
#168763=CYLINDRICAL_SURFACE ( 'NONE', #115690, 0.1000000000000028644 ) ;
#168770=ORIENTED_EDGE ( 'NONE', *, *, #10714, .F. ) ;
#168781=CARTESIAN_POINT ( 'NONE',  ( -20.54999999999999716, 76.00000000001213607, -136.5231074845243313 ) ) ;
#168797=DIRECTION ( 'NONE',  ( 1.000000000000000000, 0.000000000000000000, 0.000000000000000000 ) ) ;
#168799=CARTESIAN_POINT ( 'NONE',  ( -20.94999999999999929, 70.15000000001235492, -159.8906102602464330 ) ) ;
#168815=CARTESIAN_POINT ( 'NONE',  ( -23.25000000000000000, 71.75000000001223555, -148.8731074845244109 ) ) ;
#168831=ORIENTED_EDGE ( 'NONE', *, *, #242474, .F. ) ;
#168841=ADVANCED_FACE ( 'NONE', ( #39727 ), #63447, .T. ) ;
#168847=DIRECTION ( 'NONE',  ( -0.000000000000000000, -6.982962677686266711E-15, 1.000000000000000000 ) ) ;
#168859=ORIENTED_EDGE ( 'NONE', *, *, #141783, .T. ) ;
#168873=VERTEX_POINT ( 'NONE', #198760 ) ;
#168874=LINE ( 'NONE', #248367, #118629 ) ;
#168876=FACE_OUTER_BOUND ( 'NONE', #65103, .T. ) ;
#168893=CARTESIAN_POINT ( 'NONE',  ( -21.05000000000000071, 75.96824164695659931, -176.2819546076071902 ) ) ;
#168906=CIRCLE ( 'NONE', #218930, 11.75000000000001066 ) ;
#168916=ORIENTED_EDGE ( 'NONE', *, *, #210169, .T. ) ;
#168918=CARTESIAN_POINT ( 'NONE',  ( 20.94999999999999929, 85.00000000001222134, -145.9170766071767389 ) ) ;
#168924=DIRECTION ( 'NONE',  ( 1.000000000000000000, 0.000000000000000000, 0.000000000000000000 ) ) ;
#168942=VERTEX_POINT ( 'NONE', #52054 ) ;
#168952=ADVANCED_FACE ( 'NONE', ( #174647 ), #130314, .T. ) ;
#168955=PLANE ( 'NONE',  #102848 ) ;
#168964=DIRECTION ( 'NONE',  ( 1.000000000000000000, 0.000000000000000000, 0.000000000000000000 ) ) ;
#168966=( BOUNDED_SURFACE ( )  B_SPLINE_SURFACE ( 3, 2, ( 
 ( #172431, #155434, #211517 ),
 ( #53718, #151571, #13319 ),
 ( #32922, #233657, #113695 ),
 ( #194547, #34194, #135809 ),
 ( #73322, #17183, #234937 ),
 ( #154152, #134523, #116281 ),
 ( #133262, #77131, #212809 ),
 ( #195829, #112426, #191978 ) ),
 .UNSPECIFIED., .F., .F., .F. ) 
 B_SPLINE_SURFACE_WITH_KNOTS ( ( 4, 2, 2, 4 ),
 ( 3, 3 ),
 ( 0.0001704874539069695018, 0.0003809798300636460045, 0.0004862260181419842558, 0.0005914722062203225071 ),
 ( 0.000000000000000000, 1.000000000000000000 ),
 .UNSPECIFIED. ) 
 GEOMETRIC_REPRESENTATION_ITEM ( )  RATIONAL_B_SPLINE_SURFACE ( (
 ( 1.000000000000000000, 0.7071067811864699681, 1.000000000000000000),
 ( 1.000000000000000000, 0.7670648383577226559, 1.000000000000000000),
 ( 1.000000000000000000, 0.8204820770250529360, 1.000000000000000000),
 ( 1.000000000000000000, 0.8877218296113961182, 1.000000000000000000),
 ( 1.000000000000000000, 0.9080815932664115797, 1.000000000000000000),
 ( 1.000000000000000000, 0.9395541505862786691, 1.000000000000000000),
 ( 1.000000000000000000, 0.9506520335378314535, 1.000000000000000000),
 ( 1.000000000000000000, 0.9504532311154486601, 1.000000000000000000) ) ) 
 REPRESENTATION_ITEM ( '' )  SURFACE ( )  );
#168984=VERTEX_POINT ( 'NONE', #169500 ) ;
#169009=CARTESIAN_POINT ( 'NONE',  ( -20.64999999999999858, 68.85000000001228670, -157.6731074845243938 ) ) ;
#169010=CARTESIAN_POINT ( 'NONE',  ( 21.05000000000000071, 85.40000000001221281, -146.4170766071767389 ) ) ;
#169038=ORIENTED_EDGE ( 'NONE', *, *, #170165, .T. ) ;
#169048=LINE ( 'NONE', #90737, #237147 ) ;
#169071=ORIENTED_EDGE ( 'NONE', *, *, #214551, .T. ) ;
#169085=AXIS2_PLACEMENT_3D ( 'NONE', #224331, #225588, #46959 ) ;
#169099=DIRECTION ( 'NONE',  ( -0.000000000000000000, -6.982962677686266711E-15, 1.000000000000000000 ) ) ;
#169106=AXIS2_PLACEMENT_3D ( 'NONE', #148775, #165779, #49656 ) ;
#169128=AXIS2_PLACEMENT_3D ( 'NONE', #88358, #149668, #184917 ) ;
#169142=DIRECTION ( 'NONE',  ( 1.000000000000000000, 0.000000000000000000, 0.000000000000000000 ) ) ;
#169157=CARTESIAN_POINT ( 'NONE',  ( -22.45437739390954235, 76.00000000001246292, -181.6726782961230811 ) ) ;
#169210=ORIENTED_EDGE ( 'NONE', *, *, #243296, .T. ) ;
#169231=CARTESIAN_POINT ( 'NONE',  ( 21.07928932188134397, 69.67148334361908724, -170.1220026301787982 ) ) ;
#169245=ORIENTED_EDGE ( 'NONE', *, *, #98480, .F. ) ;
#169251=CARTESIAN_POINT ( 'NONE',  ( -21.05000000000000071, 74.25000000001229239, -158.3535959266227451 ) ) ;
#169286=CARTESIAN_POINT ( 'NONE',  ( 20.04142135623730070, 64.35000000001245724, -181.7731074845244450 ) ) ;
#169305=DIRECTION ( 'NONE',  ( 0.000000000000000000, 0.000000000000000000, 1.000000000000000000 ) ) ;
#169323=CARTESIAN_POINT ( 'NONE',  ( 20.12518398540832010, 66.02491127934462156, -162.0264392320576974 ) ) ;
#169327=CARTESIAN_POINT ( 'NONE',  ( -21.05000000000000071, 87.48912529308842068, -167.1231074845242688 ) ) ;
#169338=FACE_OUTER_BOUND ( 'NONE', #242790, .T. ) ;
#169353=CARTESIAN_POINT ( 'NONE',  ( -23.15000000000000213, 71.65000000001228386, -157.6731074845243938 ) ) ;
#169354=PLANE ( 'NONE',  #71568 ) ;
#169358=CARTESIAN_POINT ( 'NONE',  ( 20.94999999999999929, 76.00000000001213607, -136.5231074845243313 ) ) ;
#169394=DIRECTION ( 'NONE',  ( 0.000000000000000000, -6.982962677686266711E-15, 1.000000000000000000 ) ) ;
#169408=CARTESIAN_POINT ( 'NONE',  ( 20.94999999999999929, 74.16465844978787914, -158.4679561919613775 ) ) ;
#169410=CARTESIAN_POINT ( 'NONE',  ( 20.94999999999999574, 74.14897176987143723, -158.3691942151018850 ) ) ;
#169420=CARTESIAN_POINT ( 'NONE',  ( -18.59999999999999787, 66.65000000001222702, -148.8731074845244393 ) ) ;
#169424=ORIENTED_EDGE ( 'NONE', *, *, #132365, .F. ) ;
#169457=DIRECTION ( 'NONE',  ( -1.000000000000000000, -0.000000000000000000, -0.000000000000000000 ) ) ;
#169468=VECTOR ( 'NONE', #30347, 1000.000000000000000 ) ;
#169471=ORIENTED_EDGE ( 'NONE', *, *, #113175, .T. ) ;
#169484=ORIENTED_EDGE ( 'NONE', *, *, #231689, .F. ) ;
#169500=CARTESIAN_POINT ( 'NONE',  ( 20.95512820512820440, 67.12384868372417657, -157.8731074845244109 ) ) ;
#169544=ADVANCED_FACE ( 'NONE', ( #154740 ), #78996, .T. ) ;
#169548=ORIENTED_EDGE ( 'NONE', *, *, #12477, .F. ) ;
#169585=ORIENTED_EDGE ( 'NONE', *, *, #12990, .T. ) ;
#169589=DIRECTION ( 'NONE',  ( -1.000000000000000000, 0.000000000000000000, -0.000000000000000000 ) ) ;
#169633=DIRECTION ( 'NONE',  ( -1.000000000000000000, 2.952720810173289112E-16, 2.061873921506763405E-30 ) ) ;
#169676=CARTESIAN_POINT ( 'NONE',  ( -21.07928932188134041, 75.90110485435802445, -176.3516241409176644 ) ) ;
#169712=DIRECTION ( 'NONE',  ( 2.952720810173289112E-16, 1.000000000000000000, -6.088138035986627436E-46 ) ) ;
#169734=CARTESIAN_POINT ( 'NONE',  ( 23.14999999999999858, 64.35000000001218723, -143.5379132551783812 ) ) ;
#169816=AXIS2_PLACEMENT_3D ( 'NONE', #257286, #213073, #236489 ) ;
#169862=ADVANCED_FACE ( 'NONE', ( #247073 ), #159887, .T. ) ;
#169899=AXIS2_PLACEMENT_3D ( 'NONE', #11220, #90732, #51584 ) ;
#169920=CARTESIAN_POINT ( 'NONE',  ( -22.39999999999999858, 75.90000000001242597, -177.8138870828977360 ) ) ;
#169976=DIRECTION ( 'NONE',  ( 1.000000000000000000, -2.952720810173289112E-16, -2.061873921506763405E-30 ) ) ;
#169981=CARTESIAN_POINT ( 'NONE',  ( 20.94999999999999929, 76.00000000001213607, -136.5231074845243313 ) ) ;
#169989=CIRCLE ( 'NONE', #228402, 0.09999999999998898659 ) ;
#169991=FACE_OUTER_BOUND ( 'NONE', #158934, .T. ) ;
#170007=EDGE_CURVE ( 'NONE', #16708, #128766, #243070, .T. ) ;
#170063=CIRCLE ( 'NONE', #220079, 11.89999999999999325 ) ;
#170074=EDGE_CURVE ( 'NONE', #69695, #231343, #47600, .T. ) ;
#170082=CARTESIAN_POINT ( 'NONE',  ( 20.94999999999999929, 76.00000000001216449, -140.6231074845243256 ) ) ;
#170084=DIRECTION ( 'NONE',  ( 1.000000000000000000, 0.000000000000000000, 0.000000000000000000 ) ) ;
#170088=ADVANCED_FACE ( 'NONE', ( #244200 ), #210137, .T. ) ;
#170135=DIRECTION ( 'NONE',  ( 1.000000000000000000, 0.000000000000000000, 0.000000000000000000 ) ) ;
#170165=EDGE_CURVE ( 'NONE', #23345, #93776, #30346, .T. ) ;
#170182=CARTESIAN_POINT ( 'NONE',  ( 21.05000000000000071, 87.65000000001236913, -170.0231074845242745 ) ) ;
#170185=CARTESIAN_POINT ( 'NONE',  ( -21.14999999999999503, 76.00000000001243450, -176.5637644362255969 ) ) ;
#170189=CIRCLE ( 'NONE', #45053, 0.09999999999999939493 ) ;
#170230=DIRECTION ( 'NONE',  ( 0.000000000000000000, -0.9908441862701791170, 0.1350103645450472789 ) ) ;
#170238=EDGE_LOOP ( 'NONE', ( #45087, #85226, #1679, #162682 ) ) ;
#170245=CIRCLE ( 'NONE', #174533, 0.09999999999998898659 ) ;
#170308=CIRCLE ( 'NONE', #95244, 2.000000000000001776 ) ;
#170316=EDGE_CURVE ( 'NONE', #176651, #141149, #164160, .T. ) ;
#170355=EDGE_CURVE ( 'NONE', #62202, #152968, #233660, .T. ) ;
#170384=ADVANCED_FACE ( 'NONE', ( #39324 ), #53721, .T. ) ;
#170406=CIRCLE ( 'NONE', #203683, 0.2000000000000057288 ) ;
#170413=CARTESIAN_POINT ( 'NONE',  ( 20.95512820512820440, 65.37615131630045084, -162.3581939154368285 ) ) ;
#170427=AXIS2_PLACEMENT_3D ( 'NONE', #185789, #28032, #7136 ) ;
#170438=CARTESIAN_POINT ( 'NONE',  ( 20.85000000000000142, 76.00000000001213607, -136.5231074845243313 ) ) ;
#170458=CARTESIAN_POINT ( 'NONE',  ( -22.60000000000094289, 75.89914163091394528, -181.7726746080137730 ) ) ;
#170553=ORIENTED_EDGE ( 'NONE', *, *, #87392, .T. ) ;
#170590=ORIENTED_EDGE ( 'NONE', *, *, #136519, .T. ) ;
#170601=CARTESIAN_POINT ( 'NONE',  ( 20.94999999999999929, 71.00000000001223555, -148.9283735034374843 ) ) ;
#170620=CARTESIAN_POINT ( 'NONE',  ( 20.97217846901852312, 67.12455827530264685, -161.5218798005872145 ) ) ;
#170629=DIRECTION ( 'NONE',  ( 0.000000000000000000, -1.000000000000000000, -6.982962677686265922E-15 ) ) ;
#170636=CARTESIAN_POINT ( 'NONE',  ( -21.53752568617684915, 69.21319212550857003, -170.1220819458087306 ) ) ;
#170637=EDGE_CURVE ( 'NONE', #129641, #23721, #14517, .T. ) ;
#170711=CARTESIAN_POINT ( 'NONE',  ( 20.94999999999999929, 76.00000000001210765, -132.4231074845243370 ) ) ;
#170716=DIRECTION ( 'NONE',  ( -1.000000000000000000, 0.000000000000000000, -0.000000000000000000 ) ) ;
#170736=VERTEX_POINT ( 'NONE', #175625 ) ;
#170742=CARTESIAN_POINT ( 'NONE',  ( -22.39999999999999858, 75.90000000001242597, -177.8138870828977360 ) ) ;
#170750=CARTESIAN_POINT ( 'NONE',  ( 20.95224633520496127, 67.09947783345508299, -161.5298310366031558 ) ) ;
#170790=ORIENTED_EDGE ( 'NONE', *, *, #84867, .F. ) ;
#170797=CIRCLE ( 'NONE', #91637, 0.09999999999998898659 ) ;
#170814=CARTESIAN_POINT ( 'NONE',  ( -21.14999999999999858, 76.10000000001245724, -181.6726782920691505 ) ) ;
#170826=ORIENTED_EDGE ( 'NONE', *, *, #176870, .T. ) ;
#170891=DIRECTION ( 'NONE',  ( -1.000000000000000000, 0.000000000000000000, 0.000000000000000000 ) ) ;
#170902=DIRECTION ( 'NONE',  ( 1.000000000000000000, 0.000000000000000000, 0.000000000000000000 ) ) ;
#170904=DIRECTION ( 'NONE',  ( 0.000000000000000000, 6.982962677686266711E-15, -1.000000000000000000 ) ) ;
#170918=AXIS2_PLACEMENT_3D ( 'NONE', #229889, #31718, #10843 ) ;
#170923=CARTESIAN_POINT ( 'NONE',  ( 23.14999999999999147, 76.00000000001237765, -170.0231074845243597 ) ) ;
#170937=CARTESIAN_POINT ( 'NONE',  ( 20.94999999999999929, 76.00000000001213607, -136.5231074845243313 ) ) ;
#170942=ORIENTED_EDGE ( 'NONE', *, *, #188638, .F. ) ;
#170972=CARTESIAN_POINT ( 'NONE',  ( 21.11927991906888025, 69.55150688152096450, -170.0321911639983057 ) ) ;
#170986=ORIENTED_EDGE ( 'NONE', *, *, #206612, .F. ) ;
#171038=CARTESIAN_POINT ( 'NONE',  ( 21.05000000000000071, 75.90220970870363715, -176.2809220950004772 ) ) ;
#171039=EDGE_CURVE ( 'NONE', #248809, #224580, #114025, .T. ) ;
#171056=DIRECTION ( 'NONE',  ( 1.000000000000000000, 0.000000000000000000, 0.000000000000000000 ) ) ;
#171059=DIRECTION ( 'NONE',  ( 7.304098846218134667E-16, -1.000000000000000000, -6.982962677686267499E-15 ) ) ;
#171074=AXIS2_PLACEMENT_3D ( 'NONE', #231801, #234341, #141338 ) ;
#171077=CARTESIAN_POINT ( 'NONE',  ( 21.14999999999999858, 76.00000000001229239, -157.8731074845243540 ) ) ;
#171109=CIRCLE ( 'NONE', #141827, 0.09999999999999939493 ) ;
#171115=FACE_OUTER_BOUND ( 'NONE', #219113, .T. ) ;
#171131=ORIENTED_EDGE ( 'NONE', *, *, #74505, .T. ) ;
#171132=ORIENTED_EDGE ( 'NONE', *, *, #32872, .F. ) ;
#171143=ORIENTED_EDGE ( 'NONE', *, *, #256017, .F. ) ;
#171147=DIRECTION ( 'NONE',  ( -0.7071067811865475727, 0.7071067811865475727, 4.937700262164531476E-15 ) ) ;
#171176=CARTESIAN_POINT ( 'NONE',  ( -20.64999999999999858, 71.65000000001222702, -148.8731074845244109 ) ) ;
#171214=AXIS2_PLACEMENT_3D ( 'NONE', #231222, #70876, #90395 ) ;
#171227=DIRECTION ( 'NONE',  ( 0.000000000000000000, 0.000000000000000000, -1.000000000000000000 ) ) ;
#171261=EDGE_CURVE ( 'NONE', #244808, #79539, #64346, .T. ) ;
#171278=CARTESIAN_POINT ( 'NONE',  ( 22.47007471830798409, 68.27928934808592487, -170.0231074845244166 ) ) ;
#171283=DIRECTION ( 'NONE',  ( 0.000000000000000000, -1.000000000000000000, -6.982962677686265922E-15 ) ) ;
#171286=ORIENTED_EDGE ( 'NONE', *, *, #73263, .F. ) ;
#171287=DIRECTION ( 'NONE',  ( -3.265361837132813093E-16, -1.000000000000000000, -7.086529944415894657E-15 ) ) ;
#171291=DIRECTION ( 'NONE',  ( 0.000000000000000000, -0.9915357197604982575, 0.1298341882519033486 ) ) ;
#171308=ORIENTED_EDGE ( 'NONE', *, *, #75951, .T. ) ;
#171321=ORIENTED_EDGE ( 'NONE', *, *, #200063, .T. ) ;
#171332=CARTESIAN_POINT ( 'NONE',  ( -18.50000000000000000, 66.85000000001228670, -157.6731074845244223 ) ) ;
#171338=EDGE_CURVE ( 'NONE', #250601, #195729, #243979, .T. ) ;
#171369=CARTESIAN_POINT ( 'NONE',  ( 23.15000000000000213, 85.00000000001222134, -146.4170766071767389 ) ) ;
#171419=CIRCLE ( 'NONE', #4753, 0.09999999999999080458 ) ;
#171443=CIRCLE ( 'NONE', #92290, 0.09999999999999646672 ) ;
#171460=FACE_OUTER_BOUND ( 'NONE', #134021, .T. ) ;
#171524=DIRECTION ( 'NONE',  ( -1.000000000000000000, 0.000000000000000000, 0.000000000000000000 ) ) ;
#171537=DIRECTION ( 'NONE',  ( 0.000000000000000000, 0.000000000000000000, -1.000000000000000000 ) ) ;
#171554=DIRECTION ( 'NONE',  ( 0.000000000000000000, -0.3738317757008748909, -0.9274965247785733613 ) ) ;
#171570=AXIS2_PLACEMENT_3D ( 'NONE', #177033, #122172, #99995 ) ;
#171622=AXIS2_PLACEMENT_3D ( 'NONE', #94863, #11505, #130139 ) ;
#171646=VERTEX_POINT ( 'NONE', #164439 ) ;
#171719=VERTEX_POINT ( 'NONE', #146138 ) ;
#171731=EDGE_CURVE ( 'NONE', #22950, #70645, #219035, .T. ) ;
#171739=ORIENTED_EDGE ( 'NONE', *, *, #24740, .F. ) ;
#171754=CYLINDRICAL_SURFACE ( 'NONE', #198294, 0.1000000000000072220 ) ;
#171774=AXIS2_PLACEMENT_3D ( 'NONE', #71968, #131931, #53677 ) ;
#171797=ADVANCED_FACE ( 'NONE', ( #127875 ), #209985, .T. ) ;
#171808=DIRECTION ( 'NONE',  ( -0.000000000000000000, 1.000000000000000000, 6.982962677686266711E-15 ) ) ;
#171890=LINE ( 'NONE', #251381, #108835 ) ;
#171944=FACE_OUTER_BOUND ( 'NONE', #228802, .T. ) ;
#171959=ORIENTED_EDGE ( 'NONE', *, *, #80175, .T. ) ;
#171987=ADVANCED_FACE ( 'NONE', ( #74352 ), #92577, .T. ) ;
#171998=ORIENTED_EDGE ( 'NONE', *, *, #186038, .T. ) ;
#172003=VECTOR ( 'NONE', #246906, 1000.000000000000000 ) ;
#172042=CARTESIAN_POINT ( 'NONE',  ( -20.64999999999999858, 76.00000000001212186, -134.5231074845243313 ) ) ;
#172053=EDGE_LOOP ( 'NONE', ( #188046, #146820, #2230, #65563 ) ) ;
#172085=ORIENTED_EDGE ( 'NONE', *, *, #153694, .F. ) ;
#172091=AXIS2_PLACEMENT_3D ( 'NONE', #39797, #75067, #196261 ) ;
#172114=AXIS2_PLACEMENT_3D ( 'NONE', #224169, #144625, #238608 ) ;
#172120=DIRECTION ( 'NONE',  ( 2.952720810173289112E-16, 1.000000000000000000, 1.261617073437673512E-14 ) ) ;
#172168=CYLINDRICAL_SURFACE ( 'NONE', #104180, 4.000000000000003553 ) ;
#172175=ORIENTED_EDGE ( 'NONE', *, *, #14106, .F. ) ;
#172180=DIRECTION ( 'NONE',  ( 0.000000000000000000, -1.000000000000000000, 0.000000000000000000 ) ) ;
#172198=VECTOR ( 'NONE', #81863, 1000.000000000000000 ) ;
#172207=CARTESIAN_POINT ( 'NONE',  ( -20.54999999999999716, 85.00000000001222134, -146.4170766071767389 ) ) ;
#172209=DIRECTION ( 'NONE',  ( -1.000000000000000000, -0.000000000000000000, -0.000000000000000000 ) ) ;
#172219=CARTESIAN_POINT ( 'NONE',  ( 21.51976009735019346, 69.08954155835317579, -170.0231074845243882 ) ) ;
#172223=ORIENTED_EDGE ( 'NONE', *, *, #236360, .T. ) ;
#172240=DIRECTION ( 'NONE',  ( -0.000000000000000000, -1.000000000000000000, -6.982962677686266711E-15 ) ) ;
#172242=CARTESIAN_POINT ( 'NONE',  ( 21.05000000000000071, 76.00000000001213607, -136.5231074845243313 ) ) ;
#172253=DIRECTION ( 'NONE',  ( -0.000000000000000000, -6.982962677686266711E-15, 1.000000000000000000 ) ) ;
#172255=EDGE_CURVE ( 'NONE', #51370, #205761, #67584, .T. ) ;
#172258=DIRECTION ( 'NONE',  ( 0.000000000000000000, 0.000000000000000000, 1.000000000000000000 ) ) ;
#172302=CARTESIAN_POINT ( 'NONE',  ( -18.50000000000000000, 64.25000000001246292, -181.7731074845244450 ) ) ;
#172306=AXIS2_PLACEMENT_3D ( 'NONE', #105568, #207295, #3940 ) ;
#172308=ADVANCED_FACE ( 'NONE', ( #132706 ), #53154, .T. ) ;
#172349=DIRECTION ( 'NONE',  ( 0.000000000000000000, 6.982962677686266711E-15, -1.000000000000000000 ) ) ;
#172387=CIRCLE ( 'NONE', #59885, 0.1999999999999987899 ) ;
#172397=ORIENTED_EDGE ( 'NONE', *, *, #8599, .T. ) ;
#172409=AXIS2_PLACEMENT_3D ( 'NONE', #71581, #6440, #85951 ) ;
#172416=DIRECTION ( 'NONE',  ( -0.000000000000000000, 0.1350103645451807555, 0.9908441862701610203 ) ) ;
#172418=DIRECTION ( 'NONE',  ( 0.000000000000000000, 8.267618268485201230E-15, -1.000000000000000000 ) ) ;
#172431=CARTESIAN_POINT ( 'NONE',  ( 18.50000000000000000, 85.40000000001231228, -162.7258477248610120 ) ) ;
#172545=VERTEX_POINT ( 'NONE', #225990 ) ;
#172548=CARTESIAN_POINT ( 'NONE',  ( -21.05000000000000071, 69.60000000001230092, -160.0926828544628222 ) ) ;
#172556=ADVANCED_FACE ( 'NONE', ( #167369 ), #58271, .F. ) ;
#172559=ORIENTED_EDGE ( 'NONE', *, *, #18403, .T. ) ;
#172565=DIRECTION ( 'NONE',  ( 0.000000000000000000, -0.6728971962617102953, -0.7397360091702507301 ) ) ;
#172590=CARTESIAN_POINT ( 'NONE',  ( 21.14999999999999503, 64.35000000001237197, -170.0231074845244166 ) ) ;
#172599=CARTESIAN_POINT ( 'NONE',  ( -18.52309608778507766, 85.64247632006726008, -129.8085111433545649 ) ) ;
#172620=VECTOR ( 'NONE', #95025, 999.9999999999998863 ) ;
#172657=DIRECTION ( 'NONE',  ( 0.000000000000000000, -1.299197156476247485E-14, 1.000000000000000000 ) ) ;
#172667=ORIENTED_EDGE ( 'NONE', *, *, #33000, .F. ) ;
#172700=CARTESIAN_POINT ( 'NONE',  ( -20.54999999999999716, 73.60000000001230092, -156.7984855617622770 ) ) ;
#172751=DIRECTION ( 'NONE',  ( 0.000000000000000000, -1.000000000000000000, -6.982962677686265922E-15 ) ) ;
#172765=ORIENTED_EDGE ( 'NONE', *, *, #70372, .F. ) ;
#172769=CARTESIAN_POINT ( 'NONE',  ( -18.59999999999999787, 66.75000000001223555, -148.7731074845244166 ) ) ;
#172810=EDGE_LOOP ( 'NONE', ( #4572, #95013, #6620, #29529 ) ) ;
#172831=AXIS2_PLACEMENT_3D ( 'NONE', #51295, #128309, #110009 ) ;
#172834=CIRCLE ( 'NONE', #185260, 0.09999999999999939493 ) ;
#172878=CIRCLE ( 'NONE', #2116, 12.87499999999999822 ) ;
#172897=LINE ( 'NONE', #133713, #190297 ) ;
#172909=CARTESIAN_POINT ( 'NONE',  ( 20.94999999999999929, 64.35000000001218723, -143.3069731475025037 ) ) ;
#172924=ADVANCED_FACE ( 'NONE', ( #194261 ), #92547, .T. ) ;
#172927=DIRECTION ( 'NONE',  ( 0.000000000000000000, 0.000000000000000000, 1.000000000000000000 ) ) ;
#172932=CIRCLE ( 'NONE', #185369, 4.000000000000003553 ) ;
#172964=ORIENTED_EDGE ( 'NONE', *, *, #199435, .T. ) ;
#172972=AXIS2_PLACEMENT_3D ( 'NONE', #153901, #174744, #95157 ) ;
#172989=ORIENTED_EDGE ( 'NONE', *, *, #59876, .T. ) ;
#173005=AXIS2_PLACEMENT_3D ( 'NONE', #223225, #104542, #60302 ) ;
#173030=VECTOR ( 'NONE', #182166, 1000.000000000000000 ) ;
#173047=VECTOR ( 'NONE', #94372, 1000.000000000000000 ) ;
#173062=ORIENTED_EDGE ( 'NONE', *, *, #57309, .T. ) ;
#173065=VERTEX_POINT ( 'NONE', #238485 ) ;
#173091=ORIENTED_EDGE ( 'NONE', *, *, #138796, .F. ) ;
#173136=ADVANCED_FACE ( 'NONE', ( #133932 ), #250039, .F. ) ;
#173137=CARTESIAN_POINT ( 'NONE',  ( 23.14999999999999858, 76.00000000001213607, -136.5231074845243313 ) ) ;
#173203=AXIS2_PLACEMENT_3D ( 'NONE', #73187, #155293, #118719 ) ;
#173215=DIRECTION ( 'NONE',  ( 1.000000000000000000, 0.000000000000000000, 0.000000000000000000 ) ) ;
#173257=AXIS2_PLACEMENT_3D ( 'NONE', #173137, #157412, #97358 ) ;
#173259=CARTESIAN_POINT ( 'NONE',  ( -23.25000000000000000, 70.05000000001221849, -146.8288097895591875 ) ) ;
#173262=CARTESIAN_POINT ( 'NONE',  ( -23.25000000000000000, 76.00000000001213607, -136.5231074845243313 ) ) ;
#173263=ADVANCED_FACE ( 'NONE', ( #109230 ), #234315, .F. ) ;
#173269=CARTESIAN_POINT ( 'NONE',  ( -22.50000000000000000, 76.00000000001237765, -170.0231074845243597 ) ) ;
#173286=ORIENTED_EDGE ( 'NONE', *, *, #14946, .T. ) ;
#173291=ORIENTED_EDGE ( 'NONE', *, *, #7022, .F. ) ;
#173292=AXIS2_PLACEMENT_3D ( 'NONE', #164565, #61603, #65445 ) ;
#173301=FACE_OUTER_BOUND ( 'NONE', #163741, .T. ) ;
#173346=AXIS2_PLACEMENT_3D ( 'NONE', #224456, #167098, #25007 ) ;
#173349=CIRCLE ( 'NONE', #23301, 0.1000000000000026007 ) ;
#173360=ORIENTED_EDGE ( 'NONE', *, *, #131031, .F. ) ;
#173388=EDGE_LOOP ( 'NONE', ( #166839, #118324, #117810, #190448, #14151 ) ) ;
#173392=AXIS2_PLACEMENT_3D ( 'NONE', #105030, #102473, #222424 ) ;
#173406=FACE_BOUND ( 'NONE', #216480, .T. ) ;
#173436=CIRCLE ( 'NONE', #98310, 0.1000000000000028644 ) ;
#173460=ADVANCED_FACE ( 'NONE', ( #48949 ), #168955, .F. ) ;
#173485=DIRECTION ( 'NONE',  ( 0.000000000000000000, 0.000000000000000000, 1.000000000000000000 ) ) ;
#173493=DIRECTION ( 'NONE',  ( 1.000000000000000000, -3.469446951953718318E-14, 2.003086131649645455E-14 ) ) ;
#173499=CARTESIAN_POINT ( 'NONE',  ( 23.24999999999999645, 70.40000000001229807, -157.6178414656113205 ) ) ;
#173512=CARTESIAN_POINT ( 'NONE',  ( -21.12642695952773764, 69.62434007797720881, -170.1220107677137605 ) ) ;
#173522=AXIS2_PLACEMENT_3D ( 'NONE', #148666, #13019, #208645 ) ;
#173546=ORIENTED_EDGE ( 'NONE', *, *, #148301, .F. ) ;
#173580=ORIENTED_EDGE ( 'NONE', *, *, #44973, .T. ) ;
#173608=CARTESIAN_POINT ( 'NONE',  ( -1.739115166359751801E-14, 64.35000000001224407, -148.6731074845244507 ) ) ;
#173621=ORIENTED_EDGE ( 'NONE', *, *, #103009, .F. ) ;
#173662=CIRCLE ( 'NONE', #211203, 0.09999999999998898659 ) ;
#173669=CARTESIAN_POINT ( 'NONE',  ( -21.05000000000000071, 61.95000000001234497, -164.5094124137634708 ) ) ;
#173680=VERTEX_POINT ( 'NONE', #49628 ) ;
#173682=AXIS2_PLACEMENT_3D ( 'NONE', #217342, #29161, #70838 ) ;
#173705=CARTESIAN_POINT ( 'NONE',  ( -20.94999999999999929, 77.25000000001232081, -162.0231074845243313 ) ) ;
#173707=CARTESIAN_POINT ( 'NONE',  ( -20.07928932188135107, 66.77928932189364275, -157.6731074845244223 ) ) ;
#173760=EDGE_CURVE ( 'NONE', #178267, #248809, #173662, .T. ) ;
#173815=DIRECTION ( 'NONE',  ( 0.000000000000000000, -1.000000000000000000, -8.609265936414504429E-15 ) ) ;
#173827=DIRECTION ( 'NONE',  ( 0.000000000000000000, 6.938893903907222067E-15, -1.000000000000000000 ) ) ;
#173833=LINE ( 'NONE', #36875, #232091 ) ;
#173842=VECTOR ( 'NONE', #212570, 1000.000000000000000 ) ;
#173858=CARTESIAN_POINT ( 'NONE',  ( -23.15000000000000213, 64.35000000001222986, -148.7731074845244450 ) ) ;
#173859=ORIENTED_EDGE ( 'NONE', *, *, #107210, .T. ) ;
#173881=CARTESIAN_POINT ( 'NONE',  ( -18.39999999999999858, 85.50000000001210765, -129.9229180933022576 ) ) ;
#173882=VERTEX_POINT ( 'NONE', #151318 ) ;
#173901=CARTESIAN_POINT ( 'NONE',  ( -20.94999999999999929, 74.16465844978787914, -158.4679561919613775 ) ) ;
#173911=CIRCLE ( 'NONE', #153061, 0.5000000000000004441 ) ;
#173921=AXIS2_PLACEMENT_3D ( 'NONE', #201502, #22901, #197647 ) ;
#173922=EDGE_CURVE ( 'NONE', #236987, #244761, #234686, .T. ) ;
#173943=CIRCLE ( 'NONE', #98836, 0.09999999999998898659 ) ;
#173969=CARTESIAN_POINT ( 'NONE',  ( 22.50000000000000000, 68.25000000001236344, -170.1231074845244109 ) ) ;
#174032=CARTESIAN_POINT ( 'NONE',  ( -23.25000000000000000, 76.00000000001213607, -136.5231074845243313 ) ) ;
#174033=CARTESIAN_POINT ( 'NONE',  ( -21.05000000000000071, 76.10000000001242881, -176.5637644362255969 ) ) ;
#174035=ADVANCED_FACE ( 'NONE', ( #218960 ), #121192, .T. ) ;
#174046=AXIS2_PLACEMENT_3D ( 'NONE', #137143, #120186, #216674 ) ;
#174051=DIRECTION ( 'NONE',  ( -1.000000000000000000, 0.000000000000000000, -0.000000000000000000 ) ) ;
#174067=CARTESIAN_POINT ( 'NONE',  ( -23.15000000000000213, 76.00000000001213607, -136.5231074845243313 ) ) ;
#174087=EDGE_CURVE ( 'NONE', #68761, #119183, #161332, .T. ) ;
#174107=VERTEX_POINT ( 'NONE', #85842 ) ;
#174130=CARTESIAN_POINT ( 'NONE',  ( -22.59999985501179154, 64.25013020700939137, -170.0887061543239724 ) ) ;
#174169=CARTESIAN_POINT ( 'NONE',  ( 20.94999999999999574, 65.57661458509942065, -162.5310555606543232 ) ) ;
#174187=FILL_AREA_STYLE ('',( #193713 ) ) ;
#174192=CARTESIAN_POINT ( 'NONE',  ( -18.47079683080353973, 85.47166410525711910, -162.9142469435320777 ) ) ;
#174213=EDGE_CURVE ( 'NONE', #56768, #208166, #240601, .T. ) ;
#174222=CARTESIAN_POINT ( 'NONE',  ( -20.92356734117541706, 65.68026841930924320, -130.9725740131889893 ) ) ;
#174233=CARTESIAN_POINT ( 'NONE',  ( 18.59999999999999432, 77.26178616857734482, -161.9366085209788650 ) ) ;
#174254=CIRCLE ( 'NONE', #136787, 0.09999999999998712696 ) ;
#174259=EDGE_CURVE ( 'NONE', #219341, #44711, #74052, .T. ) ;
#174272=LINE ( 'NONE', #54260, #110652 ) ;
#174290=ORIENTED_EDGE ( 'NONE', *, *, #143343, .F. ) ;
#174313=ORIENTED_EDGE ( 'NONE', *, *, #256841, .T. ) ;
#174333=CIRCLE ( 'NONE', #153488, 4.000000000000003553 ) ;
#174337=CIRCLE ( 'NONE', #170427, 0.4000000000000114575 ) ;
#174380=ADVANCED_FACE ( 'NONE', ( #98665 ), #94853, .F. ) ;
#174386=DIRECTION ( 'NONE',  ( -1.000000000000000000, -0.000000000000000000, -0.000000000000000000 ) ) ;
#174388=CARTESIAN_POINT ( 'NONE',  ( -20.64999999999999858, 76.00000000001212186, -134.6231074845243256 ) ) ;
#174394=VECTOR ( 'NONE', #129789, 999.9999999999998863 ) ;
#174403=AXIS2_PLACEMENT_3D ( 'NONE', #44713, #188068, #68119 ) ;
#174410=AXIS2_PLACEMENT_3D ( 'NONE', #110174, #89319, #132308 ) ;
#174443=AXIS2_PLACEMENT_3D ( 'NONE', #124939, #148345, #203178 ) ;
#174466=CARTESIAN_POINT ( 'NONE',  ( 21.05000000000000071, 76.00000000001237765, -169.9231074845243654 ) ) ;
#174467=DIRECTION ( 'NONE',  ( 0.000000000000000000, -7.429790795770644761E-15, 1.000000000000000000 ) ) ;
#174468=ORIENTED_EDGE ( 'NONE', *, *, #254475, .F. ) ;
#174474=CARTESIAN_POINT ( 'NONE',  ( -18.59999999999999787, 70.10000000001235776, -159.8040077198679683 ) ) ;
#174479=CIRCLE ( 'NONE', #32819, 0.09999999999999939493 ) ;
#174494=ORIENTED_EDGE ( 'NONE', *, *, #179990, .T. ) ;
#174499=AXIS2_PLACEMENT_3D ( 'NONE', #29893, #205932, #145950 ) ;
#174533=AXIS2_PLACEMENT_3D ( 'NONE', #29490, #7315, #121211 ) ;
#174555=EDGE_LOOP ( 'NONE', ( #189495, #247941, #242338, #52490 ) ) ;
#174602=ORIENTED_EDGE ( 'NONE', *, *, #49283, .F. ) ;
#174606=CARTESIAN_POINT ( 'NONE',  ( -21.05000000000000426, 64.40000000001234071, -163.0949042542488883 ) ) ;
#174607=VERTEX_POINT ( 'NONE', #248492 ) ;
#174618=ORIENTED_EDGE ( 'NONE', *, *, #19713, .T. ) ;
#174627=DIRECTION ( 'NONE',  ( 0.000000000000000000, 0.000000000000000000, 1.000000000000000000 ) ) ;
#174647=FACE_OUTER_BOUND ( 'NONE', #145841, .T. ) ;
#174665=DIRECTION ( 'NONE',  ( 0.000000000000000000, -7.116814260417668513E-15, 1.000000000000000000 ) ) ;
#174689=FACE_BOUND ( 'NONE', #162593, .T. ) ;
#174696=VECTOR ( 'NONE', #194267, 1000.000000000000000 ) ;
#174711=DIRECTION ( 'NONE',  ( 0.7071067811865475727, -0.7071067811865475727, -5.142139384388981164E-15 ) ) ;
#174714=VECTOR ( 'NONE', #94881, 1000.000000000000000 ) ;
#174733=EDGE_LOOP ( 'NONE', ( #17606, #199656, #40280, #52677, #194276, #206704, #89924 ) ) ;
#174734=CARTESIAN_POINT ( 'NONE',  ( -18.50000000000000000, 77.16412189325330928, -128.8082593989527425 ) ) ;
#174744=DIRECTION ( 'NONE',  ( -1.000000000000000000, 0.000000000000000000, -0.000000000000000000 ) ) ;
#174750=EDGE_CURVE ( 'NONE', #81073, #115527, #24333, .T. ) ;
#174757=DIRECTION ( 'NONE',  ( 0.000000000000000000, -6.982962677686266711E-15, 1.000000000000000000 ) ) ;
#174759=TOROIDAL_SURFACE ( 'NONE', #33270, 2.100000000000002309, 0.1000000000000000056 ) ;
#174766=ORIENTED_EDGE ( 'NONE', *, *, #87536, .F. ) ;
#174787=CARTESIAN_POINT ( 'NONE',  ( -22.01447462590972748, 68.73619979878245090, -170.1221444845839699 ) ) ;
#174878=DIRECTION ( 'NONE',  ( 0.000000000000000000, 0.9654727137038715545, -0.2605042016806676242 ) ) ;
#174882=ORIENTED_EDGE ( 'NONE', *, *, #239377, .T. ) ;
#174920=VERTEX_POINT ( 'NONE', #106070 ) ;
#174944=CIRCLE ( 'NONE', #241527, 0.09999999999999134581 ) ;
#174960=VERTEX_POINT ( 'NONE', #184344 ) ;
#175009=AXIS2_PLACEMENT_3D ( 'NONE', #218955, #220266, #24650 ) ;
#175015=CARTESIAN_POINT ( 'NONE',  ( 20.95512820512820440, 65.37615131630040821, -157.8731074845244393 ) ) ;
#175023=TOROIDAL_SURFACE ( 'NONE', #191756, 12.97499999999999787, 0.1000000000000000056 ) ;
#175055=DIRECTION ( 'NONE',  ( 1.000000000000000000, 0.000000000000000000, 0.000000000000000000 ) ) ;
#175059=ADVANCED_FACE ( 'NONE', ( #69560 ), #149099, .F. ) ;
#175078=CIRCLE ( 'NONE', #187525, 0.1000000000000060701 ) ;
#175085=LINE ( 'NONE', #113769, #33110 ) ;
#175107=EDGE_CURVE ( 'NONE', #81073, #217454, #16143, .T. ) ;
#175109=CARTESIAN_POINT ( 'NONE',  ( 20.94999999999999574, 69.60000000001230092, -160.0926828544628222 ) ) ;
#175140=DIRECTION ( 'NONE',  ( 0.000000000000000000, -6.982962677686266711E-15, 1.000000000000000000 ) ) ;
#175156=DIRECTION ( 'NONE',  ( 1.000000000000000000, 0.000000000000000000, 0.000000000000000000 ) ) ;
#175165=CARTESIAN_POINT ( 'NONE',  ( -18.37151313414648612, 85.57101412579075372, -129.7064445752858717 ) ) ;
#175167=DIRECTION ( 'NONE',  ( 0.000000000000000000, 0.9999631594459055250, 0.008583690987131395445 ) ) ;
#175171=DIRECTION ( 'NONE',  ( 0.000000000000000000, 1.000000000000000000, 6.938893903907222067E-15 ) ) ;
#175207=CIRCLE ( 'NONE', #71119, 0.09999999999998898659 ) ;
#175247=ORIENTED_EDGE ( 'NONE', *, *, #84618, .T. ) ;
#175257=CIRCLE ( 'NONE', #133518, 0.1999999999999987899 ) ;
#175264=CARTESIAN_POINT ( 'NONE',  ( 20.95512820512820795, 67.12384868372417657, -157.8229346253956749 ) ) ;
#175290=TOROIDAL_SURFACE ( 'NONE', #62830, 0.4000000000000005773, 0.1000000000000000056 ) ;
#175356=AXIS2_PLACEMENT_3D ( 'NONE', #169009, #248502, #33346 ) ;
#175388=ADVANCED_FACE ( 'NONE', ( #177034, #137856 ), #161310, .F. ) ;
#175411=LINE ( 'NONE', #254854, #79632 ) ;
#175418=CARTESIAN_POINT ( 'NONE',  ( 21.05000000000000071, 69.35000000001231513, -160.0060803140843859 ) ) ;
#175430=AXIS2_PLACEMENT_3D ( 'NONE', #169420, #49430, #191541 ) ;
#175442=ORIENTED_EDGE ( 'NONE', *, *, #144185, .T. ) ;
#175473=ORIENTED_EDGE ( 'NONE', *, *, #195071, .F. ) ;
#175480=ORIENTED_EDGE ( 'NONE', *, *, #65889, .F. ) ;
#175483=CARTESIAN_POINT ( 'NONE',  ( -20.94999999999999929, 65.70729864261026876, -131.0657455973724836 ) ) ;
#175532=CARTESIAN_POINT ( 'NONE',  ( -2.995603634470891112E-16, 69.35000000001222986, -148.8731074845244109 ) ) ;
#175560=ORIENTED_EDGE ( 'NONE', *, *, #176133, .T. ) ;
#175586=DIRECTION ( 'NONE',  ( 0.000000000000000000, 1.000000000000000000, 6.982962677686266711E-15 ) ) ;
#175595=CARTESIAN_POINT ( 'NONE',  ( 18.47654891039379166, 85.46527494839465078, -162.8971315793296526 ) ) ;
#175624=DIRECTION ( 'NONE',  ( 1.000000000000000000, 0.000000000000000000, 0.000000000000000000 ) ) ;
#175625=CARTESIAN_POINT ( 'NONE',  ( -18.39999999999999858, 85.51932773110476660, -163.0501311079649440 ) ) ;
#175629=AXIS2_PLACEMENT_3D ( 'NONE', #164574, #244088, #47155 ) ;
#175646=CARTESIAN_POINT ( 'NONE',  ( -22.00356870070476489, 76.00000000000328271, -177.2773498462649968 ) ) ;
#175651=ORIENTED_EDGE ( 'NONE', *, *, #135049, .F. ) ;
#175654=EDGE_CURVE ( 'NONE', #248221, #4663, #149597, .T. ) ;
#175673=ORIENTED_EDGE ( 'NONE', *, *, #83653, .T. ) ;
#175697=CARTESIAN_POINT ( 'NONE',  ( 21.05000012384952868, 65.37127970113776598, -157.8451301544894534 ) ) ;
#175742=DIRECTION ( 'NONE',  ( 1.000000000000000000, -3.265361837132813093E-16, -2.280189983783949500E-30 ) ) ;
#175748=ORIENTED_EDGE ( 'NONE', *, *, #167567, .F. ) ;
#175752=CARTESIAN_POINT ( 'NONE',  ( 21.07928932188134397, 69.67148334361907303, -170.1220026301788266 ) ) ;
#175754=CARTESIAN_POINT ( 'NONE',  ( 21.22070241538126467, 75.90108096947739114, -176.4930537573939944 ) ) ;
#175772=ADVANCED_FACE ( 'NONE', ( #138808 ), #174759, .T. ) ;
#175802=CARTESIAN_POINT ( 'NONE',  ( -20.54999999999999716, 74.00000000001229239, -156.7984855617622770 ) ) ;
#175826=DIRECTION ( 'NONE',  ( 0.000000000000000000, -4.019398425746649671E-14, 1.000000000000000000 ) ) ;
#175833=LINE ( 'NONE', #235776, #24999 ) ;
#175864=AXIS2_PLACEMENT_3D ( 'NONE', #162118, #215949, #85089 ) ;
#175873=CARTESIAN_POINT ( 'NONE',  ( -20.94999999999999929, 77.84915357198811137, -124.9171408647273012 ) ) ;
#175890=VECTOR ( 'NONE', #249790, 1000.000000000000000 ) ;
#175896=CIRCLE ( 'NONE', #213272, 0.1000000000000028644 ) ;
#175945=CARTESIAN_POINT ( 'NONE',  ( 20.95052659398289308, 65.52017563223242291, -162.4478687286588183 ) ) ;
#175953=DIRECTION ( 'NONE',  ( 0.000000000000000000, -0.8660254037844387076, 0.4999999999999998335 ) ) ;
#175965=DIRECTION ( 'NONE',  ( 1.000000000000000000, -2.952720810173289112E-16, -2.061873921506763405E-30 ) ) ;
#175996=CYLINDRICAL_SURFACE ( 'NONE', #50230, 0.09999999999998898659 ) ;
#175999=EDGE_CURVE ( 'NONE', #146731, #18113, #132133, .T. ) ;
#176041=VERTEX_POINT ( 'NONE', #231254 ) ;
#176080=DIRECTION ( 'NONE',  ( 0.000000000000000000, 0.000000000000000000, 1.000000000000000000 ) ) ;
#176086=CARTESIAN_POINT ( 'NONE',  ( 21.05000000000000071, 76.00000000001237765, -170.0231074845243597 ) ) ;
#176091=CARTESIAN_POINT ( 'NONE',  ( 20.94999999999999929, 87.65000000001215597, -139.4231074845242802 ) ) ;
#176097=DIRECTION ( 'NONE',  ( 0.000000000000000000, 0.000000000000000000, 1.000000000000000000 ) ) ;
#176116=DIRECTION ( 'NONE',  ( 1.000000000000000000, -2.952720810173289112E-16, -2.061873921506763405E-30 ) ) ;
#176117=DIRECTION ( 'NONE',  ( 1.000000000000000000, 0.000000000000000000, 0.000000000000000000 ) ) ;
#176128=DIRECTION ( 'NONE',  ( 1.000000000000000000, 0.000000000000000000, 0.000000000000000000 ) ) ;
#176133=EDGE_CURVE ( 'NONE', #179596, #168233, #74795, .T. ) ;
#176160=ORIENTED_EDGE ( 'NONE', *, *, #198794, .F. ) ;
#176175=CIRCLE ( 'NONE', #209450, 0.1000000000000118433 ) ;
#176197=ORIENTED_EDGE ( 'NONE', *, *, #214449, .T. ) ;
#176211=DIRECTION ( 'NONE',  ( -0.000000000000000000, -0.1350103645451945777, 0.9908441862701590219 ) ) ;
#176219=ORIENTED_EDGE ( 'NONE', *, *, #140638, .F. ) ;
#176229=CIRCLE ( 'NONE', #213610, 0.9750000000000036415 ) ;
#176231=ORIENTED_EDGE ( 'NONE', *, *, #116503, .F. ) ;
#176235=CIRCLE ( 'NONE', #242847, 0.09999999999999939493 ) ;
#176242=DIRECTION ( 'NONE',  ( 0.000000000000000000, 0.000000000000000000, -1.000000000000000000 ) ) ;
#176244=ADVANCED_FACE ( 'NONE', ( #21676 ), #12591, .F. ) ;
#176254=PLANE ( 'NONE',  #36916 ) ;
#176291=VERTEX_POINT ( 'NONE', #201578 ) ;
#176336=CARTESIAN_POINT ( 'NONE',  ( 18.59999999999999076, 64.35000000001220144, -145.1731074845244507 ) ) ;
#176344=CARTESIAN_POINT ( 'NONE',  ( -20.64999999999999858, 74.00000000001223555, -149.7477294072864709 ) ) ;
#176366=CIRCLE ( 'NONE', #55687, 0.09999999999998898659 ) ;
#176409=CARTESIAN_POINT ( 'NONE',  ( -20.64999999999999858, 68.75000000001230660, -157.7731074845244166 ) ) ;
#176422=CARTESIAN_POINT ( 'NONE',  ( -18.44232395689948589, 85.55228255706195739, -129.6808554997166141 ) ) ;
#176438=VERTEX_POINT ( 'NONE', #106311 ) ;
#176451=DIRECTION ( 'NONE',  ( 1.000000000000000000, -0.000000000000000000, 0.000000000000000000 ) ) ;
#176477=ORIENTED_EDGE ( 'NONE', *, *, #18841, .T. ) ;
#176481=AXIS2_PLACEMENT_3D ( 'NONE', #207542, #168458, #69317 ) ;
#176497=ORIENTED_EDGE ( 'NONE', *, *, #99967, .F. ) ;
#176511=CARTESIAN_POINT ( 'NONE',  ( 21.05000000000000071, 71.00000000001230660, -157.6178414656113205 ) ) ;
#176515=AXIS2_PLACEMENT_3D ( 'NONE', #165225, #3572, #103939 ) ;
#176542=AXIS2_PLACEMENT_3D ( 'NONE', #64365, #225959, #223412 ) ;
#176573=FACE_OUTER_BOUND ( 'NONE', #84763, .T. ) ;
#176637=ORIENTED_EDGE ( 'NONE', *, *, #149231, .T. ) ;
#176651=VERTEX_POINT ( 'NONE', #180135 ) ;
#176722=CARTESIAN_POINT ( 'NONE',  ( -18.59999999999999787, 70.65875701002079268, -179.8297576910124178 ) ) ;
#176733=CARTESIAN_POINT ( 'NONE',  ( 18.56308993302918964, 65.61930884468851843, -145.2838848455861580 ) ) ;
#176742=ORIENTED_EDGE ( 'NONE', *, *, #253422, .F. ) ;
#176747=EDGE_CURVE ( 'NONE', #223317, #6603, #54903, .T. ) ;
#176753=ADVANCED_FACE ( 'NONE', ( #221783 ), #142398, .F. ) ;
#176760=VERTEX_POINT ( 'NONE', #187847 ) ;
#176769=CARTESIAN_POINT ( 'NONE',  ( -21.14999999999999858, 64.35000000001238618, -170.0231074845244166 ) ) ;
#176780=ORIENTED_EDGE ( 'NONE', *, *, #251161, .F. ) ;
#176794=CYLINDRICAL_SURFACE ( 'NONE', #144045, 0.09999999999998898659 ) ;
#176854=VERTEX_POINT ( 'NONE', #174734 ) ;
#176858=CIRCLE ( 'NONE', #22740, 0.5999999999999894307 ) ;
#176870=EDGE_CURVE ( 'NONE', #10632, #22319, #34290, .T. ) ;
#176877=CARTESIAN_POINT ( 'NONE',  ( -22.49072729836729678, 75.94351806727883059, -181.6731157336792819 ) ) ;
#176882=FACE_OUTER_BOUND ( 'NONE', #77404, .T. ) ;
#176906=CIRCLE ( 'NONE', #193645, 0.09999999999999939493 ) ;
#176907=DIRECTION ( 'NONE',  ( 1.000000000000000000, 0.000000000000000000, 0.000000000000000000 ) ) ;
#176944=DIRECTION ( 'NONE',  ( -1.000000000000000000, 0.000000000000000000, -0.000000000000000000 ) ) ;
#176960=AXIS2_PLACEMENT_3D ( 'NONE', #208709, #165732, #28819 ) ;
#177032=EDGE_LOOP ( 'NONE', ( #250568, #21851, #185995, #104659 ) ) ;
#177033=CARTESIAN_POINT ( 'NONE',  ( 18.59999999999999076, 69.55000000001230376, -160.0060803140843859 ) ) ;
#177034=FACE_BOUND ( 'NONE', #209357, .T. ) ;
#177041=CARTESIAN_POINT ( 'NONE',  ( -21.05000000000000071, 87.39257802171802325, -166.9491579046923277 ) ) ;
#177105=FACE_OUTER_BOUND ( 'NONE', #241317, .T. ) ;
#177124=EDGE_LOOP ( 'NONE', ( #3105, #106513, #68766 ) ) ;
#177145=CARTESIAN_POINT ( 'NONE',  ( 18.41815437325351823, 85.49870985315352812, -129.9191616457220277 ) ) ;
#177156=ADVANCED_FACE ( 'NONE', ( #7595 ), #224061, .T. ) ;
#177162=ORIENTED_EDGE ( 'NONE', *, *, #149128, .T. ) ;
#177176=ORIENTED_EDGE ( 'NONE', *, *, #242572, .T. ) ;
#177182=TOROIDAL_SURFACE ( 'NONE', #35708, 0.2000000000000000111, 0.1000000000000000056 ) ;
#177220=AXIS2_PLACEMENT_3D ( 'NONE', #237273, #22084, #101567 ) ;
#177229=CARTESIAN_POINT ( 'NONE',  ( 20.95265033839679347, 65.48774916754517506, -162.4573437284944646 ) ) ;
#177236=CARTESIAN_POINT ( 'NONE',  ( -18.59999999999999787, 64.35000000001234355, -163.0083017138704236 ) ) ;
#177243=VECTOR ( 'NONE', #9998, 1000.000000000000000 ) ;
#177251=DIRECTION ( 'NONE',  ( 0.000000000000000000, 0.000000000000000000, 1.000000000000000000 ) ) ;
#177300=DIRECTION ( 'NONE',  ( 0.000000000000000000, 6.938893903907222067E-15, -1.000000000000000000 ) ) ;
#177309=CARTESIAN_POINT ( 'NONE',  ( -23.25000000000000000, 76.00000000001234923, -165.9731074845243768 ) ) ;
#177326=AXIS2_PLACEMENT_3D ( 'NONE', #57810, #35730, #253450 ) ;
#177327=EDGE_LOOP ( 'NONE', ( #16109, #153110, #108742, #68129 ) ) ;
#177329=EDGE_CURVE ( 'NONE', #94706, #151867, #2135, .T. ) ;
#177336=LINE ( 'NONE', #56038, #237262 ) ;
#177340=EDGE_CURVE ( 'NONE', #50990, #251678, #245105, .T. ) ;
#177368=DIRECTION ( 'NONE',  ( -1.000000000000000000, -0.000000000000000000, -0.000000000000000000 ) ) ;
#177398=DIRECTION ( 'NONE',  ( 0.000000000000000000, 6.982962677686266711E-15, -1.000000000000000000 ) ) ;
#177418=CARTESIAN_POINT ( 'NONE',  ( -23.15000000000000213, 76.00000000001213607, -136.5231074845243313 ) ) ;
#177426=TOROIDAL_SURFACE ( 'NONE', #35763, 11.90000000000000213, 0.1000000000000000056 ) ;
#177440=CARTESIAN_POINT ( 'NONE',  ( -20.94999999999999929, 77.26178616857734482, -161.9366085209788650 ) ) ;
#177450=CARTESIAN_POINT ( 'NONE',  ( -18.59999999999999787, 66.65000000001222702, -148.6731074845244223 ) ) ;
#177472=B_SPLINE_CURVE_WITH_KNOTS ( 'NONE', 3,
 ( #38049, #194559, #97965, #160565, #134531, #96673, #177574, #78421, #158019, #237517, #217917, #101813, #242631, #121446, #6592, #144806 ),
 .UNSPECIFIED., .F., .F.,
 ( 4, 3, 3, 3, 3, 4 ),
 ( 0.000000000000000000, 3.357088238235017585E-05, 6.714213034886951743E-05, 0.0001007408646120965597, 0.0001343627955914321564, 0.0001573956632896059723 ),
 .UNSPECIFIED. ) ;
#177473=EDGE_CURVE ( 'NONE', #15038, #212171, #173911, .T. ) ;
#177490=AXIS2_PLACEMENT_3D ( 'NONE', #181364, #28401, #120122 ) ;
#177498=EDGE_CURVE ( 'NONE', #108264, #65247, #68551, .T. ) ;
#177515=CARTESIAN_POINT ( 'NONE',  ( -18.59999999999999787, 74.25000000001229239, -158.3535959266227451 ) ) ;
#177574=CARTESIAN_POINT ( 'NONE',  ( 21.07189867249812210, 65.27501972991913703, -157.8106560422477003 ) ) ;
#177602=DIRECTION ( 'NONE',  ( 0.000000000000000000, -7.086529944415886769E-15, 1.000000000000000000 ) ) ;
#177635=CARTESIAN_POINT ( 'NONE',  ( -21.05000000000000071, 76.10000000001245724, -181.6726782920691505 ) ) ;
#177709=DIRECTION ( 'NONE',  ( -0.000000000000000000, 1.000000000000000000, 6.982962677686266711E-15 ) ) ;
#177714=ORIENTED_EDGE ( 'NONE', *, *, #180856, .T. ) ;
#177742=CARTESIAN_POINT ( 'NONE',  ( 23.24999999999997513, 64.25000000001219291, -143.5379132551784096 ) ) ;
#177748=AXIS2_PLACEMENT_3D ( 'NONE', #233414, #251665, #177300 ) ;
#177752=VERTEX_POINT ( 'NONE', #57943 ) ;
#177782=ADVANCED_FACE ( 'NONE', ( #235308 ), #98327, .T. ) ;
#177801=CARTESIAN_POINT ( 'NONE',  ( -23.15000000000000213, 87.65000000001215597, -139.5231074845243029 ) ) ;
#177805=CIRCLE ( 'NONE', #194563, 0.1000000000000043771 ) ;
#177837=EDGE_LOOP ( 'NONE', ( #78198, #25355, #187585, #114277 ) ) ;
#177861=CARTESIAN_POINT ( 'NONE',  ( 18.59999999999999076, 69.60000000001230092, -160.0926828544628222 ) ) ;
#177863=VERTEX_POINT ( 'NONE', #202611 ) ;
#177893=ADVANCED_FACE ( 'NONE', ( #186931 ), #87777, .F. ) ;
#177949=FACE_OUTER_BOUND ( 'NONE', #5353, .T. ) ;
#177953=CARTESIAN_POINT ( 'NONE',  ( -18.39999999999999858, 85.50000000001233502, -162.9910380878246201 ) ) ;
#177973=CARTESIAN_POINT ( 'NONE',  ( 21.05000000000000071, 76.02138556594995578, -176.3280685972093806 ) ) ;
#177975=CARTESIAN_POINT ( 'NONE',  ( -18.59999999999999787, 77.13501884592227498, -128.8061306010920362 ) ) ;
#178021=AXIS2_PLACEMENT_3D ( 'NONE', #142253, #200947, #41902 ) ;
#178071=FACE_OUTER_BOUND ( 'NONE', #19386, .T. ) ;
#178087=ORIENTED_EDGE ( 'NONE', *, *, #200606, .F. ) ;
#178147=CIRCLE ( 'NONE', #111487, 0.09999999999998898659 ) ;
#178189=ORIENTED_EDGE ( 'NONE', *, *, #98935, .T. ) ;
#178191=DIRECTION ( 'NONE',  ( 0.000000000000000000, 0.000000000000000000, -1.000000000000000000 ) ) ;
#178215=DIRECTION ( 'NONE',  ( 0.000000000000000000, -0.8660254037844468122, -0.4999999999999859557 ) ) ;
#178224=ADVANCED_FACE ( 'NONE', ( #48039 ), #125516, .T. ) ;
#178250=CARTESIAN_POINT ( 'NONE',  ( -22.50000000000000000, 64.25000000001237765, -170.0231074845244166 ) ) ;
#178261=ADVANCED_FACE ( 'NONE', ( #188837 ), #36115, .T. ) ;
#178267=VERTEX_POINT ( 'NONE', #74063 ) ;
#178312=DIRECTION ( 'NONE',  ( 1.000000000000000000, 0.000000000000000000, 0.000000000000000000 ) ) ;
#178321=ADVANCED_FACE ( 'NONE', ( #93592 ), #19544, .F. ) ;
#178323=CARTESIAN_POINT ( 'NONE',  ( 21.09096482362048874, 69.63645563460823951, -170.0625557632986613 ) ) ;
#178329=PLANE ( 'NONE',  #199746 ) ;
#178354=VECTOR ( 'NONE', #210469, 1000.000000000000000 ) ;
#178366=CARTESIAN_POINT ( 'NONE',  ( 20.94999999999999574, 74.83729825007431202, -161.9231074845243654 ) ) ;
#178429=ORIENTED_EDGE ( 'NONE', *, *, #393, .T. ) ;
#178461=DIRECTION ( 'NONE',  ( -1.000000000000000000, -0.000000000000000000, -0.000000000000000000 ) ) ;
#178468=EDGE_CURVE ( 'NONE', #69713, #48052, #82217, .T. ) ;
#178475=AXIS2_PLACEMENT_3D ( 'NONE', #159418, #22483, #238950 ) ;
#178480=AXIS2_PLACEMENT_3D ( 'NONE', #39974, #253840, #217269 ) ;
#178501=ORIENTED_EDGE ( 'NONE', *, *, #90687, .F. ) ;
#178506=CYLINDRICAL_SURFACE ( 'NONE', #38848, 0.09999999999998898659 ) ;
#178510=CARTESIAN_POINT ( 'NONE',  ( 21.87500000000000355, 66.25000000001227818, -157.6731074845244223 ) ) ;
#178521=EDGE_LOOP ( 'NONE', ( #239812, #90572, #48679, #78284 ) ) ;
#178533=ORIENTED_EDGE ( 'NONE', *, *, #38761, .T. ) ;
#178595=ORIENTED_EDGE ( 'NONE', *, *, #350, .F. ) ;
#178607=DIRECTION ( 'NONE',  ( 1.000000000000000000, 0.000000000000000000, 0.000000000000000000 ) ) ;
#178619=FACE_OUTER_BOUND ( 'NONE', #12033, .T. ) ;
#178637=DIRECTION ( 'NONE',  ( 1.000000000000000000, 0.000000000000000000, 0.000000000000000000 ) ) ;
#178644=DIRECTION ( 'NONE',  ( 0.000000000000000000, 0.000000000000000000, 1.000000000000000000 ) ) ;
#178658=ORIENTED_EDGE ( 'NONE', *, *, #182096, .F. ) ;
#178702=CARTESIAN_POINT ( 'NONE',  ( -21.14999999999999858, 64.25000000001237765, -169.9231074845244507 ) ) ;
#178732=DIRECTION ( 'NONE',  ( 0.000000000000000000, -1.000000000000000000, -6.982962677686265922E-15 ) ) ;
#178750=CIRCLE ( 'NONE', #66078, 0.1000000000000072220 ) ;
#178771=DIRECTION ( 'NONE',  ( 0.000000000000000000, 0.000000000000000000, -1.000000000000000000 ) ) ;
#178782=B_SPLINE_CURVE_WITH_KNOTS ( 'NONE', 3,
 ( #153135, #175264, #254709, #214350, #77387, #218173 ),
 .UNSPECIFIED., .F., .F.,
 ( 4, 2, 4 ),
 ( 0.000000000000000000, 0.0001496588209255797074, 0.0002993176418511594148 ),
 .UNSPECIFIED. ) ;
#178809=FACE_OUTER_BOUND ( 'NONE', #101880, .T. ) ;
#178811=ORIENTED_EDGE ( 'NONE', *, *, #201831, .T. ) ;
#178815=ORIENTED_EDGE ( 'NONE', *, *, #98935, .F. ) ;
#178820=EDGE_LOOP ( 'NONE', ( #43013, #82803, #60448, #33968 ) ) ;
#178826=CARTESIAN_POINT ( 'NONE',  ( -18.59999999999999787, 76.00000000001237765, -170.0231074845243597 ) ) ;
#178841=VERTEX_POINT ( 'NONE', #175418 ) ;
#178850=CARTESIAN_POINT ( 'NONE',  ( 18.60000000000000497, 85.52394631232981226, -129.6410794891860974 ) ) ;
#178851=CYLINDRICAL_SURFACE ( 'NONE', #44721, 0.1000000000000026007 ) ;
#178856=CARTESIAN_POINT ( 'NONE',  ( 18.49999999999999289, 69.55000000001230376, -160.0060803140843859 ) ) ;
#178857=CIRCLE ( 'NONE', #95427, 0.09999999999999939493 ) ;
#178861=AXIS2_PLACEMENT_3D ( 'NONE', #183487, #167800, #103914 ) ;
#178886=CARTESIAN_POINT ( 'NONE',  ( 20.94999999999999929, 69.35000000001231513, -160.0060803140843859 ) ) ;
#178940=CARTESIAN_POINT ( 'NONE',  ( 21.05000000000000071, 76.00000000001213607, -136.5231074845243313 ) ) ;
#178949=ADVANCED_FACE ( 'NONE', ( #89127 ), #203937, .T. ) ;
#178975=ORIENTED_EDGE ( 'NONE', *, *, #123934, .F. ) ;
#178988=AXIS2_PLACEMENT_3D ( 'NONE', #97601, #181042, #216287 ) ;
#179000=CARTESIAN_POINT ( 'NONE',  ( 21.07928932188134397, 76.00000000001237765, -170.0231074845243597 ) ) ;
#179044=LINE ( 'NONE', #162034, #127910 ) ;
#179073=AXIS2_PLACEMENT_3D ( 'NONE', #49392, #131486, #228027 ) ;
#179080=TOROIDAL_SURFACE ( 'NONE', #170918, 0.2000000000000000111, 0.1000000000000000056 ) ;
#179112=ORIENTED_EDGE ( 'NONE', *, *, #55966, .F. ) ;
#179113=CARTESIAN_POINT ( 'NONE',  ( -18.50000000000000000, 65.70729864261028297, -131.0657455973724836 ) ) ;
#179116=DIRECTION ( 'NONE',  ( 0.000000000000000000, 7.056502275159890832E-15, -1.000000000000000000 ) ) ;
#179135=ORIENTED_EDGE ( 'NONE', *, *, #25504, .F. ) ;
#179138=DIRECTION ( 'NONE',  ( 0.000000000000000000, 0.000000000000000000, 1.000000000000000000 ) ) ;
#179156=CIRCLE ( 'NONE', #54209, 4.049999999999998046 ) ;
#179163=EDGE_CURVE ( 'NONE', #161742, #9710, #211629, .T. ) ;
#179176=EDGE_CURVE ( 'NONE', #231943, #76888, #40954, .T. ) ;
#179190=FACE_OUTER_BOUND ( 'NONE', #136075, .T. ) ;
#179204=DIRECTION ( 'NONE',  ( 0.000000000000000000, 1.000000000000000000, 0.000000000000000000 ) ) ;
#179221=ORIENTED_EDGE ( 'NONE', *, *, #166321, .T. ) ;
#179226=DIRECTION ( 'NONE',  ( 0.7071067811865474617, -0.7071067811865474617, -5.142139384388980375E-15 ) ) ;
#179246=DIRECTION ( 'NONE',  ( 0.000000000000000000, 1.069579021796876340E-15, 1.000000000000000000 ) ) ;
#179249=ADVANCED_FACE ( 'NONE', ( #19881 ), #1567, .F. ) ;
#179283=CARTESIAN_POINT ( 'NONE',  ( -21.05000000000000071, 70.10000000001220144, -146.7422072491807796 ) ) ;
#179295=ORIENTED_EDGE ( 'NONE', *, *, #195351, .T. ) ;
#179310=ORIENTED_EDGE ( 'NONE', *, *, #70519, .T. ) ;
#179313=CARTESIAN_POINT ( 'NONE',  ( -18.42609945526433535, 85.49999971050328895, -163.0237449942759156 ) ) ;
#179343=ORIENTED_EDGE ( 'NONE', *, *, #143036, .T. ) ;
#179366=CARTESIAN_POINT ( 'NONE',  ( -20.94999999999999929, 76.00000000001213607, -136.5231074845243313 ) ) ;
#179369=CARTESIAN_POINT ( 'NONE',  ( -23.15000000000000213, 87.65000000001246860, -181.7731074845242745 ) ) ;
#179374=CARTESIAN_POINT ( 'NONE',  ( 19.97071067811864609, 64.27928932189357170, -148.6731074845244507 ) ) ;
#179409=EDGE_LOOP ( 'NONE', ( #56308, #176197, #172667, #71557, #249230 ) ) ;
#179429=VECTOR ( 'NONE', #79862, 1000.000000000000000 ) ;
#179433=EDGE_CURVE ( 'NONE', #201875, #5985, #224078, .T. ) ;
#179439=CARTESIAN_POINT ( 'NONE',  ( -22.41119224318417125, 76.00000000001246292, -181.6726782920691505 ) ) ;
#179444=AXIS2_PLACEMENT_3D ( 'NONE', #84232, #146815, #28207 ) ;
#179455=CARTESIAN_POINT ( 'NONE',  ( 21.14999999999999858, 69.45934304831114048, -170.0231074845243882 ) ) ;
#179510=CIRCLE ( 'NONE', #83770, 0.09999999999998898659 ) ;
#179512=ORIENTED_EDGE ( 'NONE', *, *, #166072, .T. ) ;
#179522=CARTESIAN_POINT ( 'NONE',  ( 23.14999999999999858, 78.00000000001213607, -136.5231074845243029 ) ) ;
#179542=EDGE_CURVE ( 'NONE', #86021, #205324, #93951, .T. ) ;
#179556=DIRECTION ( 'NONE',  ( 0.000000000000000000, 0.000000000000000000, 1.000000000000000000 ) ) ;
#179566=CARTESIAN_POINT ( 'NONE',  ( 18.59999999999999787, 77.36242903720540198, -128.6342262366031548 ) ) ;
#179568=ORIENTED_EDGE ( 'NONE', *, *, #65569, .T. ) ;
#179592=AXIS2_PLACEMENT_3D ( 'NONE', #81501, #140199, #157252 ) ;
#179596=VERTEX_POINT ( 'NONE', #227882 ) ;
#179610=LINE ( 'NONE', #256495, #23163 ) ;
#179614=ORIENTED_EDGE ( 'NONE', *, *, #12329, .F. ) ;
#179637=( BOUNDED_SURFACE ( )  B_SPLINE_SURFACE ( 3, 2, ( 
 ( #167622, #111478, #9805 ),
 ( #203199, #151913, #231442 ),
 ( #230138, #129754, #250968 ),
 ( #162815, #128475, #191042 ),
 ( #242323, #108901, #29412 ),
 ( #30686, #88031, #110182 ) ),
 .UNSPECIFIED., .F., .F., .F. ) 
 B_SPLINE_SURFACE_WITH_KNOTS ( ( 4, 2, 4 ),
 ( 3, 3 ),
 ( -1.776356839400250465E-15, 0.7853981633974468357, 1.570796326794895448 ),
 ( 0.000000000000000000, 1.000000000000000000 ),
 .UNSPECIFIED. ) 
 GEOMETRIC_REPRESENTATION_ITEM ( )  RATIONAL_B_SPLINE_SURFACE ( (
 ( 1.000000000000000000, 0.5000000000000456302, 1.000000000000000000),
 ( 1.000000000000000000, 0.4993418825331401578, 1.000000000000000000),
 ( 1.000000000000000000, 0.5278258667061684895, 1.000000000000000000),
 ( 1.000000000000000000, 0.6092287576692355655, 1.000000000000000000),
 ( 1.000000000000000000, 0.6611148371781849775, 1.000000000000000000),
 ( 1.000000000000000000, 0.7071067811865597852, 1.000000000000000000) ) ) 
 REPRESENTATION_ITEM ( '' )  SURFACE ( )  );
#179661=EDGE_CURVE ( 'NONE', #18809, #214666, #95281, .T. ) ;
#179673=EDGE_CURVE ( 'NONE', #64025, #50939, #3684, .T. ) ;
#179697=CARTESIAN_POINT ( 'NONE',  ( 18.43630871534878324, 85.67980087481501528, -129.8624754165401498 ) ) ;
#179724=AXIS2_PLACEMENT_3D ( 'NONE', #204231, #24341, #23064 ) ;
#179762=VECTOR ( 'NONE', #226973, 1000.000000000000000 ) ;
#179765=ORIENTED_EDGE ( 'NONE', *, *, #60193, .F. ) ;
#179771=ORIENTED_EDGE ( 'NONE', *, *, #208854, .T. ) ;
#179772=CIRCLE ( 'NONE', #67322, 0.1000000000000043771 ) ;
#179779=DIRECTION ( 'NONE',  ( -3.265361837132813093E-16, -1.000000000000000000, -7.086529944415894657E-15 ) ) ;
#179782=CARTESIAN_POINT ( 'NONE',  ( 20.95545211741311320, 65.41358668846837077, -162.4369606249361198 ) ) ;
#179793=DIRECTION ( 'NONE',  ( -1.000000000000000000, 0.000000000000000000, 0.000000000000000000 ) ) ;
#179856=CARTESIAN_POINT ( 'NONE',  ( -18.58735405345342784, 85.56647862034870400, -129.7003928382583524 ) ) ;
#179890=DIRECTION ( 'NONE',  ( 0.000000000000000000, -7.086529944415894657E-15, 1.000000000000000000 ) ) ;
#179897=CIRCLE ( 'NONE', #34344, 0.09999999999999939493 ) ;
#179906=CARTESIAN_POINT ( 'NONE',  ( -20.54999999999999716, 73.60000000001224407, -149.7477294072864709 ) ) ;
#179913=DIRECTION ( 'NONE',  ( 0.000000000000000000, -7.172728831056617961E-15, 1.000000000000000000 ) ) ;
#179922=ORIENTED_EDGE ( 'NONE', *, *, #116193, .F. ) ;
#179942=CARTESIAN_POINT ( 'NONE',  ( 23.14999999999999858, 76.00000000001213607, -136.5231074845243313 ) ) ;
#179959=ORIENTED_EDGE ( 'NONE', *, *, #248590, .F. ) ;
#179968=CARTESIAN_POINT ( 'NONE',  ( 20.94999999999999929, 76.00000000001213607, -136.5231074845243313 ) ) ;
#179990=EDGE_CURVE ( 'NONE', #30528, #70015, #12097, .T. ) ;
#179993=CARTESIAN_POINT ( 'NONE',  ( -20.85000000000000142, 64.25000000001215028, -136.5231074845244166 ) ) ;
#179998=CIRCLE ( 'NONE', #242332, 12.87499999999999822 ) ;
#180036=VERTEX_POINT ( 'NONE', #120482 ) ;
#180049=FACE_OUTER_BOUND ( 'NONE', #255577, .T. ) ;
#180054=EDGE_CURVE ( 'NONE', #19886, #216520, #154478, .T. ) ;
#180087=CARTESIAN_POINT ( 'NONE',  ( 18.59999999999999432, 77.13501884592227498, -128.8061306010920362 ) ) ;
#180097=CARTESIAN_POINT ( 'NONE',  ( 21.05000000000000071, 87.48912529308822172, -139.5231074845243029 ) ) ;
#180102=EDGE_LOOP ( 'NONE', ( #138102, #249586, #21946 ) ) ;
#180106=EDGE_CURVE ( 'NONE', #232077, #125708, #27806, .T. ) ;
#180111=FACE_OUTER_BOUND ( 'NONE', #139286, .T. ) ;
#180117=CARTESIAN_POINT ( 'NONE',  ( 22.39999999999999503, 76.00000000001243450, -177.8138870828977360 ) ) ;
#180121=ORIENTED_EDGE ( 'NONE', *, *, #179176, .T. ) ;
#180135=CARTESIAN_POINT ( 'NONE',  ( 23.15000000000000213, 87.39257802171783851, -139.5970570643562212 ) ) ;
#180142=VERTEX_POINT ( 'NONE', #47308 ) ;
#180162=CARTESIAN_POINT ( 'NONE',  ( -20.64999999999999858, 71.65000000001222702, -148.8731074845244109 ) ) ;
#180212=CARTESIAN_POINT ( 'NONE',  ( -20.00857864376270001, 66.85000000001222986, -148.8731074845244393 ) ) ;
#180225=CARTESIAN_POINT ( 'NONE',  ( -20.54999999999999716, 76.00000000001213607, -136.5231074845243313 ) ) ;
#180237=ORIENTED_EDGE ( 'NONE', *, *, #210676, .T. ) ;
#180250=DIRECTION ( 'NONE',  ( 0.000000000000000000, 6.982962677686266711E-15, -1.000000000000000000 ) ) ;
#180251=CARTESIAN_POINT ( 'NONE',  ( -18.50000000000000000, 66.75000000001223555, -148.8731074845244393 ) ) ;
#180258=ORIENTED_EDGE ( 'NONE', *, *, #28637, .T. ) ;
#180265=CARTESIAN_POINT ( 'NONE',  ( 23.24999999999999289, 69.55000000001223270, -148.8731074845244109 ) ) ;
#180281=FACE_OUTER_BOUND ( 'NONE', #65570, .T. ) ;
#180351=AXIS2_PLACEMENT_3D ( 'NONE', #254369, #171059, #15819 ) ;
#180364=ORIENTED_EDGE ( 'NONE', *, *, #61654, .T. ) ;
#180366=CARTESIAN_POINT ( 'NONE',  ( -18.51024323315077424, 65.68895814178263493, -131.0026557862138645 ) ) ;
#180373=ADVANCED_FACE ( 'NONE', ( #248095 ), #109859, .T. ) ;
#180402=DIRECTION ( 'NONE',  ( -1.000000000000000000, 0.000000000000000000, -0.000000000000000000 ) ) ;
#180409=LINE ( 'NONE', #229797, #123662 ) ;
#180470=VECTOR ( 'NONE', #45560, 1000.000000000000000 ) ;
#180513=DIRECTION ( 'NONE',  ( -1.000000000000000000, -0.000000000000000000, -0.000000000000000000 ) ) ;
#180537=CYLINDRICAL_SURFACE ( 'NONE', #244192, 0.1000000000000028644 ) ;
#180567=ORIENTED_EDGE ( 'NONE', *, *, #3630, .T. ) ;
#180577=ORIENTED_EDGE ( 'NONE', *, *, #66429, .F. ) ;
#180592=VECTOR ( 'NONE', #251974, 1000.000000000000000 ) ;
#180623=ADVANCED_FACE ( 'NONE', ( #6617 ), #172168, .T. ) ;
#180631=EDGE_LOOP ( 'NONE', ( #237866, #241312, #216437, #23077 ) ) ;
#180636=FACE_OUTER_BOUND ( 'NONE', #106272, .T. ) ;
#180637=CARTESIAN_POINT ( 'NONE',  ( 22.47071067811864964, 75.90090754530983475, -177.7431822290224090 ) ) ;
#180671=CARTESIAN_POINT ( 'NONE',  ( 23.14999999999999858, 76.00000000001237765, -170.0231074845243597 ) ) ;
#180676=DIRECTION ( 'NONE',  ( 1.000000000000000000, -0.000000000000000000, 0.000000000000000000 ) ) ;
#180679=CIRCLE ( 'NONE', #9987, 0.2000000000000057288 ) ;
#180733=CARTESIAN_POINT ( 'NONE',  ( 20.94999999999999929, 65.70711192142388768, -131.0651054685122574 ) ) ;
#180743=CARTESIAN_POINT ( 'NONE',  ( -23.15000000000000213, 74.00000000001223555, -149.7477294072864709 ) ) ;
#180753=CYLINDRICAL_SURFACE ( 'NONE', #110846, 0.09999999999998898659 ) ;
#180773=DIRECTION ( 'NONE',  ( 1.000000000000000000, -1.875376730785737719E-16, -1.309568571767809260E-30 ) ) ;
#180823=CIRCLE ( 'NONE', #197372, 0.09999999999998898659 ) ;
#180824=CARTESIAN_POINT ( 'NONE',  ( 23.14999999999999858, 70.50000000001223555, -148.9283735034374843 ) ) ;
#180856=EDGE_CURVE ( 'NONE', #115854, #116101, #249946, .T. ) ;
#180901=VECTOR ( 'NONE', #237506, 1000.000000000000000 ) ;
#180904=AXIS2_PLACEMENT_3D ( 'NONE', #32377, #191453, #55707 ) ;
#180908=DIRECTION ( 'NONE',  ( 0.000000000000000000, 0.000000000000000000, 1.000000000000000000 ) ) ;
#180933=DIRECTION ( 'NONE',  ( 0.000000000000000000, 0.000000000000000000, -1.000000000000000000 ) ) ;
#180939=CIRCLE ( 'NONE', #114293, 0.09999999999998898659 ) ;
#180944=CIRCLE ( 'NONE', #80963, 0.5000000000000004441 ) ;
#180949=ADVANCED_FACE ( 'NONE', ( #225343 ), #128847, .T. ) ;
#180958=DIRECTION ( 'NONE',  ( 0.7071067811865475727, -0.7071067811865475727, -4.937700262164531476E-15 ) ) ;
#180970=ORIENTED_EDGE ( 'NONE', *, *, #251587, .F. ) ;
#180984=CIRCLE ( 'NONE', #18485, 0.1000000000000072220 ) ;
#181001=LINE ( 'NONE', #234540, #42114 ) ;
#181009=DIRECTION ( 'NONE',  ( -0.000000000000000000, -1.000000000000000000, -8.609265936414532828E-15 ) ) ;
#181018=LINE ( 'NONE', #2347, #172198 ) ;
#181025=DIRECTION ( 'NONE',  ( 0.000000000000000000, -6.982962677686266711E-15, 1.000000000000000000 ) ) ;
#181039=AXIS2_PLACEMENT_3D ( 'NONE', #37289, #56795, #136333 ) ;
#181042=DIRECTION ( 'NONE',  ( 1.000000000000000000, -2.952720810173289112E-16, -2.061873921506763405E-30 ) ) ;
#181079=ORIENTED_EDGE ( 'NONE', *, *, #151316, .F. ) ;
#181088=ADVANCED_FACE ( 'NONE', ( #191409 ), #74033, .F. ) ;
#181091=CARTESIAN_POINT ( 'NONE',  ( 23.24999999999999645, 76.00000000001213607, -136.5231074845243313 ) ) ;
#181098=CARTESIAN_POINT ( 'NONE',  ( -22.39999999999999858, 64.25000000001237765, -170.1231074845244393 ) ) ;
#181109=VECTOR ( 'NONE', #273, 1000.000000000000000 ) ;
#181161=CYLINDRICAL_SURFACE ( 'NONE', #63981, 0.09999999999998898659 ) ;
#181166=AXIS2_PLACEMENT_3D ( 'NONE', #120939, #21817, #221270 ) ;
#181168=DIRECTION ( 'NONE',  ( 0.000000000000000000, 1.000000000000000000, 6.982962677686266711E-15 ) ) ;
#181189=STYLED_ITEM ( 'NONE', ( #231555 ), #196328 ) ;
#181199=FACE_OUTER_BOUND ( 'NONE', #48412, .T. ) ;
#181205=CARTESIAN_POINT ( 'NONE',  ( 18.39999999999999858, 85.60000000001210196, -129.8229180933022633 ) ) ;
#181213=DIRECTION ( 'NONE',  ( 0.000000000000000000, 0.000000000000000000, -1.000000000000000000 ) ) ;
#181238=FACE_OUTER_BOUND ( 'NONE', #81655, .T. ) ;
#181243=CARTESIAN_POINT ( 'NONE',  ( 18.59117750673696534, 65.66751761918692409, -130.9282609406112670 ) ) ;
#181262=EDGE_CURVE ( 'NONE', #164498, #152420, #246845, .T. ) ;
#181286=CARTESIAN_POINT ( 'NONE',  ( -21.14999999999999858, 64.25000000001232081, -163.2392418215462726 ) ) ;
#181290=CARTESIAN_POINT ( 'NONE',  ( -22.47071067811865319, 75.90090754530983475, -177.7431822290224090 ) ) ;
#181299=EDGE_LOOP ( 'NONE', ( #52137, #226914, #89615, #194047 ) ) ;
#181300=CARTESIAN_POINT ( 'NONE',  ( -18.59999999999999787, 77.83534155023670564, -158.4679561919613491 ) ) ;
#181328=ADVANCED_FACE ( 'NONE', ( #46078 ), #26545, .T. ) ;
#181348=LINE ( 'NONE', #177515, #76257 ) ;
#181364=CARTESIAN_POINT ( 'NONE',  ( 21.05000000000000071, 85.40000000001231228, -160.1291383618718385 ) ) ;
#181376=ORIENTED_EDGE ( 'NONE', *, *, #172255, .F. ) ;
#181400=ORIENTED_EDGE ( 'NONE', *, *, #94939, .T. ) ;
#181401=DIRECTION ( 'NONE',  ( 0.000000000000000000, -1.000000000000000000, -6.982962677686265922E-15 ) ) ;
#181423=CARTESIAN_POINT ( 'NONE',  ( -20.64999999999999858, 85.50000000001222134, -146.4170766071767389 ) ) ;
#181428=DIRECTION ( 'NONE',  ( -1.000000000000000000, 3.265361837132813093E-16, 2.280189983783949500E-30 ) ) ;
#181459=ADVANCED_FACE ( 'NONE', ( #151644 ), #91641, .F. ) ;
#181478=CARTESIAN_POINT ( 'NONE',  ( 20.13684514580103624, 66.50414460725968979, -161.8800757988351791 ) ) ;
#181524=CARTESIAN_POINT ( 'NONE',  ( -21.55000000000000426, 68.25000000001223555, -148.8731074845244109 ) ) ;
#181528=ORIENTED_EDGE ( 'NONE', *, *, #130174, .F. ) ;
#181548=EDGE_CURVE ( 'NONE', #141640, #176854, #328, .T. ) ;
#181549=CARTESIAN_POINT ( 'NONE',  ( 23.14999999999999858, 70.05000000001221849, -146.8288097895591875 ) ) ;
#181575=DIRECTION ( 'NONE',  ( 0.000000000000000000, 0.000000000000000000, 1.000000000000000000 ) ) ;
#181576=EDGE_CURVE ( 'NONE', #173680, #103428, #154484, .T. ) ;
#181587=TOROIDAL_SURFACE ( 'NONE', #31575, 11.70000000000000462, 0.1000000000000000056 ) ;
#181592=FACE_OUTER_BOUND ( 'NONE', #219195, .T. ) ;
#181600=CARTESIAN_POINT ( 'NONE',  ( -18.45140287520618472, 85.48607773954165623, -129.8825843578381694 ) ) ;
#181610=EDGE_LOOP ( 'NONE', ( #1661, #79904, #7212, #228607 ) ) ;
#181646=EDGE_CURVE ( 'NONE', #127786, #222829, #250312, .T. ) ;
#181661=ORIENTED_EDGE ( 'NONE', *, *, #32797, .F. ) ;
#181679=AXIS2_PLACEMENT_3D ( 'NONE', #172242, #11865, #13134 ) ;
#181689=CARTESIAN_POINT ( 'NONE',  ( 21.04999999999999716, 65.37049252075472339, -162.3951280845285794 ) ) ;
#181695=LINE ( 'NONE', #162145, #28004 ) ;
#181717=PLANE ( 'NONE',  #238728 ) ;
#181748=EDGE_CURVE ( 'NONE', #99016, #64653, #158758, .T. ) ;
#181750=ORIENTED_EDGE ( 'NONE', *, *, #189256, .T. ) ;
#181756=AXIS2_PLACEMENT_3D ( 'NONE', #99830, #41205, #227192 ) ;
#181798=VERTEX_POINT ( 'NONE', #173499 ) ;
#181811=CARTESIAN_POINT ( 'NONE',  ( 23.24999999999999289, 64.35000000001228670, -157.8731074845244393 ) ) ;
#181821=EDGE_CURVE ( 'NONE', #25682, #95684, #25639, .T. ) ;
#181832=DIRECTION ( 'NONE',  ( 0.000000000000000000, 0.000000000000000000, -1.000000000000000000 ) ) ;
#181846=ORIENTED_EDGE ( 'NONE', *, *, #166321, .F. ) ;
#181853=AXIS2_PLACEMENT_3D ( 'NONE', #248828, #41971, #234373 ) ;
#181873=CYLINDRICAL_SURFACE ( 'NONE', #151583, 0.1000000000000028644 ) ;
#181874=EDGE_CURVE ( 'NONE', #68761, #104106, #246225, .T. ) ;
#181880=EDGE_LOOP ( 'NONE', ( #179221, #226574, #43990, #237606 ) ) ;
#181894=LINE ( 'NONE', #4520, #88933 ) ;
#181903=CIRCLE ( 'NONE', #19603, 0.5000000000000004441 ) ;
#181907=DIRECTION ( 'NONE',  ( 0.000000000000000000, -0.9915357197604982575, 0.1298341882519033486 ) ) ;
#181917=ORIENTED_EDGE ( 'NONE', *, *, #146481, .T. ) ;
#181918=CARTESIAN_POINT ( 'NONE',  ( 21.00023020733501866, 76.00000000001243450, -176.4139767297927222 ) ) ;
#181993=DIRECTION ( 'NONE',  ( -0.7071067811865474617, 0.7071067811865474617, 4.937700262164531476E-15 ) ) ;
#181998=FACE_OUTER_BOUND ( 'NONE', #27519, .T. ) ;
#182012=CARTESIAN_POINT ( 'NONE',  ( 20.94788355080264353, 65.69792220476342948, -131.0335554128461979 ) ) ;
#182022=ORIENTED_EDGE ( 'NONE', *, *, #94939, .F. ) ;
#182039=CARTESIAN_POINT ( 'NONE',  ( -22.50000000000000000, 64.35042919246758686, -170.1231074845244393 ) ) ;
#182041=SPHERICAL_SURFACE ( 'NONE', #101717, 0.1000000000000000056 ) ;
#182057=EDGE_CURVE ( 'NONE', #188351, #134102, #138048, .T. ) ;
#182095=DIRECTION ( 'NONE',  ( 0.000000000000000000, 0.000000000000000000, -1.000000000000000000 ) ) ;
#182096=EDGE_CURVE ( 'NONE', #132176, #133329, #171890, .T. ) ;
#182145=LINE ( 'NONE', #141715, #229627 ) ;
#182156=EDGE_CURVE ( 'NONE', #239159, #134685, #147145, .T. ) ;
#182166=DIRECTION ( 'NONE',  ( -0.000000000000000000, 6.982962677686266711E-15, -1.000000000000000000 ) ) ;
#182201=CARTESIAN_POINT ( 'NONE',  ( -20.94999999999999929, 87.48912529308822172, -139.4231074845242802 ) ) ;
#182244=CARTESIAN_POINT ( 'NONE',  ( -1.820710678118658388, 85.92928932189354896, -145.3731074845242972 ) ) ;
#182252=VERTEX_POINT ( 'NONE', #174474 ) ;
#182262=CARTESIAN_POINT ( 'NONE',  ( 20.94999999999999929, 70.15000000001221281, -146.6556047088023149 ) ) ;
#182266=PLANE ( 'NONE',  #143569 ) ;
#182267=B_SPLINE_CURVE_WITH_KNOTS ( 'NONE', 3,
 ( #36083, #16523, #217249, #175595, #255044, #236823, #23915, #235540, #56878, #77740 ),
 .UNSPECIFIED., .F., .F.,
 ( 4, 2, 2, 2, 4 ),
 ( 0.000000000000000000, 0.0001584437871625799649, 0.0002376656807438381125, 0.0002772766275344300930, 0.0003168875743250220735 ),
 .UNSPECIFIED. ) ;
#182270=CARTESIAN_POINT ( 'NONE',  ( -20.85000000000000142, 65.66751761918690988, -130.9282609406112670 ) ) ;
#182293=AXIS2_PLACEMENT_3D ( 'NONE', #217047, #57975, #60551 ) ;
#182300=DIRECTION ( 'NONE',  ( 0.000000000000000000, 0.8700118002898356018, -0.4930308989875170078 ) ) ;
#182306=ORIENTED_EDGE ( 'NONE', *, *, #96204, .T. ) ;
#182340=CARTESIAN_POINT ( 'NONE',  ( -20.94999999999999929, 87.29603075034764004, -166.9752083248604038 ) ) ;
#182343=CARTESIAN_POINT ( 'NONE',  ( 21.05000000000000071, 84.73084112150752389, -146.1211822035086527 ) ) ;
#182393=DIRECTION ( 'NONE',  ( -0.000000000000000000, 0.1298341882519668811, 0.9915357197604899309 ) ) ;
#182407=VECTOR ( 'NONE', #58319, 1000.000000000000000 ) ;
#182421=CARTESIAN_POINT ( 'NONE',  ( -20.64999999999999858, 76.00000000001213607, -136.5231074845243313 ) ) ;
#182441=DIRECTION ( 'NONE',  ( 1.000000000000000000, 0.000000000000000000, 0.000000000000000000 ) ) ;
#182448=AXIS2_PLACEMENT_3D ( 'NONE', #70114, #229169, #49232 ) ;
#182460=VERTEX_POINT ( 'NONE', #141698 ) ;
#182499=DIRECTION ( 'NONE',  ( 1.000000000000000000, 0.000000000000000000, 0.000000000000000000 ) ) ;
#182519=ORIENTED_EDGE ( 'NONE', *, *, #243537, .T. ) ;
#182539=DIRECTION ( 'NONE',  ( 0.000000000000000000, -6.467318590049456648E-15, 1.000000000000000000 ) ) ;
#182548=ORIENTED_EDGE ( 'NONE', *, *, #146375, .F. ) ;
#182550=AXIS2_PLACEMENT_3D ( 'NONE', #127148, #28077, #150569 ) ;
#182555=DIRECTION ( 'NONE',  ( 1.000000000000000000, -2.952720810173289112E-16, -2.061873921506763405E-30 ) ) ;
#182598=ORIENTED_EDGE ( 'NONE', *, *, #38334, .T. ) ;
#182667=CARTESIAN_POINT ( 'NONE',  ( 20.94999999999999929, 74.16465844978787914, -158.4679561919613775 ) ) ;
#182675=ORIENTED_EDGE ( 'NONE', *, *, #199048, .F. ) ;
#182677=ORIENTED_EDGE ( 'NONE', *, *, #163463, .T. ) ;
#182682=FACE_OUTER_BOUND ( 'NONE', #183772, .T. ) ;
#182683=CARTESIAN_POINT ( 'NONE',  ( 18.59999999999999432, 85.48068669529105534, -129.5819923157664562 ) ) ;
#182715=DIRECTION ( 'NONE',  ( 0.000000000000000000, 0.8660254037844378194, 0.5000000000000016653 ) ) ;
#182732=DIRECTION ( 'NONE',  ( -0.000000000000000000, 6.982962677686266711E-15, -1.000000000000000000 ) ) ;
#182764=DIRECTION ( 'NONE',  ( 0.000000000000000000, 0.000000000000000000, 1.000000000000000000 ) ) ;
#182775=ORIENTED_EDGE ( 'NONE', *, *, #243850, .F. ) ;
#182785=EDGE_CURVE ( 'NONE', #206438, #80321, #33687, .T. ) ;
#182788=AXIS2_PLACEMENT_3D ( 'NONE', #140221, #101062, #103660 ) ;
#182799=DIRECTION ( 'NONE',  ( 0.000000000000000000, -6.853228547068871147E-15, 1.000000000000000000 ) ) ;
#182800=AXIS2_PLACEMENT_3D ( 'NONE', #84596, #202032, #123780 ) ;
#182858=SPHERICAL_SURFACE ( 'NONE', #218723, 0.1000000000000000056 ) ;
#182905=AXIS2_PLACEMENT_3D ( 'NONE', #105967, #70753, #150275 ) ;
#182952=ORIENTED_EDGE ( 'NONE', *, *, #214430, .T. ) ;
#182981=CARTESIAN_POINT ( 'NONE',  ( 21.05000000000000071, 65.57661458509943486, -162.5310555606543232 ) ) ;
#182984=CYLINDRICAL_SURFACE ( 'NONE', #128639, 0.09999999999998898659 ) ;
#183010=EDGE_LOOP ( 'NONE', ( #223413, #110645, #57838, #227931 ) ) ;
#183081=EDGE_CURVE ( 'NONE', #236987, #198367, #121348, .T. ) ;
#183112=CIRCLE ( 'NONE', #41656, 0.09999999999999939493 ) ;
#183126=LINE ( 'NONE', #48728, #104483 ) ;
#183148=ORIENTED_EDGE ( 'NONE', *, *, #231921, .T. ) ;
#183151=ORIENTED_EDGE ( 'NONE', *, *, #29356, .F. ) ;
#183179=DIRECTION ( 'NONE',  ( 0.000000000000000000, 0.000000000000000000, 1.000000000000000000 ) ) ;
#183212=DIRECTION ( 'NONE',  ( 4.239556034732056743E-17, 0.1298341882519953860, 0.9915357197604862671 ) ) ;
#183221=DIRECTION ( 'NONE',  ( 0.000000000000000000, -7.056502275159890832E-15, 1.000000000000000000 ) ) ;
#183237=CARTESIAN_POINT ( 'NONE',  ( -18.59999999999999787, 77.26178616857734482, -161.9366085209788650 ) ) ;
#183264=AXIS2_PLACEMENT_3D ( 'NONE', #4695, #219912, #225024 ) ;
#183270=VERTEX_POINT ( 'NONE', #190182 ) ;
#183308=FACE_OUTER_BOUND ( 'NONE', #121607, .T. ) ;
#183311=ORIENTED_EDGE ( 'NONE', *, *, #216556, .T. ) ;
#183332=ORIENTED_EDGE ( 'NONE', *, *, #46958, .F. ) ;
#183334=CARTESIAN_POINT ( 'NONE',  ( -21.65000000000000213, 68.29142135624952914, -148.7731074845244166 ) ) ;
#183345=ORIENTED_EDGE ( 'NONE', *, *, #213656, .T. ) ;
#183395=ORIENTED_EDGE ( 'NONE', *, *, #157061, .T. ) ;
#183427=DIRECTION ( 'NONE',  ( 1.000000000000000000, 0.000000000000000000, 0.000000000000000000 ) ) ;
#183432=EDGE_CURVE ( 'NONE', #104106, #52101, #187168, .T. ) ;
#183447=VECTOR ( 'NONE', #9963, 1000.000000000000000 ) ;
#183453=EDGE_CURVE ( 'NONE', #74763, #243465, #63194, .T. ) ;
#183457=CARTESIAN_POINT ( 'NONE',  ( 18.46905048506370406, 85.47374425739451453, -129.8471211922688724 ) ) ;
#183462=CARTESIAN_POINT ( 'NONE',  ( 21.05995757104869881, 67.22461075529101038, -157.8282023615332150 ) ) ;
#183483=DIRECTION ( 'NONE',  ( 0.000000000000000000, 0.000000000000000000, -1.000000000000000000 ) ) ;
#183487=CARTESIAN_POINT ( 'NONE',  ( 20.85000000000000142, 68.97833521811203639, -132.6895420826271277 ) ) ;
#183505=CARTESIAN_POINT ( 'NONE',  ( 22.59080734064468743, 64.25000000001237765, -170.0538571926215070 ) ) ;
#183520=ADVANCED_FACE ( 'NONE', ( #171115 ), #17422, .T. ) ;
#183531=VERTEX_POINT ( 'NONE', #231062 ) ;
#183565=FACE_OUTER_BOUND ( 'NONE', #152710, .T. ) ;
#183589=DIRECTION ( 'NONE',  ( 0.000000000000000000, 6.982962677686266711E-15, -1.000000000000000000 ) ) ;
#183685=DIRECTION ( 'NONE',  ( 0.000000000000000000, 0.000000000000000000, 1.000000000000000000 ) ) ;
#183688=AXIS2_PLACEMENT_3D ( 'NONE', #176344, #193329, #159347 ) ;
#183692=EDGE_LOOP ( 'NONE', ( #249491, #44580, #161043 ) ) ;
#183727=ORIENTED_EDGE ( 'NONE', *, *, #238765, .F. ) ;
#183739=EDGE_CURVE ( 'NONE', #20227, #30979, #105047, .T. ) ;
#183772=EDGE_LOOP ( 'NONE', ( #180121, #88804, #158521, #151710 ) ) ;
#183777=AXIS2_PLACEMENT_3D ( 'NONE', #45780, #223127, #121501 ) ;
#183779=CARTESIAN_POINT ( 'NONE',  ( 19.99999999999998934, 64.25000000001220712, -145.1731074845244507 ) ) ;
#183784=CARTESIAN_POINT ( 'NONE',  ( -18.58671080940899500, 85.40693285883894248, -162.8989530196195972 ) ) ;
#183797=ORIENTED_EDGE ( 'NONE', *, *, #79432, .T. ) ;
#183847=ADVANCED_FACE ( 'NONE', ( #131627 ), #112087, .T. ) ;
#183891=DIRECTION ( 'NONE',  ( 1.000000000000000000, -7.304098846218134667E-16, -5.100424963727255829E-30 ) ) ;
#183921=ORIENTED_EDGE ( 'NONE', *, *, #20064, .F. ) ;
#183934=EDGE_CURVE ( 'NONE', #187756, #103678, #14277, .T. ) ;
#183996=DIRECTION ( 'NONE',  ( -0.000000000000000000, 1.000000000000000000, 6.982962677686266711E-15 ) ) ;
#184007=EDGE_CURVE ( 'NONE', #52602, #180036, #138205, .T. ) ;
#184023=VECTOR ( 'NONE', #241115, 1000.000000000000000 ) ;
#184041=DIRECTION ( 'NONE',  ( 1.000000000000000000, 0.000000000000000000, 0.000000000000000000 ) ) ;
#184042=AXIS2_PLACEMENT_3D ( 'NONE', #254819, #71129, #171524 ) ;
#184089=DIRECTION ( 'NONE',  ( 0.000000000000000000, 0.000000000000000000, 1.000000000000000000 ) ) ;
#184104=ORIENTED_EDGE ( 'NONE', *, *, #61952, .T. ) ;
#184134=( BOUNDED_SURFACE ( )  B_SPLINE_SURFACE ( 3, 2, ( 
 ( #256139, #3151, #197508 ),
 ( #18876, #580, #97092 ),
 ( #98370, #158430, #121849 ),
 ( #138785, #201369, #177973 ),
 ( #22764, #80098, #82671 ),
 ( #219640, #102230, #77543 ) ),
 .UNSPECIFIED., .F., .F., .F. ) 
 B_SPLINE_SURFACE_WITH_KNOTS ( ( 4, 2, 4 ),
 ( 3, 3 ),
 ( 0.0001300404313046550988, 0.0003183318589266453426, 0.0005066232865486356134 ),
 ( 0.000000000000000000, 1.000000000000000000 ),
 .UNSPECIFIED. ) 
 GEOMETRIC_REPRESENTATION_ITEM ( )  RATIONAL_B_SPLINE_SURFACE ( (
 ( 1.000000000000000000, 0.7071067811865719976, 1.000000000000000000),
 ( 1.000000000000000000, 0.7625113560537848389, 1.000000000000000000),
 ( 1.000000000000000000, 0.8126073484691938020, 1.000000000000000000),
 ( 1.000000000000000000, 0.8923049332728831828, 1.000000000000000000),
 ( 1.000000000000000000, 0.9231914937772871532, 1.000000000000000000),
 ( 1.000000000000000000, 0.9238795325112716395, 1.000000000000000000) ) ) 
 REPRESENTATION_ITEM ( '' )  SURFACE ( )  );
#184148=AXIS2_PLACEMENT_3D ( 'NONE', #223983, #7514, #124904 ) ;
#184150=DIRECTION ( 'NONE',  ( 0.000000000000000000, 0.000000000000000000, -1.000000000000000000 ) ) ;
#184170=ORIENTED_EDGE ( 'NONE', *, *, #162199, .T. ) ;
#184189=VECTOR ( 'NONE', #109484, 1000.000000000000000 ) ;
#184191=CARTESIAN_POINT ( 'NONE',  ( 20.94999999999999929, 76.00000000001213607, -136.5231074845243313 ) ) ;
#184197=CIRCLE ( 'NONE', #50907, 0.09999999999998898659 ) ;
#184205=CIRCLE ( 'NONE', #55014, 0.09999999999998898659 ) ;
#184207=CYLINDRICAL_SURFACE ( 'NONE', #222080, 0.09999999999999939493 ) ;
#184208=EDGE_LOOP ( 'NONE', ( #114317, #93695, #249545, #69006 ) ) ;
#184212=ORIENTED_EDGE ( 'NONE', *, *, #231279, .T. ) ;
#184216=EDGE_CURVE ( 'NONE', #114885, #30145, #67677, .T. ) ;
#184222=CIRCLE ( 'NONE', #84214, 0.1000000000000011990 ) ;
#184240=AXIS2_PLACEMENT_3D ( 'NONE', #38659, #196434, #178191 ) ;
#184248=FACE_OUTER_BOUND ( 'NONE', #84778, .T. ) ;
#184269=CIRCLE ( 'NONE', #101020, 0.1000000000000026007 ) ;
#184291=DIRECTION ( 'NONE',  ( -0.000000000000000000, -1.000000000000000000, -6.982962677686266711E-15 ) ) ;
#184317=FACE_OUTER_BOUND ( 'NONE', #86301, .T. ) ;
#184336=VERTEX_POINT ( 'NONE', #151873 ) ;
#184344=CARTESIAN_POINT ( 'NONE',  ( 21.05000000000000071, 69.74218538953624602, -170.1208977758331855 ) ) ;
#184351=ORIENTED_EDGE ( 'NONE', *, *, #134141, .T. ) ;
#184395=ORIENTED_EDGE ( 'NONE', *, *, #114790, .T. ) ;
#184396=VECTOR ( 'NONE', #75144, 1000.000000000000000 ) ;
#184405=CYLINDRICAL_SURFACE ( 'NONE', #134558, 0.1000000000000033362 ) ;
#184415=LINE ( 'NONE', #223528, #31445 ) ;
#184423=EDGE_CURVE ( 'NONE', #212994, #58091, #88498, .T. ) ;
#184430=ORIENTED_EDGE ( 'NONE', *, *, #245032, .F. ) ;
#184470=ORIENTED_EDGE ( 'NONE', *, *, #173760, .F. ) ;
#184475=CYLINDRICAL_SURFACE ( 'NONE', #133956, 0.1000000000000046685 ) ;
#184476=EDGE_LOOP ( 'NONE', ( #227785, #68007, #60068, #163541 ) ) ;
#184497=VERTEX_POINT ( 'NONE', #197378 ) ;
#184504=EDGE_CURVE ( 'NONE', #129641, #120222, #138660, .T. ) ;
#184505=ORIENTED_EDGE ( 'NONE', *, *, #103714, .T. ) ;
#184508=FACE_OUTER_BOUND ( 'NONE', #105803, .T. ) ;
#184514=DIRECTION ( 'NONE',  ( -0.000000000000000000, 6.982962677686266711E-15, -1.000000000000000000 ) ) ;
#184522=CIRCLE ( 'NONE', #68019, 11.64999999999999325 ) ;
#184564=CARTESIAN_POINT ( 'NONE',  ( 20.94403535211772294, 65.69367753730678317, -131.0189238066348594 ) ) ;
#184623=CARTESIAN_POINT ( 'NONE',  ( -23.15000000000000213, 70.10000000001220144, -146.7422072491807796 ) ) ;
#184679=ORIENTED_EDGE ( 'NONE', *, *, #28217, .F. ) ;
#184691=LINE ( 'NONE', #8638, #9218 ) ;
#184715=CARTESIAN_POINT ( 'NONE',  ( -18.50000000000000000, 77.16412189325330928, -128.6082593989527254 ) ) ;
#184718=CARTESIAN_POINT ( 'NONE',  ( 21.05000000000000071, 76.00000000001213607, -136.5231074845243313 ) ) ;
#184748=CARTESIAN_POINT ( 'NONE',  ( -20.94999999999999929, 77.16270174995034381, -162.1231074845243540 ) ) ;
#184789=EDGE_CURVE ( 'NONE', #193723, #173680, #209507, .T. ) ;
#184821=DIRECTION ( 'NONE',  ( 2.694716079187273439E-16, 1.000000000000000000, 6.467318590049456648E-15 ) ) ;
#184835=ORIENTED_EDGE ( 'NONE', *, *, #220977, .F. ) ;
#184837=CARTESIAN_POINT ( 'NONE',  ( 22.50014994444007144, 64.25028026812033488, -170.1061876412437641 ) ) ;
#184856=DIRECTION ( 'NONE',  ( 1.000000000000000000, 0.000000000000000000, 0.000000000000000000 ) ) ;
#184875=ADVANCED_FACE ( 'NONE', ( #198368 ), #158007, .T. ) ;
#184899=EDGE_LOOP ( 'NONE', ( #201837, #198334, #171739 ) ) ;
#184911=CARTESIAN_POINT ( 'NONE',  ( -21.05000000000000071, 76.00000000001234923, -167.1231074845243825 ) ) ;
#184917=DIRECTION ( 'NONE',  ( 0.000000000000000000, 6.467318590049456648E-15, -1.000000000000000000 ) ) ;
#184946=ORIENTED_EDGE ( 'NONE', *, *, #215719, .F. ) ;
#184971=LINE ( 'NONE', #205813, #42556 ) ;
#184973=DIRECTION ( 'NONE',  ( 0.000000000000000000, 6.982962677686266711E-15, -1.000000000000000000 ) ) ;
#184976=FACE_OUTER_BOUND ( 'NONE', #191425, .T. ) ;
#184995=FACE_OUTER_BOUND ( 'NONE', #245815, .T. ) ;
#185002=CARTESIAN_POINT ( 'NONE',  ( 22.40736611211992368, 76.00000000001246292, -181.6726782920691505 ) ) ;
#185021=CARTESIAN_POINT ( 'NONE',  ( 20.94999999999999929, 85.00000000001222134, -146.4170766071767389 ) ) ;
#185044=DIRECTION ( 'NONE',  ( -1.000000000000000000, 0.000000000000000000, -0.000000000000000000 ) ) ;
#185049=ORIENTED_EDGE ( 'NONE', *, *, #186038, .F. ) ;
#185067=AXIS2_PLACEMENT_3D ( 'NONE', #78895, #60624, #77608 ) ;
#185081=CARTESIAN_POINT ( 'NONE',  ( 23.14999999999999503, 69.35000000001222986, -148.8731074845244109 ) ) ;
#185144=ORIENTED_EDGE ( 'NONE', *, *, #165108, .T. ) ;
#185148=CARTESIAN_POINT ( 'NONE',  ( -22.50000000000000000, 64.35023708198045256, -170.1119174609113713 ) ) ;
#185177=AXIS2_PLACEMENT_3D ( 'NONE', #245216, #233041, #225607 ) ;
#185188=CARTESIAN_POINT ( 'NONE',  ( 20.94999999999999929, 70.10000000001220144, -146.7422072491807796 ) ) ;
#185217=CARTESIAN_POINT ( 'NONE',  ( -20.64999999999999858, 85.50000000001232081, -160.1291383618718385 ) ) ;
#185223=AXIS2_PLACEMENT_3D ( 'NONE', #132370, #210624, #35857 ) ;
#185235=CARTESIAN_POINT ( 'NONE',  ( 19.90621891164687440, 64.25000000001220712, -145.1946622066474220 ) ) ;
#185258=CIRCLE ( 'NONE', #135155, 0.09999999999998898659 ) ;
#185260=AXIS2_PLACEMENT_3D ( 'NONE', #132807, #169394, #212346 ) ;
#185272=CARTESIAN_POINT ( 'NONE',  ( -23.15000000000000213, 71.65000000001222702, -148.7731074845243882 ) ) ;
#185296=EDGE_CURVE ( 'NONE', #210038, #70242, #105801, .T. ) ;
#185330=EDGE_CURVE ( 'NONE', #49587, #61696, #226415, .T. ) ;
#185333=CARTESIAN_POINT ( 'NONE',  ( 22.39999999999999503, 76.10000000001245724, -181.6726782920691505 ) ) ;
#185368=ADVANCED_FACE ( 'NONE', ( #204471 ), #27169, .T. ) ;
#185369=AXIS2_PLACEMENT_3D ( 'NONE', #217719, #5077, #101602 ) ;
#185403=DIRECTION ( 'NONE',  ( -0.000000000000000000, 1.000000000000000000, 6.982962677686267499E-15 ) ) ;
#185418=DIRECTION ( 'NONE',  ( 0.000000000000000000, 0.000000000000000000, 1.000000000000000000 ) ) ;
#185420=EDGE_CURVE ( 'NONE', #224923, #127762, #89063, .T. ) ;
#185425=CIRCLE ( 'NONE', #135517, 12.87499999999999822 ) ;
#185427=CARTESIAN_POINT ( 'NONE',  ( -21.04999999999999716, 69.70076908992010090, -170.1215449845247463 ) ) ;
#185446=CARTESIAN_POINT ( 'NONE',  ( 21.04999999999999716, 67.12872031401664685, -157.8731074845244109 ) ) ;
#185453=EDGE_LOOP ( 'NONE', ( #160866, #161998, #5836 ) ) ;
#185460=DIRECTION ( 'NONE',  ( 0.000000000000000000, -0.9876197685951263461, 0.1568667991644794590 ) ) ;
#185467=ORIENTED_EDGE ( 'NONE', *, *, #162, .T. ) ;
#185473=ORIENTED_EDGE ( 'NONE', *, *, #134283, .T. ) ;
#185497=CARTESIAN_POINT ( 'NONE',  ( 21.87500000000000355, 66.25000000001223555, -148.8731074845244393 ) ) ;
#185498=CIRCLE ( 'NONE', #31413, 0.09999999999999939493 ) ;
#185520=B_SPLINE_CURVE_WITH_KNOTS ( 'NONE', 3,
 ( #68345, #203984, #25378, #5763, #206562, #27960 ),
 .UNSPECIFIED., .F., .F.,
 ( 4, 2, 4 ),
 ( 0.000000000000000000, 0.0001895189928937332253, 0.0003790379857874664506 ),
 .UNSPECIFIED. ) ;
#185524=EDGE_LOOP ( 'NONE', ( #102852, #229384, #33237, #156125, #71737 ) ) ;
#185563=LINE ( 'NONE', #199393, #254734 ) ;
#185588=ADVANCED_FACE ( 'NONE', ( #113091 ), #148367, .F. ) ;
#185602=AXIS2_PLACEMENT_3D ( 'NONE', #217207, #76423, #256281 ) ;
#185635=DIRECTION ( 'NONE',  ( 1.000000000000000000, 0.000000000000000000, 0.000000000000000000 ) ) ;
#185639=AXIS2_PLACEMENT_3D ( 'NONE', #27294, #185044, #205886 ) ;
#185663=DIRECTION ( 'NONE',  ( 0.000000000000000000, -1.000000000000000000, -7.272083257015735086E-15 ) ) ;
#185705=ORIENTED_EDGE ( 'NONE', *, *, #16448, .T. ) ;
#185726=DIRECTION ( 'NONE',  ( -0.000000000000000000, 1.000000000000000000, 6.982962677686266711E-15 ) ) ;
#185782=EDGE_CURVE ( 'NONE', #19886, #237795, #105982, .T. ) ;
#185789=CARTESIAN_POINT ( 'NONE',  ( -20.54999999999999716, 85.00000000001232081, -160.1291383618718385 ) ) ;
#185850=CARTESIAN_POINT ( 'NONE',  ( -20.99780126800916591, 64.39461131213562339, -143.4357549128189362 ) ) ;
#185854=CARTESIAN_POINT ( 'NONE',  ( -21.05000000000000782, 69.66772772607673403, -169.9855714212388023 ) ) ;
#185908=VECTOR ( 'NONE', #221297, 1000.000000000000000 ) ;
#185939=DIRECTION ( 'NONE',  ( 0.000000000000000000, -1.000000000000000000, -6.982962677686265922E-15 ) ) ;
#185947=DIRECTION ( 'NONE',  ( 1.000000000000000000, -0.000000000000000000, 0.000000000000000000 ) ) ;
#185983=DIRECTION ( 'NONE',  ( 0.000000000000000000, -1.000000000000000000, -6.982962677686265922E-15 ) ) ;
#185995=ORIENTED_EDGE ( 'NONE', *, *, #210239, .F. ) ;
#186014=ORIENTED_EDGE ( 'NONE', *, *, #243296, .F. ) ;
#186015=CARTESIAN_POINT ( 'NONE',  ( 18.50000000000000000, 85.40000000001208491, -129.6410656363516125 ) ) ;
#186038=EDGE_CURVE ( 'NONE', #26287, #168738, #160391, .T. ) ;
#186047=VECTOR ( 'NONE', #238580, 1000.000000000000000 ) ;
#186054=FACE_OUTER_BOUND ( 'NONE', #192492, .T. ) ;
#186076=LINE ( 'NONE', #86937, #59408 ) ;
#186115=EDGE_LOOP ( 'NONE', ( #30591, #91856, #102051, #196201, #64213, #201093, #257511, #169471, #93794, #124255, #62714, #243604, #255236, #13918, #97870, #20902, #185705, #35789, #108116, #167686, #145955, #198459, #22261, #168831, #100348, #161856, #174494 ) ) ;
#186118=CARTESIAN_POINT ( 'NONE',  ( 21.05000000000000071, 76.00000000001237765, -170.0231074845243597 ) ) ;
#186148=LINE ( 'NONE', #53048, #31687 ) ;
#186208=AXIS2_PLACEMENT_3D ( 'NONE', #132603, #175586, #130003 ) ;
#186226=EDGE_CURVE ( 'NONE', #134102, #241641, #255978, .T. ) ;
#186228=ORIENTED_EDGE ( 'NONE', *, *, #248453, .F. ) ;
#186242=DIRECTION ( 'NONE',  ( 1.000000000000000000, 0.000000000000000000, 0.000000000000000000 ) ) ;
#186287=CARTESIAN_POINT ( 'NONE',  ( 20.53930447208010790, 67.02285131248730465, -161.5806003429519535 ) ) ;
#186304=CARTESIAN_POINT ( 'NONE',  ( -22.39999999999999503, 68.20922040163897293, -170.0231074845244166 ) ) ;
#186313=ORIENTED_EDGE ( 'NONE', *, *, #210950, .F. ) ;
#186326=DIRECTION ( 'NONE',  ( -1.000000000000000000, -9.012599976027990443E-15, -6.882867235861669241E-14 ) ) ;
#186332=ORIENTED_EDGE ( 'NONE', *, *, #92641, .T. ) ;
#186340=EDGE_CURVE ( 'NONE', #220534, #219647, #131313, .T. ) ;
#186362=AXIS2_PLACEMENT_3D ( 'NONE', #29626, #50413, #146953 ) ;
#186367=EDGE_CURVE ( 'NONE', #109875, #70645, #127225, .T. ) ;
#186402=FACE_OUTER_BOUND ( 'NONE', #143642, .T. ) ;
#186436=TOROIDAL_SURFACE ( 'NONE', #11655, 1.900000000000002576, 0.1000000000000000056 ) ;
#186473=EDGE_CURVE ( 'NONE', #51370, #219226, #114580, .T. ) ;
#186492=ORIENTED_EDGE ( 'NONE', *, *, #142487, .T. ) ;
#186542=CIRCLE ( 'NONE', #140735, 0.09999999999998898659 ) ;
#186573=CARTESIAN_POINT ( 'NONE',  ( -21.55000000000000426, 68.25000000001223555, -148.7731074845244166 ) ) ;
#186587=DIRECTION ( 'NONE',  ( -1.000000000000000000, -0.000000000000000000, -0.000000000000000000 ) ) ;
#186590=CARTESIAN_POINT ( 'NONE',  ( 20.94999999999999929, 77.16270174995034381, -162.1231074845243540 ) ) ;
#186600=AXIS2_PLACEMENT_3D ( 'NONE', #13531, #130893, #228737 ) ;
#186625=DIRECTION ( 'NONE',  ( 0.000000000000000000, -7.026728003956695223E-15, 1.000000000000000000 ) ) ;
#186646=CARTESIAN_POINT ( 'NONE',  ( 21.11101077988997332, 69.57631526528633970, -170.0383927534386999 ) ) ;
#186742=CARTESIAN_POINT ( 'NONE',  ( 19.75857864376268935, 64.35000000001220144, -145.2731074845244450 ) ) ;
#186746=AXIS2_PLACEMENT_3D ( 'NONE', #64870, #189965, #165260 ) ;
#186752=ORIENTED_EDGE ( 'NONE', *, *, #20064, .T. ) ;
#186771=VERTEX_POINT ( 'NONE', #74039 ) ;
#186776=FACE_OUTER_BOUND ( 'NONE', #153830, .T. ) ;
#186799=AXIS2_PLACEMENT_3D ( 'NONE', #11584, #10298, #192775 ) ;
#186806=ORIENTED_EDGE ( 'NONE', *, *, #4274, .F. ) ;
#186817=ORIENTED_EDGE ( 'NONE', *, *, #198245, .T. ) ;
#186822=AXIS2_PLACEMENT_3D ( 'NONE', #250740, #13433, #229903 ) ;
#186838=DIRECTION ( 'NONE',  ( 4.408576920032447355E-17, 0.1350103645451807555, 0.9908441862701610203 ) ) ;
#186850=ORIENTED_EDGE ( 'NONE', *, *, #75946, .T. ) ;
#186854=EDGE_CURVE ( 'NONE', #101496, #43638, #127895, .T. ) ;
#186856=DIRECTION ( 'NONE',  ( 1.000000000000000000, 0.000000000000000000, 0.000000000000000000 ) ) ;
#186865=EDGE_CURVE ( 'NONE', #176854, #115699, #32049, .T. ) ;
#186931=FACE_OUTER_BOUND ( 'NONE', #126636, .T. ) ;
#186948=AXIS2_PLACEMENT_3D ( 'NONE', #74055, #255161, #252640 ) ;
#186970=DIRECTION ( 'NONE',  ( 0.000000000000000000, -0.2605042016806740079, 0.9654727137038698892 ) ) ;
#186984=ORIENTED_EDGE ( 'NONE', *, *, #232260, .F. ) ;
#186992=CARTESIAN_POINT ( 'NONE',  ( -20.64999999999999858, 85.00000000001223555, -145.9170766071767389 ) ) ;
#187018=DIRECTION ( 'NONE',  ( 0.000000000000000000, -7.304098846218085561E-15, 1.000000000000000000 ) ) ;
#187019=CONICAL_SURFACE ( 'NONE', #137101, 4.299999999999970512, 0.7853981633974466137 ) ;
#187025=FACE_OUTER_BOUND ( 'NONE', #231775, .T. ) ;
#187026=EDGE_CURVE ( 'NONE', #239159, #161742, #119526, .T. ) ;
#187040=ORIENTED_EDGE ( 'NONE', *, *, #213032, .T. ) ;
#187049=LINE ( 'NONE', #47487, #203139 ) ;
#187120=ADVANCED_FACE ( 'NONE', ( #39600 ), #227133, .F. ) ;
#187132=ORIENTED_EDGE ( 'NONE', *, *, #242989, .T. ) ;
#187135=CARTESIAN_POINT ( 'NONE',  ( -20.85000000000000142, 87.65000000001214175, -136.5231074845242745 ) ) ;
#187168=LINE ( 'NONE', #8514, #246392 ) ;
#187233=CARTESIAN_POINT ( 'NONE',  ( -23.25000000000000000, 76.00000000001237765, -170.0231074845243597 ) ) ;
#187246=SPHERICAL_SURFACE ( 'NONE', #48986, 0.1000000000000000056 ) ;
#187251=CARTESIAN_POINT ( 'NONE',  ( -23.15000000000000213, 74.00000000001229239, -157.2984855617622770 ) ) ;
#187293=ORIENTED_EDGE ( 'NONE', *, *, #224821, .F. ) ;
#187312=CIRCLE ( 'NONE', #253922, 7.899999999999990585 ) ;
#187323=AXIS2_PLACEMENT_3D ( 'NONE', #71188, #8634, #226362 ) ;
#187326=ORIENTED_EDGE ( 'NONE', *, *, #175999, .F. ) ;
#187346=ORIENTED_EDGE ( 'NONE', *, *, #99230, .F. ) ;
#187358=DIRECTION ( 'NONE',  ( -1.000000000000000000, 2.952720810173289112E-16, 2.061873921506763405E-30 ) ) ;
#187395=LINE ( 'NONE', #189953, #79716 ) ;
#187400=CARTESIAN_POINT ( 'NONE',  ( -23.15000000000000213, 76.00000000001213607, -136.5231074845243313 ) ) ;
#187408=CIRCLE ( 'NONE', #237297, 0.09999999999998898659 ) ;
#187429=CIRCLE ( 'NONE', #83333, 0.09999999999998898659 ) ;
#187462=EDGE_LOOP ( 'NONE', ( #238758, #199653, #35465, #245960 ) ) ;
#187464=TOROIDAL_SURFACE ( 'NONE', #233273, 3.899999999999999467, 0.1000000000000000056 ) ;
#187478=ORIENTED_EDGE ( 'NONE', *, *, #183934, .T. ) ;
#187497=LINE ( 'NONE', #128797, #195664 ) ;
#187518=CYLINDRICAL_SURFACE ( 'NONE', #112678, 0.1000000000000028644 ) ;
#187525=AXIS2_PLACEMENT_3D ( 'NONE', #163433, #199993, #242952 ) ;
#187535=DIRECTION ( 'NONE',  ( 0.000000000000000000, -0.9908441862701420355, -0.1350103645453197554 ) ) ;
#187542=DIRECTION ( 'NONE',  ( 0.000000000000000000, 0.000000000000000000, 1.000000000000000000 ) ) ;
#187560=ORIENTED_EDGE ( 'NONE', *, *, #207720, .F. ) ;
#187561=DIRECTION ( 'NONE',  ( 0.000000000000000000, 0.000000000000000000, 1.000000000000000000 ) ) ;
#187575=ORIENTED_EDGE ( 'NONE', *, *, #239591, .F. ) ;
#187583=CARTESIAN_POINT ( 'NONE',  ( 20.77766267348356166, 65.55095760939360616, -162.4303985686467513 ) ) ;
#187585=ORIENTED_EDGE ( 'NONE', *, *, #224816, .F. ) ;
#187591=CARTESIAN_POINT ( 'NONE',  ( 18.59999999999999432, 77.83585931145570669, -125.0186683157258045 ) ) ;
#187634=LINE ( 'NONE', #228029, #73249 ) ;
#187654=ORIENTED_EDGE ( 'NONE', *, *, #87360, .T. ) ;
#187679=DIRECTION ( 'NONE',  ( 1.000000000000000000, 0.000000000000000000, 0.000000000000000000 ) ) ;
#187680=CIRCLE ( 'NONE', #208525, 0.09999999999998708533 ) ;
#187685=VERTEX_POINT ( 'NONE', #64116 ) ;
#187689=ORIENTED_EDGE ( 'NONE', *, *, #95491, .T. ) ;
#187708=ORIENTED_EDGE ( 'NONE', *, *, #213257, .T. ) ;
#187713=ORIENTED_EDGE ( 'NONE', *, *, #7681, .F. ) ;
#187756=VERTEX_POINT ( 'NONE', #191472 ) ;
#187840=ORIENTED_EDGE ( 'NONE', *, *, #24625, .T. ) ;
#187847=CARTESIAN_POINT ( 'NONE',  ( 18.50000000000000000, 85.40000000001208491, -129.6410656363516125 ) ) ;
#187869=CARTESIAN_POINT ( 'NONE',  ( -23.15000000000000213, 76.00000000001237765, -170.0231074845243597 ) ) ;
#187874=DIRECTION ( 'NONE',  ( 0.000000000000000000, 6.982962677686266711E-15, -1.000000000000000000 ) ) ;
#187883=EDGE_LOOP ( 'NONE', ( #220821, #186492, #143509, #190150 ) ) ;
#187904=DIRECTION ( 'NONE',  ( 0.000000000000000000, 6.982962677686266711E-15, -1.000000000000000000 ) ) ;
#187909=DIRECTION ( 'NONE',  ( 0.000000000000000000, -0.9999631594459057471, 0.008583690987121077309 ) ) ;
#187913=VECTOR ( 'NONE', #154854, 1000.000000000000000 ) ;
#187917=DIRECTION ( 'NONE',  ( 0.000000000000000000, 0.000000000000000000, 1.000000000000000000 ) ) ;
#188001=CARTESIAN_POINT ( 'NONE',  ( -21.05000000000000071, 69.69503888732782571, -170.0017219185873216 ) ) ;
#188007=DIRECTION ( 'NONE',  ( 1.000000000000000000, 0.000000000000000000, 0.000000000000000000 ) ) ;
#188046=ORIENTED_EDGE ( 'NONE', *, *, #213514, .T. ) ;
#188067=ORIENTED_EDGE ( 'NONE', *, *, #239684, .F. ) ;
#188068=DIRECTION ( 'NONE',  ( -0.000000000000000000, 6.982962677686266711E-15, -1.000000000000000000 ) ) ;
#188084=FACE_OUTER_BOUND ( 'NONE', #34774, .T. ) ;
#188098=EDGE_CURVE ( 'NONE', #168984, #50990, #150722, .T. ) ;
#188099=ORIENTED_EDGE ( 'NONE', *, *, #14754, .T. ) ;
#188105=DIRECTION ( 'NONE',  ( 0.1538461538461484146, -0.9880948137434723000, 0.000000000000000000 ) ) ;
#188107=CARTESIAN_POINT ( 'NONE',  ( -23.15000000000000213, 85.50000000001232081, -160.1291383618718385 ) ) ;
#188108=DIRECTION ( 'NONE',  ( 1.000000000000000000, -3.265361837132813093E-16, -2.280189983783949500E-30 ) ) ;
#188109=DIRECTION ( 'NONE',  ( 0.000000000000000000, 0.000000000000000000, 1.000000000000000000 ) ) ;
#188111=CARTESIAN_POINT ( 'NONE',  ( 22.40000000000010516, 76.00000000001340084, -181.7735403769832772 ) ) ;
#188114=EDGE_CURVE ( 'NONE', #127762, #56976, #7351, .T. ) ;
#188227=ORIENTED_EDGE ( 'NONE', *, *, #4897, .F. ) ;
#188242=ORIENTED_EDGE ( 'NONE', *, *, #231689, .T. ) ;
#188243=CIRCLE ( 'NONE', #63317, 0.1000000000000046685 ) ;
#188250=CIRCLE ( 'NONE', #67629, 0.1000000000000028644 ) ;
#188264=VERTEX_POINT ( 'NONE', #38477 ) ;
#188292=CARTESIAN_POINT ( 'NONE',  ( -20.64999999999999858, 68.75000000001223555, -148.8731074845244109 ) ) ;
#188315=EDGE_CURVE ( 'NONE', #94890, #132176, #172897, .T. ) ;
#188317=DIRECTION ( 'NONE',  ( 1.000000000000000000, 0.000000000000000000, 0.000000000000000000 ) ) ;
#188341=AXIS2_PLACEMENT_3D ( 'NONE', #164801, #180513, #179246 ) ;
#188351=VERTEX_POINT ( 'NONE', #137552 ) ;
#188375=ORIENTED_EDGE ( 'NONE', *, *, #220196, .T. ) ;
#188396=CARTESIAN_POINT ( 'NONE',  ( -23.25000000000000000, 76.00000000001237765, -170.0231074845243597 ) ) ;
#188412=VECTOR ( 'NONE', #98953, 1000.000000000000000 ) ;
#188418=AXIS2_PLACEMENT_3D ( 'NONE', #72338, #172751, #252225 ) ;
#188447=CYLINDRICAL_SURFACE ( 'NONE', #12504, 0.1000000000000072220 ) ;
#188474=LINE ( 'NONE', #248460, #136291 ) ;
#188480=FACE_OUTER_BOUND ( 'NONE', #135163, .T. ) ;
#188485=DIRECTION ( 'NONE',  ( 1.000000000000000000, 0.000000000000000000, 0.000000000000000000 ) ) ;
#188492=ORIENTED_EDGE ( 'NONE', *, *, #140386, .F. ) ;
#188522=CARTESIAN_POINT ( 'NONE',  ( 21.14999999999999858, 64.35000000001237197, -169.9231074845244507 ) ) ;
#188523=CARTESIAN_POINT ( 'NONE',  ( 21.05000000000000071, 71.00000000001223555, -148.5283735034374786 ) ) ;
#188526=CARTESIAN_POINT ( 'NONE',  ( -23.25000000000000000, 87.65000000001215597, -139.6231074845242688 ) ) ;
#188537=VECTOR ( 'NONE', #133169, 1000.000000000000000 ) ;
#188549=DIRECTION ( 'NONE',  ( 1.000000000000000000, -7.304098846218134667E-16, -5.100424963727255829E-30 ) ) ;
#188596=DIRECTION ( 'NONE',  ( -4.239556034732056743E-17, -0.1298341882519953583, -0.9915357197604862671 ) ) ;
#188599=EDGE_CURVE ( 'NONE', #256686, #62499, #34351, .T. ) ;
#188638=EDGE_CURVE ( 'NONE', #204085, #148976, #10657, .T. ) ;
#188641=DIRECTION ( 'NONE',  ( -0.000000000000000000, 0.9887567792719327286, 0.1495327102803745423 ) ) ;
#188664=CARTESIAN_POINT ( 'NONE',  ( -21.64999999999999858, 68.75000000001224976, -148.8731074845244109 ) ) ;
#188683=CIRCLE ( 'NONE', #247116, 0.09999999999999939493 ) ;
#188695=AXIS2_PLACEMENT_3D ( 'NONE', #166604, #164015, #226518 ) ;
#188776=DIRECTION ( 'NONE',  ( 0.000000000000000000, 6.982962677686266711E-15, -1.000000000000000000 ) ) ;
#188805=DIRECTION ( 'NONE',  ( 0.000000000000000000, 6.982962677686266711E-15, -1.000000000000000000 ) ) ;
#188807=EDGE_LOOP ( 'NONE', ( #121895, #175560, #47093, #116234 ) ) ;
#188837=FACE_OUTER_BOUND ( 'NONE', #231677, .T. ) ;
#188847=AXIS2_PLACEMENT_3D ( 'NONE', #181549, #45865, #105811 ) ;
#188885=CARTESIAN_POINT ( 'NONE',  ( -21.05000000000000071, 74.16465844978787914, -158.4679561919613775 ) ) ;
#188905=EDGE_CURVE ( 'NONE', #92370, #139006, #48238, .T. ) ;
#188906=CARTESIAN_POINT ( 'NONE',  ( 21.00000000000000000, 66.25000000001223555, -148.8731074845244393 ) ) ;
#188932=ORIENTED_EDGE ( 'NONE', *, *, #7022, .T. ) ;
#188946=DIRECTION ( 'NONE',  ( 0.000000000000000000, -7.147358527629766941E-15, 1.000000000000000000 ) ) ;
#188947=CARTESIAN_POINT ( 'NONE',  ( -18.59999999999999787, 66.75000000001230660, -157.6731074845244223 ) ) ;
#188952=AXIS2_PLACEMENT_3D ( 'NONE', #223278, #202450, #206306 ) ;
#188980=AXIS2_PLACEMENT_3D ( 'NONE', #220067, #38877, #19300 ) ;
#189031=CIRCLE ( 'NONE', #251383, 0.1000000000000072220 ) ;
#189068=ORIENTED_EDGE ( 'NONE', *, *, #202249, .T. ) ;
#189079=EDGE_LOOP ( 'NONE', ( #211373, #83769, #35408, #44647 ) ) ;
#189141=ORIENTED_EDGE ( 'NONE', *, *, #235572, .T. ) ;
#189151=ADVANCED_FACE ( 'NONE', ( #193101 ), #40086, .F. ) ;
#189163=CARTESIAN_POINT ( 'NONE',  ( -23.25000000000000000, 77.83585931145570669, -125.0186683157258329 ) ) ;
#189165=ORIENTED_EDGE ( 'NONE', *, *, #4274, .T. ) ;
#189213=CARTESIAN_POINT ( 'NONE',  ( -21.05000000000000071, 74.14897176987143723, -158.3691942151018850 ) ) ;
#189225=AXIS2_PLACEMENT_3D ( 'NONE', #178366, #240888, #122222 ) ;
#189256=EDGE_CURVE ( 'NONE', #245795, #14612, #189885, .T. ) ;
#189272=CARTESIAN_POINT ( 'NONE',  ( -22.39999999999999858, 75.90000000001242597, -177.8138870828977360 ) ) ;
#189289=CARTESIAN_POINT ( 'NONE',  ( -21.05000000000000071, 70.15000000001235492, -159.8906102602464330 ) ) ;
#189295=AXIS2_PLACEMENT_3D ( 'NONE', #195292, #251380, #209695 ) ;
#189311=ORIENTED_EDGE ( 'NONE', *, *, #216367, .F. ) ;
#189333=ORIENTED_EDGE ( 'NONE', *, *, #248356, .T. ) ;
#189346=VECTOR ( 'NONE', #89881, 1000.000000000000000 ) ;
#189352=DIRECTION ( 'NONE',  ( 0.000000000000000000, 0.000000000000000000, 1.000000000000000000 ) ) ;
#189360=DIRECTION ( 'NONE',  ( 0.000000000000000000, 0.000000000000000000, 1.000000000000000000 ) ) ;
#189366=CARTESIAN_POINT ( 'NONE',  ( 20.85000000000000142, 69.01799029515568407, -132.8269553662681233 ) ) ;
#189383=ORIENTED_EDGE ( 'NONE', *, *, #204174, .T. ) ;
#189389=CARTESIAN_POINT ( 'NONE',  ( 21.05000000000000071, 64.40000000001218439, -143.4513107147999449 ) ) ;
#189392=DIRECTION ( 'NONE',  ( 0.000000000000000000, 6.982962677686267499E-15, -1.000000000000000000 ) ) ;
#189420=EDGE_CURVE ( 'NONE', #236987, #11381, #15311, .T. ) ;
#189423=VERTEX_POINT ( 'NONE', #169410 ) ;
#189457=CARTESIAN_POINT ( 'NONE',  ( -23.25000000000000000, 76.00000000001213607, -136.5231074845243313 ) ) ;
#189467=FACE_OUTER_BOUND ( 'NONE', #66458, .T. ) ;
#189468=CARTESIAN_POINT ( 'NONE',  ( 18.59999999999999432, 77.16270174995034381, -161.9231074845243370 ) ) ;
#189481=LINE ( 'NONE', #167372, #208283 ) ;
#189495=ORIENTED_EDGE ( 'NONE', *, *, #103954, .T. ) ;
#189506=CIRCLE ( 'NONE', #77060, 0.09999999999999939493 ) ;
#189509=AXIS2_PLACEMENT_3D ( 'NONE', #219918, #17855, #3421 ) ;
#189510=ORIENTED_EDGE ( 'NONE', *, *, #239908, .T. ) ;
#189615=DIRECTION ( 'NONE',  ( 0.000000000000000000, 0.000000000000000000, -1.000000000000000000 ) ) ;
#189656=DIRECTION ( 'NONE',  ( 0.000000000000000000, -1.000000000000000000, -6.982962677686265922E-15 ) ) ;
#189659=CARTESIAN_POINT ( 'NONE',  ( -20.85000000000000142, 68.87972903831452243, -132.8635444426850825 ) ) ;
#189662=ORIENTED_EDGE ( 'NONE', *, *, #204809, .F. ) ;
#189666=CIRCLE ( 'NONE', #93790, 0.09999999999998898659 ) ;
#189700=DIRECTION ( 'NONE',  ( -1.000000000000000000, 0.000000000000000000, 0.000000000000000000 ) ) ;
#189706=ORIENTED_EDGE ( 'NONE', *, *, #15033, .F. ) ;
#189708=AXIS2_PLACEMENT_3D ( 'NONE', #95574, #175167, #155594 ) ;
#189723=EDGE_CURVE ( 'NONE', #242166, #143129, #44705, .T. ) ;
#189816=CARTESIAN_POINT ( 'NONE',  ( 20.85000000000000142, 77.83585931145570669, -124.9186683157258102 ) ) ;
#189834=VECTOR ( 'NONE', #33393, 1000.000000000000000 ) ;
#189880=ADVANCED_FACE ( 'NONE', ( #42089 ), #111149, .F. ) ;
#189882=EDGE_CURVE ( 'NONE', #140162, #248221, #179044, .T. ) ;
#189885=CIRCLE ( 'NONE', #77434, 0.09999999999999939493 ) ;
#189886=CARTESIAN_POINT ( 'NONE',  ( 20.94999999999999574, 87.65000000001235492, -167.1231074845242688 ) ) ;
#189895=DIRECTION ( 'NONE',  ( -1.000000000000000000, -0.000000000000000000, -0.000000000000000000 ) ) ;
#189922=CARTESIAN_POINT ( 'NONE',  ( -21.05000000000000071, 76.00000000001222134, -148.3231074845243427 ) ) ;
#189933=ADVANCED_FACE ( 'NONE', ( #181592 ), #37198, .T. ) ;
#189953=CARTESIAN_POINT ( 'NONE',  ( -23.25000000000000000, 76.10085836911117951, -181.7726746080137445 ) ) ;
#189965=DIRECTION ( 'NONE',  ( 0.000000000000000000, 6.982962677686266711E-15, -1.000000000000000000 ) ) ;
#189971=ORIENTED_EDGE ( 'NONE', *, *, #170007, .F. ) ;
#189978=ORIENTED_EDGE ( 'NONE', *, *, #26193, .F. ) ;
#189987=AXIS2_PLACEMENT_3D ( 'NONE', #157388, #176944, #255111 ) ;
#189992=CARTESIAN_POINT ( 'NONE',  ( -22.57320508075687115, 64.25000000001237765, -170.0231074845244166 ) ) ;
#190019=ORIENTED_EDGE ( 'NONE', *, *, #194804, .T. ) ;
#190068=ORIENTED_EDGE ( 'NONE', *, *, #158843, .F. ) ;
#190070=VECTOR ( 'NONE', #219614, 1000.000000000000000 ) ;
#190073=CIRCLE ( 'NONE', #119335, 4.000000000000003553 ) ;
#190081=AXIS2_PLACEMENT_3D ( 'NONE', #14171, #230636, #248915 ) ;
#190099=EDGE_CURVE ( 'NONE', #210220, #237787, #63836, .T. ) ;
#190118=CARTESIAN_POINT ( 'NONE',  ( -18.59999999999999787, 64.35000000001222986, -148.6731074845244507 ) ) ;
#190136=AXIS2_PLACEMENT_3D ( 'NONE', #58105, #193793, #252461 ) ;
#190137=CARTESIAN_POINT ( 'NONE',  ( 20.87631937322878883, 65.52850496324654728, -162.4433616099437927 ) ) ;
#190150=ORIENTED_EDGE ( 'NONE', *, *, #59685, .T. ) ;
#190173=PLANE ( 'NONE',  #128082 ) ;
#190182=CARTESIAN_POINT ( 'NONE',  ( 20.94999999999999929, 65.70729864261026876, -131.0657455973724836 ) ) ;
#190186=AXIS2_PLACEMENT_3D ( 'NONE', #158366, #16274, #197440 ) ;
#190208=LINE ( 'NONE', #191513, #18663 ) ;
#190219=ORIENTED_EDGE ( 'NONE', *, *, #181874, .F. ) ;
#190220=DIRECTION ( 'NONE',  ( 0.000000000000000000, 7.162729191130010591E-15, -1.000000000000000000 ) ) ;
#190223=ORIENTED_EDGE ( 'NONE', *, *, #210950, .T. ) ;
#190271=CARTESIAN_POINT ( 'NONE',  ( 20.95483826173899899, 67.12383379524233362, -161.4768319316249006 ) ) ;
#190297=VECTOR ( 'NONE', #35926, 1000.000000000000000 ) ;
#190320=ORIENTED_EDGE ( 'NONE', *, *, #47039, .F. ) ;
#190341=EDGE_CURVE ( 'NONE', #134542, #229965, #36542, .T. ) ;
#190349=ORIENTED_EDGE ( 'NONE', *, *, #49432, .T. ) ;
#190389=VERTEX_POINT ( 'NONE', #228113 ) ;
#190393=DIRECTION ( 'NONE',  ( 1.000000000000000000, -0.000000000000000000, 0.000000000000000000 ) ) ;
#190427=ADVANCED_FACE ( 'NONE', ( #205964 ), #211473, .T. ) ;
#190432=CARTESIAN_POINT ( 'NONE',  ( 20.94999999999999574, 76.00000000001237765, -170.0231074845243597 ) ) ;
#190448=ORIENTED_EDGE ( 'NONE', *, *, #251983, .T. ) ;
#190511=DIRECTION ( 'NONE',  ( 0.000000000000000000, 6.982962677686266711E-15, -1.000000000000000000 ) ) ;
#190513=AXIS2_PLACEMENT_3D ( 'NONE', #92176, #200273, #77731 ) ;
#190514=ORIENTED_EDGE ( 'NONE', *, *, #248266, .F. ) ;
#190561=ORIENTED_EDGE ( 'NONE', *, *, #120686, .T. ) ;
#190596=CARTESIAN_POINT ( 'NONE',  ( 18.49999999999999289, 68.87972903831452243, -132.8635444426850825 ) ) ;
#190610=EDGE_LOOP ( 'NONE', ( #200253, #210302, #141965, #30780, #135681, #140489, #105069 ) ) ;
#190618=B_SPLINE_CURVE_WITH_KNOTS ( 'NONE', 3,
 ( #105575, #111701, #84721, #191267, #242547, #185148, #12623 ),
 .UNSPECIFIED., .F., .F.,
 ( 4, 3, 4 ),
 ( 0.000000000000000000, 1.860045280646148997E-05, 5.251155757305323837E-05 ),
 .UNSPECIFIED. ) ;
#190640=FACE_OUTER_BOUND ( 'NONE', #236181, .T. ) ;
#190647=ORIENTED_EDGE ( 'NONE', *, *, #126416, .F. ) ;
#190663=ORIENTED_EDGE ( 'NONE', *, *, #206907, .T. ) ;
#190709=CARTESIAN_POINT ( 'NONE',  ( 22.45463910399148233, 76.00000000001334399, -181.6726782947127958 ) ) ;
#190713=AXIS2_PLACEMENT_3D ( 'NONE', #141589, #103720, #243248 ) ;
#190724=AXIS2_PLACEMENT_3D ( 'NONE', #86567, #21507, #143989 ) ;
#190727=DIRECTION ( 'NONE',  ( 7.304098846218134667E-16, 1.000000000000000000, 6.982962677686267499E-15 ) ) ;
#190734=CARTESIAN_POINT ( 'NONE',  ( 21.05000000000000071, 69.55000000001230376, -160.0060803140843859 ) ) ;
#190745=LINE ( 'NONE', #10795, #45703 ) ;
#190773=DIRECTION ( 'NONE',  ( 0.000000000000000000, -1.000000000000000000, -6.982962677686266711E-15 ) ) ;
#190803=CARTESIAN_POINT ( 'NONE',  ( -21.05000000000000071, 64.37928932189367970, -163.1546908321834337 ) ) ;
#190807=ORIENTED_EDGE ( 'NONE', *, *, #183453, .F. ) ;
#190808=DIRECTION ( 'NONE',  ( -1.000000000000000000, -0.000000000000000000, -0.000000000000000000 ) ) ;
#190814=DIRECTION ( 'NONE',  ( 1.000000000000000000, 0.000000000000000000, 0.000000000000000000 ) ) ;
#190828=FACE_OUTER_BOUND ( 'NONE', #125794, .T. ) ;
#190829=ADVANCED_FACE ( 'NONE', ( #148244 ), #24479, .T. ) ;
#190841=AXIS2_PLACEMENT_3D ( 'NONE', #255875, #60281, #77279 ) ;
#190844=DIRECTION ( 'NONE',  ( 0.000000000000000000, 1.000000000000000000, 6.352154140967427193E-15 ) ) ;
#190847=TOROIDAL_SURFACE ( 'NONE', #86719, 7.791421356237316687, 0.1000000000000000056 ) ;
#190850=FACE_OUTER_BOUND ( 'NONE', #191515, .T. ) ;
#190851=AXIS2_PLACEMENT_3D ( 'NONE', #225501, #69046, #104277 ) ;
#190854=VECTOR ( 'NONE', #38163, 1000.000000000000000 ) ;
#190859=DIRECTION ( 'NONE',  ( -0.000000000000000000, 6.982962677686266711E-15, -1.000000000000000000 ) ) ;
#190873=CYLINDRICAL_SURFACE ( 'NONE', #226950, 0.09999999999999939493 ) ;
#190879=DIRECTION ( 'NONE',  ( 0.000000000000000000, 0.000000000000000000, 1.000000000000000000 ) ) ;
#190917=ORIENTED_EDGE ( 'NONE', *, *, #131801, .T. ) ;
#190936=FACE_OUTER_BOUND ( 'NONE', #254322, .T. ) ;
#190981=DIRECTION ( 'NONE',  ( 0.000000000000000000, -2.771150684185008344E-14, -1.000000000000000000 ) ) ;
#190984=CARTESIAN_POINT ( 'NONE',  ( -18.50000000000000000, 64.25000000001223555, -148.6731074845244507 ) ) ;
#191018=DIRECTION ( 'NONE',  ( 0.000000000000000000, 0.000000000000000000, 1.000000000000000000 ) ) ;
#191042=CARTESIAN_POINT ( 'NONE',  ( 20.87155475150661132, 64.25000000001219291, -143.4275209553667878 ) ) ;
#191057=ADVANCED_FACE ( 'NONE', ( #238777 ), #176254, .T. ) ;
#191060=DIRECTION ( 'NONE',  ( 1.000000000000000000, 0.000000000000000000, 0.000000000000000000 ) ) ;
#191061=EDGE_LOOP ( 'NONE', ( #199174, #158028, #223460, #135440 ) ) ;
#191109=CARTESIAN_POINT ( 'NONE',  ( 21.05000000000000071, 71.14953271029261828, -148.5573748935260880 ) ) ;
#191116=ORIENTED_EDGE ( 'NONE', *, *, #109131, .F. ) ;
#191131=DIRECTION ( 'NONE',  ( 0.000000000000000000, 6.982962677686266711E-15, -1.000000000000000000 ) ) ;
#191157=DIRECTION ( 'NONE',  ( 0.000000000000000000, -1.000000000000000000, -6.352154140967427193E-15 ) ) ;
#191184=VERTEX_POINT ( 'NONE', #180097 ) ;
#191241=CARTESIAN_POINT ( 'NONE',  ( -18.50000000000000000, 64.35000000001230092, -157.7731074845244450 ) ) ;
#191255=CARTESIAN_POINT ( 'NONE',  ( -23.15000000000000213, 84.66355140188147743, -160.4990063664569959 ) ) ;
#191259=ORIENTED_EDGE ( 'NONE', *, *, #130271, .T. ) ;
#191267=CARTESIAN_POINT ( 'NONE',  ( -22.49436431346200038, 64.35004905235891215, -170.0900110142466986 ) ) ;
#191284=CARTESIAN_POINT ( 'NONE',  ( -22.40000000000000213, 76.00000000001246292, -181.7735403769829645 ) ) ;
#191291=ADVANCED_FACE ( 'NONE', ( #212500 ), #53629, .T. ) ;
#191323=CARTESIAN_POINT ( 'NONE',  ( -23.15000000000000213, 73.40000000001222702, -149.7477294072864709 ) ) ;
#191364=CARTESIAN_POINT ( 'NONE',  ( 21.05000000000000071, 85.00000000001222134, -146.4170766071767389 ) ) ;
#191366=CARTESIAN_POINT ( 'NONE',  ( -18.59999999999999787, 77.16270174995034381, -162.0231074845243313 ) ) ;
#191386=VECTOR ( 'NONE', #76308, 1000.000000000000114 ) ;
#191395=AXIS2_PLACEMENT_3D ( 'NONE', #255737, #77140, #257017 ) ;
#191409=FACE_OUTER_BOUND ( 'NONE', #138075, .T. ) ;
#191425=EDGE_LOOP ( 'NONE', ( #85741, #205246, #74540, #149591 ) ) ;
#191434=EDGE_CURVE ( 'NONE', #34074, #4792, #178750, .T. ) ;
#191453=DIRECTION ( 'NONE',  ( 0.000000000000000000, -0.1350103645451835865, -0.9908441862701605762 ) ) ;
#191459=EDGE_LOOP ( 'NONE', ( #54447, #212650, #182775, #114498 ) ) ;
#191472=CARTESIAN_POINT ( 'NONE',  ( -21.55000000000000071, 68.65000000001222702, -148.8731074845244109 ) ) ;
#191479=CARTESIAN_POINT ( 'NONE',  ( 22.50000000000000000, 76.00000000001237765, -170.0231074845243597 ) ) ;
#191489=CIRCLE ( 'NONE', #224752, 0.09999999999998898659 ) ;
#191513=CARTESIAN_POINT ( 'NONE',  ( 20.94999999999999929, 76.00000000001210765, -132.5231074845243313 ) ) ;
#191515=EDGE_LOOP ( 'NONE', ( #229478, #92728, #100060, #248045 ) ) ;
#191521=CARTESIAN_POINT ( 'NONE',  ( -20.85000000000000142, 77.26327546522934142, -128.6212428177779543 ) ) ;
#191529=ORIENTED_EDGE ( 'NONE', *, *, #138454, .F. ) ;
#191541=DIRECTION ( 'NONE',  ( 0.000000000000000000, 0.000000000000000000, -1.000000000000000000 ) ) ;
#191543=DIRECTION ( 'NONE',  ( 0.000000000000000000, -1.000000000000000000, 0.000000000000000000 ) ) ;
#191598=EDGE_CURVE ( 'NONE', #206936, #61341, #62188, .T. ) ;
#191612=VECTOR ( 'NONE', #59864, 1000.000000000000000 ) ;
#191614=ORIENTED_EDGE ( 'NONE', *, *, #216492, .T. ) ;
#191626=CIRCLE ( 'NONE', #237572, 0.09999999999998898659 ) ;
#191643=DIRECTION ( 'NONE',  ( 0.000000000000000000, 0.000000000000000000, 1.000000000000000000 ) ) ;
#191652=DIRECTION ( 'NONE',  ( -0.000000000000000000, 1.000000000000000000, 7.272083257015735086E-15 ) ) ;
#191661=DIRECTION ( 'NONE',  ( 0.000000000000000000, -1.000000000000000000, -6.860497997771531562E-15 ) ) ;
#191678=EDGE_CURVE ( 'NONE', #52922, #229236, #101471, .T. ) ;
#191685=CARTESIAN_POINT ( 'NONE',  ( -22.50000000000000000, 76.00000000001242029, -176.2731074845243597 ) ) ;
#191756=AXIS2_PLACEMENT_3D ( 'NONE', #87770, #167360, #246854 ) ;
#191763=ORIENTED_EDGE ( 'NONE', *, *, #14754, .F. ) ;
#191780=ORIENTED_EDGE ( 'NONE', *, *, #4964, .T. ) ;
#191797=CARTESIAN_POINT ( 'NONE',  ( 21.08198257630413508, 69.66340326599731725, -170.0957508083090204 ) ) ;
#191812=EDGE_CURVE ( 'NONE', #224580, #23498, #187497, .T. ) ;
#191827=DIRECTION ( 'NONE',  ( 1.000000000000000000, 0.000000000000000000, 0.000000000000000000 ) ) ;
#191868=CARTESIAN_POINT ( 'NONE',  ( -20.54999999999999716, 85.00000000001232081, -160.1291383618718385 ) ) ;
#191908=ORIENTED_EDGE ( 'NONE', *, *, #214551, .F. ) ;
#191920=ADVANCED_FACE ( 'NONE', ( #217279 ), #197736, .F. ) ;
#191923=CARTESIAN_POINT ( 'NONE',  ( 21.05000000000000071, 87.75000000001215028, -139.4231074845242802 ) ) ;
#191953=CARTESIAN_POINT ( 'NONE',  ( -20.93284271247462058, 64.25000000001220712, -143.5379132551784096 ) ) ;
#191978=CARTESIAN_POINT ( 'NONE',  ( 18.40000000000000568, 85.51932773110476660, -163.0501311079649724 ) ) ;
#191981=CARTESIAN_POINT ( 'NONE',  ( -20.54999999999999716, 76.00000000001213607, -136.5231074845243313 ) ) ;
#192002=EDGE_LOOP ( 'NONE', ( #207895, #98733, #136345, #144003 ) ) ;
#192013=FACE_OUTER_BOUND ( 'NONE', #168363, .T. ) ;
#192017=DIRECTION ( 'NONE',  ( 0.000000000000000000, -0.1350103645451974088, 0.9908441862701587999 ) ) ;
#192041=ORIENTED_EDGE ( 'NONE', *, *, #239697, .F. ) ;
#192044=CIRCLE ( 'NONE', #133741, 0.9750000000000036415 ) ;
#192062=DIRECTION ( 'NONE',  ( -0.000000000000000000, -6.982962677686266711E-15, 1.000000000000000000 ) ) ;
#192154=CARTESIAN_POINT ( 'NONE',  ( 20.94999999999999574, 87.48912529308842068, -166.9231074845242802 ) ) ;
#192177=DIRECTION ( 'NONE',  ( 1.000000000000000000, 0.000000000000000000, 0.000000000000000000 ) ) ;
#192189=DIRECTION ( 'NONE',  ( 1.000000000000000000, -0.000000000000000000, 0.000000000000000000 ) ) ;
#192250=ORIENTED_EDGE ( 'NONE', *, *, #193163, .T. ) ;
#192283=CARTESIAN_POINT ( 'NONE',  ( -21.05000000000000071, 76.01465611852547966, -176.5197940702919084 ) ) ;
#192316=ORIENTED_EDGE ( 'NONE', *, *, #255386, .T. ) ;
#192319=ORIENTED_EDGE ( 'NONE', *, *, #14185, .F. ) ;
#192325=ADVANCED_FACE ( 'NONE', ( #5618 ), #233269, .T. ) ;
#192326=ORIENTED_EDGE ( 'NONE', *, *, #257453, .T. ) ;
#192333=CIRCLE ( 'NONE', #34153, 4.000000000000003553 ) ;
#192334=LINE ( 'NONE', #56629, #67226 ) ;
#192366=CIRCLE ( 'NONE', #79896, 0.09999999999998900047 ) ;
#192368=CARTESIAN_POINT ( 'NONE',  ( -22.48660254037843131, 64.35000000001237197, -170.0731074845244279 ) ) ;
#192406=CIRCLE ( 'NONE', #96690, 1.900000000000012790 ) ;
#192407=ADVANCED_FACE ( 'NONE', ( #225946 ), #244244, .T. ) ;
#192411=CARTESIAN_POINT ( 'NONE',  ( -20.00857864376270001, 66.65000000001229807, -157.6731074845244223 ) ) ;
#192417=EDGE_CURVE ( 'NONE', #174920, #164268, #130732, .T. ) ;
#192448=DIRECTION ( 'NONE',  ( 0.000000000000000000, -0.9915357197604982575, 0.1298341882519033486 ) ) ;
#192452=VECTOR ( 'NONE', #193717, 1000.000000000000000 ) ;
#192492=EDGE_LOOP ( 'NONE', ( #18313, #126249, #169484, #186228 ) ) ;
#192503=ORIENTED_EDGE ( 'NONE', *, *, #114632, .F. ) ;
#192527=ADVANCED_FACE ( 'NONE', ( #20768 ), #175996, .T. ) ;
#192530=EDGE_CURVE ( 'NONE', #227362, #209114, #58614, .T. ) ;
#192571=DIRECTION ( 'NONE',  ( -2.952720810173289112E-16, -1.000000000000000000, -6.982962677686266711E-15 ) ) ;
#192633=DIRECTION ( 'NONE',  ( -0.000000000000000000, 0.9908441862701591329, 0.1350103645451946055 ) ) ;
#192644=TOROIDAL_SURFACE ( 'NONE', #21956, 0.6000000000000013101, 0.1000000000000000056 ) ;
#192694=ORIENTED_EDGE ( 'NONE', *, *, #210911, .T. ) ;
#192698=DIRECTION ( 'NONE',  ( 0.000000000000000000, -7.086529944415886769E-15, 1.000000000000000000 ) ) ;
#192722=AXIS2_PLACEMENT_3D ( 'NONE', #141278, #215661, #198682 ) ;
#192736=CARTESIAN_POINT ( 'NONE',  ( 18.49999999999998934, 56.14960075277880946, -167.7428044267231257 ) ) ;
#192739=CARTESIAN_POINT ( 'NONE',  ( 21.40925344232282868, 75.90104981139276674, -176.6816263439148145 ) ) ;
#192758=ADVANCED_FACE ( 'NONE', ( #233095 ), #241788, .F. ) ;
#192775=DIRECTION ( 'NONE',  ( 0.000000000000000000, 0.1568667991644355497, -0.9876197685951332295 ) ) ;
#192869=CARTESIAN_POINT ( 'NONE',  ( 23.15000000000000213, 85.50000000001232081, -160.1291383618718385 ) ) ;
#192875=CARTESIAN_POINT ( 'NONE',  ( 19.58285714285715073, 65.61500148966089796, -162.3934228171344785 ) ) ;
#192907=CARTESIAN_POINT ( 'NONE',  ( -21.05000000000000071, 75.90220970870363715, -176.2809220950004487 ) ) ;
#192910=EDGE_LOOP ( 'NONE', ( #137903, #58683, #3837, #59450, #232377 ) ) ;
#192939=ADVANCED_FACE ( 'NONE', ( #223753 ), #4079, .T. ) ;
#192944=CARTESIAN_POINT ( 'NONE',  ( -20.85000000000000142, 68.97833521811203639, -132.7895420826271220 ) ) ;
#192952=CIRCLE ( 'NONE', #51260, 0.09999999999998898659 ) ;
#192975=DIRECTION ( 'NONE',  ( 1.000000000000000000, 0.000000000000000000, 0.000000000000000000 ) ) ;
#192987=CARTESIAN_POINT ( 'NONE',  ( -21.52071067811865746, 68.22071067813087097, -148.8731074845244109 ) ) ;
#193008=DIRECTION ( 'NONE',  ( -1.000000000000000000, 0.000000000000000000, -0.000000000000000000 ) ) ;
#193038=DIRECTION ( 'NONE',  ( -3.265361837132813093E-16, -1.000000000000000000, -6.982962677686266711E-15 ) ) ;
#193093=FACE_OUTER_BOUND ( 'NONE', #206177, .T. ) ;
#193097=ORIENTED_EDGE ( 'NONE', *, *, #233872, .T. ) ;
#193101=FACE_OUTER_BOUND ( 'NONE', #132636, .T. ) ;
#193120=ORIENTED_EDGE ( 'NONE', *, *, #5696, .T. ) ;
#193163=EDGE_CURVE ( 'NONE', #70645, #168421, #132371, .T. ) ;
#193215=ORIENTED_EDGE ( 'NONE', *, *, #242261, .T. ) ;
#193235=AXIS2_PLACEMENT_3D ( 'NONE', #145027, #22541, #220727 ) ;
#193272=( NAMED_UNIT ( * ) PLANE_ANGLE_UNIT ( ) SI_UNIT ( $, .RADIAN. ) );
#193280=CARTESIAN_POINT ( 'NONE',  ( 20.94999999999999929, 77.13501884592227498, -128.8061306010920362 ) ) ;
#193283=ORIENTED_EDGE ( 'NONE', *, *, #246957, .F. ) ;
#193305=CARTESIAN_POINT ( 'NONE',  ( 20.85000000000000142, 68.87972903831452243, -132.8635444426850825 ) ) ;
#193309=DIRECTION ( 'NONE',  ( 0.000000000000000000, -7.026728003956695223E-15, 1.000000000000000000 ) ) ;
#193312=ORIENTED_EDGE ( 'NONE', *, *, #145704, .F. ) ;
#193315=CIRCLE ( 'NONE', #60008, 0.09999999999999939493 ) ;
#193329=DIRECTION ( 'NONE',  ( 1.000000000000000000, 0.000000000000000000, 0.000000000000000000 ) ) ;
#193348=VECTOR ( 'NONE', #225215, 1000.000000000000000 ) ;
#193358=CARTESIAN_POINT ( 'NONE',  ( 20.04142135623730070, 64.35000000001222986, -148.7731074845244450 ) ) ;
#193360=EDGE_CURVE ( 'NONE', #23846, #253904, #145195, .T. ) ;
#193405=ORIENTED_EDGE ( 'NONE', *, *, #56019, .T. ) ;
#193447=CIRCLE ( 'NONE', #68534, 0.09999999999999939493 ) ;
#193448=AXIS2_PLACEMENT_3D ( 'NONE', #179366, #137628, #238025 ) ;
#193464=CIRCLE ( 'NONE', #122541, 0.1000000000000118433 ) ;
#193473=DIRECTION ( 'NONE',  ( 0.000000000000000000, -1.000000000000000000, 0.000000000000000000 ) ) ;
#193499=AXIS2_PLACEMENT_3D ( 'NONE', #224241, #207277, #123881 ) ;
#193506=CARTESIAN_POINT ( 'NONE',  ( 20.84999999999998721, 87.75000000001215028, -136.5231074845242745 ) ) ;
#193544=ADVANCED_FACE ( 'NONE', ( #149082 ), #179080, .T. ) ;
#193548=EDGE_CURVE ( 'NONE', #66273, #178841, #189481, .T. ) ;
#193550=DIRECTION ( 'NONE',  ( 0.000000000000000000, -7.086529944415894657E-15, 1.000000000000000000 ) ) ;
#193560=CARTESIAN_POINT ( 'NONE',  ( -21.05000000000000071, 75.90220970870363715, -176.2809220950004772 ) ) ;
#193565=ORIENTED_EDGE ( 'NONE', *, *, #239776, .F. ) ;
#193569=CARTESIAN_POINT ( 'NONE',  ( -18.50000000000000000, 74.65925378207876406, -180.2959699899455472 ) ) ;
#193593=CARTESIAN_POINT ( 'NONE',  ( -18.59999999999999787, 77.63717271298267519, -158.4409541190523214 ) ) ;
#193599=LINE ( 'NONE', #13669, #59339 ) ;
#193625=CARTESIAN_POINT ( 'NONE',  ( -21.05000000000000071, 61.95000000001234497, -164.5094124137634708 ) ) ;
#193645=AXIS2_PLACEMENT_3D ( 'NONE', #140225, #115544, #56826 ) ;
#193650=CARTESIAN_POINT ( 'NONE',  ( 23.15000000000000213, 87.65000000001215597, -139.6231074845242688 ) ) ;
#193655=CARTESIAN_POINT ( 'NONE',  ( -22.50014994444008565, 64.25028026812007909, -170.1061876412429399 ) ) ;
#193665=CARTESIAN_POINT ( 'NONE',  ( -18.59999999999999787, 77.16412189325330928, -128.6082593989527254 ) ) ;
#193713=FILL_AREA_STYLE_COLOUR ( '', #114536 ) ;
#193717=DIRECTION ( 'NONE',  ( 0.000000000000000000, 6.982962677686266711E-15, -1.000000000000000000 ) ) ;
#193719=CARTESIAN_POINT ( 'NONE',  ( -18.39999999999999858, 85.50000000001233502, -162.9910380878246485 ) ) ;
#193723=VERTEX_POINT ( 'NONE', #203590 ) ;
#193751=VERTEX_POINT ( 'NONE', #217992 ) ;
#193774=AXIS2_PLACEMENT_3D ( 'NONE', #111992, #128984, #166856 ) ;
#193793=DIRECTION ( 'NONE',  ( 1.000000000000000000, 0.000000000000000000, 0.000000000000000000 ) ) ;
#193806=FACE_OUTER_BOUND ( 'NONE', #102803, .T. ) ;
#193823=ORIENTED_EDGE ( 'NONE', *, *, #248356, .F. ) ;
#193830=FACE_OUTER_BOUND ( 'NONE', #60235, .T. ) ;
#193852=VECTOR ( 'NONE', #82136, 1000.000000000000000 ) ;
#193882=TOROIDAL_SURFACE ( 'NONE', #77166, 0.2000000000000000111, 0.1000000000000000056 ) ;
#193900=CYLINDRICAL_SURFACE ( 'NONE', #70890, 0.1000000000000033362 ) ;
#193935=ORIENTED_EDGE ( 'NONE', *, *, #39375, .F. ) ;
#194014=ORIENTED_EDGE ( 'NONE', *, *, #200825, .F. ) ;
#194031=CARTESIAN_POINT ( 'NONE',  ( -23.25000000000000000, 87.65000000001215597, -139.6231074845242688 ) ) ;
#194047=ORIENTED_EDGE ( 'NONE', *, *, #57280, .F. ) ;
#194051=DIRECTION ( 'NONE',  ( 0.000000000000000000, -6.517943393102675675E-15, 1.000000000000000000 ) ) ;
#194071=VECTOR ( 'NONE', #212816, 1000.000000000000000 ) ;
#194095=CARTESIAN_POINT ( 'NONE',  ( -23.15000000000000213, 76.00000000001240608, -174.1731074845243654 ) ) ;
#194112=CARTESIAN_POINT ( 'NONE',  ( -22.50000000000000000, 75.90000000001236913, -170.0231074845243597 ) ) ;
#194134=FACE_OUTER_BOUND ( 'NONE', #161624, .T. ) ;
#194145=ADVANCED_FACE ( 'NONE', ( #178619 ), #150398, .T. ) ;
#194161=TOROIDAL_SURFACE ( 'NONE', #181679, 1.900000000000002576, 0.1000000000000000056 ) ;
#194175=ORIENTED_EDGE ( 'NONE', *, *, #179661, .F. ) ;
#194238=ADVANCED_FACE ( 'NONE', ( #54149 ), #101581, .T. ) ;
#194261=FACE_OUTER_BOUND ( 'NONE', #96235, .T. ) ;
#194267=DIRECTION ( 'NONE',  ( -0.7071067811865389130, 4.937700262164590641E-15, -0.7071067811865561215 ) ) ;
#194270=LINE ( 'NONE', #153885, #211844 ) ;
#194276=ORIENTED_EDGE ( 'NONE', *, *, #8767, .T. ) ;
#194292=LINE ( 'NONE', #15659, #12960 ) ;
#194313=FACE_OUTER_BOUND ( 'NONE', #12686, .T. ) ;
#194389=FACE_OUTER_BOUND ( 'NONE', #107124, .T. ) ;
#194409=CARTESIAN_POINT ( 'NONE',  ( -21.44999999999999929, 68.85000000001228670, -157.6731074845243938 ) ) ;
#194412=DIRECTION ( 'NONE',  ( 0.000000000000000000, -0.2605042016806647931, -0.9654727137038724427 ) ) ;
#194421=ORIENTED_EDGE ( 'NONE', *, *, #102232, .F. ) ;
#194422=CARTESIAN_POINT ( 'NONE',  ( 21.05000000000000426, 75.93429838969034051, -176.2814235418563840 ) ) ;
#194437=CARTESIAN_POINT ( 'NONE',  ( -20.94999999999999929, 64.35000000001220144, -143.3069731475025321 ) ) ;
#194472=DIRECTION ( 'NONE',  ( 0.000000000000000000, 1.000000000000000000, 6.982962677686266711E-15 ) ) ;
#194488=CARTESIAN_POINT ( 'NONE',  ( -23.15000000000000213, 64.25000000001246292, -181.7731074845244450 ) ) ;
#194497=DIRECTION ( 'NONE',  ( 0.7071067811865475727, 0.7071067811865475727, 4.937700262164531476E-15 ) ) ;
#194524=CARTESIAN_POINT ( 'NONE',  ( -20.54999999999999716, 85.00000000001222134, -146.4170766071767389 ) ) ;
#194527=AXIS2_PLACEMENT_3D ( 'NONE', #113154, #213525, #174467 ) ;
#194535=EDGE_CURVE ( 'NONE', #99384, #10361, #171443, .T. ) ;
#194547=CARTESIAN_POINT ( 'NONE',  ( 18.47073956224741309, 85.47172941248430789, -162.9144217317066250 ) ) ;
#194559=CARTESIAN_POINT ( 'NONE',  ( 21.05000000000000071, 65.27628289530476025, -157.8619171903969800 ) ) ;
#194563=AXIS2_PLACEMENT_3D ( 'NONE', #13125, #187909, #31433 ) ;
#194565=CIRCLE ( 'NONE', #148758, 0.1000000000000028644 ) ;
#194586=DIRECTION ( 'NONE',  ( -1.000000000000000000, 0.000000000000000000, -0.000000000000000000 ) ) ;
#194619=VERTEX_POINT ( 'NONE', #92298 ) ;
#194644=EDGE_CURVE ( 'NONE', #144130, #220534, #113324, .T. ) ;
#194651=B_SPLINE_CURVE_WITH_KNOTS ( 'NONE', 3,
 ( #127438, #226510, #29655, #208274, #47885, #28379, #166595, #12649 ),
 .UNSPECIFIED., .F., .F.,
 ( 4, 2, 2, 4 ),
 ( 0.000000000000000000, 0.0002114466876442027635, 0.0003171700314663131984, 0.0004228933752884235790 ),
 .UNSPECIFIED. ) ;
#194653=DIRECTION ( 'NONE',  ( 1.000000000000000000, 0.000000000000000000, 0.000000000000000000 ) ) ;
#194707=CARTESIAN_POINT ( 'NONE',  ( -18.50000000000000000, 85.42129027953477305, -129.6992253054985156 ) ) ;
#194738=EDGE_CURVE ( 'NONE', #133329, #147377, #84042, .T. ) ;
#194759=CARTESIAN_POINT ( 'NONE',  ( -20.94999999999999929, 87.65000000001215597, -139.4231074845242802 ) ) ;
#194801=DIRECTION ( 'NONE',  ( 0.000000000000000000, -6.982962677686266711E-15, 1.000000000000000000 ) ) ;
#194804=EDGE_CURVE ( 'NONE', #94515, #250601, #159151, .T. ) ;
#194806=VERTEX_POINT ( 'NONE', #119591 ) ;
#194811=EDGE_CURVE ( 'NONE', #252845, #177752, #199107, .T. ) ;
#194825=VERTEX_POINT ( 'NONE', #59556 ) ;
#194867=DIRECTION ( 'NONE',  ( 0.000000000000000000, 0.1350103645451807555, 0.9908441862701609093 ) ) ;
#194873=AXIS2_PLACEMENT_3D ( 'NONE', #210205, #147648, #27741 ) ;
#194891=PLANE ( 'NONE',  #57914 ) ;
#194892=CARTESIAN_POINT ( 'NONE',  ( -21.12844524849339223, 64.25000000001233502, -163.1186940136820169 ) ) ;
#194998=CIRCLE ( 'NONE', #65799, 0.1000000000000028644 ) ;
#195009=DIRECTION ( 'NONE',  ( 3.469446951953635015E-14, 6.982962677686266711E-15, -1.000000000000000000 ) ) ;
#195026=EDGE_CURVE ( 'NONE', #207287, #182252, #88355, .T. ) ;
#195047=CARTESIAN_POINT ( 'NONE',  ( -20.93975676684922504, 65.68895814178263493, -131.0026557862138645 ) ) ;
#195071=EDGE_CURVE ( 'NONE', #244761, #97109, #200822, .T. ) ;
#195079=EDGE_CURVE ( 'NONE', #161999, #245009, #132415, .T. ) ;
#195085=FACE_OUTER_BOUND ( 'NONE', #181299, .T. ) ;
#195087=DIRECTION ( 'NONE',  ( -1.000000000000000000, 0.000000000000000000, 0.000000000000000000 ) ) ;
#195092=VERTEX_POINT ( 'NONE', #148125 ) ;
#195104=ORIENTED_EDGE ( 'NONE', *, *, #146375, .T. ) ;
#195132=DIRECTION ( 'NONE',  ( -1.000000000000000000, 0.000000000000000000, -0.000000000000000000 ) ) ;
#195151=CARTESIAN_POINT ( 'NONE',  ( -23.25000000000000000, 77.73670573947964613, -125.0056848969006182 ) ) ;
#195165=CARTESIAN_POINT ( 'NONE',  ( -22.49917693094574389, 75.91477003579079508, -181.6729032690550127 ) ) ;
#195197=DIRECTION ( 'NONE',  ( 0.000000000000000000, -0.9908441862701791170, 0.1350103645450472789 ) ) ;
#195226=CARTESIAN_POINT ( 'NONE',  ( -22.47071067811865319, 75.90090754530983475, -177.7431822290224090 ) ) ;
#195236=ORIENTED_EDGE ( 'NONE', *, *, #206907, .F. ) ;
#195246=DIRECTION ( 'NONE',  ( 0.000000000000000000, 0.8777080977375655291, -0.4791956752370622463 ) ) ;
#195273=DIRECTION ( 'NONE',  ( 0.000000000000000000, 1.000000000000000000, 1.321694076934707365E-14 ) ) ;
#195283=LINE ( 'NONE', #253928, #250440 ) ;
#195292=CARTESIAN_POINT ( 'NONE',  ( 21.05000000000000071, 87.65000000001215597, -139.6231074845242688 ) ) ;
#195312=CARTESIAN_POINT ( 'NONE',  ( -20.00857864376270001, 66.85000000001222986, -148.7731074845244166 ) ) ;
#195319=ORIENTED_EDGE ( 'NONE', *, *, #254868, .F. ) ;
#195325=AXIS2_PLACEMENT_3D ( 'NONE', #233430, #173493, #114745 ) ;
#195351=EDGE_CURVE ( 'NONE', #133516, #255891, #214502, .T. ) ;
#195375=CARTESIAN_POINT ( 'NONE',  ( -18.59999999999999787, 64.25000000001215028, -136.5231074845244166 ) ) ;
#195380=CARTESIAN_POINT ( 'NONE',  ( 21.05000000000000071, 76.00000000001216449, -139.4231074845243654 ) ) ;
#195390=DIRECTION ( 'NONE',  ( 0.000000000000000000, -6.982962677686266711E-15, 1.000000000000000000 ) ) ;
#195432=CARTESIAN_POINT ( 'NONE',  ( 18.59999999999999787, 87.75000000001222134, -148.6731074845242802 ) ) ;
#195437=EDGE_LOOP ( 'NONE', ( #120392, #92095, #14871, #168308 ) ) ;
#195490=ADVANCED_FACE ( 'NONE', ( #68290 ), #138593, .T. ) ;
#195527=EDGE_CURVE ( 'NONE', #229354, #193751, #108694, .T. ) ;
#195611=EDGE_CURVE ( 'NONE', #93811, #95210, #155559, .T. ) ;
#195620=CARTESIAN_POINT ( 'NONE',  ( -21.05000000000000071, 77.85102823015316176, -158.3691942151018566 ) ) ;
#195629=EDGE_CURVE ( 'NONE', #75529, #49319, #255856, .T. ) ;
#195636=CARTESIAN_POINT ( 'NONE',  ( -18.59999999999999787, 64.35000000001230092, -157.8731074845244393 ) ) ;
#195642=AXIS2_PLACEMENT_3D ( 'NONE', #90109, #91422, #169712 ) ;
#195654=EDGE_LOOP ( 'NONE', ( #57528, #153850, #159801 ) ) ;
#195655=DIRECTION ( 'NONE',  ( -0.000000000000000000, -6.982962677686266711E-15, 1.000000000000000000 ) ) ;
#195659=EDGE_CURVE ( 'NONE', #92784, #138590, #80338, .T. ) ;
#195664=VECTOR ( 'NONE', #167943, 1000.000000000000000 ) ;
#195666=ORIENTED_EDGE ( 'NONE', *, *, #24142, .T. ) ;
#195684=ORIENTED_EDGE ( 'NONE', *, *, #164508, .F. ) ;
#195693=ORIENTED_EDGE ( 'NONE', *, *, #132410, .T. ) ;
#195708=VERTEX_POINT ( 'NONE', #133400 ) ;
#195728=ORIENTED_EDGE ( 'NONE', *, *, #155037, .T. ) ;
#195729=VERTEX_POINT ( 'NONE', #137238 ) ;
#195732=DIRECTION ( 'NONE',  ( 0.000000000000000000, -7.147358527629766941E-15, 1.000000000000000000 ) ) ;
#195734=EDGE_LOOP ( 'NONE', ( #130660, #39931, #52198, #247740 ) ) ;
#195743=AXIS2_PLACEMENT_3D ( 'NONE', #93048, #90472, #72223 ) ;
#195744=ORIENTED_EDGE ( 'NONE', *, *, #28494, .T. ) ;
#195762=EDGE_CURVE ( 'NONE', #218186, #41308, #22454, .T. ) ;
#195775=CIRCLE ( 'NONE', #79200, 0.8750000000000007772 ) ;
#195797=ORIENTED_EDGE ( 'NONE', *, *, #103447, .T. ) ;
#195829=CARTESIAN_POINT ( 'NONE',  ( 18.40000000000000213, 85.50000000001233502, -162.9910380878246485 ) ) ;
#195898=FACE_OUTER_BOUND ( 'NONE', #7722, .T. ) ;
#195933=FACE_OUTER_BOUND ( 'NONE', #12972, .T. ) ;
#195942=CARTESIAN_POINT ( 'NONE',  ( -23.15000000000000213, 64.35000000001222986, -148.6731074845244507 ) ) ;
#195953=CARTESIAN_POINT ( 'NONE',  ( -18.50000000000000000, 85.40000000001209912, -129.6084491415546154 ) ) ;
#195955=CARTESIAN_POINT ( 'NONE',  ( 21.05000000000000071, 65.57661458509942065, -162.5310555606543232 ) ) ;
#195978=LINE ( 'NONE', #233813, #19736 ) ;
#195990=EDGE_CURVE ( 'NONE', #53585, #52602, #113882, .T. ) ;
#196001=ADVANCED_FACE ( 'NONE', ( #108392 ), #209551, .F. ) ;
#196025=FACE_OUTER_BOUND ( 'NONE', #168249, .T. ) ;
#196029=CARTESIAN_POINT ( 'NONE',  ( -20.94999999999999929, 77.85102823015316176, -158.3691942151018566 ) ) ;
#196070=EDGE_CURVE ( 'NONE', #42435, #80243, #48040, .T. ) ;
#196073=LINE ( 'NONE', #96923, #99440 ) ;
#196107=EDGE_CURVE ( 'NONE', #15038, #210038, #120923, .T. ) ;
#196116=VECTOR ( 'NONE', #212603, 1000.000000000000000 ) ;
#196138=DIRECTION ( 'NONE',  ( 0.000000000000000000, -0.8660254037844377084, -0.5000000000000016653 ) ) ;
#196151=DIRECTION ( 'NONE',  ( -1.000000000000000000, -7.304098846218135653E-16, -4.639676173203994055E-30 ) ) ;
#196188=DIRECTION ( 'NONE',  ( 1.000000000000000000, 0.000000000000000000, 0.000000000000000000 ) ) ;
#196201=ORIENTED_EDGE ( 'NONE', *, *, #157752, .F. ) ;
#196215=ORIENTED_EDGE ( 'NONE', *, *, #111760, .T. ) ;
#196223=CARTESIAN_POINT ( 'NONE',  ( 22.50000000000000000, 64.35042919246758686, -170.1231074845244393 ) ) ;
#196228=DIRECTION ( 'NONE',  ( 0.000000000000000000, 1.000000000000000000, 0.000000000000000000 ) ) ;
#196260=CARTESIAN_POINT ( 'NONE',  ( 21.13614978966381486, 76.00000000001239187, -176.5222121863581322 ) ) ;
#196261=DIRECTION ( 'NONE',  ( 0.000000000000000000, -6.688090509790120484E-15, 1.000000000000000000 ) ) ;
#196262=DIRECTION ( 'NONE',  ( 1.000000000000000000, 0.000000000000000000, 0.000000000000000000 ) ) ;
#196273=CIRCLE ( 'NONE', #229604, 0.1000000000000046685 ) ;
#196281=DIRECTION ( 'NONE',  ( 0.000000000000000000, 0.9893560106964510714, -0.1455152366551481502 ) ) ;
#196327=CIRCLE ( 'NONE', #50578, 12.87499999999999822 ) ;
#196328=MANIFOLD_SOLID_BREP ( 'Stock-MAS-200-1', #215926 ) ;
#196358=PLANE ( 'NONE',  #132364 ) ;
#196379=ORIENTED_EDGE ( 'NONE', *, *, #223630, .T. ) ;
#196393=( BOUNDED_SURFACE ( )  B_SPLINE_SURFACE ( 3, 2, ( 
 ( #13634, #33235, #193560 ),
 ( #211841, #250936, #168893 ),
 ( #12371, #30649, #94442 ),
 ( #233957, #210549, #112732 ),
 ( #232694, #192283, #248391 ),
 ( #170185, #93157, #174033 ) ),
 .UNSPECIFIED., .F., .F., .F. ) 
 B_SPLINE_SURFACE_WITH_KNOTS ( ( 4, 2, 4 ),
 ( 3, 3 ),
 ( 0.0001792624049599621759, 0.0003686986002124818611, 0.0005581347954650015463 ),
 ( 0.000000000000000000, 1.000000000000000000 ),
 .UNSPECIFIED. ) 
 GEOMETRIC_REPRESENTATION_ITEM ( )  RATIONAL_B_SPLINE_SURFACE ( (
 ( 1.000000000000000000, 0.9238795325113097201, 1.000000000000000000),
 ( 1.000000000000000000, 0.9229318695240524839, 1.000000000000000000),
 ( 1.000000000000000000, 0.8926288119227774320, 1.000000000000000000),
 ( 1.000000000000000000, 0.8123777807274952245, 1.000000000000000000),
 ( 1.000000000000000000, 0.7629087100928820808, 1.000000000000000000),
 ( 1.000000000000000000, 0.7071067811865597852, 1.000000000000000000) ) ) 
 REPRESENTATION_ITEM ( '' )  SURFACE ( )  );
#196425=ORIENTED_EDGE ( 'NONE', *, *, #198662, .F. ) ;
#196429=ORIENTED_EDGE ( 'NONE', *, *, #154407, .F. ) ;
#196434=DIRECTION ( 'NONE',  ( 1.000000000000000000, -0.000000000000000000, 0.000000000000000000 ) ) ;
#196473=ORIENTED_EDGE ( 'NONE', *, *, #148183, .F. ) ;
#196476=CARTESIAN_POINT ( 'NONE',  ( -22.39999999999999503, 68.20922040163897293, -170.1231074845244109 ) ) ;
#196479=LINE ( 'NONE', #218601, #157200 ) ;
#196507=DIRECTION ( 'NONE',  ( 0.000000000000000000, -1.000000000000000000, -6.982962677686265922E-15 ) ) ;
#196519=ADVANCED_FACE ( 'NONE', ( #220959 ), #184405, .T. ) ;
#196597=AXIS2_PLACEMENT_3D ( 'NONE', #79453, #182441, #220286 ) ;
#196624=CARTESIAN_POINT ( 'NONE',  ( -21.65000000000000213, 68.25000000001230660, -157.6731074845243938 ) ) ;
#196644=DIRECTION ( 'NONE',  ( -1.000000000000000000, -0.000000000000000000, -0.000000000000000000 ) ) ;
#196666=CARTESIAN_POINT ( 'NONE',  ( 18.39999999999999858, 85.68240343348848853, -129.8662641071115047 ) ) ;
#196700=CARTESIAN_POINT ( 'NONE',  ( 21.05000000000000071, 76.00000000001237765, -170.0231074845243597 ) ) ;
#196715=DIRECTION ( 'NONE',  ( -1.000000000000000000, 0.000000000000000000, -0.000000000000000000 ) ) ;
#196752=CARTESIAN_POINT ( 'NONE',  ( 20.95132126680579887, 65.51005012986553311, -162.4527829460899113 ) ) ;
#196775=CARTESIAN_POINT ( 'NONE',  ( -20.12071067811865888, 66.67928932189363422, -157.6731074845244223 ) ) ;
#196790=CARTESIAN_POINT ( 'NONE',  ( 20.94999999999999929, 85.00000000001222134, -146.4170766071767389 ) ) ;
#196800=ORIENTED_EDGE ( 'NONE', *, *, #143408, .T. ) ;
#196818=CARTESIAN_POINT ( 'NONE',  ( -23.25000000000000000, 74.00000000001223555, -149.7477294072864709 ) ) ;
#196834=ORIENTED_EDGE ( 'NONE', *, *, #227532, .F. ) ;
#196856=LINE ( 'NONE', #100312, #30477 ) ;
#196869=CIRCLE ( 'NONE', #213428, 11.89999999999999325 ) ;
#196891=VERTEX_POINT ( 'NONE', #4180 ) ;
#196914=EDGE_CURVE ( 'NONE', #2577, #22950, #40785, .T. ) ;
#196924=CARTESIAN_POINT ( 'NONE',  ( 18.51024323315077069, 65.68895814178262071, -131.0026557862138361 ) ) ;
#196927=DIRECTION ( 'NONE',  ( 1.000000000000000000, 0.000000000000000000, 0.000000000000000000 ) ) ;
#196940=DIRECTION ( 'NONE',  ( 0.000000000000000000, 1.000000000000000000, 6.982962677686266711E-15 ) ) ;
#196947=CIRCLE ( 'NONE', #209417, 0.09999999999998898659 ) ;
#196958=DIRECTION ( 'NONE',  ( -1.000000000000000000, 0.000000000000000000, 0.000000000000000000 ) ) ;
#197006=ADVANCED_FACE ( 'NONE', ( #144967 ), #224517, .F. ) ;
#197014=ORIENTED_EDGE ( 'NONE', *, *, #192530, .T. ) ;
#197035=AXIS2_PLACEMENT_3D ( 'NONE', #240374, #20050, #179138 ) ;
#197057=ORIENTED_EDGE ( 'NONE', *, *, #185296, .T. ) ;
#197103=EDGE_CURVE ( 'NONE', #70015, #109498, #87559, .T. ) ;
#197105=EDGE_CURVE ( 'NONE', #144474, #151867, #59724, .T. ) ;
#197164=EDGE_CURVE ( 'NONE', #123954, #174920, #9862, .T. ) ;
#197166=DIRECTION ( 'NONE',  ( -3.265361837132813093E-16, -1.000000000000000000, -6.938893903907229955E-15 ) ) ;
#197200=EDGE_CURVE ( 'NONE', #219843, #127058, #68321, .T. ) ;
#197213=VERTEX_POINT ( 'NONE', #202090 ) ;
#197215=ORIENTED_EDGE ( 'NONE', *, *, #188905, .T. ) ;
#197237=DIRECTION ( 'NONE',  ( -1.000000000000000000, 0.000000000000000000, -0.000000000000000000 ) ) ;
#197272=ADVANCED_FACE ( 'NONE', ( #199542 ), #20908, .F. ) ;
#197289=DIRECTION ( 'NONE',  ( 0.000000000000000000, 6.982962677686266711E-15, -1.000000000000000000 ) ) ;
#197329=AXIS2_PLACEMENT_3D ( 'NONE', #201838, #59732, #102708 ) ;
#197372=AXIS2_PLACEMENT_3D ( 'NONE', #20525, #37515, #118334 ) ;
#197378=CARTESIAN_POINT ( 'NONE',  ( -23.15000000000000213, 87.48912529308822172, -139.5231074845243029 ) ) ;
#197417=DIRECTION ( 'NONE',  ( -0.000000000000000000, -6.982962677686266711E-15, 1.000000000000000000 ) ) ;
#197425=CIRCLE ( 'NONE', #39253, 0.1000000000000046685 ) ;
#197440=DIRECTION ( 'NONE',  ( 0.000000000000000000, 3.543264972207943384E-15, -1.000000000000000000 ) ) ;
#197445=ADVANCED_FACE ( 'NONE', ( #168139 ), #247362, .T. ) ;
#197508=CARTESIAN_POINT ( 'NONE',  ( 21.05000000000000071, 76.10000000001241460, -176.5637644362255969 ) ) ;
#197534=CYLINDRICAL_SURFACE ( 'NONE', #157108, 0.09999999999999939493 ) ;
#197556=CARTESIAN_POINT ( 'NONE',  ( -18.49719636458545935, 85.44636535924018972, -162.9514936146412651 ) ) ;
#197586=DIRECTION ( 'NONE',  ( 0.000000000000000000, -6.982962677686266711E-15, 1.000000000000000000 ) ) ;
#197587=CIRCLE ( 'NONE', #139315, 0.5000000000000004441 ) ;
#197592=CARTESIAN_POINT ( 'NONE',  ( -23.25000000000000000, 71.85000000001224407, -148.8731074845244109 ) ) ;
#197608=DIRECTION ( 'NONE',  ( 0.000000000000000000, 0.000000000000000000, 1.000000000000000000 ) ) ;
#197613=AXIS2_PLACEMENT_3D ( 'NONE', #23285, #41561, #200611 ) ;
#197618=ORIENTED_EDGE ( 'NONE', *, *, #167733, .T. ) ;
#197647=DIRECTION ( 'NONE',  ( 0.000000000000000000, 1.000000000000000000, 6.853228547068871147E-15 ) ) ;
#197658=CARTESIAN_POINT ( 'NONE',  ( -22.50000000000000000, 64.35000000001240039, -170.0231074845244166 ) ) ;
#197660=LINE ( 'NONE', #19030, #56939 ) ;
#197663=ORIENTED_EDGE ( 'NONE', *, *, #111197, .T. ) ;
#197672=AXIS2_PLACEMENT_3D ( 'NONE', #186118, #32203, #46584 ) ;
#197683=DIRECTION ( 'NONE',  ( 0.000000000000000000, 0.000000000000000000, 1.000000000000000000 ) ) ;
#197690=DIRECTION ( 'NONE',  ( 0.000000000000000000, -1.387778780781406043E-13, 1.000000000000000000 ) ) ;
#197698=CARTESIAN_POINT ( 'NONE',  ( -21.05000000000000071, 87.75000000001216449, -139.4231074845242802 ) ) ;
#197699=ORIENTED_EDGE ( 'NONE', *, *, #34503, .F. ) ;
#197736=CYLINDRICAL_SURFACE ( 'NONE', #166450, 0.09999999999998898659 ) ;
#197742=ADVANCED_FACE ( 'NONE', ( #130894, #70964, #31834 ), #253410, .F. ) ;
#197778=CARTESIAN_POINT ( 'NONE',  ( 20.12500000000000000, 66.25000000001232081, -161.9113362024101548 ) ) ;
#197782=VECTOR ( 'NONE', #48618, 1000.000000000000000 ) ;
#197848=CARTESIAN_POINT ( 'NONE',  ( 21.05000000000000071, 69.74218538953624602, -170.1208977758331855 ) ) ;
#197864=DIRECTION ( 'NONE',  ( 0.000000000000000000, 0.000000000000000000, -1.000000000000000000 ) ) ;
#197865=AXIS2_PLACEMENT_3D ( 'NONE', #129155, #24935, #206120 ) ;
#197874=LINE ( 'NONE', #161342, #226384 ) ;
#197875=ADVANCED_FACE ( 'NONE', ( #155639 ), #117752, .F. ) ;
#197916=ORIENTED_EDGE ( 'NONE', *, *, #141267, .F. ) ;
#197972=ADVANCED_FACE ( 'NONE', ( #160769 ), #245421, .T. ) ;
#197992=EDGE_CURVE ( 'NONE', #7914, #193723, #147797, .T. ) ;
#197996=DIRECTION ( 'NONE',  ( -0.7071067811865475727, 0.7071067811865475727, 4.937700262164531476E-15 ) ) ;
#198025=VERTEX_POINT ( 'NONE', #65480 ) ;
#198029=ORIENTED_EDGE ( 'NONE', *, *, #22510, .F. ) ;
#198031=ORIENTED_EDGE ( 'NONE', *, *, #159592, .T. ) ;
#198034=CARTESIAN_POINT ( 'NONE',  ( 20.95420533658165141, 65.45413552525275236, -162.4556014638312149 ) ) ;
#198041=CARTESIAN_POINT ( 'NONE',  ( 18.49999999999999289, 65.50857864377491069, -145.1731074845244507 ) ) ;
#198073=CIRCLE ( 'NONE', #56570, 0.09999999999998898659 ) ;
#198134=CARTESIAN_POINT ( 'NONE',  ( -18.59999999999999787, 64.25000000001229239, -157.8731074845244393 ) ) ;
#198144=DIRECTION ( 'NONE',  ( -1.000000000000000000, 0.000000000000000000, -0.000000000000000000 ) ) ;
#198181=DIRECTION ( 'NONE',  ( 1.000000000000000000, 0.000000000000000000, 0.000000000000000000 ) ) ;
#198206=DIRECTION ( 'NONE',  ( 0.000000000000000000, 1.000000000000000000, 0.000000000000000000 ) ) ;
#198213=DIRECTION ( 'NONE',  ( -1.000000000000000000, 0.000000000000000000, 0.000000000000000000 ) ) ;
#198216=DIRECTION ( 'NONE',  ( -0.000000000000000000, -6.982962677686266711E-15, 1.000000000000000000 ) ) ;
#198233=AXIS2_PLACEMENT_3D ( 'NONE', #4541, #84037, #140189 ) ;
#198243=EDGE_CURVE ( 'NONE', #91227, #2383, #43911, .T. ) ;
#198245=EDGE_CURVE ( 'NONE', #73802, #149398, #189666, .T. ) ;
#198263=DIRECTION ( 'NONE',  ( -1.000000000000000000, 0.000000000000000000, 0.000000000000000000 ) ) ;
#198294=AXIS2_PLACEMENT_3D ( 'NONE', #92177, #73937, #133872 ) ;
#198305=CIRCLE ( 'NONE', #156657, 0.09999999999998898659 ) ;
#198310=ADVANCED_FACE ( 'NONE', ( #157782 ), #59883, .T. ) ;
#198334=ORIENTED_EDGE ( 'NONE', *, *, #70609, .T. ) ;
#198343=ORIENTED_EDGE ( 'NONE', *, *, #168329, .F. ) ;
#198365=EDGE_CURVE ( 'NONE', #73802, #168523, #23090, .T. ) ;
#198367=VERTEX_POINT ( 'NONE', #198134 ) ;
#198368=FACE_OUTER_BOUND ( 'NONE', #36689, .T. ) ;
#198419=CARTESIAN_POINT ( 'NONE',  ( -18.50000000000000000, 77.86671491006960366, -158.2704322382423356 ) ) ;
#198459=ORIENTED_EDGE ( 'NONE', *, *, #196914, .T. ) ;
#198462=AXIS2_PLACEMENT_3D ( 'NONE', #230096, #51427, #130999 ) ;
#198505=CARTESIAN_POINT ( 'NONE',  ( 22.39999999999999503, 64.25000000001237765, -170.0231074845244166 ) ) ;
#198517=AXIS2_PLACEMENT_3D ( 'NONE', #252878, #256684, #235878 ) ;
#198534=AXIS2_PLACEMENT_3D ( 'NONE', #94133, #189392, #249376 ) ;
#198541=ORIENTED_EDGE ( 'NONE', *, *, #171338, .T. ) ;
#198555=AXIS2_PLACEMENT_3D ( 'NONE', #35864, #116661, #171537 ) ;
#198565=ORIENTED_EDGE ( 'NONE', *, *, #118391, .T. ) ;
#198588=ORIENTED_EDGE ( 'NONE', *, *, #59422, .F. ) ;
#198605=DIRECTION ( 'NONE',  ( 0.000000000000000000, 0.000000000000000000, 1.000000000000000000 ) ) ;
#198616=FACE_OUTER_BOUND ( 'NONE', #3703, .T. ) ;
#198631=CARTESIAN_POINT ( 'NONE',  ( -18.53317502108577131, 65.67736539654967487, -130.9625116876572406 ) ) ;
#198635=EDGE_CURVE ( 'NONE', #194825, #90961, #101756, .T. ) ;
#198662=EDGE_CURVE ( 'NONE', #122358, #105820, #206410, .T. ) ;
#198664=TOROIDAL_SURFACE ( 'NONE', #32291, 0.2000000000000000111, 0.1000000000000000056 ) ;
#198667=EDGE_CURVE ( 'NONE', #255891, #151389, #68479, .T. ) ;
#198682=DIRECTION ( 'NONE',  ( 1.000000000000000000, 0.000000000000000000, 0.000000000000000000 ) ) ;
#198683=EDGE_CURVE ( 'NONE', #61341, #156062, #31098, .T. ) ;
#198738=ORIENTED_EDGE ( 'NONE', *, *, #35705, .T. ) ;
#198745=FACE_OUTER_BOUND ( 'NONE', #123915, .T. ) ;
#198747=DIRECTION ( 'NONE',  ( -0.000000000000000000, -1.000000000000000000, -6.982962677686266711E-15 ) ) ;
#198748=ORIENTED_EDGE ( 'NONE', *, *, #129573, .T. ) ;
#198755=ORIENTED_EDGE ( 'NONE', *, *, #21398, .F. ) ;
#198760=CARTESIAN_POINT ( 'NONE',  ( 20.85000000000000142, 87.75000000001215028, -139.4231074845242802 ) ) ;
#198794=EDGE_CURVE ( 'NONE', #34074, #48521, #2379, .T. ) ;
#198799=DIRECTION ( 'NONE',  ( 0.000000000000000000, 0.1455152366551700771, 0.9893560106964479628 ) ) ;
#198821=FACE_OUTER_BOUND ( 'NONE', #13575, .T. ) ;
#198843=CARTESIAN_POINT ( 'NONE',  ( -18.59999996769639097, 85.36327376984262116, -162.8416135690584667 ) ) ;
#198905=CARTESIAN_POINT ( 'NONE',  ( -20.64999999999999858, 71.65000000001228386, -157.6731074845243938 ) ) ;
#198944=ORIENTED_EDGE ( 'NONE', *, *, #233630, .T. ) ;
#198980=CARTESIAN_POINT ( 'NONE',  ( -22.43310005002225438, 75.99436305787158119, -181.6727696116587651 ) ) ;
#199001=EDGE_CURVE ( 'NONE', #44761, #253610, #26985, .T. ) ;
#199048=EDGE_CURVE ( 'NONE', #61384, #90961, #220620, .T. ) ;
#199064=CARTESIAN_POINT ( 'NONE',  ( -18.59999999999999787, 64.25000000001246292, -181.7731074845244450 ) ) ;
#199107=LINE ( 'NONE', #174466, #4963 ) ;
#199144=CARTESIAN_POINT ( 'NONE',  ( 21.14999999999999858, 69.45934304831114048, -170.0231074845243882 ) ) ;
#199164=CARTESIAN_POINT ( 'NONE',  ( 23.24999999999999289, 69.45000000001222418, -148.6731074845243938 ) ) ;
#199173=CIRCLE ( 'NONE', #128440, 0.5999999999999894307 ) ;
#199174=ORIENTED_EDGE ( 'NONE', *, *, #198667, .T. ) ;
#199186=CARTESIAN_POINT ( 'NONE',  ( 22.57320508075687115, 64.25000000001237765, -170.0231074845244166 ) ) ;
#199205=EDGE_CURVE ( 'NONE', #38071, #4663, #35296, .T. ) ;
#199239=VECTOR ( 'NONE', #79997, 1000.000000000000114 ) ;
#199240=DIRECTION ( 'NONE',  ( 0.000000000000000000, -0.9908441862701420355, -0.1350103645453197554 ) ) ;
#199252=CARTESIAN_POINT ( 'NONE',  ( -18.59999999999999787, 74.83729825007431202, -161.9231074845243654 ) ) ;
#199258=CARTESIAN_POINT ( 'NONE',  ( 18.50000000000000355, 85.42107434499909857, -129.6986354250934710 ) ) ;
#199290=DIRECTION ( 'NONE',  ( 1.000000000000000000, 0.000000000000000000, 0.000000000000000000 ) ) ;
#199355=AXIS2_PLACEMENT_3D ( 'NONE', #142786, #62006, #21599 ) ;
#199366=ORIENTED_EDGE ( 'NONE', *, *, #213656, .F. ) ;
#199367=DIRECTION ( 'NONE',  ( -1.000000000000000000, -0.000000000000000000, -0.000000000000000000 ) ) ;
#199393=CARTESIAN_POINT ( 'NONE',  ( 18.50000000000000000, 85.40000000001232650, -163.0238218066854472 ) ) ;
#199396=VECTOR ( 'NONE', #186838, 999.9999999999998863 ) ;
#199407=DIRECTION ( 'NONE',  ( 1.000000000000000000, -0.000000000000000000, 0.000000000000000000 ) ) ;
#199435=EDGE_CURVE ( 'NONE', #157237, #148346, #172932, .T. ) ;
#199449=DIRECTION ( 'NONE',  ( 0.000000000000000000, 5.551115123126393596E-13, -1.000000000000000000 ) ) ;
#199463=SHAPE_DEFINITION_REPRESENTATION ( #251405, #106899 ) ;
#199542=FACE_OUTER_BOUND ( 'NONE', #27607, .T. ) ;
#199543=AXIS2_PLACEMENT_3D ( 'NONE', #112748, #52754, #94456 ) ;
#199557=ORIENTED_EDGE ( 'NONE', *, *, #123115, .F. ) ;
#199598=LINE ( 'NONE', #216563, #84726 ) ;
#199610=AXIS2_PLACEMENT_3D ( 'NONE', #184715, #42644, #85581 ) ;
#199618=PLANE ( 'NONE',  #20914 ) ;
#199634=CARTESIAN_POINT ( 'NONE',  ( -20.64999999999999858, 76.00000000001222134, -149.3981074845243313 ) ) ;
#199636=B_SPLINE_CURVE_WITH_KNOTS ( 'NONE', 3,
 ( #169676, #133075, #210055, #131780, #212618, #152664, #14434, #71830, #92647, #253007, #91382, #151369, #70561, #10566, #228328, #50936, #129222, #113505, #109639 ),
 .UNSPECIFIED., .F., .F.,
 ( 4, 3, 3, 3, 3, 3, 4 ),
 ( 0.000000000000000000, 1.655171619025938174E-05, 2.773500582849094026E-05, 5.941817267379380797E-05, 0.0001114174635873529072, 0.0001914169455916513380, 0.0002627181070750865912 ),
 .UNSPECIFIED. ) ;
#199653=ORIENTED_EDGE ( 'NONE', *, *, #155348, .T. ) ;
#199656=ORIENTED_EDGE ( 'NONE', *, *, #200825, .T. ) ;
#199722=FACE_OUTER_BOUND ( 'NONE', #249289, .T. ) ;
#199740=VERTEX_POINT ( 'NONE', #2214 ) ;
#199746=AXIS2_PLACEMENT_3D ( 'NONE', #140442, #216131, #62209 ) ;
#199789=EDGE_CURVE ( 'NONE', #216103, #255384, #2366, .T. ) ;
#199802=VERTEX_POINT ( 'NONE', #77907 ) ;
#199820=( BOUNDED_SURFACE ( )  B_SPLINE_SURFACE ( 3, 2, ( 
 ( #186304, #48058, #7666 ),
 ( #70227, #91043, #50611 ),
 ( #231855, #130156, #170636 ),
 ( #27255, #32388, #209709 ) ),
 .UNSPECIFIED., .F., .F., .T. ) 
 B_SPLINE_SURFACE_WITH_KNOTS ( ( 4, 4 ),
 ( 3, 3 ),
 ( 0.04058434257139457990, 0.04256401539001584966 ),
 ( 0.000000000000000000, 1.000000000000000000 ),
 .UNSPECIFIED. ) 
 GEOMETRIC_REPRESENTATION_ITEM ( )  RATIONAL_B_SPLINE_SURFACE ( (
 ( 1.000000000000000000, 0.7103081912007894738, 1.000000000000000000),
 ( 1.000000000000000000, 0.7104998333556562518, 1.000000000000000000),
 ( 1.000000000000000000, 0.7107238315754180746, 1.000000000000000000),
 ( 1.000000000000000000, 0.7110073749539692622, 1.000000000000000000) ) ) 
 REPRESENTATION_ITEM ( '' )  SURFACE ( )  );
#199834=ORIENTED_EDGE ( 'NONE', *, *, #218642, .T. ) ;
#199863=DIRECTION ( 'NONE',  ( 1.000000000000000000, 0.000000000000000000, 0.000000000000000000 ) ) ;
#199866=( BOUNDED_SURFACE ( )  B_SPLINE_SURFACE ( 3, 2, ( 
 ( #34595, #232794, #228930 ),
 ( #54124, #193655, #174130 ),
 ( #15027, #72436, #29478 ),
 ( #192368, #13726, #253601 ) ),
 .UNSPECIFIED., .F., .F., .F. ) 
 B_SPLINE_SURFACE_WITH_KNOTS ( ( 4, 4 ),
 ( 3, 3 ),
 ( 0.0006461284895273765793, 0.0007503702773986202284 ),
 ( 0.000000000000000000, 1.000000000000000000 ),
 .UNSPECIFIED. ) 
 GEOMETRIC_REPRESENTATION_ITEM ( )  RATIONAL_B_SPLINE_SURFACE ( (
 ( 1.000000000000000000, 0.7071067811865475727, 1.000000000000000000),
 ( 1.000000000000000000, 0.7076476444649162367, 1.000000000000000000),
 ( 1.000000000000000000, 0.7075727925191654943, 1.000000000000000000),
 ( 1.000000000000000000, 0.7071067811865581199, 1.000000000000000000) ) ) 
 REPRESENTATION_ITEM ( '' )  SURFACE ( )  );
#199881=FACE_OUTER_BOUND ( 'NONE', #147670, .T. ) ;
#199889=CARTESIAN_POINT ( 'NONE',  ( -23.15000000000000213, 71.85000000001224407, -148.8731074845244109 ) ) ;
#199899=ORIENTED_EDGE ( 'NONE', *, *, #111600, .T. ) ;
#199917=ORIENTED_EDGE ( 'NONE', *, *, #126510, .T. ) ;
#199925=ORIENTED_EDGE ( 'NONE', *, *, #90199, .F. ) ;
#199928=CARTESIAN_POINT ( 'NONE',  ( -20.64999999999999858, 71.65000000001228386, -157.7731074845243882 ) ) ;
#199993=DIRECTION ( 'NONE',  ( 0.5000000000001141309, -6.047423072554455661E-15, 0.8660254037843729824 ) ) ;
#200018=CARTESIAN_POINT ( 'NONE',  ( -20.95613430942426092, 64.25000000001233502, -163.1659448363049876 ) ) ;
#200033=EDGE_CURVE ( 'NONE', #242376, #56828, #84277, .T. ) ;
#200038=VERTEX_POINT ( 'NONE', #133729 ) ;
#200050=EDGE_CURVE ( 'NONE', #147041, #256686, #235394, .T. ) ;
#200063=EDGE_CURVE ( 'NONE', #52101, #227362, #110724, .T. ) ;
#200088=ORIENTED_EDGE ( 'NONE', *, *, #103803, .F. ) ;
#200125=ORIENTED_EDGE ( 'NONE', *, *, #208654, .T. ) ;
#200138=CARTESIAN_POINT ( 'NONE',  ( -23.25000000000000000, 64.35000000001238618, -170.0231074845244166 ) ) ;
#200146=CIRCLE ( 'NONE', #145965, 1.900000000000012790 ) ;
#200182=VERTEX_POINT ( 'NONE', #200138 ) ;
#200199=LINE ( 'NONE', #115511, #101822 ) ;
#200232=ORIENTED_EDGE ( 'NONE', *, *, #466, .F. ) ;
#200243=VERTEX_POINT ( 'NONE', #120619 ) ;
#200245=ORIENTED_EDGE ( 'NONE', *, *, #179542, .T. ) ;
#200253=ORIENTED_EDGE ( 'NONE', *, *, #117734, .F. ) ;
#200273=DIRECTION ( 'NONE',  ( 0.000000000000000000, -0.7397360091702802620, 0.6728971962616779878 ) ) ;
#200305=ORIENTED_EDGE ( 'NONE', *, *, #18161, .F. ) ;
#200318=CIRCLE ( 'NONE', #121259, 11.80000000000000426 ) ;
#200347=DIRECTION ( 'NONE',  ( 1.000000000000000000, 0.000000000000000000, 0.000000000000000000 ) ) ;
#200353=CARTESIAN_POINT ( 'NONE',  ( 18.59999999999999432, 77.16270174995034381, -162.0231074845243313 ) ) ;
#200431=CARTESIAN_POINT ( 'NONE',  ( -20.54999999999999716, 85.00000000001232081, -160.6291383618718385 ) ) ;
#200433=CIRCLE ( 'NONE', #87973, 0.2000000000000057288 ) ;
#200441=AXIS2_PLACEMENT_3D ( 'NONE', #170742, #31221, #110709 ) ;
#200493=DIRECTION ( 'NONE',  ( -1.000000000000000000, 0.000000000000000000, -0.000000000000000000 ) ) ;
#200498=ORIENTED_EDGE ( 'NONE', *, *, #59422, .T. ) ;
#200506=EDGE_CURVE ( 'NONE', #183531, #123954, #211712, .T. ) ;
#200527=CARTESIAN_POINT ( 'NONE',  ( 18.46163235739484421, 85.48015080693031109, -129.8654969446463383 ) ) ;
#200556=ORIENTED_EDGE ( 'NONE', *, *, #144280, .F. ) ;
#200604=VECTOR ( 'NONE', #223141, 1000.000000000000000 ) ;
#200606=EDGE_CURVE ( 'NONE', #147041, #228499, #136003, .T. ) ;
#200611=DIRECTION ( 'NONE',  ( 0.7071067811865127117, 0.7071067811865821007, 0.000000000000000000 ) ) ;
#200623=CARTESIAN_POINT ( 'NONE',  ( -18.59999999999999787, 77.16270174995034381, -161.9231074845243370 ) ) ;
#200658=CARTESIAN_POINT ( 'NONE',  ( -20.54999999999999716, 76.00000000001213607, -136.5231074845243313 ) ) ;
#200721=ORIENTED_EDGE ( 'NONE', *, *, #234321, .T. ) ;
#200728=CARTESIAN_POINT ( 'NONE',  ( 23.24999999999999645, 71.22429906543287359, -158.1743393804784148 ) ) ;
#200729=AXIS2_PLACEMENT_3D ( 'NONE', #137708, #239406, #19064 ) ;
#200730=VERTEX_POINT ( 'NONE', #53270 ) ;
#200764=ORIENTED_EDGE ( 'NONE', *, *, #208654, .F. ) ;
#200788=TOROIDAL_SURFACE ( 'NONE', #175864, 0.9750000000000019762, 0.1000000000000000056 ) ;
#200793=DIRECTION ( 'NONE',  ( 0.000000000000000000, 0.9915357197604982575, -0.1298341882519033486 ) ) ;
#200794=EDGE_LOOP ( 'NONE', ( #130069, #186806, #140668, #12992 ) ) ;
#200799=CIRCLE ( 'NONE', #246572, 0.09999999999998898659 ) ;
#200822=CIRCLE ( 'NONE', #138429, 0.09999999999998898659 ) ;
#200825=EDGE_CURVE ( 'NONE', #23721, #236193, #81773, .T. ) ;
#200826=CIRCLE ( 'NONE', #188341, 12.97499999999998721 ) ;
#200871=FACE_OUTER_BOUND ( 'NONE', #148969, .T. ) ;
#200883=DIRECTION ( 'NONE',  ( -7.304098846217948299E-16, -1.000000000000000000, 0.000000000000000000 ) ) ;
#200927=ORIENTED_EDGE ( 'NONE', *, *, #185420, .T. ) ;
#200947=DIRECTION ( 'NONE',  ( -0.000000000000000000, 1.000000000000000000, 6.982962677686266711E-15 ) ) ;
#200955=ORIENTED_EDGE ( 'NONE', *, *, #116473, .F. ) ;
#200975=VERTEX_POINT ( 'NONE', #46515 ) ;
#200980=DIRECTION ( 'NONE',  ( 0.000000000000000000, 1.000000000000000000, 6.982962677686266711E-15 ) ) ;
#200990=ORIENTED_EDGE ( 'NONE', *, *, #92586, .F. ) ;
#201027=CARTESIAN_POINT ( 'NONE',  ( -18.50000000000000000, 77.83585931145570669, -125.0186683157258045 ) ) ;
#201028=CARTESIAN_POINT ( 'NONE',  ( 20.97438252431638972, 67.07457649393631982, -161.5507367955136147 ) ) ;
#201049=EDGE_CURVE ( 'NONE', #247434, #240428, #15120, .T. ) ;
#201065=CARTESIAN_POINT ( 'NONE',  ( 23.24999999999999645, 76.00000000001237765, -170.0231074845243597 ) ) ;
#201093=ORIENTED_EDGE ( 'NONE', *, *, #250862, .T. ) ;
#201104=EDGE_LOOP ( 'NONE', ( #44993, #74174, #33692, #217482 ) ) ;
#201107=ADVANCED_FACE ( 'NONE', ( #217133 ), #211230, .F. ) ;
#201158=VECTOR ( 'NONE', #241727, 1000.000000000000000 ) ;
#201160=CARTESIAN_POINT ( 'NONE',  ( 23.14999999999999503, 64.25000000001222134, -148.6731074845244507 ) ) ;
#201205=ORIENTED_EDGE ( 'NONE', *, *, #4350, .F. ) ;
#201218=EDGE_CURVE ( 'NONE', #125758, #105820, #82746, .T. ) ;
#201219=CARTESIAN_POINT ( 'NONE',  ( -20.85000000000000142, 77.83585931145570669, -125.0186683157258329 ) ) ;
#201242=DIRECTION ( 'NONE',  ( 0.000000000000000000, 0.000000000000000000, -1.000000000000000000 ) ) ;
#201250=CARTESIAN_POINT ( 'NONE',  ( -18.59999999999999787, 77.16412189325330928, -128.6082593989527254 ) ) ;
#201266=FACE_OUTER_BOUND ( 'NONE', #137087, .T. ) ;
#201267=TOROIDAL_SURFACE ( 'NONE', #247051, 7.800000000000000711, 0.1000000000000000056 ) ;
#201270=ORIENTED_EDGE ( 'NONE', *, *, #78535, .T. ) ;
#201273=CARTESIAN_POINT ( 'NONE',  ( 18.59999999999999076, 69.01799029515566986, -132.8269553662681233 ) ) ;
#201313=CARTESIAN_POINT ( 'NONE',  ( -20.64999999999999858, 73.50000000001229239, -156.7984855617622770 ) ) ;
#201369=CARTESIAN_POINT ( 'NONE',  ( 21.05000000000000071, 75.98528214348799281, -176.3678308886158561 ) ) ;
#201371=EDGE_CURVE ( 'NONE', #240241, #94754, #157266, .T. ) ;
#201416=ADVANCED_FACE ( 'NONE', ( #55182 ), #154369, .F. ) ;
#201427=VECTOR ( 'NONE', #171056, 1000.000000000000000 ) ;
#201467=ORIENTED_EDGE ( 'NONE', *, *, #46683, .T. ) ;
#201477=ORIENTED_EDGE ( 'NONE', *, *, #166314, .F. ) ;
#201502=CARTESIAN_POINT ( 'NONE',  ( 23.14999999999998437, 76.00000000001237765, -170.0231074845243597 ) ) ;
#201519=EDGE_LOOP ( 'NONE', ( #40744, #114626, #150596, #248348 ) ) ;
#201567=AXIS2_PLACEMENT_3D ( 'NONE', #123841, #2585, #82106 ) ;
#201568=CARTESIAN_POINT ( 'NONE',  ( 21.97500000000000497, 66.25000000001223555, -148.8731074845244393 ) ) ;
#201578=CARTESIAN_POINT ( 'NONE',  ( 20.94999999999999929, 84.73084112150753811, -146.1211822035086527 ) ) ;
#201617=EDGE_CURVE ( 'NONE', #109454, #204085, #67826, .T. ) ;
#201630=CARTESIAN_POINT ( 'NONE',  ( 20.12500000000000355, 66.74195072709500209, -161.6597686473819806 ) ) ;
#201683=LINE ( 'NONE', #20505, #83283 ) ;
#201704=CARTESIAN_POINT ( 'NONE',  ( 21.07954763557393818, 69.67070900997511274, -170.0889834031426915 ) ) ;
#201710=FACE_OUTER_BOUND ( 'NONE', #159568, .T. ) ;
#201718=CIRCLE ( 'NONE', #155959, 0.09999999999998898659 ) ;
#201785=DIRECTION ( 'NONE',  ( 0.000000000000000000, 0.000000000000000000, 1.000000000000000000 ) ) ;
#201819=CIRCLE ( 'NONE', #51769, 0.09999999999998898659 ) ;
#201831=EDGE_CURVE ( 'NONE', #222470, #159949, #107343, .T. ) ;
#201837=ORIENTED_EDGE ( 'NONE', *, *, #81499, .F. ) ;
#201838=CARTESIAN_POINT ( 'NONE',  ( -21.14999999999999858, 64.35000000001238618, -169.9231074845244507 ) ) ;
#201858=CARTESIAN_POINT ( 'NONE',  ( -20.85000000000000142, 76.00000000001207923, -128.6231074845243540 ) ) ;
#201872=EDGE_LOOP ( 'NONE', ( #118802, #174618 ) ) ;
#201875=VERTEX_POINT ( 'NONE', #59788 ) ;
#201883=LINE ( 'NONE', #42811, #219520 ) ;
#201885=CIRCLE ( 'NONE', #35519, 11.75000000000001066 ) ;
#201888=ORIENTED_EDGE ( 'NONE', *, *, #103009, .T. ) ;
#201905=DIRECTION ( 'NONE',  ( 1.000000000000000000, 0.000000000000000000, 0.000000000000000000 ) ) ;
#201925=CARTESIAN_POINT ( 'NONE',  ( -21.14999999999999858, 76.00000000001246292, -181.6726782920691505 ) ) ;
#201949=EDGE_CURVE ( 'NONE', #66247, #88568, #40762, .T. ) ;
#201956=EDGE_LOOP ( 'NONE', ( #129947, #148315, #214042, #183921 ) ) ;
#201975=DIRECTION ( 'NONE',  ( -1.000000000000000000, 0.000000000000000000, 0.000000000000000000 ) ) ;
#201991=FACE_OUTER_BOUND ( 'NONE', #38259, .T. ) ;
#202000=CIRCLE ( 'NONE', #218717, 2.099999999999990763 ) ;
#202008=ORIENTED_EDGE ( 'NONE', *, *, #53661, .F. ) ;
#202010=AXIS2_PLACEMENT_3D ( 'NONE', #124158, #120336, #121606 ) ;
#202032=DIRECTION ( 'NONE',  ( 0.000000000000000000, -0.8660254037844468122, -0.4999999999999859557 ) ) ;
#202089=DIRECTION ( 'NONE',  ( -0.000000000000000000, 1.000000000000000000, 6.982962677686266711E-15 ) ) ;
#202090=CARTESIAN_POINT ( 'NONE',  ( -20.94999999999999929, 77.83534155023670564, -158.3679561919613548 ) ) ;
#202098=ORIENTED_EDGE ( 'NONE', *, *, #255835, .F. ) ;
#202145=CARTESIAN_POINT ( 'NONE',  ( 20.94999999999999574, 62.00000000001233502, -164.5960149541419071 ) ) ;
#202162=DIRECTION ( 'NONE',  ( 1.000000000000000000, 0.000000000000000000, 0.000000000000000000 ) ) ;
#202195=CARTESIAN_POINT ( 'NONE',  ( 20.94999999999999574, 69.45000000001230944, -160.1792853948412869 ) ) ;
#202198=ORIENTED_EDGE ( 'NONE', *, *, #238765, .T. ) ;
#202236=AXIS2_PLACEMENT_3D ( 'NONE', #45911, #88865, #204963 ) ;
#202248=ORIENTED_EDGE ( 'NONE', *, *, #179673, .F. ) ;
#202249=EDGE_CURVE ( 'NONE', #21932, #15038, #78479, .T. ) ;
#202254=CARTESIAN_POINT ( 'NONE',  ( 21.05000000000000071, 67.22371735104120205, -161.5355151060043113 ) ) ;
#202340=ORIENTED_EDGE ( 'NONE', *, *, #69720, .F. ) ;
#202346=ORIENTED_EDGE ( 'NONE', *, *, #176747, .T. ) ;
#202349=CARTESIAN_POINT ( 'NONE',  ( 18.49999999999999289, 64.35000000001214460, -136.5231074845244166 ) ) ;
#202354=ORIENTED_EDGE ( 'NONE', *, *, #236028, .F. ) ;
#202396=DIRECTION ( 'NONE',  ( 1.000000000000000000, 0.000000000000000000, 0.000000000000000000 ) ) ;
#202404=DIRECTION ( 'NONE',  ( 0.000000000000000000, -6.982962677686266711E-15, 1.000000000000000000 ) ) ;
#202406=LINE ( 'NONE', #177742, #179429 ) ;
#202416=FACE_OUTER_BOUND ( 'NONE', #12302, .T. ) ;
#202429=CARTESIAN_POINT ( 'NONE',  ( -23.15000000000000213, 71.65000000001222702, -148.8731074845244109 ) ) ;
#202439=EDGE_LOOP ( 'NONE', ( #49185, #160090, #184679, #80012 ) ) ;
#202445=ORIENTED_EDGE ( 'NONE', *, *, #170165, .F. ) ;
#202450=DIRECTION ( 'NONE',  ( 1.000000000000000000, 0.000000000000000000, 0.000000000000000000 ) ) ;
#202493=CARTESIAN_POINT ( 'NONE',  ( -18.50016250449483479, 65.70233904877031250, -131.0487410911968595 ) ) ;
#202510=DIRECTION ( 'NONE',  ( 0.000000000000000000, 1.000000000000000000, 6.982962677686266711E-15 ) ) ;
#202512=EDGE_CURVE ( 'NONE', #43685, #188264, #20435, .T. ) ;
#202514=TOROIDAL_SURFACE ( 'NONE', #173346, 11.89999999999999858, 0.1000000000000000056 ) ;
#202531=FACE_OUTER_BOUND ( 'NONE', #51617, .T. ) ;
#202574=DIRECTION ( 'NONE',  ( 0.000000000000000000, 0.6728971962617102953, 0.7397360091702507301 ) ) ;
#202582=DIRECTION ( 'NONE',  ( 0.000000000000000000, 0.000000000000000000, 1.000000000000000000 ) ) ;
#202611=CARTESIAN_POINT ( 'NONE',  ( 22.50000000000000000, 64.35042919246758686, -170.1231074845244393 ) ) ;
#202680=EDGE_LOOP ( 'NONE', ( #169548, #160271, #35642, #190807 ) ) ;
#202706=DIRECTION ( 'NONE',  ( 0.000000000000000000, -6.938893903907030216E-14, 1.000000000000000000 ) ) ;
#202722=CARTESIAN_POINT ( 'NONE',  ( -21.05000000000000071, 64.35000000001234355, -163.2392418215462726 ) ) ;
#202757=DIRECTION ( 'NONE',  ( -1.000000000000000000, 2.952720810173289112E-16, 2.061873921506763405E-30 ) ) ;
#202771=EDGE_CURVE ( 'NONE', #127786, #228568, #25747, .T. ) ;
#202777=ORIENTED_EDGE ( 'NONE', *, *, #81195, .F. ) ;
#202817=ADVANCED_FACE ( 'NONE', ( #192013 ), #116299, .T. ) ;
#202833=AXIS2_PLACEMENT_3D ( 'NONE', #212249, #196507, #56978 ) ;
#202841=ORIENTED_EDGE ( 'NONE', *, *, #135616, .F. ) ;
#202862=ADVANCED_FACE ( 'NONE', ( #51160 ), #107307, .F. ) ;
#202878=LINE ( 'NONE', #5942, #71872 ) ;
#202884=DIRECTION ( 'NONE',  ( 1.000000000000000000, -3.265361837132813093E-16, -2.280189983783949500E-30 ) ) ;
#202905=PLANE ( 'NONE',  #156525 ) ;
#202928=ORIENTED_EDGE ( 'NONE', *, *, #167212, .T. ) ;
#203000=DIRECTION ( 'NONE',  ( -1.000000000000000000, 2.952720810173289112E-16, 2.061873921506763405E-30 ) ) ;
#203003=CARTESIAN_POINT ( 'NONE',  ( 18.42636655943171675, 85.49694431578275555, -129.9140269133687866 ) ) ;
#203007=CARTESIAN_POINT ( 'NONE',  ( 21.05095171578076574, 67.22382012124126049, -157.8572342078865347 ) ) ;
#203010=ORIENTED_EDGE ( 'NONE', *, *, #25504, .T. ) ;
#203043=EDGE_CURVE ( 'NONE', #200038, #49697, #133047, .T. ) ;
#203105=CYLINDRICAL_SURFACE ( 'NONE', #213356, 0.1000000000000033362 ) ;
#203109=CIRCLE ( 'NONE', #228071, 0.1000000000000028644 ) ;
#203123=CARTESIAN_POINT ( 'NONE',  ( 22.57320508075688537, 64.25000000001236344, -170.0231074845244450 ) ) ;
#203137=AXIS2_PLACEMENT_3D ( 'NONE', #149070, #147775, #113765 ) ;
#203139=VECTOR ( 'NONE', #65786, 1000.000000000000000 ) ;
#203141=CARTESIAN_POINT ( 'NONE',  ( -18.59999999999999787, 66.65000000001229807, -157.7731074845244166 ) ) ;
#203170=ORIENTED_EDGE ( 'NONE', *, *, #144185, .F. ) ;
#203178=DIRECTION ( 'NONE',  ( 0.000000000000000000, 0.000000000000000000, 1.000000000000000000 ) ) ;
#203196=CARTESIAN_POINT ( 'NONE',  ( 23.15000000000000213, 87.65000000001215597, -139.6231074845242688 ) ) ;
#203199=CARTESIAN_POINT ( 'NONE',  ( 21.02374657821587434, 64.39999999919200491, -143.4513107143263824 ) ) ;
#203204=DIRECTION ( 'NONE',  ( 0.000000000000000000, 6.982962677686267499E-15, -1.000000000000000000 ) ) ;
#203249=CYLINDRICAL_SURFACE ( 'NONE', #175009, 0.09999999999999939493 ) ;
#203274=CARTESIAN_POINT ( 'NONE',  ( -23.25000000000000000, 76.10000000001245724, -181.6726782920691505 ) ) ;
#203295=CARTESIAN_POINT ( 'NONE',  ( 19.75857864376268935, 64.35000000001220144, -145.2731074845244450 ) ) ;
#203303=ORIENTED_EDGE ( 'NONE', *, *, #131801, .F. ) ;
#203309=CARTESIAN_POINT ( 'NONE',  ( -23.25000000000000000, 68.97833521811203639, -132.6895420826271277 ) ) ;
#203324=VERTEX_POINT ( 'NONE', #185272 ) ;
#203326=FACE_OUTER_BOUND ( 'NONE', #8425, .T. ) ;
#203358=ADVANCED_FACE ( 'NONE', ( #829 ), #220701, .T. ) ;
#203365=EDGE_LOOP ( 'NONE', ( #44467, #209716, #200955 ) ) ;
#203398=CARTESIAN_POINT ( 'NONE',  ( -18.59999999999999787, 77.83534155023670564, -158.4679561919613491 ) ) ;
#203404=ORIENTED_EDGE ( 'NONE', *, *, #223728, .T. ) ;
#203407=VERTEX_POINT ( 'NONE', #179522 ) ;
#203417=ORIENTED_EDGE ( 'NONE', *, *, #104843, .F. ) ;
#203428=CARTESIAN_POINT ( 'NONE',  ( -23.25000000000000000, 64.35000000001218723, -143.5379132551784096 ) ) ;
#203528=ORIENTED_EDGE ( 'NONE', *, *, #142557, .T. ) ;
#203566=DIRECTION ( 'NONE',  ( 0.000000000000000000, -8.232585987686539041E-15, 1.000000000000000000 ) ) ;
#203590=CARTESIAN_POINT ( 'NONE',  ( -20.94999999999999929, 87.29603075034744109, -139.5710066441881452 ) ) ;
#203595=EDGE_CURVE ( 'NONE', #39887, #95398, #151953, .T. ) ;
#203626=CARTESIAN_POINT ( 'NONE',  ( 18.49999999999999289, 64.25000000001232081, -161.9231074845244223 ) ) ;
#203632=ADVANCED_FACE ( 'NONE', ( #188480 ), #210614, .F. ) ;
#203641=CYLINDRICAL_SURFACE ( 'NONE', #100912, 0.09999999999999939493 ) ;
#203683=AXIS2_PLACEMENT_3D ( 'NONE', #20609, #100092, #135385 ) ;
#203751=VERTEX_POINT ( 'NONE', #240450 ) ;
#203754=CARTESIAN_POINT ( 'NONE',  ( -21.05000000000000071, 76.00000000001237765, -170.0231074845243597 ) ) ;
#203765=AXIS2_PLACEMENT_3D ( 'NONE', #30364, #48617, #52456 ) ;
#203766=ORIENTED_EDGE ( 'NONE', *, *, #58259, .T. ) ;
#203815=CYLINDRICAL_SURFACE ( 'NONE', #105375, 0.09999999999998898659 ) ;
#203846=CIRCLE ( 'NONE', #12347, 0.09999999999999459321 ) ;
#203857=AXIS2_PLACEMENT_3D ( 'NONE', #169920, #212861, #32977 ) ;
#203871=CARTESIAN_POINT ( 'NONE',  ( 18.59999999999999787, 86.35479209693758662, -142.7665665014505407 ) ) ;
#203877=LINE ( 'NONE', #25267, #201158 ) ;
#203887=DIRECTION ( 'NONE',  ( 0.000000000000000000, 0.000000000000000000, -1.000000000000000000 ) ) ;
#203890=DIRECTION ( 'NONE',  ( 1.000000000000000000, 0.000000000000000000, 0.000000000000000000 ) ) ;
#203892=ORIENTED_EDGE ( 'NONE', *, *, #138143, .F. ) ;
#203902=CARTESIAN_POINT ( 'NONE',  ( -22.47071067811865319, 68.27992525551432834, -170.1221999392270163 ) ) ;
#203907=ORIENTED_EDGE ( 'NONE', *, *, #93518, .F. ) ;
#203937=PLANE ( 'NONE',  #11536 ) ;
#203966=DIRECTION ( 'NONE',  ( 1.000000000000000000, -3.265361837132813093E-16, -2.280189983783949500E-30 ) ) ;
#203981=TOROIDAL_SURFACE ( 'NONE', #78875, 11.70000000000000639, 0.1000000000000000056 ) ;
#203984=CARTESIAN_POINT ( 'NONE',  ( 21.05000000000000071, 69.52293297888763846, -169.9231074845244507 ) ) ;
#203999=AXIS2_PLACEMENT_3D ( 'NONE', #180162, #81024, #160615 ) ;
#204032=CIRCLE ( 'NONE', #62400, 0.2000000000000057288 ) ;
#204042=ADVANCED_FACE ( 'NONE', ( #236286 ), #235017, .T. ) ;
#204085=VERTEX_POINT ( 'NONE', #177635 ) ;
#204104=CARTESIAN_POINT ( 'NONE',  ( 20.94999999999999929, 85.40000000001221281, -146.4170766071767389 ) ) ;
#204115=EDGE_CURVE ( 'NONE', #228568, #209999, #175085, .T. ) ;
#204118=CARTESIAN_POINT ( 'NONE',  ( -20.94999999999999929, 64.36312671090811932, -143.3448666978491133 ) ) ;
#204124=DIRECTION ( 'NONE',  ( -0.000000000000000000, 0.8700118002898356018, -0.4930308989875170078 ) ) ;
#204147=DIRECTION ( 'NONE',  ( 1.000000000000000000, 0.000000000000000000, 0.000000000000000000 ) ) ;
#204150=CIRCLE ( 'NONE', #233426, 4.049999999999998046 ) ;
#204174=EDGE_CURVE ( 'NONE', #14224, #109498, #211952, .T. ) ;
#204192=ORIENTED_EDGE ( 'NONE', *, *, #9600, .F. ) ;
#204195=CARTESIAN_POINT ( 'NONE',  ( 21.14999999999999503, 76.00000000001237765, -170.0231074845243597 ) ) ;
#204230=FACE_OUTER_BOUND ( 'NONE', #111628, .T. ) ;
#204231=CARTESIAN_POINT ( 'NONE',  ( 18.49999999999999645, 76.00000000001237765, -170.0231074845243597 ) ) ;
#204235=ORIENTED_EDGE ( 'NONE', *, *, #171261, .T. ) ;
#204243=ORIENTED_EDGE ( 'NONE', *, *, #12990, .F. ) ;
#204247=LINE ( 'NONE', #25626, #247321 ) ;
#204251=DIRECTION ( 'NONE',  ( 0.000000000000000000, 0.000000000000000000, 1.000000000000000000 ) ) ;
#204304=VECTOR ( 'NONE', #15037, 1000.000000000000114 ) ;
#204348=DIRECTION ( 'NONE',  ( 3.616040088954490704E-32, 7.105427357601001859E-15, -1.000000000000000000 ) ) ;
#204349=CARTESIAN_POINT ( 'NONE',  ( 21.05000000000000071, 67.17357026049512569, -161.6090527715807070 ) ) ;
#204392=ORIENTED_EDGE ( 'NONE', *, *, #157563, .T. ) ;
#204401=ADVANCED_FACE ( 'NONE', ( #28854 ), #91356, .F. ) ;
#204408=ADVANCED_FACE ( 'NONE', ( #131750 ), #108348, .T. ) ;
#204444=EDGE_CURVE ( 'NONE', #7639, #23846, #177336, .T. ) ;
#204452=DIRECTION ( 'NONE',  ( 1.000000000000000000, 0.000000000000000000, 0.000000000000000000 ) ) ;
#204454=CARTESIAN_POINT ( 'NONE',  ( 22.42357213249528769, 68.32706761365247417, -170.1221944485259314 ) ) ;
#204461=EDGE_LOOP ( 'NONE', ( #257577, #36966, #256253, #67074 ) ) ;
#204471=FACE_OUTER_BOUND ( 'NONE', #52400, .T. ) ;
#204494=ORIENTED_EDGE ( 'NONE', *, *, #31110, .F. ) ;
#204504=LINE ( 'NONE', #224065, #168514 ) ;
#204580=DIRECTION ( 'NONE',  ( 0.000000000000000000, 0.000000000000000000, 1.000000000000000000 ) ) ;
#204588=ORIENTED_EDGE ( 'NONE', *, *, #113924, .F. ) ;
#204589=ADVANCED_FACE ( 'NONE', ( #101576 ), #139434, .T. ) ;
#204609=ORIENTED_EDGE ( 'NONE', *, *, #80074, .T. ) ;
#204637=AXIS2_PLACEMENT_3D ( 'NONE', #228789, #127101, #107531 ) ;
#204647=ORIENTED_EDGE ( 'NONE', *, *, #11389, .F. ) ;
#204657=DIRECTION ( 'NONE',  ( -1.000000000000000000, 0.000000000000000000, -0.000000000000000000 ) ) ;
#204711=AXIS2_PLACEMENT_3D ( 'NONE', #167194, #245423, #107174 ) ;
#204742=DIRECTION ( 'NONE',  ( 0.000000000000000000, 0.000000000000000000, -1.000000000000000000 ) ) ;
#204781=CARTESIAN_POINT ( 'NONE',  ( 18.49999999999998934, 65.75000000001222134, -145.3731074845244109 ) ) ;
#204800=ADVANCED_FACE ( 'NONE', ( #209704 ), #88437, .T. ) ;
#204809=EDGE_CURVE ( 'NONE', #127058, #33291, #87168, .T. ) ;
#204822=CARTESIAN_POINT ( 'NONE',  ( -20.85000000000000142, 76.00000000001213607, -136.5231074845243313 ) ) ;
#204826=CARTESIAN_POINT ( 'NONE',  ( -23.25000000000000000, 76.00000000001240608, -174.0731074845243711 ) ) ;
#204864=DIRECTION ( 'NONE',  ( -1.000000000000000000, -0.000000000000000000, -0.000000000000000000 ) ) ;
#204878=VECTOR ( 'NONE', #196188, 1000.000000000000000 ) ;
#204905=VERTEX_POINT ( 'NONE', #76599 ) ;
#204914=AXIS2_PLACEMENT_3D ( 'NONE', #72496, #152039, #44917 ) ;
#204940=DIRECTION ( 'NONE',  ( 1.000000000000000000, 0.000000000000000000, 0.000000000000000000 ) ) ;
#204941=DIRECTION ( 'NONE',  ( 0.000000000000000000, -1.000000000000000000, -6.982962677686265922E-15 ) ) ;
#204963=DIRECTION ( 'NONE',  ( 0.000000000000000000, 1.000000000000000000, 6.938893903907222067E-15 ) ) ;
#204969=DIRECTION ( 'NONE',  ( 0.000000000000000000, 1.000000000000000000, 1.321694076934707365E-14 ) ) ;
#204977=CARTESIAN_POINT ( 'NONE',  ( 23.15000000000000213, 87.48912529308822172, -139.6231074845242688 ) ) ;
#204978=CARTESIAN_POINT ( 'NONE',  ( 21.09787244211742419, 67.22462929267497600, -157.7838541002068666 ) ) ;
#204982=DIRECTION ( 'NONE',  ( -1.000000000000000000, 0.000000000000000000, -0.000000000000000000 ) ) ;
#204990=DIRECTION ( 'NONE',  ( 0.000000000000000000, -0.1568667991644355497, -0.9876197685951332295 ) ) ;
#204991=EDGE_CURVE ( 'NONE', #166025, #141665, #149974, .T. ) ;
#205023=CARTESIAN_POINT ( 'NONE',  ( -20.94999999999999929, 87.39257802171802325, -166.9491579046923277 ) ) ;
#205034=EDGE_CURVE ( 'NONE', #250601, #135741, #201683, .T. ) ;
#205057=ORIENTED_EDGE ( 'NONE', *, *, #99455, .F. ) ;
#205078=DIRECTION ( 'NONE',  ( -1.000000000000000000, 0.000000000000000000, -0.000000000000000000 ) ) ;
#205079=DIRECTION ( 'NONE',  ( -1.836970198721029934E-16, -1.000000000000000000, -6.982962677686266711E-15 ) ) ;
#205101=FACE_OUTER_BOUND ( 'NONE', #87476, .T. ) ;
#205123=CARTESIAN_POINT ( 'NONE',  ( -20.85000000000000142, 77.16412189325330928, -128.7082593989527197 ) ) ;
#205154=ORIENTED_EDGE ( 'NONE', *, *, #151131, .F. ) ;
#205156=CARTESIAN_POINT ( 'NONE',  ( 18.49999999999999289, 69.15387683765952431, -132.7853812176745407 ) ) ;
#205169=ORIENTED_EDGE ( 'NONE', *, *, #96406, .F. ) ;
#205188=DIRECTION ( 'NONE',  ( 1.000000000000000000, 0.000000000000000000, 0.000000000000000000 ) ) ;
#205190=ORIENTED_EDGE ( 'NONE', *, *, #65539, .T. ) ;
#205220=CARTESIAN_POINT ( 'NONE',  ( -23.15000000000000213, 76.00000000001215028, -138.6231074845243256 ) ) ;
#205224=AXIS2_PLACEMENT_3D ( 'NONE', #126108, #32188, #169142 ) ;
#205244=AXIS2_PLACEMENT_3D ( 'NONE', #218285, #14996, #138730 ) ;
#205246=ORIENTED_EDGE ( 'NONE', *, *, #160644, .T. ) ;
#205266=EDGE_CURVE ( 'NONE', #12740, #177752, #108442, .T. ) ;
#205284=DIRECTION ( 'NONE',  ( 0.000000000000000000, -0.8660254037844445918, -0.4999999999999897304 ) ) ;
#205301=ADVANCED_FACE ( 'NONE', ( #249783 ), #83459, .T. ) ;
#205303=CARTESIAN_POINT ( 'NONE',  ( 21.05000000000000071, 76.00000000001229239, -157.8731074845243540 ) ) ;
#205324=VERTEX_POINT ( 'NONE', #189816 ) ;
#205332=CARTESIAN_POINT ( 'NONE',  ( -23.15000000000000213, 76.00000000001237765, -170.0231074845243597 ) ) ;
#205344=AXIS2_PLACEMENT_3D ( 'NONE', #44907, #203966, #222225 ) ;
#205360=DIRECTION ( 'NONE',  ( -4.801466763864314121E-15, 0.2605042016806606298, 0.9654727137038736640 ) ) ;
#205394=CARTESIAN_POINT ( 'NONE',  ( -21.05000000000000071, 64.25000000001220712, -143.5379132551784096 ) ) ;
#205401=CARTESIAN_POINT ( 'NONE',  ( 20.88420186297724612, 65.66974365629688748, -130.9360145562605169 ) ) ;
#205412=DIRECTION ( 'NONE',  ( -0.000000000000000000, 1.000000000000000000, 6.982962677686266711E-15 ) ) ;
#205436=ORIENTED_EDGE ( 'NONE', *, *, #85638, .T. ) ;
#205456=AXIS2_PLACEMENT_3D ( 'NONE', #158594, #135131, #99841 ) ;
#205493=CARTESIAN_POINT ( 'NONE',  ( -18.59999999999999787, 77.25000000001232081, -162.0231074845243313 ) ) ;
#205497=CYLINDRICAL_SURFACE ( 'NONE', #20803, 0.1000000000000028644 ) ;
#205508=DIRECTION ( 'NONE',  ( 0.000000000000000000, -1.000000000000000000, -6.982962677686266711E-15 ) ) ;
#205525=CIRCLE ( 'NONE', #1332, 0.5000000000000004441 ) ;
#205596=ADVANCED_FACE ( 'NONE', ( #223477 ), #175290, .F. ) ;
#205598=CARTESIAN_POINT ( 'NONE',  ( 23.14999999999999858, 71.22429906543287359, -158.1743393804784148 ) ) ;
#205619=CIRCLE ( 'NONE', #218093, 0.09999999999998898659 ) ;
#205649=ADVANCED_FACE ( 'NONE', ( #169991 ), #154446, .T. ) ;
#205658=ORIENTED_EDGE ( 'NONE', *, *, #91118, .T. ) ;
#205714=ORIENTED_EDGE ( 'NONE', *, *, #197103, .F. ) ;
#205757=DIRECTION ( 'NONE',  ( 0.000000000000000000, 0.8068669527897506244, 0.5907332058516622242 ) ) ;
#205761=VERTEX_POINT ( 'NONE', #238910 ) ;
#205776=ORIENTED_EDGE ( 'NONE', *, *, #69585, .T. ) ;
#205784=DIRECTION ( 'NONE',  ( -4.408576920032447972E-17, -0.1350103645451946055, 0.9908441862701591329 ) ) ;
#205790=VECTOR ( 'NONE', #127294, 1000.000000000000000 ) ;
#205801=TOROIDAL_SURFACE ( 'NONE', #135042, 0.6000000000000015321, 0.1000000000000000056 ) ;
#205813=CARTESIAN_POINT ( 'NONE',  ( 21.05000000000000071, 87.75000000001234923, -167.1231074845242688 ) ) ;
#205845=CARTESIAN_POINT ( 'NONE',  ( 22.49806830649814060, 75.92253568368695937, -181.6729971393634457 ) ) ;
#205852=CYLINDRICAL_SURFACE ( 'NONE', #74563, 11.74999999999999645 ) ;
#205886=DIRECTION ( 'NONE',  ( 0.000000000000000000, 0.000000000000000000, -1.000000000000000000 ) ) ;
#205932=DIRECTION ( 'NONE',  ( 1.000000000000000000, 0.000000000000000000, 0.000000000000000000 ) ) ;
#205959=AXIS2_PLACEMENT_3D ( 'NONE', #93055, #151778, #235144 ) ;
#205964=FACE_OUTER_BOUND ( 'NONE', #149937, .T. ) ;
#206007=EDGE_CURVE ( 'NONE', #205761, #34506, #13605, .T. ) ;
#206013=EDGE_CURVE ( 'NONE', #242376, #168873, #42821, .T. ) ;
#206039=EDGE_CURVE ( 'NONE', #52417, #54460, #227035, .T. ) ;
#206054=CARTESIAN_POINT ( 'NONE',  ( -18.59999999999999787, 77.86671491006960366, -158.2704322382423356 ) ) ;
#206075=STYLED_ITEM ( 'NONE', ( #116311 ), #154111 ) ;
#206119=MECHANICAL_DESIGN_GEOMETRIC_PRESENTATION_REPRESENTATION('',(#181189),#139458);
#206120=DIRECTION ( 'NONE',  ( 0.000000000000000000, 0.000000000000000000, 1.000000000000000000 ) ) ;
#206177=EDGE_LOOP ( 'NONE', ( #73295, #18119, #198738, #138715 ) ) ;
#206182=DIRECTION ( 'NONE',  ( 0.000000000000000000, -1.000000000000000000, -8.717686153663073805E-15 ) ) ;
#206213=ORIENTED_EDGE ( 'NONE', *, *, #211222, .F. ) ;
#206222=EDGE_CURVE ( 'NONE', #242166, #159849, #254651, .T. ) ;
#206224=DIRECTION ( 'NONE',  ( 0.000000000000000000, 0.000000000000000000, 1.000000000000000000 ) ) ;
#206239=VERTEX_POINT ( 'NONE', #216456 ) ;
#206240=AXIS2_PLACEMENT_3D ( 'NONE', #246252, #224104, #221521 ) ;
#206289=CIRCLE ( 'NONE', #202010, 4.099999999999992539 ) ;
#206296=DIRECTION ( 'NONE',  ( -0.000000000000000000, -0.8660254037844420383, 0.4999999999999943379 ) ) ;
#206306=DIRECTION ( 'NONE',  ( 0.000000000000000000, 0.000000000000000000, 1.000000000000000000 ) ) ;
#206325=VERTEX_POINT ( 'NONE', #84608 ) ;
#206367=DIRECTION ( 'NONE',  ( 0.000000000000000000, 0.000000000000000000, 1.000000000000000000 ) ) ;
#206379=FACE_OUTER_BOUND ( 'NONE', #213166, .T. ) ;
#206386=DIRECTION ( 'NONE',  ( 0.000000000000000000, 0.000000000000000000, 1.000000000000000000 ) ) ;
#206390=DIRECTION ( 'NONE',  ( 0.000000000000000000, 1.000000000000000000, 6.982962677686266711E-15 ) ) ;
#206408=CIRCLE ( 'NONE', #235624, 3.899999999999987033 ) ;
#206410=CIRCLE ( 'NONE', #180904, 0.1000000000000033362 ) ;
#206428=TOROIDAL_SURFACE ( 'NONE', #56549, 11.90000000000000213, 0.1000000000000000056 ) ;
#206429=CARTESIAN_POINT ( 'NONE',  ( -20.85000000000000142, 77.16412189325330928, -128.6082593989527254 ) ) ;
#206438=VERTEX_POINT ( 'NONE', #126346 ) ;
#206477=CARTESIAN_POINT ( 'NONE',  ( 22.59999999999999787, 64.35042919246758686, -170.1231074845244393 ) ) ;
#206490=CARTESIAN_POINT ( 'NONE',  ( 21.05000000000000071, 74.83729825007431202, -162.1231074845243540 ) ) ;
#206525=DIRECTION ( 'NONE',  ( 0.000000000000000000, -1.000000000000000000, -6.860497997771532351E-15 ) ) ;
#206562=CARTESIAN_POINT ( 'NONE',  ( 21.05000000000000426, 69.74118280533089376, -170.0567402198580567 ) ) ;
#206567=EDGE_CURVE ( 'NONE', #14224, #235594, #52989, .T. ) ;
#206600=CARTESIAN_POINT ( 'NONE',  ( 20.94999999999999929, 77.83585931145570669, -125.0186683157258045 ) ) ;
#206607=ORIENTED_EDGE ( 'NONE', *, *, #110891, .T. ) ;
#206612=EDGE_CURVE ( 'NONE', #156062, #115699, #188243, .T. ) ;
#206631=ORIENTED_EDGE ( 'NONE', *, *, #195629, .F. ) ;
#206639=FACE_OUTER_BOUND ( 'NONE', #24750, .T. ) ;
#206662=EDGE_LOOP ( 'NONE', ( #70454, #121714, #208925, #35075 ) ) ;
#206663=VERTEX_POINT ( 'NONE', #68324 ) ;
#206665=ORIENTED_EDGE ( 'NONE', *, *, #210333, .F. ) ;
#206669=CIRCLE ( 'NONE', #11037, 0.09999999999998898659 ) ;
#206704=ORIENTED_EDGE ( 'NONE', *, *, #224177, .T. ) ;
#206734=CIRCLE ( 'NONE', #219198, 0.1000000000000033362 ) ;
#206737=VERTEX_POINT ( 'NONE', #231266 ) ;
#206738=ORIENTED_EDGE ( 'NONE', *, *, #200506, .F. ) ;
#206765=DIRECTION ( 'NONE',  ( 1.000000000000000000, 0.000000000000000000, 0.000000000000000000 ) ) ;
#206774=CARTESIAN_POINT ( 'NONE',  ( -20.64999999999999858, 85.00000000001232081, -160.1291383618718385 ) ) ;
#206818=EDGE_CURVE ( 'NONE', #106358, #91629, #154325, .T. ) ;
#206860=DIRECTION ( 'NONE',  ( 0.000000000000000000, -6.608470384673580212E-15, 1.000000000000000000 ) ) ;
#206889=CARTESIAN_POINT ( 'NONE',  ( -23.15000000000000213, 76.00000000001229239, -157.2481074845243540 ) ) ;
#206907=EDGE_CURVE ( 'NONE', #102268, #132210, #192333, .T. ) ;
#206923=CARTESIAN_POINT ( 'NONE',  ( 23.14999999999999503, 69.45000000001229523, -157.6731074845243938 ) ) ;
#206936=VERTEX_POINT ( 'NONE', #244071 ) ;
#206946=EDGE_CURVE ( 'NONE', #25682, #206663, #55116, .T. ) ;
#206974=ORIENTED_EDGE ( 'NONE', *, *, #135049, .T. ) ;
#206982=CIRCLE ( 'NONE', #223530, 0.09999999999999939493 ) ;
#207016=AXIS2_PLACEMENT_3D ( 'NONE', #63902, #24810, #143432 ) ;
#207042=CARTESIAN_POINT ( 'NONE',  ( 21.95218792049437795, 68.79849243876572018, -170.1221359243243114 ) ) ;
#207054=AXIS2_PLACEMENT_3D ( 'NONE', #249976, #192571, #154747 ) ;
#207085=ORIENTED_EDGE ( 'NONE', *, *, #25541, .T. ) ;
#207107=CARTESIAN_POINT ( 'NONE',  ( -23.15000000000000213, 64.25000000001246292, -181.7731074845244450 ) ) ;
#207113=ORIENTED_EDGE ( 'NONE', *, *, #200050, .F. ) ;
#207140=CARTESIAN_POINT ( 'NONE',  ( 22.41477678272288188, 75.99917613424950957, -181.6726927690397417 ) ) ;
#207200=DIRECTION ( 'NONE',  ( -2.952720810173289112E-16, -1.000000000000000000, -6.982962677686266711E-15 ) ) ;
#207207=AXIS2_PLACEMENT_3D ( 'NONE', #36433, #76806, #59786 ) ;
#207212=VECTOR ( 'NONE', #102682, 1000.000000000000000 ) ;
#207248=VERTEX_POINT ( 'NONE', #178702 ) ;
#207260=CIRCLE ( 'NONE', #15738, 0.09999999999998708533 ) ;
#207271=ORIENTED_EDGE ( 'NONE', *, *, #150347, .T. ) ;
#207277=DIRECTION ( 'NONE',  ( -0.000000000000000000, 0.8660254037844424824, 0.4999999999999934497 ) ) ;
#207287=VERTEX_POINT ( 'NONE', #26022 ) ;
#207293=DIRECTION ( 'NONE',  ( -0.8660254037844653530, 0.000000000000000000, -0.4999999999999539257 ) ) ;
#207295=DIRECTION ( 'NONE',  ( 0.000000000000000000, 0.9893560106964510714, -0.1455152366551481502 ) ) ;
#207380=DIRECTION ( 'NONE',  ( 0.000000000000000000, 0.000000000000000000, 1.000000000000000000 ) ) ;
#207403=DIRECTION ( 'NONE',  ( 0.000000000000000000, 0.000000000000000000, 1.000000000000000000 ) ) ;
#207407=DIRECTION ( 'NONE',  ( 0.000000000000000000, 6.982962677686267499E-15, -1.000000000000000000 ) ) ;
#207430=DIRECTION ( 'NONE',  ( -4.408576920032447355E-17, -0.1350103645451945777, 0.9908441862701589109 ) ) ;
#207435=DIRECTION ( 'NONE',  ( 1.000000000000000000, 0.000000000000000000, -0.000000000000000000 ) ) ;
#207542=CARTESIAN_POINT ( 'NONE',  ( 18.59999999999999076, 69.35000000001222986, -148.8731074845244109 ) ) ;
#207565=ADVANCED_FACE ( 'NONE', ( #74157 ), #238318, .F. ) ;
#207569=CARTESIAN_POINT ( 'NONE',  ( -20.54999999999999716, 74.07476635515241981, -149.2533510176504876 ) ) ;
#207581=CARTESIAN_POINT ( 'NONE',  ( -18.59999999999999787, 66.85000000001245724, -181.7731074845244166 ) ) ;
#207628=EDGE_LOOP ( 'NONE', ( #169038, #229147, #89661, #40459 ) ) ;
#207636=ORIENTED_EDGE ( 'NONE', *, *, #10949, .T. ) ;
#207669=AXIS2_PLACEMENT_3D ( 'NONE', #132086, #14734, #227329 ) ;
#207682=CARTESIAN_POINT ( 'NONE',  ( 20.85000000000000142, 77.85161776048096272, -124.9199177649206689 ) ) ;
#207720=EDGE_CURVE ( 'NONE', #35577, #6603, #240902, .T. ) ;
#207729=B_SPLINE_CURVE_WITH_KNOTS ( 'NONE', 3,
 ( #186015, #245996, #85589, #227694, #183457, #88163, #4779, #203003, #165168, #24397 ),
 .UNSPECIFIED., .F., .F.,
 ( 4, 2, 2, 2, 4 ),
 ( 0.000000000000000000, 0.0001660831991682657036, 0.0002491247987523985690, 0.0002906455985444294263, 0.0003321663983364602293 ),
 .UNSPECIFIED. ) ;
#207789=ADVANCED_FACE ( 'NONE', ( #230308 ), #248595, .T. ) ;
#207802=AXIS2_PLACEMENT_3D ( 'NONE', #223832, #203000, #915 ) ;
#207811=CIRCLE ( 'NONE', #24657, 7.800000000000001599 ) ;
#207883=CARTESIAN_POINT ( 'NONE',  ( -21.14999999999999858, 87.75000000001236344, -167.1231074845242688 ) ) ;
#207895=ORIENTED_EDGE ( 'NONE', *, *, #230927, .T. ) ;
#207906=TOROIDAL_SURFACE ( 'NONE', #249588, 0.4000000000000009104, 0.1000000000000000056 ) ;
#207909=VECTOR ( 'NONE', #215674, 1000.000000000000000 ) ;
#207921=DIRECTION ( 'NONE',  ( -0.000000000000000000, 1.000000000000000000, 6.982962677686266711E-15 ) ) ;
#207956=CARTESIAN_POINT ( 'NONE',  ( 21.05000000000000071, 70.50000000001223555, -148.9283735034374843 ) ) ;
#207957=DIRECTION ( 'NONE',  ( 1.000000000000000000, 0.000000000000000000, 0.000000000000000000 ) ) ;
#207966=ORIENTED_EDGE ( 'NONE', *, *, #132365, .T. ) ;
#207974=AXIS2_PLACEMENT_3D ( 'NONE', #152431, #31214, #50699 ) ;
#207997=CYLINDRICAL_SURFACE ( 'NONE', #156994, 0.1000000000000028644 ) ;
#208007=CARTESIAN_POINT ( 'NONE',  ( 20.95520789717937404, 65.42306940062736942, -162.4428745106495739 ) ) ;
#208041=ORIENTED_EDGE ( 'NONE', *, *, #82060, .F. ) ;
#208056=DIRECTION ( 'NONE',  ( 0.000000000000000000, 0.1298341882519953583, 0.9915357197604862671 ) ) ;
#208095=CARTESIAN_POINT ( 'NONE',  ( 23.25000000000000000, 87.65000000001245439, -181.7731074845242745 ) ) ;
#208101=TOROIDAL_SURFACE ( 'NONE', #66437, 3.899999999999999467, 0.1000000000000000056 ) ;
#208103=ORIENTED_EDGE ( 'NONE', *, *, #161270, .T. ) ;
#208118=TOROIDAL_SURFACE ( 'NONE', #241427, 11.65000000000000036, 0.1000000000000000056 ) ;
#208146=EDGE_CURVE ( 'NONE', #168221, #84927, #90158, .T. ) ;
#208151=SURFACE_SIDE_STYLE ('',( #249829 ) ) ;
#208166=VERTEX_POINT ( 'NONE', #113597 ) ;
#208206=CARTESIAN_POINT ( 'NONE',  ( 23.14999999999999858, 76.00000000001213607, -136.5231074845243313 ) ) ;
#208221=AXIS2_PLACEMENT_3D ( 'NONE', #6353, #31104, #28549 ) ;
#208251=DIRECTION ( 'NONE',  ( 0.000000000000000000, -1.000000000000000000, -6.860497997771531562E-15 ) ) ;
#208274=CARTESIAN_POINT ( 'NONE',  ( 18.54116936837189655, 85.46356419838478757, -162.9745649936360223 ) ) ;
#208283=VECTOR ( 'NONE', #151662, 1000.000000000000000 ) ;
#208321=DIRECTION ( 'NONE',  ( 1.000000000000000000, -0.000000000000000000, 0.000000000000000000 ) ) ;
#208360=DIRECTION ( 'NONE',  ( 0.000000000000000000, -0.1350103645451945777, 0.9908441862701590219 ) ) ;
#208369=ADVANCED_FACE ( 'NONE', ( #31087 ), #231829, .F. ) ;
#208390=DIRECTION ( 'NONE',  ( 1.000000000000000000, -2.952720810173289112E-16, -2.061873921506763405E-30 ) ) ;
#208437=EDGE_CURVE ( 'NONE', #112448, #123398, #41340, .T. ) ;
#208462=DIRECTION ( 'NONE',  ( 1.000000000000000000, 0.000000000000000000, 0.000000000000000000 ) ) ;
#208470=FACE_OUTER_BOUND ( 'NONE', #141951, .T. ) ;
#208490=DIRECTION ( 'NONE',  ( 0.000000000000000000, 6.982962677686266711E-15, -1.000000000000000000 ) ) ;
#208517=ORIENTED_EDGE ( 'NONE', *, *, #251587, .T. ) ;
#208525=AXIS2_PLACEMENT_3D ( 'NONE', #105579, #126458, #224269 ) ;
#208541=PLANE ( 'NONE',  #207974 ) ;
#208546=DIRECTION ( 'NONE',  ( 1.000000000000000000, 0.000000000000000000, 0.000000000000000000 ) ) ;
#208556=CARTESIAN_POINT ( 'NONE',  ( 20.94999999999999574, 67.07338541492521244, -161.5514244653012952 ) ) ;
#208629=CARTESIAN_POINT ( 'NONE',  ( -18.59999999999999787, 66.75000000001230660, -157.7731074845244166 ) ) ;
#208645=DIRECTION ( 'NONE',  ( 0.000000000000000000, 0.000000000000000000, 1.000000000000000000 ) ) ;
#208648=ORIENTED_EDGE ( 'NONE', *, *, #170007, .T. ) ;
#208654=EDGE_CURVE ( 'NONE', #94515, #69727, #130879, .T. ) ;
#208658=VERTEX_POINT ( 'NONE', #82967 ) ;
#208679=EDGE_LOOP ( 'NONE', ( #83914, #128807, #202445, #168525 ) ) ;
#208684=CIRCLE ( 'NONE', #13056, 0.09999999999998898659 ) ;
#208698=CARTESIAN_POINT ( 'NONE',  ( -18.50000000000000000, 64.35000000001214460, -136.5231074845244166 ) ) ;
#208705=ORIENTED_EDGE ( 'NONE', *, *, #75017, .T. ) ;
#208709=CARTESIAN_POINT ( 'NONE',  ( -23.15000000000000213, 74.00000000001229239, -156.7984855617622770 ) ) ;
#208738=AXIS2_PLACEMENT_3D ( 'NONE', #108125, #187679, #188946 ) ;
#208752=CIRCLE ( 'NONE', #426, 11.74999999999999645 ) ;
#208786=VERTEX_POINT ( 'NONE', #254157 ) ;
#208839=ORIENTED_EDGE ( 'NONE', *, *, #87723, .F. ) ;
#208851=EDGE_LOOP ( 'NONE', ( #234492, #240243, #213423, #149801 ) ) ;
#208854=EDGE_CURVE ( 'NONE', #97109, #56847, #26861, .T. ) ;
#208857=DIRECTION ( 'NONE',  ( 0.000000000000000000, -1.000000000000000000, -6.982962677686265922E-15 ) ) ;
#208866=EDGE_CURVE ( 'NONE', #132867, #228310, #130837, .T. ) ;
#208881=CARTESIAN_POINT ( 'NONE',  ( 23.14999999999999858, 76.00000000001229239, -157.1481074845243882 ) ) ;
#208925=ORIENTED_EDGE ( 'NONE', *, *, #91019, .F. ) ;
#208937=EDGE_CURVE ( 'NONE', #250411, #168984, #193447, .T. ) ;
#208940=EDGE_CURVE ( 'NONE', #44364, #160821, #241837, .T. ) ;
#208944=ORIENTED_EDGE ( 'NONE', *, *, #92457, .T. ) ;
#208957=ORIENTED_EDGE ( 'NONE', *, *, #16643, .T. ) ;
#209024=ADVANCED_FACE ( 'NONE', ( #96057 ), #85245, .T. ) ;
#209030=EDGE_LOOP ( 'NONE', ( #54158, #25693, #77611, #246072 ) ) ;
#209048=DIRECTION ( 'NONE',  ( -1.000000000000000000, 0.000000000000000000, -0.000000000000000000 ) ) ;
#209068=CARTESIAN_POINT ( 'NONE',  ( 21.00023020733438273, 69.60913075474465472, -170.0231074845244166 ) ) ;
#209078=DIRECTION ( 'NONE',  ( 1.000000000000000000, 0.000000000000000000, 0.000000000000000000 ) ) ;
#209085=ORIENTED_EDGE ( 'NONE', *, *, #31454, .F. ) ;
#209098=CARTESIAN_POINT ( 'NONE',  ( -21.64999999999999858, 68.65000000001222702, -148.8731074845244109 ) ) ;
#209111=DIRECTION ( 'NONE',  ( -1.000000000000000000, 0.000000000000000000, -0.000000000000000000 ) ) ;
#209114=VERTEX_POINT ( 'NONE', #75256 ) ;
#209155=CIRCLE ( 'NONE', #63406, 0.1000000000000141609 ) ;
#209156=FACE_OUTER_BOUND ( 'NONE', #257178, .T. ) ;
#209173=VECTOR ( 'NONE', #228643, 1000.000000000000000 ) ;
#209214=VERTEX_POINT ( 'NONE', #81603 ) ;
#209289=VECTOR ( 'NONE', #141915, 1000.000000000000000 ) ;
#209327=( BOUNDED_SURFACE ( )  B_SPLINE_SURFACE ( 3, 2, ( 
 ( #141269, #64301, #21350 ),
 ( #20054, #181689, #100810 ),
 ( #143820, #42182, #138662 ),
 ( #223360, #59126, #3021 ),
 ( #43454, #121727, #162138 ),
 ( #182981, #39637, #78704 ) ),
 .UNSPECIFIED., .F., .F., .F. ) 
 B_SPLINE_SURFACE_WITH_KNOTS ( ( 4, 2, 4 ),
 ( 3, 3 ),
 ( 6.719893378901192380E-05, 0.0002757154632485820170, 0.0004842319927081520695 ),
 ( 0.000000000000000000, 1.000000000000000000 ),
 .UNSPECIFIED. ) 
 GEOMETRIC_REPRESENTATION_ITEM ( )  RATIONAL_B_SPLINE_SURFACE ( (
 ( 1.000000000000000000, 0.7250110520819756932, 1.000000000000000000),
 ( 1.000000000000000000, 0.7277932058358641543, 1.000000000000000000),
 ( 1.000000000000000000, 0.7278452872618367264, 1.000000000000000000),
 ( 1.000000000000000000, 0.7221445671548437639, 1.000000000000000000),
 ( 1.000000000000000000, 0.7163662143780165081, 1.000000000000000000),
 ( 1.000000000000000000, 0.7071067811865475727, 1.000000000000000000) ) ) 
 REPRESENTATION_ITEM ( '' )  SURFACE ( )  );
#209330=CIRCLE ( 'NONE', #96871, 0.09999999999999938105 ) ;
#209341=ORIENTED_EDGE ( 'NONE', *, *, #56813, .F. ) ;
#209352=CIRCLE ( 'NONE', #88535, 0.1000000000000028644 ) ;
#209357=EDGE_LOOP ( 'NONE', ( #24933, #187689 ) ) ;
#209381=EDGE_CURVE ( 'NONE', #75529, #33291, #226336, .T. ) ;
#209417=AXIS2_PLACEMENT_3D ( 'NONE', #147842, #190844, #31771 ) ;
#209450=AXIS2_PLACEMENT_3D ( 'NONE', #164075, #19430, #243601 ) ;
#209477=AXIS2_PLACEMENT_3D ( 'NONE', #188523, #111561, #107700 ) ;
#209507=CIRCLE ( 'NONE', #97036, 11.69999999999998863 ) ;
#209511=DIRECTION ( 'NONE',  ( -1.836970198721029934E-16, -1.000000000000000000, -6.982962677686266711E-15 ) ) ;
#209516=AXIS2_PLACEMENT_3D ( 'NONE', #110408, #106539, #27059 ) ;
#209535=ORIENTED_EDGE ( 'NONE', *, *, #40528, .F. ) ;
#209551=TOROIDAL_SURFACE ( 'NONE', #47212, 11.70000000000000107, 0.1000000000000000056 ) ;
#209555=LINE ( 'NONE', #195151, #47211 ) ;
#209574=ORIENTED_EDGE ( 'NONE', *, *, #66187, .F. ) ;
#209598=EDGE_LOOP ( 'NONE', ( #231805, #117478, #123219, #244061, #26208 ) ) ;
#209652=CARTESIAN_POINT ( 'NONE',  ( 21.05000000000000071, 85.00000000001222134, -146.4170766071767389 ) ) ;
#209676=AXIS2_PLACEMENT_3D ( 'NONE', #173901, #85594, #225125 ) ;
#209691=CARTESIAN_POINT ( 'NONE',  ( 20.96937028524355284, 65.37553062838564699, -162.5316813833548508 ) ) ;
#209695=DIRECTION ( 'NONE',  ( 0.000000000000000000, 0.000000000000000000, -1.000000000000000000 ) ) ;
#209704=FACE_OUTER_BOUND ( 'NONE', #6558, .T. ) ;
#209709=CARTESIAN_POINT ( 'NONE',  ( -21.07094088545304444, 69.67983277809588571, -170.1220011870766200 ) ) ;
#209716=ORIENTED_EDGE ( 'NONE', *, *, #168329, .T. ) ;
#209774=DIRECTION ( 'NONE',  ( 0.000000000000000000, -7.026728003956695223E-15, 1.000000000000000000 ) ) ;
#209780=CARTESIAN_POINT ( 'NONE',  ( 21.14999999999999858, 76.00000000001242029, -176.5637644362255969 ) ) ;
#209793=ADVANCED_FACE ( 'NONE', ( #7923 ), #5944, .T. ) ;
#209805=ORIENTED_EDGE ( 'NONE', *, *, #253149, .T. ) ;
#209831=TOROIDAL_SURFACE ( 'NONE', #188980, 0.2000000000000000111, 0.1000000000000000056 ) ;
#209849=CARTESIAN_POINT ( 'NONE',  ( 23.25000000000000000, 85.00000000001222134, -146.4170766071767389 ) ) ;
#209963=ORIENTED_EDGE ( 'NONE', *, *, #242814, .T. ) ;
#209964=ORIENTED_EDGE ( 'NONE', *, *, #107918, .T. ) ;
#209977=AXIS2_PLACEMENT_3D ( 'NONE', #114843, #196940, #215231 ) ;
#209985=CYLINDRICAL_SURFACE ( 'NONE', #40192, 12.87499999999999822 ) ;
#209999=VERTEX_POINT ( 'NONE', #71751 ) ;
#210010=ADVANCED_FACE ( 'NONE', ( #251654, #73060 ), #232110, .T. ) ;
#210029=LINE ( 'NONE', #229586, #59444 ) ;
#210038=VERTEX_POINT ( 'NONE', #217633 ) ;
#210046=VECTOR ( 'NONE', #212418, 1000.000000000000000 ) ;
#210055=CARTESIAN_POINT ( 'NONE',  ( -21.07971444708686093, 75.91217656369460087, -176.3528995661508816 ) ) ;
#210087=AXIS2_PLACEMENT_3D ( 'NONE', #130838, #151723, #74762 ) ;
#210129=LINE ( 'NONE', #53610, #110034 ) ;
#210137=TOROIDAL_SURFACE ( 'NONE', #5905, 0.2000000000000000111, 0.1000000000000000056 ) ;
#210149=ORIENTED_EDGE ( 'NONE', *, *, #83939, .F. ) ;
#210157=TOROIDAL_SURFACE ( 'NONE', #198233, 0.2000000000000000111, 0.1000000000000000056 ) ;
#210169=EDGE_CURVE ( 'NONE', #104858, #113005, #180944, .T. ) ;
#210180=EDGE_CURVE ( 'NONE', #68928, #162856, #204504, .T. ) ;
#210193=DIRECTION ( 'NONE',  ( 0.000000000000000000, -7.056502275159890043E-15, 1.000000000000000000 ) ) ;
#210199=CIRCLE ( 'NONE', #147642, 0.6000000000000033085 ) ;
#210202=ORIENTED_EDGE ( 'NONE', *, *, #112127, .F. ) ;
#210205=CARTESIAN_POINT ( 'NONE',  ( 23.14999999999999858, 72.10000000001214460, -136.5231074845243597 ) ) ;
#210220=VERTEX_POINT ( 'NONE', #243640 ) ;
#210236=DIRECTION ( 'NONE',  ( -1.000000000000000000, -0.000000000000000000, -0.000000000000000000 ) ) ;
#210238=EDGE_LOOP ( 'NONE', ( #214545, #251221, #187478, #195797 ) ) ;
#210239=EDGE_CURVE ( 'NONE', #235746, #30238, #151752, .T. ) ;
#210242=DIRECTION ( 'NONE',  ( 0.000000000000000000, 0.000000000000000000, -1.000000000000000000 ) ) ;
#210253=FACE_OUTER_BOUND ( 'NONE', #168451, .T. ) ;
#210268=DIRECTION ( 'NONE',  ( 1.000000000000000000, 0.000000000000000000, 0.000000000000000000 ) ) ;
#210285=DIRECTION ( 'NONE',  ( 0.000000000000000000, -0.8660254037844343777, 0.5000000000000074385 ) ) ;
#210295=ADVANCED_FACE ( 'NONE', ( #128843 ), #122700, .F. ) ;
#210302=ORIENTED_EDGE ( 'NONE', *, *, #87822, .T. ) ;
#210333=EDGE_CURVE ( 'NONE', #193751, #225850, #10269, .T. ) ;
#210341=EDGE_CURVE ( 'NONE', #10632, #8831, #33633, .T. ) ;
#210370=CARTESIAN_POINT ( 'NONE',  ( 18.59999999999999076, 76.00000000001213607, -136.5231074845243313 ) ) ;
#210389=SPHERICAL_SURFACE ( 'NONE', #210087, 0.1000000000000000056 ) ;
#210390=EDGE_LOOP ( 'NONE', ( #93843, #170826, #187346, #168466 ) ) ;
#210411=FACE_OUTER_BOUND ( 'NONE', #172053, .T. ) ;
#210420=DIRECTION ( 'NONE',  ( 0.000000000000000000, 0.000000000000000000, -1.000000000000000000 ) ) ;
#210427=CARTESIAN_POINT ( 'NONE',  ( -21.05000000000000071, 77.83534155023670564, -158.4679561919613491 ) ) ;
#210433=ADVANCED_FACE ( 'NONE', ( #840 ), #19148, .T. ) ;
#210439=EDGE_CURVE ( 'NONE', #237280, #35927, #2035, .T. ) ;
#210446=CIRCLE ( 'NONE', #72915, 0.1000000000000028644 ) ;
#210455=CARTESIAN_POINT ( 'NONE',  ( -23.25000000000000000, 64.25000000001246292, -181.7731074845244450 ) ) ;
#210468=DIRECTION ( 'NONE',  ( -1.000000000000000000, -0.000000000000000000, -0.000000000000000000 ) ) ;
#210469=DIRECTION ( 'NONE',  ( -1.000000000000000000, 0.000000000000000000, -0.000000000000000000 ) ) ;
#210504=CARTESIAN_POINT ( 'NONE',  ( 21.05000000000000071, 71.00000000001223555, -148.4283735034374843 ) ) ;
#210522=ORIENTED_EDGE ( 'NONE', *, *, #177473, .T. ) ;
#210547=CARTESIAN_POINT ( 'NONE',  ( -20.95000000000000284, 64.35000000001220144, -143.5379132551784096 ) ) ;
#210549=CARTESIAN_POINT ( 'NONE',  ( -21.05000000000000071, 76.01771943332080639, -176.4641921729960643 ) ) ;
#210560=LINE ( 'NONE', #193569, #115200 ) ;
#210614=PLANE ( 'NONE',  #136928 ) ;
#210615=LINE ( 'NONE', #214453, #204878 ) ;
#210624=DIRECTION ( 'NONE',  ( 0.000000000000000000, -0.01562499999999307672, 0.9998779222360100194 ) ) ;
#210676=EDGE_CURVE ( 'NONE', #55258, #240571, #56201, .T. ) ;
#210693=CARTESIAN_POINT ( 'NONE',  ( -22.50000000000000000, 76.00000000001237765, -170.1231074845243540 ) ) ;
#210741=DIRECTION ( 'NONE',  ( 1.000000000000000000, 0.000000000000000000, 0.000000000000000000 ) ) ;
#210750=ORIENTED_EDGE ( 'NONE', *, *, #31110, .T. ) ;
#210760=ADVANCED_FACE ( 'NONE', ( #102191 ), #20139, .T. ) ;
#210777=ORIENTED_EDGE ( 'NONE', *, *, #164913, .F. ) ;
#210816=CARTESIAN_POINT ( 'NONE',  ( -22.50047199487426752, 75.95509394809670312, -181.7731549034402008 ) ) ;
#210830=DIRECTION ( 'NONE',  ( 0.000000000000000000, 6.982962677686266711E-15, -1.000000000000000000 ) ) ;
#210831=AXIS2_PLACEMENT_3D ( 'NONE', #168668, #66940, #108638 ) ;
#210838=CARTESIAN_POINT ( 'NONE',  ( -22.59999999999999787, 64.25043287652299284, -170.1239658536231616 ) ) ;
#210911=EDGE_CURVE ( 'NONE', #46965, #109416, #4401, .T. ) ;
#210921=LINE ( 'NONE', #11453, #49176 ) ;
#210939=DIRECTION ( 'NONE',  ( 1.000000000000000000, -2.952720810173289112E-16, -2.061873921506763405E-30 ) ) ;
#210942=AXIS2_PLACEMENT_3D ( 'NONE', #124289, #85108, #43455 ) ;
#210950=EDGE_CURVE ( 'NONE', #160550, #58185, #9539, .T. ) ;
#210971=CARTESIAN_POINT ( 'NONE',  ( 20.94999999999999929, 61.95000000001218154, -142.0368025552853624 ) ) ;
#210989=ORIENTED_EDGE ( 'NONE', *, *, #201049, .F. ) ;
#211042=CARTESIAN_POINT ( 'NONE',  ( -21.05000000000000071, 87.65000000001235492, -167.1231074845242688 ) ) ;
#211088=DIRECTION ( 'NONE',  ( 0.000000000000000000, 0.000000000000000000, 1.000000000000000000 ) ) ;
#211114=AXIS2_PLACEMENT_3D ( 'NONE', #44636, #82438, #62909 ) ;
#211170=DIRECTION ( 'NONE',  ( 1.000000000000000000, -3.265361837132813093E-16, -2.280189983783949500E-30 ) ) ;
#211179=CARTESIAN_POINT ( 'NONE',  ( -21.05000000000000071, 75.96636726467876599, -176.2819246792058152 ) ) ;
#211188=EDGE_LOOP ( 'NONE', ( #233037, #35392, #3076, #162999, #120403, #210750, #225620, #50309, #250230, #68425, #102450, #87287, #34820, #45022, #104548, #177162 ) ) ;
#211203=AXIS2_PLACEMENT_3D ( 'NONE', #186590, #228278, #7950 ) ;
#211222=EDGE_CURVE ( 'NONE', #96638, #247235, #64954, .T. ) ;
#211230=TOROIDAL_SURFACE ( 'NONE', #132125, 0.4000000000000003553, 0.1000000000000000056 ) ;
#211242=VERTEX_POINT ( 'NONE', #169327 ) ;
#211266=CARTESIAN_POINT ( 'NONE',  ( -18.39999999999999858, 85.68240343348850274, -129.8662641071115047 ) ) ;
#211294=DIRECTION ( 'NONE',  ( 1.000000000000000000, 0.000000000000000000, 0.000000000000000000 ) ) ;
#211309=DIRECTION ( 'NONE',  ( 0.000000000000000000, -1.000000000000000000, 0.000000000000000000 ) ) ;
#211322=TOROIDAL_SURFACE ( 'NONE', #69685, 11.65000000000000036, 0.1000000000000000056 ) ;
#211336=CARTESIAN_POINT ( 'NONE',  ( 21.05000000000000071, 76.00000000001237765, -170.0231074845243597 ) ) ;
#211345=ORIENTED_EDGE ( 'NONE', *, *, #84650, .T. ) ;
#211347=ORIENTED_EDGE ( 'NONE', *, *, #57878, .F. ) ;
#211351=DIRECTION ( 'NONE',  ( 1.000000000000000000, 0.000000000000000000, 0.000000000000000000 ) ) ;
#211355=EDGE_CURVE ( 'NONE', #16105, #184497, #76591, .T. ) ;
#211373=ORIENTED_EDGE ( 'NONE', *, *, #73082, .T. ) ;
#211403=DIRECTION ( 'NONE',  ( -1.000000000000000000, 1.836970198721029934E-16, 1.601412966608202925E-30 ) ) ;
#211464=DIRECTION ( 'NONE',  ( 1.000000000000000000, 0.000000000000000000, 0.000000000000000000 ) ) ;
#211473=TOROIDAL_SURFACE ( 'NONE', #190851, 6.258578643762700899, 0.1000000000000000056 ) ;
#211481=CARTESIAN_POINT ( 'NONE',  ( -20.64999999999999858, 74.00000000001223555, -149.7477294072864709 ) ) ;
#211487=ORIENTED_EDGE ( 'NONE', *, *, #122009, .T. ) ;
#211509=AXIS2_PLACEMENT_3D ( 'NONE', #14751, #52547, #172565 ) ;
#211517=CARTESIAN_POINT ( 'NONE',  ( 18.59999999999999787, 85.32100840337362513, -162.7871692354464130 ) ) ;
#211527=SPHERICAL_SURFACE ( 'NONE', #191395, 0.1000000000000000056 ) ;
#211543=CARTESIAN_POINT ( 'NONE',  ( -18.50000000000000000, 85.50000000001233502, -161.9231074845242802 ) ) ;
#211592=CIRCLE ( 'NONE', #24348, 11.80000000000000426 ) ;
#211593=EDGE_CURVE ( 'NONE', #151867, #223317, #144234, .T. ) ;
#211597=EDGE_LOOP ( 'NONE', ( #41815, #243841, #58485, #13451 ) ) ;
#211621=AXIS2_PLACEMENT_3D ( 'NONE', #51073, #31586, #250589 ) ;
#211627=CARTESIAN_POINT ( 'NONE',  ( -21.05000000000000071, 64.35000000001234355, -163.2392418215462726 ) ) ;
#211629=CIRCLE ( 'NONE', #16012, 0.1000000000000046685 ) ;
#211647=( BOUNDED_CURVE ( )  B_SPLINE_CURVE ( 3, ( #111233, #150373, #190803, #211627 ),
 .UNSPECIFIED., .F., .F. ) 
 B_SPLINE_CURVE_WITH_KNOTS ( ( 4, 4 ),
 ( 3.141592653589793116, 4.712388980384689674 ),
 .UNSPECIFIED. ) 
 CURVE ( )  GEOMETRIC_REPRESENTATION_ITEM ( )  RATIONAL_B_SPLINE_CURVE ( ( 1.000000000000000000, 0.8047378541243649375, 0.8047378541243649375, 1.000000000000000000 ) ) 
 REPRESENTATION_ITEM ( '' )  );
#211662=CARTESIAN_POINT ( 'NONE',  ( -22.50000000000000000, 76.00000000001237765, -170.0231074845243597 ) ) ;
#211663=CYLINDRICAL_SURFACE ( 'NONE', #103822, 0.1000000000000028644 ) ;
#211691=DIRECTION ( 'NONE',  ( 1.000000000000000000, 0.000000000000000000, 0.000000000000000000 ) ) ;
#211693=CARTESIAN_POINT ( 'NONE',  ( -18.59999999999999787, 85.48068669529106955, -129.5819923157664562 ) ) ;
#211707=CARTESIAN_POINT ( 'NONE',  ( 18.59999999999999076, 69.55000000001223270, -148.7731074845244166 ) ) ;
#211712=LINE ( 'NONE', #34370, #165065 ) ;
#211738=FACE_OUTER_BOUND ( 'NONE', #7818, .T. ) ;
#211740=DIRECTION ( 'NONE',  ( 0.000000000000000000, -6.982962677686266711E-15, 1.000000000000000000 ) ) ;
#211777=AXIS2_PLACEMENT_3D ( 'NONE', #160409, #120001, #196927 ) ;
#211792=CARTESIAN_POINT ( 'NONE',  ( -18.58222699835055280, 65.66799936921553638, -130.9299399888601272 ) ) ;
#211834=DIRECTION ( 'NONE',  ( 2.952720810173289112E-16, 1.000000000000000000, 6.938893903907222067E-15 ) ) ;
#211841=CARTESIAN_POINT ( 'NONE',  ( -21.07954763557765432, 75.93412408139404590, -176.3523984745653195 ) ) ;
#211842=ORIENTED_EDGE ( 'NONE', *, *, #52524, .F. ) ;
#211844=VECTOR ( 'NONE', #73048, 1000.000000000000114 ) ;
#211851=ADVANCED_FACE ( 'NONE', ( #218343 ), #180537, .T. ) ;
#211860=ADVANCED_FACE ( 'NONE', ( #17584 ), #184134, .T. ) ;
#211886=DIRECTION ( 'NONE',  ( 0.7071067811865475727, 0.7071067811865475727, 4.937700262164531476E-15 ) ) ;
#211935=DIRECTION ( 'NONE',  ( -4.701977403289178058E-30, -2.433019743745433765E-14, 1.000000000000000000 ) ) ;
#211944=CIRCLE ( 'NONE', #86996, 0.1000000000000011990 ) ;
#211949=EDGE_CURVE ( 'NONE', #58594, #194619, #119320, .T. ) ;
#211952=CIRCLE ( 'NONE', #37169, 0.09999999999999939493 ) ;
#211976=ORIENTED_EDGE ( 'NONE', *, *, #191598, .T. ) ;
#211985=DIRECTION ( 'NONE',  ( -1.000000000000000000, -0.000000000000000000, -0.000000000000000000 ) ) ;
#212005=CARTESIAN_POINT ( 'NONE',  ( 20.94999999999999929, 85.50000000001232081, -160.1291383618718385 ) ) ;
#212094=ADVANCED_FACE ( 'NONE', ( #122697 ), #103086, .F. ) ;
#212128=AXIS2_PLACEMENT_3D ( 'NONE', #108895, #168924, #228857 ) ;
#212129=CARTESIAN_POINT ( 'NONE',  ( 18.52928932188133970, 65.72071067813085676, -145.2731074845244450 ) ) ;
#212132=AXIS2_PLACEMENT_3D ( 'NONE', #3800, #181168, #2494 ) ;
#212171=VERTEX_POINT ( 'NONE', #185217 ) ;
#212177=ORIENTED_EDGE ( 'NONE', *, *, #23240, .T. ) ;
#212196=DIRECTION ( 'NONE',  ( 0.000000000000000000, 0.000000000000000000, 1.000000000000000000 ) ) ;
#212249=CARTESIAN_POINT ( 'NONE',  ( -18.59999999999999787, 64.35000000001234355, -163.0083017138704236 ) ) ;
#212263=VECTOR ( 'NONE', #38087, 1000.000000000000000 ) ;
#212271=CARTESIAN_POINT ( 'NONE',  ( 21.14999999999999503, 76.00000000001237765, -170.0231074845243597 ) ) ;
#212346=DIRECTION ( 'NONE',  ( -1.000000000000000000, 0.000000000000000000, 0.000000000000000000 ) ) ;
#212349=ORIENTED_EDGE ( 'NONE', *, *, #49037, .F. ) ;
#212372=DIRECTION ( 'NONE',  ( 0.000000000000000000, 0.000000000000000000, 1.000000000000000000 ) ) ;
#212378=CARTESIAN_POINT ( 'NONE',  ( 23.14999999999999858, 70.40000000001229807, -157.6178414656113205 ) ) ;
#212409=CIRCLE ( 'NONE', #70765, 0.5000000000000004441 ) ;
#212418=DIRECTION ( 'NONE',  ( -0.000000000000000000, 6.982962677686266711E-15, -1.000000000000000000 ) ) ;
#212425=ORIENTED_EDGE ( 'NONE', *, *, #209381, .F. ) ;
#212443=CARTESIAN_POINT ( 'NONE',  ( 20.94999999999999574, 65.52661458509942349, -162.4444530202758870 ) ) ;
#212454=ORIENTED_EDGE ( 'NONE', *, *, #35057, .F. ) ;
#212467=ORIENTED_EDGE ( 'NONE', *, *, #246644, .T. ) ;
#212491=DIRECTION ( 'NONE',  ( -1.000000000000000000, -0.000000000000000000, -0.000000000000000000 ) ) ;
#212500=FACE_OUTER_BOUND ( 'NONE', #192910, .T. ) ;
#212505=ORIENTED_EDGE ( 'NONE', *, *, #231841, .F. ) ;
#212544=ORIENTED_EDGE ( 'NONE', *, *, #248052, .T. ) ;
#212551=CARTESIAN_POINT ( 'NONE',  ( 22.39999999999999503, 68.20922040163900135, -170.0231074845243882 ) ) ;
#212570=DIRECTION ( 'NONE',  ( -0.000000000000000000, 6.982962677686266711E-15, -1.000000000000000000 ) ) ;
#212603=DIRECTION ( 'NONE',  ( -1.000000000000000000, -0.000000000000000000, -0.000000000000000000 ) ) ;
#212618=CARTESIAN_POINT ( 'NONE',  ( -21.08078803292166725, 75.92081401285471998, -176.3561204489614909 ) ) ;
#212641=LINE ( 'NONE', #113527, #251148 ) ;
#212650=ORIENTED_EDGE ( 'NONE', *, *, #90687, .T. ) ;
#212711=CARTESIAN_POINT ( 'NONE',  ( 20.94999999999999929, 76.00000000001213607, -136.5231074845243313 ) ) ;
#212751=AXIS2_PLACEMENT_3D ( 'NONE', #26257, #164482, #182764 ) ;
#212762=AXIS2_PLACEMENT_3D ( 'NONE', #167185, #246672, #32813 ) ;
#212809=CARTESIAN_POINT ( 'NONE',  ( 18.43579564894457690, 85.51932753530486764, -163.0501308406639964 ) ) ;
#212812=DIRECTION ( 'NONE',  ( -1.000000000000000000, 0.000000000000000000, -0.000000000000000000 ) ) ;
#212816=DIRECTION ( 'NONE',  ( -0.000000000000000000, 7.109473446599835262E-15, -1.000000000000000000 ) ) ;
#212831=VERTEX_POINT ( 'NONE', #240592 ) ;
#212861=DIRECTION ( 'NONE',  ( 0.000000000000000000, -1.000000000000000000, -6.982962677686265922E-15 ) ) ;
#212863=CARTESIAN_POINT ( 'NONE',  ( -20.64999999999999858, 74.00000000001223555, -149.7477294072864709 ) ) ;
#212931=DIRECTION ( 'NONE',  ( 0.000000000000000000, -1.000000000000000000, 0.000000000000000000 ) ) ;
#212959=CARTESIAN_POINT ( 'NONE',  ( -18.41817142474038960, 85.49870306661419761, -129.9191419968872765 ) ) ;
#212977=DIRECTION ( 'NONE',  ( -1.000000000000000000, 0.000000000000000000, -0.000000000000000000 ) ) ;
#212978=CARTESIAN_POINT ( 'NONE',  ( 21.05000000000000071, 64.35000000001237197, -170.0231074845244166 ) ) ;
#212982=CARTESIAN_POINT ( 'NONE',  ( 21.14999999999999858, 69.45000000001229523, -157.8731074845244109 ) ) ;
#212989=AXIS2_PLACEMENT_3D ( 'NONE', #187233, #129798, #86805 ) ;
#212994=VERTEX_POINT ( 'NONE', #206600 ) ;
#213014=CARTESIAN_POINT ( 'NONE',  ( -18.59999999999999787, 85.48068669529106955, -129.5819923157664562 ) ) ;
#213031=VERTEX_POINT ( 'NONE', #213014 ) ;
#213032=EDGE_CURVE ( 'NONE', #43685, #997, #236389, .T. ) ;
#213035=AXIS2_PLACEMENT_3D ( 'NONE', #57022, #75366, #32395 ) ;
#213073=DIRECTION ( 'NONE',  ( -1.000000000000000000, 3.265361837132813093E-16, 2.280189983783949500E-30 ) ) ;
#213085=B_SPLINE_CURVE_WITH_KNOTS ( 'NONE', 3,
 ( #22994, #245863, #65942, #84158, #5939, #82898 ),
 .UNSPECIFIED., .F., .F.,
 ( 4, 2, 4 ),
 ( 0.000000000000000000, 0.0001497467027049226784, 0.0002994934054098453567 ),
 .UNSPECIFIED. ) ;
#213093=CARTESIAN_POINT ( 'NONE',  ( -23.25000000000000000, 76.00000000001213607, -136.5231074845243313 ) ) ;
#213126=ORIENTED_EDGE ( 'NONE', *, *, #197164, .F. ) ;
#213145=DIRECTION ( 'NONE',  ( 0.7071067811865474617, -0.7071067811865474617, -4.937700262164531476E-15 ) ) ;
#213151=ORIENTED_EDGE ( 'NONE', *, *, #224816, .T. ) ;
#213166=EDGE_LOOP ( 'NONE', ( #183148, #105299, #16666, #227857 ) ) ;
#213254=VECTOR ( 'NONE', #194586, 1000.000000000000000 ) ;
#213257=EDGE_CURVE ( 'NONE', #64653, #171719, #28520, .T. ) ;
#213259=CARTESIAN_POINT ( 'NONE',  ( 18.58143601961852909, 65.56427058491723869, -145.2731074845244166 ) ) ;
#213261=CARTESIAN_POINT ( 'NONE',  ( -18.50000000000000355, 85.40000000001229807, -162.7258477248610404 ) ) ;
#213272=AXIS2_PLACEMENT_3D ( 'NONE', #144354, #204348, #225184 ) ;
#213292=DIRECTION ( 'NONE',  ( 0.000000000000000000, -1.000000000000000000, -6.982962677686265922E-15 ) ) ;
#213356=AXIS2_PLACEMENT_3D ( 'NONE', #41491, #141842, #83117 ) ;
#213368=CIRCLE ( 'NONE', #221733, 0.1000000000000072220 ) ;
#213388=CARTESIAN_POINT ( 'NONE',  ( -18.59999999999999787, 64.35000000001234355, -163.1083017138704179 ) ) ;
#213389=DIRECTION ( 'NONE',  ( -0.000000000000000000, 1.000000000000000000, 6.982962677686266711E-15 ) ) ;
#213423=ORIENTED_EDGE ( 'NONE', *, *, #181646, .F. ) ;
#213428=AXIS2_PLACEMENT_3D ( 'NONE', #67726, #126408, #105528 ) ;
#213450=EDGE_LOOP ( 'NONE', ( #133335, #90137, #205776, #49590, #175247, #12128, #60803, #98613 ) ) ;
#213459=ORIENTED_EDGE ( 'NONE', *, *, #230621, .F. ) ;
#213503=ORIENTED_EDGE ( 'NONE', *, *, #251721, .F. ) ;
#213504=DIRECTION ( 'NONE',  ( 0.000000000000000000, 0.000000000000000000, -1.000000000000000000 ) ) ;
#213514=EDGE_CURVE ( 'NONE', #219341, #91448, #128608, .T. ) ;
#213516=ORIENTED_EDGE ( 'NONE', *, *, #75155, .F. ) ;
#213525=DIRECTION ( 'NONE',  ( 1.000000000000000000, 0.000000000000000000, 0.000000000000000000 ) ) ;
#213558=AXIS2_PLACEMENT_3D ( 'NONE', #64961, #164079, #25860 ) ;
#213567=CIRCLE ( 'NONE', #59603, 0.09999999999999939493 ) ;
#213610=AXIS2_PLACEMENT_3D ( 'NONE', #34490, #56556, #76143 ) ;
#213635=CIRCLE ( 'NONE', #80322, 0.09999999999998898659 ) ;
#213656=EDGE_CURVE ( 'NONE', #187685, #35927, #190618, .T. ) ;
#213673=CIRCLE ( 'NONE', #126162, 0.09999999999998898659 ) ;
#213698=CARTESIAN_POINT ( 'NONE',  ( -21.05000000000000071, 76.00000000001216449, -140.5231074845243597 ) ) ;
#213741=CARTESIAN_POINT ( 'NONE',  ( -21.05000000000000426, 76.10000000001241460, -176.5001745056490847 ) ) ;
#213777=DIRECTION ( 'NONE',  ( 0.000000000000000000, -6.982962677686266711E-15, 1.000000000000000000 ) ) ;
#213825=LINE ( 'NONE', #36502, #125368 ) ;
#213831=CARTESIAN_POINT ( 'NONE',  ( -22.50000000000000000, 76.00000000001246292, -181.6726782920691505 ) ) ;
#213845=ADVANCED_FACE ( 'NONE', ( #217196 ), #98502, .F. ) ;
#213847=DIRECTION ( 'NONE',  ( 0.000000000000000000, -1.000000000000000000, -6.982962677686265922E-15 ) ) ;
#213860=ORIENTED_EDGE ( 'NONE', *, *, #186473, .T. ) ;
#213872=CARTESIAN_POINT ( 'NONE',  ( 18.49999999999999645, 77.16412189325330928, -128.6082593989527254 ) ) ;
#213895=CARTESIAN_POINT ( 'NONE',  ( 23.14999999999999858, 70.10000000001220144, -146.7422072491807796 ) ) ;
#213914=ADVANCED_FACE ( 'NONE', ( #164943 ), #70374, .F. ) ;
#213921=DIRECTION ( 'NONE',  ( -1.000000000000000000, -0.000000000000000000, -0.000000000000000000 ) ) ;
#213935=DIRECTION ( 'NONE',  ( 0.000000000000000000, 7.056502275159890043E-15, -1.000000000000000000 ) ) ;
#213949=CIRCLE ( 'NONE', #9742, 0.1000000000000028644 ) ;
#213969=CARTESIAN_POINT ( 'NONE',  ( -21.05000000000000071, 87.65000000001238334, -170.0231074845242745 ) ) ;
#213993=DIRECTION ( 'NONE',  ( -0.000000000000000000, -1.000000000000000000, -7.272083257015735086E-15 ) ) ;
#213995=ADVANCED_FACE ( 'NONE', ( #206639 ), #124512, .T. ) ;
#214022=ORIENTED_EDGE ( 'NONE', *, *, #133559, .F. ) ;
#214028=DIRECTION ( 'NONE',  ( -1.000000000000000000, -0.000000000000000000, -0.000000000000000000 ) ) ;
#214041=CARTESIAN_POINT ( 'NONE',  ( 18.49999999999998934, 65.75000000001222134, -145.2731074845244450 ) ) ;
#214042=ORIENTED_EDGE ( 'NONE', *, *, #35705, .F. ) ;
#214051=ORIENTED_EDGE ( 'NONE', *, *, #254475, .T. ) ;
#214078=ORIENTED_EDGE ( 'NONE', *, *, #42809, .F. ) ;
#214085=DIRECTION ( 'NONE',  ( 0.000000000000000000, 0.000000000000000000, 1.000000000000000000 ) ) ;
#214093=FACE_OUTER_BOUND ( 'NONE', #13925, .T. ) ;
#214115=SURFACE_SIDE_STYLE ('',( #70779 ) ) ;
#214147=CARTESIAN_POINT ( 'NONE',  ( -21.05000000000000071, 69.70000000001236629, -169.9231074845244223 ) ) ;
#214160=DIRECTION ( 'NONE',  ( -0.000000000000000000, -6.982962677686266711E-15, 1.000000000000000000 ) ) ;
#214168=CARTESIAN_POINT ( 'NONE',  ( 19.99999999999998934, 64.35000000001222986, -148.7731074845244450 ) ) ;
#214284=AXIS2_PLACEMENT_3D ( 'NONE', #137033, #54907, #52335 ) ;
#214327=ORIENTED_EDGE ( 'NONE', *, *, #183739, .T. ) ;
#214328=DIRECTION ( 'NONE',  ( -0.000000000000000000, 1.000000000000000000, 6.352154140967427193E-15 ) ) ;
#214340=DIRECTION ( 'NONE',  ( 0.000000000000000000, 0.000000000000000000, 1.000000000000000000 ) ) ;
#214341=EDGE_LOOP ( 'NONE', ( #92195, #176742, #122136, #75999 ) ) ;
#214350=CARTESIAN_POINT ( 'NONE',  ( 21.03675099975490070, 67.12481996722748079, -157.6975653477463766 ) ) ;
#214357=VECTOR ( 'NONE', #204147, 1000.000000000000000 ) ;
#214364=ORIENTED_EDGE ( 'NONE', *, *, #243585, .T. ) ;
#214368=AXIS2_PLACEMENT_3D ( 'NONE', #4133, #105778, #86214 ) ;
#214378=DIRECTION ( 'NONE',  ( 0.000000000000000000, 0.5907332058517377193, -0.8068669527896954463 ) ) ;
#214385=DIRECTION ( 'NONE',  ( -3.265361837132813093E-16, -1.000000000000000000, -6.982962677686266711E-15 ) ) ;
#214423=CARTESIAN_POINT ( 'NONE',  ( -21.03922262424653056, 64.37609936600757976, -163.1638994416307469 ) ) ;
#214430=EDGE_CURVE ( 'NONE', #219647, #163114, #215676, .T. ) ;
#214446=CARTESIAN_POINT ( 'NONE',  ( -23.15000000000000213, 87.39257802171783851, -139.5970570643562212 ) ) ;
#214449=EDGE_CURVE ( 'NONE', #61696, #102268, #74090, .T. ) ;
#214451=LINE ( 'NONE', #151952, #250041 ) ;
#214453=CARTESIAN_POINT ( 'NONE',  ( -21.05000000000000071, 77.83534155023670564, -158.3679561919613548 ) ) ;
#214464=VECTOR ( 'NONE', #30621, 1000.000000000000000 ) ;
#214481=ORIENTED_EDGE ( 'NONE', *, *, #11621, .F. ) ;
#214494=ADVANCED_FACE ( 'NONE', ( #246733 ), #108519, .F. ) ;
#214502=LINE ( 'NONE', #97088, #238405 ) ;
#214545=ORIENTED_EDGE ( 'NONE', *, *, #9279, .T. ) ;
#214551=EDGE_CURVE ( 'NONE', #44660, #235293, #45013, .T. ) ;
#214561=EDGE_LOOP ( 'NONE', ( #135946, #254487, #202777, #91110 ) ) ;
#214569=ORIENTED_EDGE ( 'NONE', *, *, #86968, .T. ) ;
#214576=CARTESIAN_POINT ( 'NONE',  ( -20.90851465518106167, 65.67467670974440352, -130.9531731826884879 ) ) ;
#214607=ORIENTED_EDGE ( 'NONE', *, *, #174259, .F. ) ;
#214609=DIRECTION ( 'NONE',  ( -1.000000000000000000, 0.000000000000000000, 0.000000000000000000 ) ) ;
#214630=ORIENTED_EDGE ( 'NONE', *, *, #195079, .F. ) ;
#214655=DIRECTION ( 'NONE',  ( -1.000000000000000000, 3.265361837132813093E-16, 2.280189983783949500E-30 ) ) ;
#214660=ORIENTED_EDGE ( 'NONE', *, *, #114701, .T. ) ;
#214666=VERTEX_POINT ( 'NONE', #35441 ) ;
#214686=CARTESIAN_POINT ( 'NONE',  ( -22.39999999999999858, 76.00000000001246292, -181.6726782920691505 ) ) ;
#214705=AXIS2_PLACEMENT_3D ( 'NONE', #65584, #126845, #23923 ) ;
#214715=ORIENTED_EDGE ( 'NONE', *, *, #245377, .T. ) ;
#214737=CARTESIAN_POINT ( 'NONE',  ( 20.94999999999999929, 76.00000000001213607, -136.5231074845243313 ) ) ;
#214742=CARTESIAN_POINT ( 'NONE',  ( -23.25000000000000000, 71.65000000001222702, -148.6731074845243938 ) ) ;
#214791=CARTESIAN_POINT ( 'NONE',  ( -18.50000000000000000, 77.16412189325330928, -128.6082593989527254 ) ) ;
#214796=CARTESIAN_POINT ( 'NONE',  ( 21.06280952165552023, 65.37286769941131581, -157.8190535977451248 ) ) ;
#214813=DIRECTION ( 'NONE',  ( 0.000000000000000000, -1.000000000000000000, -6.352154140967427193E-15 ) ) ;
#214828=DIRECTION ( 'NONE',  ( 0.000000000000000000, 1.000000000000000000, 6.982962677686267499E-15 ) ) ;
#214851=CIRCLE ( 'NONE', #169106, 0.1000000000000046685 ) ;
#214858=CARTESIAN_POINT ( 'NONE',  ( 21.05000000000000071, 77.83534155023671985, -158.4679561919613491 ) ) ;
#214871=CARTESIAN_POINT ( 'NONE',  ( -23.25000000000000000, 76.00000000001237765, -170.0231074845243597 ) ) ;
#214960=CARTESIAN_POINT ( 'NONE',  ( -21.65000000000000213, 68.29142135624960019, -157.7731074845244166 ) ) ;
#214979=FACE_OUTER_BOUND ( 'NONE', #39572, .T. ) ;
#214990=EDGE_CURVE ( 'NONE', #139006, #28076, #253473, .T. ) ;
#214995=CARTESIAN_POINT ( 'NONE',  ( 21.14999999999999858, 69.74218538953624602, -170.1208977758331855 ) ) ;
#215004=ORIENTED_EDGE ( 'NONE', *, *, #237296, .F. ) ;
#215009=CARTESIAN_POINT ( 'NONE',  ( 23.24999999999999289, 69.35000000001228670, -157.6731074845243938 ) ) ;
#215042=DIRECTION ( 'NONE',  ( 3.616040088954490704E-32, 7.105427357601001859E-15, -1.000000000000000000 ) ) ;
#215050=DIRECTION ( 'NONE',  ( 0.000000000000000000, -0.4999999999999088507, -0.8660254037844913322 ) ) ;
#215120=VECTOR ( 'NONE', #180773, 1000.000000000000000 ) ;
#215132=CARTESIAN_POINT ( 'NONE',  ( -20.64999999999999858, 68.85000000001222986, -148.8731074845244109 ) ) ;
#215133=AXIS2_PLACEMENT_3D ( 'NONE', #42565, #122115, #116037 ) ;
#215178=ORIENTED_EDGE ( 'NONE', *, *, #248453, .T. ) ;
#215217=DIRECTION ( 'NONE',  ( 1.000000000000000000, -0.000000000000000000, 0.000000000000000000 ) ) ;
#215231=DIRECTION ( 'NONE',  ( 0.000000000000000000, 0.000000000000000000, 1.000000000000000000 ) ) ;
#215268=DIRECTION ( 'NONE',  ( 0.000000000000000000, 0.000000000000000000, -1.000000000000000000 ) ) ;
#215269=CARTESIAN_POINT ( 'NONE',  ( -22.39999999999999858, 75.90000000001242597, -177.8138870828977360 ) ) ;
#215282=ORIENTED_EDGE ( 'NONE', *, *, #247778, .T. ) ;
#215283=CYLINDRICAL_SURFACE ( 'NONE', #80986, 0.09999999999999939493 ) ;
#215304=DIRECTION ( 'NONE',  ( -1.000000000000000000, 0.000000000000000000, -0.000000000000000000 ) ) ;
#215308=ORIENTED_EDGE ( 'NONE', *, *, #59685, .F. ) ;
#215344=ORIENTED_EDGE ( 'NONE', *, *, #161091, .T. ) ;
#215347=DIRECTION ( 'NONE',  ( 0.000000000000000000, -6.982962677686266711E-15, 1.000000000000000000 ) ) ;
#215407=LINE ( 'NONE', #57605, #40454 ) ;
#215435=ORIENTED_EDGE ( 'NONE', *, *, #195026, .T. ) ;
#215452=FACE_OUTER_BOUND ( 'NONE', #234314, .T. ) ;
#215470=DIRECTION ( 'NONE',  ( 1.000000000000000000, 0.000000000000000000, 0.000000000000000000 ) ) ;
#215478=CARTESIAN_POINT ( 'NONE',  ( 20.84999999999999432, 68.97833521811203639, -132.6895420826271277 ) ) ;
#215500=VERTEX_POINT ( 'NONE', #98562 ) ;
#215511=DIRECTION ( 'NONE',  ( 0.000000000000000000, 0.000000000000000000, -1.000000000000000000 ) ) ;
#215547=EDGE_CURVE ( 'NONE', #161999, #145174, #175257, .T. ) ;
#215591=CARTESIAN_POINT ( 'NONE',  ( 21.05000000000000071, 88.41227409416185878, -139.5231074845242745 ) ) ;
#215593=FACE_OUTER_BOUND ( 'NONE', #86938, .T. ) ;
#215609=DIRECTION ( 'NONE',  ( 1.000000000000000000, 0.000000000000000000, 0.000000000000000000 ) ) ;
#215634=DIRECTION ( 'NONE',  ( -0.000000000000000000, -6.982962677686266711E-15, 1.000000000000000000 ) ) ;
#215651=CYLINDRICAL_SURFACE ( 'NONE', #140179, 0.09999999999999939493 ) ;
#215653=EDGE_CURVE ( 'NONE', #65247, #168942, #139717, .T. ) ;
#215661=DIRECTION ( 'NONE',  ( 0.000000000000000000, -1.000000000000000000, -6.982962677686265922E-15 ) ) ;
#215674=DIRECTION ( 'NONE',  ( -1.000000000000000000, 0.000000000000000000, 0.000000000000000000 ) ) ;
#215676=CIRCLE ( 'NONE', #253106, 0.1999999999999987899 ) ;
#215690=DIRECTION ( 'NONE',  ( 0.000000000000000000, -7.109473446599835262E-15, 1.000000000000000000 ) ) ;
#215713=ORIENTED_EDGE ( 'NONE', *, *, #231921, .F. ) ;
#215719=EDGE_CURVE ( 'NONE', #132498, #29869, #4682, .T. ) ;
#215739=ADVANCED_FACE ( 'NONE', ( #74612 ), #168966, .T. ) ;
#215741=DIRECTION ( 'NONE',  ( 0.000000000000000000, 7.109473446599835262E-15, -1.000000000000000000 ) ) ;
#215764=EDGE_CURVE ( 'NONE', #229965, #60057, #38055, .T. ) ;
#215766=CIRCLE ( 'NONE', #257414, 0.09999999999999939493 ) ;
#215774=CARTESIAN_POINT ( 'NONE',  ( 22.48660254037844197, 64.35000000001237197, -170.0731074845244279 ) ) ;
#215792=CARTESIAN_POINT ( 'NONE',  ( -23.15000000000000213, 76.00000000001213607, -136.5231074845243313 ) ) ;
#215815=CARTESIAN_POINT ( 'NONE',  ( 18.49999999999999289, 65.50857864377491069, -145.1731074845244223 ) ) ;
#215825=CARTESIAN_POINT ( 'NONE',  ( -20.85000000000000142, 77.13501884592227498, -128.8061306010920362 ) ) ;
#215831=EDGE_CURVE ( 'NONE', #138584, #166820, #250198, .T. ) ;
#215834=CIRCLE ( 'NONE', #103404, 12.97499999999998721 ) ;
#215837=EDGE_CURVE ( 'NONE', #56828, #212994, #250235, .T. ) ;
#215842=CYLINDRICAL_SURFACE ( 'NONE', #167090, 0.09999999999998898659 ) ;
#215862=CARTESIAN_POINT ( 'NONE',  ( -20.85000000000000142, 87.65000000001215597, -139.4231074845242802 ) ) ;
#215871=ORIENTED_EDGE ( 'NONE', *, *, #237385, .T. ) ;
#215916=CYLINDRICAL_SURFACE ( 'NONE', #111014, 0.1000000000000106914 ) ;
#215919=ORIENTED_EDGE ( 'NONE', *, *, #127757, .F. ) ;
#215925=ORIENTED_EDGE ( 'NONE', *, *, #28217, .T. ) ;
#215926=CLOSED_SHELL ( 'NONE', ( #35312, #69781, #209793, #203358, #109764, #124688, #210295, #89330, #120512, #162414, #201107, #189880, #88015, #54001, #191291, #99001, #57594, #15632, #19766, #256795, #140444, #254769, #59257, #27966, #80295, #22831, #247993, #115298, #40258, #85104, #61741, #106204, #205301, #102634, #97281, #116684, #67855, #202817, #85934, #63790, #92653, #32337, #1635, #121911, #180623, #255393, #177893, #28093, #170384, #64711, #171797, #148954, #214494, #220227, #34616, #119935, #238055, #108536, #197742, #178949, #46080, #32548, #74990, #175388, #33635, #197272, #84817, #98795, #179249, #162701, #45236, #78155, #180373, #8956, #1683, #32355, #109911, #116081, #239150, #217786, #173460, #41651, #152640, #123290, #98170, #231294, #233981, #164579, #11978, #15837, #163192, #185588, #227430, #103114, #149377, #167371, #168369, #203632, #220375, #243463, #210010, #225750, #172556, #137364, #43096, #50236, #197972, #197006, #208369, #44311, #35292, #59054, #204401, #220997, #2612, #89071, #247406, #157166, #9916, #96515, #173136, #47683, #85017, #97456, #139029, #2938, #144174, #14343, #6636, #74712, #210760, #242750, #191057, #158693, #82028, #132743, #115157, #236345, #171987, #216216, #158070, #82334, #73239, #145559, #7537, #50634, #34263, #60672, #165258, #79006, #65446, #81414, #194145, #40898, #83194, #120390, #96493, #83404, #42267, #201416, #37149, #1663, #12735, #234195, #143939, #176753, #49954, #70642, #35089, #207565, #241251, #181088, #184875, #35297, #198310, #72775, #55256, #118031, #109302, #103096, #238691, #20091, #254452, #178261, #135369, #175059, #229964, #247746, #241125, #98130, #237728, #194238, #71425, #252592, #17311, #153570, #195490, #46383, #104133, #233830, #113790, #223189, #189151, #85896, #166232, #54376, #125390, #130924, #64747, #154146, #180949, #137116, #138073, #39450, #14687, #146998, #48527, #34712, #113690, #213914, #70638, #62501, #36027, #169544, #158288, #229016, #60635, #144742, #147101, #7241, #25513, #130045, #10147, #170088, #17621, #24011, #154869, #107590, #250087, #256153, #130533, #196001, #169862, #9424, #13294, #229363, #96974, #110764, #211851, #204589, #173263, #178224, #202862, #246627, #172924, #223942, #250130, #10239, #209024, #185368, #49291, #221579, #48802, #218638, #152253, #142146, #10761, #42481, #90854, #44615, #197445, #17002, #44416, #32800, #41093, #117419, #20823, #154302, #204042, #144099, #187120, #126033, #112742, #93858, #89901, #14043, #94083, #235991, #152389, #161644, #181328, #101179, #62302, #29277, #78724, #8163, #204800, #100373, #386, #149563, #31847, #243735, #75815, #253951, #46856, #204408, #229971, #819, #20320, #226331, #86043, #237678, #72308, #88238, #46029, #12003, #232092, #207789, #123286, #221870, #107456, #9445, #135934, #50560, #221543, #164681, #37830, #174380, #109076, #221379, #40092, #80107, #11939, #236751, #164163, #120592, #190829, #236590, #86208, #44805, #232542, #163977, #242249, #7339, #73529, #27649, #115108, #114173, #212094, #181459, #85666, #42032, #124870, #117536, #197875, #63686, #192527, #233078, #103730, #241379, #215739, #5402, #64786, #134668, #156623, #124967, #196519, #64963, #52371, #79256, #91195, #66402, #70855, #60285, #80531, #168841, #129729, #32091, #168952, #191920, #155668, #192758, #28073, #250957, #221849, #32960, #47868, #82913, #192939, #36197, #85534, #175772, #221511, #242070, #147792, #162716, #125521, #250543, #178321, #226667, #254091, #121841, #67718, #132631, #155113, #85696, #128528, #70627, #176244, #49766, #233389, #118641, #205596, #44443, #213995, #229192, #183520, #231830, #37747, #30174, #139126, #143374, #62399, #223257, #205649, #221641, #71517, #29072, #140644, #96014, #61371, #61296, #192407, #190427, #189933, #58522, #9081, #229065, #237607, #94004, #192325, #210433, #85263, #55773, #103628, #235793, #231967, #224408, #145912, #107894, #85922, #162703, #183847, #55269, #124137, #251212, #246799, #193544, #177782, #95682, #61831, #111819, #241929, #172308, #213845, #140515, #211860, #68014, #177156, #13813, #73089, #112393, #16598, #118835, #223401, #174035, #244630, #29867 ) ) ;
#215949=DIRECTION ( 'NONE',  ( 0.000000000000000000, 6.982962677686266711E-15, -1.000000000000000000 ) ) ;
#215953=ORIENTED_EDGE ( 'NONE', *, *, #206013, .T. ) ;
#215992=DIRECTION ( 'NONE',  ( -1.000000000000000000, 0.000000000000000000, 0.000000000000000000 ) ) ;
#216025=CARTESIAN_POINT ( 'NONE',  ( -21.93340585898181061, 76.00000000001243450, -177.3472545066570945 ) ) ;
#216042=DIRECTION ( 'NONE',  ( 1.000000000000000000, 7.304098846218134667E-16, 4.639676173203993355E-30 ) ) ;
#216052=ORIENTED_EDGE ( 'NONE', *, *, #32141, .T. ) ;
#216090=CARTESIAN_POINT ( 'NONE',  ( -20.94999999999999929, 74.83729825007431202, -161.9231074845243654 ) ) ;
#216092=AXIS2_PLACEMENT_3D ( 'NONE', #48079, #49373, #204580 ) ;
#216102=VECTOR ( 'NONE', #250350, 1000.000000000000000 ) ;
#216103=VERTEX_POINT ( 'NONE', #47862 ) ;
#216125=CARTESIAN_POINT ( 'NONE',  ( 21.05000000000000071, 69.74115287693328469, -170.0548658375798823 ) ) ;
#216127=CARTESIAN_POINT ( 'NONE',  ( 22.47071067811865319, 75.90090754530983475, -177.7431822290224090 ) ) ;
#216131=DIRECTION ( 'NONE',  ( 0.000000000000000000, 1.000000000000000000, 6.982962677686266711E-15 ) ) ;
#216157=ORIENTED_EDGE ( 'NONE', *, *, #114540, .F. ) ;
#216171=CARTESIAN_POINT ( 'NONE',  ( 18.59999999999999787, 77.83534155023670564, -158.3679561919613548 ) ) ;
#216188=AXIS2_PLACEMENT_3D ( 'NONE', #2220, #218700, #120935 ) ;
#216202=DIRECTION ( 'NONE',  ( 0.000000000000000000, 0.000000000000000000, 1.000000000000000000 ) ) ;
#216207=CARTESIAN_POINT ( 'NONE',  ( -20.94999999999999929, 75.74389420792016381, -170.0580039261966476 ) ) ;
#216216=ADVANCED_FACE ( 'NONE', ( #235493 ), #138931, .F. ) ;
#216226=FACE_OUTER_BOUND ( 'NONE', #238550, .T. ) ;
#216231=ORIENTED_EDGE ( 'NONE', *, *, #100993, .T. ) ;
#216245=DIRECTION ( 'NONE',  ( 1.000000000000000000, 0.000000000000000000, 0.000000000000000000 ) ) ;
#216287=DIRECTION ( 'NONE',  ( 2.715809747126117987E-16, 1.000000000000000000, 1.303588678620536555E-14 ) ) ;
#216289=ORIENTED_EDGE ( 'NONE', *, *, #1581, .T. ) ;
#216304=EDGE_LOOP ( 'NONE', ( #40513, #234642, #237028, #76864, #144560, #254495, #224033, #70656, #10874 ) ) ;
#216322=CARTESIAN_POINT ( 'NONE',  ( 18.49999999999999289, 65.79142135624951493, -145.3731074845244109 ) ) ;
#216359=CARTESIAN_POINT ( 'NONE',  ( 18.49999999999999645, 74.13328508995498112, -158.2704322382423641 ) ) ;
#216367=EDGE_CURVE ( 'NONE', #168233, #5474, #142711, .T. ) ;
#216386=CARTESIAN_POINT ( 'NONE',  ( 23.25000000000000000, 84.59626168225520360, -145.9732350016745954 ) ) ;
#216408=ORIENTED_EDGE ( 'NONE', *, *, #122009, .F. ) ;
#216412=CARTESIAN_POINT ( 'NONE',  ( -18.59999999999999787, 76.00000000001213607, -136.5231074845243313 ) ) ;
#216428=CARTESIAN_POINT ( 'NONE',  ( 21.05000000000000071, 69.45934304831114048, -169.9231074845244223 ) ) ;
#216437=ORIENTED_EDGE ( 'NONE', *, *, #125053, .F. ) ;
#216456=CARTESIAN_POINT ( 'NONE',  ( -23.15000000000000213, 76.00000000001240608, -174.0731074845243711 ) ) ;
#216459=DIRECTION ( 'NONE',  ( 1.000000000000000000, 0.000000000000000000, 0.000000000000000000 ) ) ;
#216480=EDGE_LOOP ( 'NONE', ( #138638, #231457 ) ) ;
#216485=CARTESIAN_POINT ( 'NONE',  ( -18.43569575749026157, 85.51932773110478081, -163.0501311079650009 ) ) ;
#216491=CARTESIAN_POINT ( 'NONE',  ( 18.50000972452444969, 65.70673848566984532, -131.0638252334829872 ) ) ;
#216492=EDGE_CURVE ( 'NONE', #248304, #172545, #155611, .T. ) ;
#216509=PLANE ( 'NONE',  #127349 ) ;
#216520=VERTEX_POINT ( 'NONE', #97900 ) ;
#216556=EDGE_CURVE ( 'NONE', #135741, #43638, #181348, .T. ) ;
#216563=CARTESIAN_POINT ( 'NONE',  ( 22.50000000000000000, 75.90000000001245439, -181.7731074845243597 ) ) ;
#216592=DIRECTION ( 'NONE',  ( -0.000000000000000000, 6.982962677686266711E-15, -1.000000000000000000 ) ) ;
#216616=LINE ( 'NONE', #36734, #144501 ) ;
#216633=EDGE_CURVE ( 'NONE', #125708, #57514, #251216, .T. ) ;
#216646=CARTESIAN_POINT ( 'NONE',  ( 23.15000000000000213, 87.48912529308822172, -139.6231074845242688 ) ) ;
#216674=DIRECTION ( 'NONE',  ( 0.000000000000000000, 0.000000000000000000, 1.000000000000000000 ) ) ;
#216685=VERTEX_POINT ( 'NONE', #122657 ) ;
#216716=EDGE_LOOP ( 'NONE', ( #56913, #257386, #203417, #174602 ) ) ;
#216741=CARTESIAN_POINT ( 'NONE',  ( -23.15000000000000213, 74.00000000001223555, -149.7477294072864709 ) ) ;
#216759=DIRECTION ( 'NONE',  ( 0.000000000000000000, -1.000000000000000000, -6.982962677686265922E-15 ) ) ;
#216771=DIRECTION ( 'NONE',  ( 0.000000000000000000, -6.982962677686266711E-15, 1.000000000000000000 ) ) ;
#216787=ORIENTED_EDGE ( 'NONE', *, *, #84650, .F. ) ;
#216799=ORIENTED_EDGE ( 'NONE', *, *, #36860, .T. ) ;
#216867=EDGE_CURVE ( 'NONE', #95210, #43942, #18201, .T. ) ;
#216901=DIRECTION ( 'NONE',  ( 1.000000000000000000, 0.000000000000000000, 0.000000000000000000 ) ) ;
#216952=AXIS2_PLACEMENT_3D ( 'NONE', #195636, #19554, #239884 ) ;
#217007=AXIS2_PLACEMENT_3D ( 'NONE', #20156, #204864, #140065 ) ;
#217022=ORIENTED_EDGE ( 'NONE', *, *, #215837, .F. ) ;
#217045=ORIENTED_EDGE ( 'NONE', *, *, #5983, .T. ) ;
#217047=CARTESIAN_POINT ( 'NONE',  ( 20.94999999999999929, 85.00000000001222134, -146.4170766071767389 ) ) ;
#217081=CARTESIAN_POINT ( 'NONE',  ( -23.25000000000000000, 77.85161776048096272, -124.9199177649206689 ) ) ;
#217087=CARTESIAN_POINT ( 'NONE',  ( 21.09610168723073542, 75.96641049312093230, -176.4020631997491932 ) ) ;
#217104=AXIS2_PLACEMENT_3D ( 'NONE', #43886, #66013, #120884 ) ;
#217126=EDGE_CURVE ( 'NONE', #31922, #28696, #168267, .T. ) ;
#217133=FACE_OUTER_BOUND ( 'NONE', #147034, .T. ) ;
#217196=FACE_OUTER_BOUND ( 'NONE', #235941, .T. ) ;
#217202=DIRECTION ( 'NONE',  ( 1.000000000000000000, 0.000000000000000000, 0.000000000000000000 ) ) ;
#217207=CARTESIAN_POINT ( 'NONE',  ( 21.14999999999999858, 69.35000000001228670, -157.8731074845244109 ) ) ;
#217208=B_SPLINE_CURVE_WITH_KNOTS ( 'NONE', 3,
 ( #166758, #185002, #207140, #6346, #147148, #85864, #5046, #226681, #83299, #168046, #145858, #84562, #128889, #205845, #144572, #164162 ),
 .UNSPECIFIED., .F., .F.,
 ( 4, 3, 3, 3, 3, 4 ),
 ( 0.000000000000000000, 2.209833635978094077E-05, 5.595056164119032002E-05, 8.979992002654962630E-05, 0.0001236482757198868558, 0.0001574984039362969837 ),
 .UNSPECIFIED. ) ;
#217210=DIRECTION ( 'NONE',  ( -1.000000000000000000, 7.304098846218135653E-16, 4.639676173203994055E-30 ) ) ;
#217235=DIRECTION ( 'NONE',  ( -1.000000000000000000, -0.000000000000000000, -0.000000000000000000 ) ) ;
#217249=CARTESIAN_POINT ( 'NONE',  ( 18.49505832270841310, 85.43802806279519757, -162.8246343096303974 ) ) ;
#217252=ORIENTED_EDGE ( 'NONE', *, *, #117734, .T. ) ;
#217269=DIRECTION ( 'NONE',  ( 0.000000000000000000, 0.000000000000000000, 1.000000000000000000 ) ) ;
#217279=FACE_OUTER_BOUND ( 'NONE', #37309, .T. ) ;
#217313=CARTESIAN_POINT ( 'NONE',  ( 21.05000000000000071, 76.00000000001213607, -136.5231074845243313 ) ) ;
#217315=DIRECTION ( 'NONE',  ( -1.000000000000000000, 3.265361837132813093E-16, 2.280189983783949500E-30 ) ) ;
#217316=EDGE_CURVE ( 'NONE', #88042, #3049, #197425, .T. ) ;
#217330=DIRECTION ( 'NONE',  ( 0.000000000000000000, -0.9999631594459053030, -0.008583690987162452199 ) ) ;
#217342=CARTESIAN_POINT ( 'NONE',  ( -22.50000000000000000, 64.25000000001237765, -170.0231074845244166 ) ) ;
#217362=EDGE_CURVE ( 'NONE', #238448, #94706, #16518, .T. ) ;
#217403=CARTESIAN_POINT ( 'NONE',  ( 21.04999999999999716, 69.69981666374616225, -170.0744349168656129 ) ) ;
#217411=FACE_OUTER_BOUND ( 'NONE', #250954, .T. ) ;
#217454=VERTEX_POINT ( 'NONE', #81571 ) ;
#217455=ORIENTED_EDGE ( 'NONE', *, *, #186854, .T. ) ;
#217482=ORIENTED_EDGE ( 'NONE', *, *, #142978, .F. ) ;
#217487=DIRECTION ( 'NONE',  ( -0.000000000000000000, 1.000000000000000000, 6.982962677686266711E-15 ) ) ;
#217503=CARTESIAN_POINT ( 'NONE',  ( 18.52326479938734849, 85.64236444492715350, -129.8083500711180136 ) ) ;
#217559=ORIENTED_EDGE ( 'NONE', *, *, #142305, .F. ) ;
#217585=CARTESIAN_POINT ( 'NONE',  ( 23.25000000000000000, 87.75000000001246292, -181.7731074845242745 ) ) ;
#217593=DIRECTION ( 'NONE',  ( 0.000000000000000000, -6.982962677686266711E-15, 1.000000000000000000 ) ) ;
#217610=CARTESIAN_POINT ( 'NONE',  ( -20.54999999999999716, 74.05981308412438580, -149.3522266955776843 ) ) ;
#217622=CARTESIAN_POINT ( 'NONE',  ( 20.94999999999999929, 84.66355140188136374, -146.0472086025916099 ) ) ;
#217630=ORIENTED_EDGE ( 'NONE', *, *, #153670, .T. ) ;
#217633=CARTESIAN_POINT ( 'NONE',  ( -23.15000000000000213, 85.00000000001232081, -160.6291383618718385 ) ) ;
#217635=DIRECTION ( 'NONE',  ( 0.000000000000000000, 0.000000000000000000, 1.000000000000000000 ) ) ;
#217649=CARTESIAN_POINT ( 'NONE',  ( 20.94999999999999574, 74.16465844978787914, -158.4679561919613775 ) ) ;
#217719=CARTESIAN_POINT ( 'NONE',  ( 23.14999999999999858, 76.00000000001213607, -136.5231074845243313 ) ) ;
#217721=FACE_OUTER_BOUND ( 'NONE', #217928, .T. ) ;
#217727=DIRECTION ( 'NONE',  ( -0.000000000000000000, 7.272083257015735086E-15, -1.000000000000000000 ) ) ;
#217730=AXIS2_PLACEMENT_3D ( 'NONE', #204977, #208857, #48488 ) ;
#217770=EDGE_CURVE ( 'NONE', #222470, #70015, #151862, .T. ) ;
#217775=ORIENTED_EDGE ( 'NONE', *, *, #46308, .F. ) ;
#217786=ADVANCED_FACE ( 'NONE', ( #176573 ), #237814, .T. ) ;
#217800=AXIS2_PLACEMENT_3D ( 'NONE', #196624, #96237, #76675 ) ;
#217806=CARTESIAN_POINT ( 'NONE',  ( 22.60000000000000142, 76.00000000001237765, -170.0231074845243597 ) ) ;
#217822=VECTOR ( 'NONE', #38594, 1000.000000000000000 ) ;
#217840=ORIENTED_EDGE ( 'NONE', *, *, #220977, .T. ) ;
#217843=CARTESIAN_POINT ( 'NONE',  ( -21.44999999999999929, 68.65000000001222702, -148.8731074845244109 ) ) ;
#217847=VERTEX_POINT ( 'NONE', #121736 ) ;
#217860=VECTOR ( 'NONE', #248354, 1000.000000000000000 ) ;
#217888=DIRECTION ( 'NONE',  ( 0.000000000000000000, 6.938893903907222067E-15, -1.000000000000000000 ) ) ;
#217899=EDGE_LOOP ( 'NONE', ( #17008, #90913, #138349, #223909 ) ) ;
#217902=ORIENTED_EDGE ( 'NONE', *, *, #122780, .T. ) ;
#217911=CARTESIAN_POINT ( 'NONE',  ( 18.52351027002947248, 85.64216290470727699, -129.8080605340145439 ) ) ;
#217917=CARTESIAN_POINT ( 'NONE',  ( 21.10642757222115407, 65.27684371085369719, -157.7824099607392156 ) ) ;
#217928=EDGE_LOOP ( 'NONE', ( #198031, #141643, #128170, #92466 ) ) ;
#217940=DIRECTION ( 'NONE',  ( -1.000000000000000000, -0.000000000000000000, -0.000000000000000000 ) ) ;
#217947=DIRECTION ( 'NONE',  ( 0.000000000000000000, -6.982962677686266711E-15, 1.000000000000000000 ) ) ;
#217986=CARTESIAN_POINT ( 'NONE',  ( -21.05000000000000071, 74.14897176987143723, -158.3691942151018850 ) ) ;
#217992=CARTESIAN_POINT ( 'NONE',  ( 23.14999999999999858, 76.00000000001212186, -134.5231074845243313 ) ) ;
#218008=FACE_OUTER_BOUND ( 'NONE', #237781, .T. ) ;
#218013=CIRCLE ( 'NONE', #80647, 0.2000000000000057288 ) ;
#218015=FACE_OUTER_BOUND ( 'NONE', #245144, .T. ) ;
#218017=DIRECTION ( 'NONE',  ( 0.000000000000000000, 0.000000000000000000, -1.000000000000000000 ) ) ;
#218055=CARTESIAN_POINT ( 'NONE',  ( -18.39999999999999858, 85.60000000001211617, -129.9229180933022576 ) ) ;
#218059=DIRECTION ( 'NONE',  ( 1.000000000000000000, -0.000000000000000000, -0.000000000000000000 ) ) ;
#218084=ORIENTED_EDGE ( 'NONE', *, *, #133559, .T. ) ;
#218088=DIRECTION ( 'NONE',  ( -1.000000000000000000, 1.836970198721029934E-16, 1.282749433769087757E-30 ) ) ;
#218092=ORIENTED_EDGE ( 'NONE', *, *, #79432, .F. ) ;
#218093=AXIS2_PLACEMENT_3D ( 'NONE', #132588, #213389, #13930 ) ;
#218164=AXIS2_PLACEMENT_3D ( 'NONE', #156331, #235823, #134153 ) ;
#218172=CARTESIAN_POINT ( 'NONE',  ( -18.52643265882458579, 65.68026841930924320, -130.9725740131889893 ) ) ;
#218173=CARTESIAN_POINT ( 'NONE',  ( 21.13461538461538325, 67.11458296203782936, -157.6731074845244223 ) ) ;
#218179=DIRECTION ( 'NONE',  ( 0.000000000000000000, 0.000000000000000000, 1.000000000000000000 ) ) ;
#218186=VERTEX_POINT ( 'NONE', #96676 ) ;
#218196=AXIS2_PLACEMENT_3D ( 'NONE', #95009, #256598, #252793 ) ;
#218213=B_SPLINE_CURVE_WITH_KNOTS ( 'NONE', 3,
 ( #129196, #10534, #172219, #30109, #109613, #251701, #110906 ),
 .UNSPECIFIED., .F., .F.,
 ( 4, 3, 4 ),
 ( 0.000000000000000000, 0.0007844235214594318627, 0.001767853679404347454 ),
 .UNSPECIFIED. ) ;
#218222=AXIS2_PLACEMENT_3D ( 'NONE', #250223, #49459, #11635 ) ;
#218235=AXIS2_PLACEMENT_3D ( 'NONE', #51909, #114476, #53221 ) ;
#218238=CIRCLE ( 'NONE', #147539, 4.099999999999992539 ) ;
#218259=VECTOR ( 'NONE', #114313, 1000.000000000000114 ) ;
#218262=LINE ( 'NONE', #137445, #74552 ) ;
#218285=CARTESIAN_POINT ( 'NONE',  ( 23.14999999999999503, 64.35000000001218723, -143.5379132551783812 ) ) ;
#218288=CYLINDRICAL_SURFACE ( 'NONE', #66459, 0.1000000000000070832 ) ;
#218343=FACE_OUTER_BOUND ( 'NONE', #219302, .T. ) ;
#218373=CARTESIAN_POINT ( 'NONE',  ( 20.94999999999999929, 85.00000000001222134, -146.0170766071767332 ) ) ;
#218384=AXIS2_PLACEMENT_3D ( 'NONE', #176722, #99705, #76301 ) ;
#218390=CARTESIAN_POINT ( 'NONE',  ( -18.58693740092132884, 85.40643215026535984, -162.8982910280230385 ) ) ;
#218443=ORIENTED_EDGE ( 'NONE', *, *, #206567, .F. ) ;
#218445=CARTESIAN_POINT ( 'NONE',  ( 23.14999999999999858, 71.22429906543278832, -148.3718755885703331 ) ) ;
#218452=CARTESIAN_POINT ( 'NONE',  ( 18.49999999999999289, 65.79142135624952914, -148.6731074845244223 ) ) ;
#218463=VERTEX_POINT ( 'NONE', #110501 ) ;
#218490=CARTESIAN_POINT ( 'NONE',  ( 20.94999999999999929, 85.00000000001222134, -146.4170766071767389 ) ) ;
#218493=VERTEX_POINT ( 'NONE', #32286 ) ;
#218500=EDGE_CURVE ( 'NONE', #51561, #200730, #51641, .T. ) ;
#218529=ORIENTED_EDGE ( 'NONE', *, *, #225781, .F. ) ;
#218530=B_SPLINE_CURVE_WITH_KNOTS ( 'NONE', 3,
 ( #45222, #25670, #203007, #143016, #102594, #183462, #3518, #246000, #242133, #4785, #47768, #105147, #68650, #63490, #88168, #222556 ),
 .UNSPECIFIED., .F., .F.,
 ( 4, 3, 3, 3, 3, 4 ),
 ( 0.000000000000000000, 2.372700795694925591E-05, 5.739057815867077772E-05, 9.073899019181627494E-05, 0.0001243544287365772689, 0.0001585386695601308422 ),
 .UNSPECIFIED. ) ;
#218534=ORIENTED_EDGE ( 'NONE', *, *, #228730, .T. ) ;
#218547=CIRCLE ( 'NONE', #89568, 0.09999999999998898659 ) ;
#218569=EDGE_CURVE ( 'NONE', #62106, #243885, #218238, .T. ) ;
#218601=CARTESIAN_POINT ( 'NONE',  ( -23.25000000000000000, 87.65000000001246860, -181.7731074845242745 ) ) ;
#218618=VERTEX_POINT ( 'NONE', #116929 ) ;
#218638=ADVANCED_FACE ( 'NONE', ( #24267 ), #182041, .T. ) ;
#218642=EDGE_CURVE ( 'NONE', #69695, #58185, #213085, .T. ) ;
#218654=DIRECTION ( 'NONE',  ( 0.000000000000000000, 0.000000000000000000, 1.000000000000000000 ) ) ;
#218691=EDGE_CURVE ( 'NONE', #146731, #59304, #162491, .T. ) ;
#218700=DIRECTION ( 'NONE',  ( -0.000000000000000000, 0.7397360091702708251, 0.6728971962616883129 ) ) ;
#218717=AXIS2_PLACEMENT_3D ( 'NONE', #9943, #105142, #206860 ) ;
#218723=AXIS2_PLACEMENT_3D ( 'NONE', #100687, #204941, #202396 ) ;
#218739=ORIENTED_EDGE ( 'NONE', *, *, #185420, .F. ) ;
#218766=DIRECTION ( 'NONE',  ( 0.000000000000000000, -6.608470384673536035E-15, 1.000000000000000000 ) ) ;
#218772=CIRCLE ( 'NONE', #202236, 4.000000000000003553 ) ;
#218825=CARTESIAN_POINT ( 'NONE',  ( 23.15000000000000213, 87.75000000001222134, -148.6731074845242802 ) ) ;
#218827=DIRECTION ( 'NONE',  ( 0.000000000000000000, -0.4930308989875170078, -0.8700118002898356018 ) ) ;
#218857=VERTEX_POINT ( 'NONE', #35821 ) ;
#218873=CARTESIAN_POINT ( 'NONE',  ( 20.95566103547454517, 65.38175234906526612, -162.3912672915438407 ) ) ;
#218918=VECTOR ( 'NONE', #93008, 1000.000000000000000 ) ;
#218919=DIRECTION ( 'NONE',  ( 0.000000000000000000, 7.056502275159890832E-15, -1.000000000000000000 ) ) ;
#218930=AXIS2_PLACEMENT_3D ( 'NONE', #151555, #130667, #172418 ) ;
#218955=CARTESIAN_POINT ( 'NONE',  ( -21.44999999999999929, 68.65000000001222702, -148.7731074845244166 ) ) ;
#218960=FACE_OUTER_BOUND ( 'NONE', #9640, .T. ) ;
#218979=DIRECTION ( 'NONE',  ( 1.000000000000000000, -0.000000000000000000, 0.000000000000000000 ) ) ;
#219010=CARTESIAN_POINT ( 'NONE',  ( -20.94999999999999929, 77.16270174995034381, -161.9231074845243370 ) ) ;
#219035=CIRCLE ( 'NONE', #256586, 0.09999999999999938105 ) ;
#219041=FACE_OUTER_BOUND ( 'NONE', #216304, .T. ) ;
#219046=CARTESIAN_POINT ( 'NONE',  ( 19.97071067811864609, 64.27928932189355749, -145.3731074845244109 ) ) ;
#219048=CARTESIAN_POINT ( 'NONE',  ( 21.14999999999999503, 64.35000000001237197, -169.9231074845244507 ) ) ;
#219066=DIRECTION ( 'NONE',  ( -0.000000000000000000, -0.1350103645451718737, 0.9908441862701622416 ) ) ;
#219101=DIRECTION ( 'NONE',  ( -1.000000000000000000, 0.000000000000000000, 0.000000000000000000 ) ) ;
#219113=EDGE_LOOP ( 'NONE', ( #255885, #173291, #164910, #148087, #105659 ) ) ;
#219125=DIRECTION ( 'NONE',  ( -1.000000000000000000, -0.000000000000000000, -0.000000000000000000 ) ) ;
#219195=EDGE_LOOP ( 'NONE', ( #196800, #139252, #77744, #180237 ) ) ;
#219198=AXIS2_PLACEMENT_3D ( 'NONE', #238650, #219066, #23488 ) ;
#219200=VERTEX_POINT ( 'NONE', #168646 ) ;
#219225=AXIS2_PLACEMENT_3D ( 'NONE', #122550, #119999, #101647 ) ;
#219226=VERTEX_POINT ( 'NONE', #203428 ) ;
#219242=CARTESIAN_POINT ( 'NONE',  ( -23.25000000000000000, 87.75000000001215028, -136.5231074845242745 ) ) ;
#219272=ORIENTED_EDGE ( 'NONE', *, *, #129127, .F. ) ;
#219301=CYLINDRICAL_SURFACE ( 'NONE', #227324, 0.1000000000000106914 ) ;
#219302=EDGE_LOOP ( 'NONE', ( #105271, #212544, #148248, #72402 ) ) ;
#219303=LINE ( 'NONE', #163202, #91869 ) ;
#219310=DIRECTION ( 'NONE',  ( 0.000000000000000000, 0.000000000000000000, 1.000000000000000000 ) ) ;
#219321=CARTESIAN_POINT ( 'NONE',  ( 20.02499999999999858, 66.25000000001223555, -148.8731074845244393 ) ) ;
#219326=ORIENTED_EDGE ( 'NONE', *, *, #211355, .T. ) ;
#219341=VERTEX_POINT ( 'NONE', #225519 ) ;
#219352=DIRECTION ( 'NONE',  ( 1.000000000000000000, 0.000000000000000000, -0.000000000000000000 ) ) ;
#219402=CYLINDRICAL_SURFACE ( 'NONE', #83669, 0.09999999999998898659 ) ;
#219407=DIRECTION ( 'NONE',  ( 0.000000000000000000, -6.982962677686266711E-15, 1.000000000000000000 ) ) ;
#219452=FACE_OUTER_BOUND ( 'NONE', #112904, .T. ) ;
#219460=FACE_OUTER_BOUND ( 'NONE', #233135, .T. ) ;
#219468=CARTESIAN_POINT ( 'NONE',  ( -18.55807992284872299, 65.67101464000523947, -130.9404391622479977 ) ) ;
#219471=EDGE_CURVE ( 'NONE', #144130, #163114, #43860, .T. ) ;
#219478=B_SPLINE_CURVE_WITH_KNOTS ( 'NONE', 3,
 ( #25383, #144009, #223537, #239275, #60615, #69641 ),
 .UNSPECIFIED., .F., .F.,
 ( 4, 2, 4 ),
 ( 0.000000000000000000, 0.0001569047307838624609, 0.0003138094615677249218 ),
 .UNSPECIFIED. ) ;
#219491=ORIENTED_EDGE ( 'NONE', *, *, #15509, .T. ) ;
#219520=VECTOR ( 'NONE', #143176, 1000.000000000000000 ) ;
#219528=ORIENTED_EDGE ( 'NONE', *, *, #188905, .F. ) ;
#219555=FACE_OUTER_BOUND ( 'NONE', #11772, .T. ) ;
#219557=AXIS2_PLACEMENT_3D ( 'NONE', #28511, #3761, #187561 ) ;
#219579=LINE ( 'NONE', #155800, #24449 ) ;
#219607=DIRECTION ( 'NONE',  ( 0.000000000000000000, -7.086529944415886769E-15, 1.000000000000000000 ) ) ;
#219614=DIRECTION ( 'NONE',  ( 0.000000000000000000, 1.000000000000000000, 7.272083257015735086E-15 ) ) ;
#219626=CIRCLE ( 'NONE', #65506, 0.09999999999999971412 ) ;
#219640=CARTESIAN_POINT ( 'NONE',  ( 21.07928932188134397, 75.90110485435778287, -176.3516241409230929 ) ) ;
#219647=VERTEX_POINT ( 'NONE', #248826 ) ;
#219696=AXIS2_PLACEMENT_3D ( 'NONE', #196700, #178461, #96304 ) ;
#219730=DIRECTION ( 'NONE',  ( -1.000000000000000000, 0.000000000000000000, 0.000000000000000000 ) ) ;
#219750=ORIENTED_EDGE ( 'NONE', *, *, #194804, .F. ) ;
#219778=EDGE_CURVE ( 'NONE', #159949, #138157, #122972, .T. ) ;
#219843=VERTEX_POINT ( 'NONE', #158729 ) ;
#219844=VERTEX_POINT ( 'NONE', #117004 ) ;
#219861=CIRCLE ( 'NONE', #107448, 0.09999999999998898659 ) ;
#219865=VECTOR ( 'NONE', #81934, 1000.000000000000000 ) ;
#219887=CARTESIAN_POINT ( 'NONE',  ( -21.53752568622122254, 75.90102553874163505, -176.8099153590727894 ) ) ;
#219912=DIRECTION ( 'NONE',  ( -1.000000000000000000, -0.000000000000000000, -0.000000000000000000 ) ) ;
#219918=CARTESIAN_POINT ( 'NONE',  ( 21.14999999999999858, 76.00000000001237765, -169.9231074845243654 ) ) ;
#220067=CARTESIAN_POINT ( 'NONE',  ( 21.05000000000000071, 87.65000000001215597, -139.4231074845242802 ) ) ;
#220079=AXIS2_PLACEMENT_3D ( 'NONE', #48676, #104771, #243026 ) ;
#220096=CARTESIAN_POINT ( 'NONE',  ( 18.50000000000001421, 85.48068669529106955, -129.5819923157664562 ) ) ;
#220177=CYLINDRICAL_SURFACE ( 'NONE', #230364, 4.049999999999998046 ) ;
#220182=CARTESIAN_POINT ( 'NONE',  ( 20.95576188350343116, 65.39101945504891944, -162.4118737617701242 ) ) ;
#220188=DIRECTION ( 'NONE',  ( 0.000000000000000000, 0.000000000000000000, 1.000000000000000000 ) ) ;
#220196=EDGE_CURVE ( 'NONE', #208658, #16708, #232492, .T. ) ;
#220212=FACE_OUTER_BOUND ( 'NONE', #42492, .T. ) ;
#220227=ADVANCED_FACE ( 'NONE', ( #218015 ), #240184, .T. ) ;
#220239=ORIENTED_EDGE ( 'NONE', *, *, #73665, .F. ) ;
#220266=DIRECTION ( 'NONE',  ( 0.000000000000000000, -6.982962677686266711E-15, 1.000000000000000000 ) ) ;
#220269=AXIS2_PLACEMENT_3D ( 'NONE', #191868, #70637, #13212 ) ;
#220286=DIRECTION ( 'NONE',  ( 0.000000000000000000, 0.000000000000000000, 1.000000000000000000 ) ) ;
#220306=DIRECTION ( 'NONE',  ( 1.000000000000000000, 0.000000000000000000, 0.000000000000000000 ) ) ;
#220312=DIRECTION ( 'NONE',  ( 1.000000000000000000, 0.000000000000000000, 0.000000000000000000 ) ) ;
#220315=DIRECTION ( 'NONE',  ( 1.000000000000000000, 0.000000000000000000, 0.000000000000000000 ) ) ;
#220316=CARTESIAN_POINT ( 'NONE',  ( 20.94999999999999929, 85.50000000001222134, -146.4170766071767389 ) ) ;
#220349=LINE ( 'NONE', #17017, #142194 ) ;
#220354=DIRECTION ( 'NONE',  ( -7.304098846218134667E-16, 1.000000000000000000, 6.982962677686266711E-15 ) ) ;
#220360=CARTESIAN_POINT ( 'NONE',  ( 18.55807992284871588, 65.67101464000523947, -130.9404391622479977 ) ) ;
#220375=ADVANCED_FACE ( 'NONE', ( #30134 ), #67951, .F. ) ;
#220437=CARTESIAN_POINT ( 'NONE',  ( 20.93284271247462414, 64.25000000001219291, -143.5379132551784096 ) ) ;
#220494=ORIENTED_EDGE ( 'NONE', *, *, #43570, .T. ) ;
#220534=VERTEX_POINT ( 'NONE', #92640 ) ;
#220549=DIRECTION ( 'NONE',  ( 0.000000000000000000, 6.982962677686266711E-15, -1.000000000000000000 ) ) ;
#220578=CARTESIAN_POINT ( 'NONE',  ( -21.05000000000000071, 76.00000000001222134, -148.2231074845243199 ) ) ;
#220613=CARTESIAN_POINT ( 'NONE',  ( 20.94999999999999929, 76.00000000001213607, -136.5231074845243313 ) ) ;
#220620=LINE ( 'NONE', #99359, #181109 ) ;
#220635=DIRECTION ( 'NONE',  ( -1.000000000000000000, 2.952720810173289112E-16, 2.061873921506763405E-30 ) ) ;
#220643=ORIENTED_EDGE ( 'NONE', *, *, #112127, .T. ) ;
#220669=ORIENTED_EDGE ( 'NONE', *, *, #134290, .T. ) ;
#220701=TOROIDAL_SURFACE ( 'NONE', #99855, 12.77499999999999858, 0.1000000000000000056 ) ;
#220705=EDGE_CURVE ( 'NONE', #132009, #101907, #159070, .T. ) ;
#220710=CARTESIAN_POINT ( 'NONE',  ( -22.50000000000000000, 76.00000000001237765, -170.0231074845243597 ) ) ;
#220727=DIRECTION ( 'NONE',  ( 0.000000000000000000, -7.086529944415886769E-15, 1.000000000000000000 ) ) ;
#220732=CIRCLE ( 'NONE', #8368, 0.5000000000000004441 ) ;
#220786=FACE_OUTER_BOUND ( 'NONE', #121388, .T. ) ;
#220792=VECTOR ( 'NONE', #35115, 1000.000000000000000 ) ;
#220812=AXIS2_PLACEMENT_3D ( 'NONE', #164715, #120480, #139984 ) ;
#220821=ORIENTED_EDGE ( 'NONE', *, *, #247947, .T. ) ;
#220832=CARTESIAN_POINT ( 'NONE',  ( -20.54999999999999716, 68.85000000001225828, -153.2731074845244166 ) ) ;
#220869=CARTESIAN_POINT ( 'NONE',  ( -18.50000000000000000, 85.40000000001232650, -162.7258477248610120 ) ) ;
#220891=FACE_OUTER_BOUND ( 'NONE', #177124, .T. ) ;
#220900=CARTESIAN_POINT ( 'NONE',  ( -18.44362607810622023, 85.49049615809714453, -162.9651536176772026 ) ) ;
#220958=CYLINDRICAL_SURFACE ( 'NONE', #61523, 0.1000000000000118433 ) ;
#220959=FACE_OUTER_BOUND ( 'NONE', #247850, .T. ) ;
#220968=AXIS2_PLACEMENT_3D ( 'NONE', #72288, #189656, #170135 ) ;
#220977=EDGE_CURVE ( 'NONE', #200038, #177863, #73830, .T. ) ;
#220996=LINE ( 'NONE', #65790, #154502 ) ;
#220997=ADVANCED_FACE ( 'NONE', ( #113191 ), #51907, .T. ) ;
#221036=AXIS2_PLACEMENT_3D ( 'NONE', #138165, #19537, #118648 ) ;
#221050=CYLINDRICAL_SURFACE ( 'NONE', #136876, 0.1000000000000028644 ) ;
#221065=EDGE_LOOP ( 'NONE', ( #232290, #218534, #49148, #61592 ) ) ;
#221184=CARTESIAN_POINT ( 'NONE',  ( 20.46382478191414833, 67.09862044130970560, -161.4773793896413565 ) ) ;
#221205=AXIS2_PLACEMENT_3D ( 'NONE', #212982, #150462, #151755 ) ;
#221214=ORIENTED_EDGE ( 'NONE', *, *, #247314, .T. ) ;
#221266=CARTESIAN_POINT ( 'NONE',  ( -18.59999999999999787, 74.83729825007431202, -161.9231074845243654 ) ) ;
#221268=VERTEX_POINT ( 'NONE', #88145 ) ;
#221270=DIRECTION ( 'NONE',  ( 0.000000000000000000, -6.467318590049456648E-15, 1.000000000000000000 ) ) ;
#221288=CARTESIAN_POINT ( 'NONE',  ( -21.05000000000000071, 76.00000000001237765, -170.0231074845243597 ) ) ;
#221297=DIRECTION ( 'NONE',  ( 1.000000000000000000, 0.000000000000000000, 0.000000000000000000 ) ) ;
#221326=EDGE_CURVE ( 'NONE', #59416, #248967, #248977, .T. ) ;
#221328=FACE_OUTER_BOUND ( 'NONE', #141248, .T. ) ;
#221333=DIRECTION ( 'NONE',  ( 0.000000000000000000, 0.000000000000000000, 1.000000000000000000 ) ) ;
#221344=AXIS2_PLACEMENT_3D ( 'NONE', #86426, #103431, #223384 ) ;
#221379=ADVANCED_FACE ( 'NONE', ( #59282 ), #157172, .T. ) ;
#221383=CARTESIAN_POINT ( 'NONE',  ( 22.59999999999999432, 64.25043287652299284, -170.1239658536231616 ) ) ;
#221387=CARTESIAN_POINT ( 'NONE',  ( -23.25000000000000000, 69.01799029515568407, -132.8269553662681233 ) ) ;
#221392=ORIENTED_EDGE ( 'NONE', *, *, #171039, .T. ) ;
#221396=DIRECTION ( 'NONE',  ( 0.000000000000000000, -6.853228547068871147E-15, 1.000000000000000000 ) ) ;
#221434=ORIENTED_EDGE ( 'NONE', *, *, #84728, .T. ) ;
#221442=ORIENTED_EDGE ( 'NONE', *, *, #185782, .T. ) ;
#221459=EDGE_CURVE ( 'NONE', #205761, #195708, #124073, .T. ) ;
#221484=DIRECTION ( 'NONE',  ( 0.000000000000000000, 0.000000000000000000, 1.000000000000000000 ) ) ;
#221488=ORIENTED_EDGE ( 'NONE', *, *, #117959, .F. ) ;
#221511=ADVANCED_FACE ( 'NONE', ( #56719 ), #186436, .F. ) ;
#221521=DIRECTION ( 'NONE',  ( 0.000000000000000000, -8.232585987686539041E-15, 1.000000000000000000 ) ) ;
#221543=ADVANCED_FACE ( 'NONE', ( #102269 ), #65750, .T. ) ;
#221572=SPHERICAL_SURFACE ( 'NONE', #70256, 0.1000000000000000056 ) ;
#221579=ADVANCED_FACE ( 'NONE', ( #63168 ), #220958, .T. ) ;
#221588=AXIS2_PLACEMENT_3D ( 'NONE', #250620, #34190, #210242 ) ;
#221611=DIRECTION ( 'NONE',  ( 1.000000000000000000, 0.000000000000000000, 0.000000000000000000 ) ) ;
#221615=CIRCLE ( 'NONE', #254885, 0.09999999999999939493 ) ;
#221634=AXIS2_PLACEMENT_3D ( 'NONE', #149101, #169976, #55086 ) ;
#221641=ADVANCED_FACE ( 'NONE', ( #194389 ), #168763, .T. ) ;
#221699=ORIENTED_EDGE ( 'NONE', *, *, #112237, .T. ) ;
#221717=LINE ( 'NONE', #185188, #139767 ) ;
#221721=AXIS2_PLACEMENT_3D ( 'NONE', #151887, #16223, #133574 ) ;
#221726=DIRECTION ( 'NONE',  ( 0.000000000000000000, -0.8660254037844377084, -0.5000000000000016653 ) ) ;
#221733=AXIS2_PLACEMENT_3D ( 'NONE', #63873, #224217, #83401 ) ;
#221745=AXIS2_PLACEMENT_3D ( 'NONE', #211662, #252049, #113820 ) ;
#221750=ORIENTED_EDGE ( 'NONE', *, *, #137499, .F. ) ;
#221771=ORIENTED_EDGE ( 'NONE', *, *, #127393, .F. ) ;
#221780=CARTESIAN_POINT ( 'NONE',  ( 20.95263205890715952, 67.10425989211827869, -161.5335990775828066 ) ) ;
#221783=FACE_OUTER_BOUND ( 'NONE', #100037, .T. ) ;
#221839=CARTESIAN_POINT ( 'NONE',  ( 20.74897398619119215, 65.40430697834587193, -162.3437960282675192 ) ) ;
#221849=ADVANCED_FACE ( 'NONE', ( #157847 ), #23460, .T. ) ;
#221859=LINE ( 'NONE', #66672, #163201 ) ;
#221861=DIRECTION ( 'NONE',  ( 1.000000000000000000, 0.000000000000000000, 0.000000000000000000 ) ) ;
#221870=ADVANCED_FACE ( 'NONE', ( #181238 ), #102940, .F. ) ;
#221909=DIRECTION ( 'NONE',  ( 1.000000000000000000, 0.000000000000000000, 0.000000000000000000 ) ) ;
#221926=CIRCLE ( 'NONE', #134622, 11.80000000000000426 ) ;
#221950=DIRECTION ( 'NONE',  ( -1.000000000000000000, 0.000000000000000000, -0.000000000000000000 ) ) ;
#221951=EDGE_LOOP ( 'NONE', ( #203303, #81142, #120439, #245514 ) ) ;
#221958=CARTESIAN_POINT ( 'NONE',  ( -18.44448725179914206, 85.49008171549542112, -129.8941471904618368 ) ) ;
#221959=ORIENTED_EDGE ( 'NONE', *, *, #5696, .F. ) ;
#222005=ORIENTED_EDGE ( 'NONE', *, *, #99230, .T. ) ;
#222055=CARTESIAN_POINT ( 'NONE',  ( -22.39999999999999858, 76.00000000001242029, -176.2731074845243597 ) ) ;
#222060=CARTESIAN_POINT ( 'NONE',  ( -20.94999999999999929, 87.65000000001235492, -167.1231074845242688 ) ) ;
#222080=AXIS2_PLACEMENT_3D ( 'NONE', #102085, #20031, #162109 ) ;
#222094=EDGE_CURVE ( 'NONE', #174607, #189423, #61886, .T. ) ;
#222099=CIRCLE ( 'NONE', #172306, 0.09999999999998802902 ) ;
#222109=EDGE_CURVE ( 'NONE', #219226, #22920, #114513, .T. ) ;
#222168=CARTESIAN_POINT ( 'NONE',  ( 20.94999999999999929, 76.00000000001207923, -128.7231074845243484 ) ) ;
#222211=DIRECTION ( 'NONE',  ( -1.000000000000000000, -0.000000000000000000, -0.000000000000000000 ) ) ;
#222225=DIRECTION ( 'NONE',  ( -4.391705002472927119E-16, -1.000000000000000000, -7.026728003956683390E-15 ) ) ;
#222227=EDGE_LOOP ( 'NONE', ( #138463, #133839, #25589, #73808 ) ) ;
#222244=ORIENTED_EDGE ( 'NONE', *, *, #142978, .T. ) ;
#222270=CARTESIAN_POINT ( 'NONE',  ( -23.15000000000000213, 87.65000000001215597, -139.6231074845242688 ) ) ;
#222284=CARTESIAN_POINT ( 'NONE',  ( -21.55000000000000071, 68.65000000001229807, -157.6731074845243938 ) ) ;
#222324=DIRECTION ( 'NONE',  ( 2.952720810173289112E-16, 1.000000000000000000, 6.467318590049456648E-15 ) ) ;
#222373=VERTEX_POINT ( 'NONE', #145610 ) ;
#222416=CIRCLE ( 'NONE', #110022, 0.09999999999999939493 ) ;
#222424=DIRECTION ( 'NONE',  ( -1.000000000000000000, 0.000000000000000000, 0.000000000000000000 ) ) ;
#222454=CIRCLE ( 'NONE', #64268, 0.2000000000000057288 ) ;
#222459=AXIS2_PLACEMENT_3D ( 'NONE', #189886, #111630, #248569 ) ;
#222470=VERTEX_POINT ( 'NONE', #242152 ) ;
#222505=CYLINDRICAL_SURFACE ( 'NONE', #44970, 0.1000000000000033362 ) ;
#222556=CARTESIAN_POINT ( 'NONE',  ( 21.14999999999999858, 67.21339244341217523, -157.7731074845244166 ) ) ;
#222592=EDGE_CURVE ( 'NONE', #244844, #48052, #73823, .T. ) ;
#222599=ORIENTED_EDGE ( 'NONE', *, *, #158665, .F. ) ;
#222634=AXIS2_PLACEMENT_3D ( 'NONE', #116097, #216459, #172258 ) ;
#222670=CARTESIAN_POINT ( 'NONE',  ( 22.49999999999999645, 64.35012909624819599, -170.1056273753973755 ) ) ;
#222674=CARTESIAN_POINT ( 'NONE',  ( -23.15000000000000213, 71.85000000001228670, -157.6731074845243654 ) ) ;
#222692=CARTESIAN_POINT ( 'NONE',  ( -18.59999999999999787, 74.73821383144729680, -161.9366085209788935 ) ) ;
#222702=ORIENTED_EDGE ( 'NONE', *, *, #175107, .F. ) ;
#222725=CARTESIAN_POINT ( 'NONE',  ( 20.95556889135987788, 65.37805641227723186, -162.3807132626669159 ) ) ;
#222733=CARTESIAN_POINT ( 'NONE',  ( 22.47071067811865319, 68.27992525551434255, -170.1221999392270163 ) ) ;
#222753=DIRECTION ( 'NONE',  ( 0.000000000000000000, -1.000000000000000000, 0.000000000000000000 ) ) ;
#222754=LINE ( 'NONE', #119845, #219865 ) ;
#222829=VERTEX_POINT ( 'NONE', #202722 ) ;
#222852=EDGE_LOOP ( 'NONE', ( #66933, #16162, #214078, #99882 ) ) ;
#222861=CARTESIAN_POINT ( 'NONE',  ( 21.05000000000000071, 76.00000000001237765, -170.0231074845243597 ) ) ;
#222878=EDGE_CURVE ( 'NONE', #30979, #68928, #187049, .T. ) ;
#222891=ORIENTED_EDGE ( 'NONE', *, *, #247314, .F. ) ;
#222893=EDGE_LOOP ( 'NONE', ( #200125, #38005, #120039, #128760 ) ) ;
#222923=DIRECTION ( 'NONE',  ( 1.000000000000000000, 0.000000000000000000, 0.000000000000000000 ) ) ;
#222955=EDGE_CURVE ( 'NONE', #255897, #135478, #3395, .T. ) ;
#223127=DIRECTION ( 'NONE',  ( -0.000000000000000000, 0.1350103645451835865, 0.9908441862701605762 ) ) ;
#223141=DIRECTION ( 'NONE',  ( 1.000000000000000000, 0.000000000000000000, 0.000000000000000000 ) ) ;
#223147=VERTEX_POINT ( 'NONE', #253409 ) ;
#223154=ORIENTED_EDGE ( 'NONE', *, *, #242088, .F. ) ;
#223169=DIRECTION ( 'NONE',  ( 1.224646799147353207E-16, -1.000000000000000000, -6.982962677686266711E-15 ) ) ;
#223189=ADVANCED_FACE ( 'NONE', ( #35243 ), #103171, .T. ) ;
#223217=ORIENTED_EDGE ( 'NONE', *, *, #198365, .T. ) ;
#223225=CARTESIAN_POINT ( 'NONE',  ( -23.15000000000000213, 74.08971962618045382, -149.1544753397233194 ) ) ;
#223231=CARTESIAN_POINT ( 'NONE',  ( -23.15000000000000213, 74.00000000001223555, -149.1477294072864765 ) ) ;
#223246=AXIS2_PLACEMENT_3D ( 'NONE', #244886, #150932, #205757 ) ;
#223252=CARTESIAN_POINT ( 'NONE',  ( -21.05000000000000071, 69.52192177891774350, -169.9231075492199352 ) ) ;
#223257=ADVANCED_FACE ( 'NONE', ( #152621 ), #240754, .T. ) ;
#223261=CARTESIAN_POINT ( 'NONE',  ( -18.39999999999999858, 85.50000000001210765, -129.9229180933022576 ) ) ;
#223269=CARTESIAN_POINT ( 'NONE',  ( 20.95512828230159030, 67.12384868768700130, -157.8206772190212916 ) ) ;
#223273=ORIENTED_EDGE ( 'NONE', *, *, #195026, .F. ) ;
#223278=CARTESIAN_POINT ( 'NONE',  ( 18.49999999999998934, 69.55000000001230376, -160.0060803140843859 ) ) ;
#223292=VERTEX_POINT ( 'NONE', #247833 ) ;
#223308=EDGE_LOOP ( 'NONE', ( #202008, #151360, #4285, #83749 ) ) ;
#223312=DIRECTION ( 'NONE',  ( 0.000000000000000000, -0.8700118002898357128, 0.4930308989875171188 ) ) ;
#223317=VERTEX_POINT ( 'NONE', #237267 ) ;
#223358=DIRECTION ( 'NONE',  ( 0.000000000000000000, 0.000000000000000000, -1.000000000000000000 ) ) ;
#223360=CARTESIAN_POINT ( 'NONE',  ( 21.05000000000000071, 65.43728505328384415, -162.5663053788799743 ) ) ;
#223384=DIRECTION ( 'NONE',  ( 0.000000000000000000, -6.608470384673536035E-15, 1.000000000000000000 ) ) ;
#223401=ADVANCED_FACE ( 'NONE', ( #5846 ), #221050, .T. ) ;
#223412=DIRECTION ( 'NONE',  ( 0.000000000000000000, 0.000000000000000000, 1.000000000000000000 ) ) ;
#223413=ORIENTED_EDGE ( 'NONE', *, *, #170637, .T. ) ;
#223427=CARTESIAN_POINT ( 'NONE',  ( 19.97071067811864609, 64.27928932189355749, -145.2731074845244450 ) ) ;
#223460=ORIENTED_EDGE ( 'NONE', *, *, #206013, .F. ) ;
#223474=DIRECTION ( 'NONE',  ( 0.000000000000000000, -0.8660254037844377084, -0.5000000000000016653 ) ) ;
#223477=FACE_OUTER_BOUND ( 'NONE', #62291, .T. ) ;
#223493=VECTOR ( 'NONE', #108000, 1000.000000000000000 ) ;
#223498=EDGE_LOOP ( 'NONE', ( #97908, #247526, #38156, #64931 ) ) ;
#223528=CARTESIAN_POINT ( 'NONE',  ( 21.14999999999999858, 64.25000000001244871, -181.7731074845244450 ) ) ;
#223530=AXIS2_PLACEMENT_3D ( 'NONE', #160243, #217593, #179793 ) ;
#223537=CARTESIAN_POINT ( 'NONE',  ( 22.57856590037849287, 76.00412833007679581, -181.7731659471998000 ) ) ;
#223587=DIRECTION ( 'NONE',  ( 0.000000000000000000, 0.000000000000000000, 1.000000000000000000 ) ) ;
#223630=EDGE_CURVE ( 'NONE', #126961, #121672, #174337, .T. ) ;
#223637=VERTEX_POINT ( 'NONE', #130954 ) ;
#223645=VECTOR ( 'NONE', #159047, 1000.000000000000000 ) ;
#223653=DIRECTION ( 'NONE',  ( 0.000000000000000000, 0.000000000000000000, -1.000000000000000000 ) ) ;
#223709=DIRECTION ( 'NONE',  ( 0.000000000000000000, -1.000000000000000000, -6.982962677686265922E-15 ) ) ;
#223713=CARTESIAN_POINT ( 'NONE',  ( 23.15000000000000213, 85.60000000001230092, -160.1291383618718385 ) ) ;
#223714=DIRECTION ( 'NONE',  ( -3.265361837132813093E-16, -1.000000000000000000, -6.982962677686266711E-15 ) ) ;
#223721=ORIENTED_EDGE ( 'NONE', *, *, #240335, .T. ) ;
#223728=EDGE_CURVE ( 'NONE', #7914, #18470, #196073, .T. ) ;
#223753=FACE_OUTER_BOUND ( 'NONE', #187462, .T. ) ;
#223763=DIRECTION ( 'NONE',  ( -1.000000000000000000, 0.000000000000000000, -0.000000000000000000 ) ) ;
#223764=ORIENTED_EDGE ( 'NONE', *, *, #69148, .F. ) ;
#223773=DIRECTION ( 'NONE',  ( 1.000000000000000000, 0.000000000000000000, 0.000000000000000000 ) ) ;
#223792=VERTEX_POINT ( 'NONE', #172700 ) ;
#223802=AXIS2_PLACEMENT_3D ( 'NONE', #230429, #208321, #28422 ) ;
#223827=DIRECTION ( 'NONE',  ( 0.000000000000000000, -6.982962677686266711E-15, 1.000000000000000000 ) ) ;
#223832=CARTESIAN_POINT ( 'NONE',  ( 23.14999999999999858, 76.00000000001213607, -136.5231074845243313 ) ) ;
#223838=LINE ( 'NONE', #2225, #245862 ) ;
#223853=CARTESIAN_POINT ( 'NONE',  ( -23.25000000000000000, 87.65000000001238334, -170.0231074845242745 ) ) ;
#223857=DIRECTION ( 'NONE',  ( 1.000000000000000000, 0.000000000000000000, 0.000000000000000000 ) ) ;
#223873=CIRCLE ( 'NONE', #123952, 11.74999999999999645 ) ;
#223909=ORIENTED_EDGE ( 'NONE', *, *, #11040, .T. ) ;
#223929=DIRECTION ( 'NONE',  ( 0.000000000000000000, -0.1350103645451945777, 0.9908441862701590219 ) ) ;
#223942=ADVANCED_FACE ( 'NONE', ( #219460 ), #241610, .T. ) ;
#223945=CARTESIAN_POINT ( 'NONE',  ( 21.05000000000000071, 87.29603075034764004, -166.9752083248604038 ) ) ;
#223983=CARTESIAN_POINT ( 'NONE',  ( -21.05000000000000071, 87.48912529308822172, -139.6231074845242688 ) ) ;
#223986=EDGE_LOOP ( 'NONE', ( #202198, #158587, #62162, #178595 ) ) ;
#224005=EDGE_LOOP ( 'NONE', ( #53995, #121877, #224507, #90411 ) ) ;
#224033=ORIENTED_EDGE ( 'NONE', *, *, #111501, .T. ) ;
#224061=SPHERICAL_SURFACE ( 'NONE', #92503, 0.1000000000000000056 ) ;
#224065=CARTESIAN_POINT ( 'NONE',  ( -21.55000000000000071, 68.85000000001222986, -148.7731074845244166 ) ) ;
#224078=CIRCLE ( 'NONE', #257337, 0.09999999999998898659 ) ;
#224104=DIRECTION ( 'NONE',  ( -1.000000000000000000, -0.000000000000000000, -0.000000000000000000 ) ) ;
#224122=EDGE_CURVE ( 'NONE', #251542, #64025, #49756, .T. ) ;
#224152=ORIENTED_EDGE ( 'NONE', *, *, #145802, .F. ) ;
#224163=AXIS2_PLACEMENT_3D ( 'NONE', #90282, #9475, #227238 ) ;
#224169=CARTESIAN_POINT ( 'NONE',  ( -23.25000000000000000, 74.00000000001229239, -156.7984855617622770 ) ) ;
#224177=EDGE_CURVE ( 'NONE', #1798, #99053, #251870, .T. ) ;
#224192=CARTESIAN_POINT ( 'NONE',  ( 21.56666275994540172, 76.00000000001242029, -176.9804758914176830 ) ) ;
#224210=EDGE_LOOP ( 'NONE', ( #214569, #46670, #154836, #235399 ) ) ;
#224217=DIRECTION ( 'NONE',  ( 4.336808689942128965E-15, -0.8660254037844367092, 0.5000000000000037748 ) ) ;
#224229=AXIS2_PLACEMENT_3D ( 'NONE', #96526, #176116, #255572 ) ;
#224238=ORIENTED_EDGE ( 'NONE', *, *, #36832, .T. ) ;
#224241=CARTESIAN_POINT ( 'NONE',  ( 18.59999999999999076, 69.55000000001230376, -160.0060803140843859 ) ) ;
#224269=DIRECTION ( 'NONE',  ( 0.000000000000000000, -0.01562499999996560217, -0.9998779222360102414 ) ) ;
#224313=CARTESIAN_POINT ( 'NONE',  ( 20.94999999999999929, 71.00000000001223555, -148.5283735034374786 ) ) ;
#224316=ORIENTED_EDGE ( 'NONE', *, *, #68477, .T. ) ;
#224331=CARTESIAN_POINT ( 'NONE',  ( -20.64999999999999858, 74.00000000001229239, -156.7984855617622770 ) ) ;
#224352=CARTESIAN_POINT ( 'NONE',  ( 20.04142135623731136, 64.25000000001220712, -145.3731074845244109 ) ) ;
#224389=CARTESIAN_POINT ( 'NONE',  ( 18.49999999999999645, 74.36282728704190959, -158.4409541190523498 ) ) ;
#224390=FACE_OUTER_BOUND ( 'NONE', #155712, .T. ) ;
#224399=LINE ( 'NONE', #7945, #164425 ) ;
#224408=ADVANCED_FACE ( 'NONE', ( #166941 ), #147335, .F. ) ;
#224456=CARTESIAN_POINT ( 'NONE',  ( 23.14999999999999858, 76.00000000001213607, -136.5231074845243313 ) ) ;
#224476=DIRECTION ( 'NONE',  ( 0.000000000000000000, -6.982962677686266711E-15, 1.000000000000000000 ) ) ;
#224477=AXIS2_PLACEMENT_3D ( 'NONE', #119660, #81762, #180908 ) ;
#224484=CIRCLE ( 'NONE', #87099, 0.09999999999999134581 ) ;
#224499=CYLINDRICAL_SURFACE ( 'NONE', #68614, 0.09999999999998898659 ) ;
#224502=EDGE_LOOP ( 'NONE', ( #200088, #195666, #147355, #225553 ) ) ;
#224507=ORIENTED_EDGE ( 'NONE', *, *, #11192, .F. ) ;
#224517=PLANE ( 'NONE',  #138817 ) ;
#224529=ORIENTED_EDGE ( 'NONE', *, *, #179176, .F. ) ;
#224552=( BOUNDED_CURVE ( )  B_SPLINE_CURVE ( 3, ( #28318, #149537, #107813, #170413 ),
 .UNSPECIFIED., .F., .F. ) 
 B_SPLINE_CURVE_WITH_KNOTS ( ( 4, 4 ),
 ( 4.712388980384689674, 6.231880751915386263 ),
 .UNSPECIFIED. ) 
 CURVE ( )  GEOMETRIC_REPRESENTATION_ITEM ( )  RATIONAL_B_SPLINE_CURVE ( ( 1.000000000000000000, 0.8166740347213228279, 0.8166740347213228279, 1.000000000000000000 ) ) 
 REPRESENTATION_ITEM ( '' )  );
#224555=CARTESIAN_POINT ( 'NONE',  ( 21.06277459767450111, 67.12713756174402135, -157.8191082921680675 ) ) ;
#224580=VERTEX_POINT ( 'NONE', #70411 ) ;
#224656=CARTESIAN_POINT ( 'NONE',  ( -23.24999999999999645, 85.60000000001210196, -129.9229180933022576 ) ) ;
#224730=EDGE_CURVE ( 'NONE', #247235, #10361, #149918, .T. ) ;
#224740=DIRECTION ( 'NONE',  ( 0.000000000000000000, 0.000000000000000000, 1.000000000000000000 ) ) ;
#224744=EDGE_CURVE ( 'NONE', #4036, #25616, #170797, .T. ) ;
#224747=AXIS2_PLACEMENT_3D ( 'NONE', #98402, #196262, #76302 ) ;
#224752=AXIS2_PLACEMENT_3D ( 'NONE', #83249, #124984, #221484 ) ;
#224758=ORIENTED_EDGE ( 'NONE', *, *, #17210, .T. ) ;
#224816=EDGE_CURVE ( 'NONE', #223292, #191184, #191626, .T. ) ;
#224821=EDGE_CURVE ( 'NONE', #92784, #135478, #58466, .T. ) ;
#224845=CARTESIAN_POINT ( 'NONE',  ( 18.59999999999999787, 77.26327546522934142, -128.6212428177779543 ) ) ;
#224872=DIRECTION ( 'NONE',  ( -1.000000000000000000, -0.000000000000000000, -0.000000000000000000 ) ) ;
#224900=CARTESIAN_POINT ( 'NONE',  ( -23.15000000000000213, 87.65000000001238334, -170.0231074845242745 ) ) ;
#224907=LINE ( 'NONE', #207956, #32835 ) ;
#224922=CARTESIAN_POINT ( 'NONE',  ( 23.15000000000000213, 87.48912529308822172, -139.6231074845242688 ) ) ;
#224923=VERTEX_POINT ( 'NONE', #94749 ) ;
#224956=CARTESIAN_POINT ( 'NONE',  ( -21.05315837477650120, 64.25000000001220712, -143.3647514783579595 ) ) ;
#225024=DIRECTION ( 'NONE',  ( 0.000000000000000000, -6.938893903907222067E-15, 1.000000000000000000 ) ) ;
#225029=DIRECTION ( 'NONE',  ( 1.000000000000000000, 0.000000000000000000, 0.000000000000000000 ) ) ;
#225049=AXIS2_PLACEMENT_3D ( 'NONE', #62344, #102717, #41513 ) ;
#225089=EDGE_CURVE ( 'NONE', #92784, #132009, #182267, .T. ) ;
#225125=DIRECTION ( 'NONE',  ( 0.000000000000000000, 0.000000000000000000, 1.000000000000000000 ) ) ;
#225143=LINE ( 'NONE', #126050, #122090 ) ;
#225152=AXIS2_PLACEMENT_3D ( 'NONE', #216207, #59689, #199240 ) ;
#225184=DIRECTION ( 'NONE',  ( 0.000000000000000000, 1.000000000000000000, 0.000000000000000000 ) ) ;
#225207=VERTEX_POINT ( 'NONE', #229786 ) ;
#225215=DIRECTION ( 'NONE',  ( -0.000000000000000000, 1.000000000000000000, 6.982962677686266711E-15 ) ) ;
#225229=CARTESIAN_POINT ( 'NONE',  ( 22.48660254037844197, 64.35000000001237197, -170.0731074845244564 ) ) ;
#225236=ORIENTED_EDGE ( 'NONE', *, *, #218691, .T. ) ;
#225277=FACE_OUTER_BOUND ( 'NONE', #21039, .T. ) ;
#225282=CARTESIAN_POINT ( 'NONE',  ( 20.94999999999999929, 85.00000000001222134, -146.4170766071767389 ) ) ;
#225329=CARTESIAN_POINT ( 'NONE',  ( 18.59999999999999432, 77.29973367124323147, -179.9949779616549392 ) ) ;
#225343=FACE_OUTER_BOUND ( 'NONE', #109250, .T. ) ;
#225361=CARTESIAN_POINT ( 'NONE',  ( -20.64999999999999858, 76.00000000001215028, -138.5231074845243313 ) ) ;
#225367=DIRECTION ( 'NONE',  ( 0.000000000000000000, -6.982962677686266711E-15, 1.000000000000000000 ) ) ;
#225376=AXIS2_PLACEMENT_3D ( 'NONE', #138568, #219407, #18659 ) ;
#225437=ORIENTED_EDGE ( 'NONE', *, *, #179661, .T. ) ;
#225464=ORIENTED_EDGE ( 'NONE', *, *, #108225, .F. ) ;
#225491=AXIS2_PLACEMENT_3D ( 'NONE', #195312, #16661, #2193 ) ;
#225501=CARTESIAN_POINT ( 'NONE',  ( -21.14999999999999858, 76.00000000001237765, -170.0231074845243597 ) ) ;
#225519=CARTESIAN_POINT ( 'NONE',  ( -18.59999999999999787, 69.06610602788578035, -132.7374616501508342 ) ) ;
#225553=ORIENTED_EDGE ( 'NONE', *, *, #145019, .F. ) ;
#225570=ORIENTED_EDGE ( 'NONE', *, *, #4293, .T. ) ;
#225575=ORIENTED_EDGE ( 'NONE', *, *, #11389, .T. ) ;
#225588=DIRECTION ( 'NONE',  ( 1.000000000000000000, 0.000000000000000000, 0.000000000000000000 ) ) ;
#225607=DIRECTION ( 'NONE',  ( 0.000000000000000000, 0.000000000000000000, 1.000000000000000000 ) ) ;
#225620=ORIENTED_EDGE ( 'NONE', *, *, #10188, .F. ) ;
#225639=VECTOR ( 'NONE', #5066, 1000.000000000000000 ) ;
#225645=ORIENTED_EDGE ( 'NONE', *, *, #215837, .T. ) ;
#225652=EDGE_CURVE ( 'NONE', #200730, #228810, #155047, .T. ) ;
#225659=AXIS2_PLACEMENT_3D ( 'NONE', #127283, #64735, #144250 ) ;
#225686=EDGE_LOOP ( 'NONE', ( #54418, #170590, #64453, #242209 ) ) ;
#225729=CARTESIAN_POINT ( 'NONE',  ( 21.09316766718127667, 69.62984668753796313, -170.0623708868390906 ) ) ;
#225750=ADVANCED_FACE ( 'NONE', ( #16878 ), #254169, .F. ) ;
#225752=ORIENTED_EDGE ( 'NONE', *, *, #157215, .F. ) ;
#225765=FACE_OUTER_BOUND ( 'NONE', #174733, .T. ) ;
#225776=CARTESIAN_POINT ( 'NONE',  ( 21.14999999999999858, 76.10000000001238618, -170.0231074845243313 ) ) ;
#225781=EDGE_CURVE ( 'NONE', #11381, #198367, #125964, .T. ) ;
#225792=CARTESIAN_POINT ( 'NONE',  ( -20.94999999999999929, 88.41227409416185878, -139.5231074845242745 ) ) ;
#225822=CARTESIAN_POINT ( 'NONE',  ( -20.94999999999999929, 76.00000000001213607, -136.5231074845243313 ) ) ;
#225837=ORIENTED_EDGE ( 'NONE', *, *, #134187, .F. ) ;
#225848=CYLINDRICAL_SURFACE ( 'NONE', #89110, 0.09999999999999939493 ) ;
#225850=VERTEX_POINT ( 'NONE', #239765 ) ;
#225876=AXIS2_PLACEMENT_3D ( 'NONE', #79486, #39120, #118657 ) ;
#225880=AXIS2_PLACEMENT_3D ( 'NONE', #57012, #160021, #256456 ) ;
#225919=ORIENTED_EDGE ( 'NONE', *, *, #92026, .F. ) ;
#225942=LINE ( 'NONE', #85142, #197782 ) ;
#225946=FACE_OUTER_BOUND ( 'NONE', #237570, .T. ) ;
#225959=DIRECTION ( 'NONE',  ( 1.000000000000000000, 0.000000000000000000, 0.000000000000000000 ) ) ;
#225980=AXIS2_PLACEMENT_3D ( 'NONE', #137175, #81031, #138435 ) ;
#225990=CARTESIAN_POINT ( 'NONE',  ( -20.64999999999999858, 84.66355140188136374, -146.0472086025916099 ) ) ;
#225991=CARTESIAN_POINT ( 'NONE',  ( -21.05000000000000071, 74.16465844978787914, -158.3679561919613832 ) ) ;
#225993=EDGE_LOOP ( 'NONE', ( #17276, #84365, #252243, #151677 ) ) ;
#225997=EDGE_CURVE ( 'NONE', #167959, #44364, #55304, .T. ) ;
#226027=CARTESIAN_POINT ( 'NONE',  ( 21.05000000000000071, 85.00000000001222134, -146.4170766071767389 ) ) ;
#226029=CARTESIAN_POINT ( 'NONE',  ( -23.25000000000000000, 76.00000000001213607, -136.5231074845243313 ) ) ;
#226048=AXIS2_PLACEMENT_3D ( 'NONE', #12637, #214655, #13907 ) ;
#226078=DIRECTION ( 'NONE',  ( 0.000000000000000000, 0.9908441862701791170, -0.1350103645450472789 ) ) ;
#226092=VECTOR ( 'NONE', #216771, 1000.000000000000000 ) ;
#226103=CIRCLE ( 'NONE', #51137, 0.09999999999998898659 ) ;
#226119=LINE ( 'NONE', #230986, #158586 ) ;
#226172=DIRECTION ( 'NONE',  ( 0.000000000000000000, 0.000000000000000000, 1.000000000000000000 ) ) ;
#226182=EDGE_LOOP ( 'NONE', ( #144, #12843, #184170, #230338, #88639, #184104, #73521 ) ) ;
#226195=EDGE_LOOP ( 'NONE', ( #145779, #148455, #159209, #192503 ) ) ;
#226197=DIRECTION ( 'NONE',  ( 0.000000000000000000, -6.982962677686266711E-15, 1.000000000000000000 ) ) ;
#226266=DIRECTION ( 'NONE',  ( 1.000000000000000000, 0.000000000000000000, 0.000000000000000000 ) ) ;
#226276=FACE_OUTER_BOUND ( 'NONE', #241383, .T. ) ;
#226308=VERTEX_POINT ( 'NONE', #183334 ) ;
#226328=DIRECTION ( 'NONE',  ( 0.000000000000000000, -1.000000000000000000, 0.000000000000000000 ) ) ;
#226331=ADVANCED_FACE ( 'NONE', ( #226276 ), #201267, .T. ) ;
#226336=CIRCLE ( 'NONE', #64058, 0.09999999999998898659 ) ;
#226352=CIRCLE ( 'NONE', #39148, 0.1000000000000033362 ) ;
#226362=DIRECTION ( 'NONE',  ( 1.000000000000000000, 0.000000000000000000, 0.000000000000000000 ) ) ;
#226384=VECTOR ( 'NONE', #20554, 1000.000000000000000 ) ;
#226413=VECTOR ( 'NONE', #250519, 1000.000000000000000 ) ;
#226415=CIRCLE ( 'NONE', #151652, 3.900000000000000799 ) ;
#226421=AXIS2_PLACEMENT_3D ( 'NONE', #116713, #41057, #140108 ) ;
#226440=CARTESIAN_POINT ( 'NONE',  ( 20.94999999999999929, 68.87972903831452243, -132.8635444426850825 ) ) ;
#226472=CARTESIAN_POINT ( 'NONE',  ( -20.94999999999999929, 65.70729864261026876, -131.0657455973724836 ) ) ;
#226480=AXIS2_PLACEMENT_3D ( 'NONE', #17464, #95707, #193550 ) ;
#226487=FACE_OUTER_BOUND ( 'NONE', #122403, .T. ) ;
#226503=EDGE_LOOP ( 'NONE', ( #229402, #178087, #72245, #178815 ) ) ;
#226510=CARTESIAN_POINT ( 'NONE',  ( 18.60000000000000497, 85.36423601037908782, -162.8428530837996675 ) ) ;
#226518=DIRECTION ( 'NONE',  ( -0.7071067811865127117, -0.7071067811865821007, 0.000000000000000000 ) ) ;
#226529=DIRECTION ( 'NONE',  ( 0.000000000000000000, -1.000000000000000000, -7.272083257015735086E-15 ) ) ;
#226566=DIRECTION ( 'NONE',  ( 1.000000000000000000, 0.000000000000000000, 0.000000000000000000 ) ) ;
#226568=DIRECTION ( 'NONE',  ( 0.000000000000000000, 0.000000000000000000, 1.000000000000000000 ) ) ;
#226574=ORIENTED_EDGE ( 'NONE', *, *, #146392, .F. ) ;
#226667=ADVANCED_FACE ( 'NONE', ( #123056 ), #64094, .F. ) ;
#226678=DIRECTION ( 'NONE',  ( 1.000000000000000000, 0.000000000000000000, 0.000000000000000000 ) ) ;
#226681=CARTESIAN_POINT ( 'NONE',  ( 22.46250603428203618, 75.97885582387365844, -181.6729705818644334 ) ) ;
#226694=CARTESIAN_POINT ( 'NONE',  ( -18.59999999999999787, 64.35000000001222986, -148.6731074845244507 ) ) ;
#226720=EDGE_LOOP ( 'NONE', ( #49208, #245496, #239083, #27355 ) ) ;
#226723=AXIS2_PLACEMENT_3D ( 'NONE', #11468, #210939, #251330 ) ;
#226728=DIRECTION ( 'NONE',  ( 1.000000000000000000, 0.000000000000000000, 0.000000000000000000 ) ) ;
#226745=ORIENTED_EDGE ( 'NONE', *, *, #114632, .T. ) ;
#226764=CIRCLE ( 'NONE', #168565, 0.09999999999998898659 ) ;
#226835=LINE ( 'NONE', #5192, #189346 ) ;
#226867=VERTEX_POINT ( 'NONE', #2645 ) ;
#226870=CARTESIAN_POINT ( 'NONE',  ( 22.39999999999999503, 75.90000000001242597, -176.2731074845243597 ) ) ;
#226914=ORIENTED_EDGE ( 'NONE', *, *, #248266, .T. ) ;
#226950=AXIS2_PLACEMENT_3D ( 'NONE', #211707, #246947, #30502 ) ;
#226961=ORIENTED_EDGE ( 'NONE', *, *, #227726, .T. ) ;
#226973=DIRECTION ( 'NONE',  ( 1.000000000000000000, 0.000000000000000000, 0.000000000000000000 ) ) ;
#227000=DIRECTION ( 'NONE',  ( 0.000000000000000000, -0.008583690987162452199, 0.9999631594459053030 ) ) ;
#227003=DIRECTION ( 'NONE',  ( 0.000000000000000000, -6.982962677686266711E-15, 1.000000000000000000 ) ) ;
#227035=LINE ( 'NONE', #30148, #71882 ) ;
#227106=CARTESIAN_POINT ( 'NONE',  ( 23.25000000000000355, 98.45632476063525473, -163.2292090367925823 ) ) ;
#227115=ORIENTED_EDGE ( 'NONE', *, *, #74173, .F. ) ;
#227120=SPHERICAL_SURFACE ( 'NONE', #217730, 0.1000000000000000056 ) ;
#227133=TOROIDAL_SURFACE ( 'NONE', #85443, 0.9750000000000019762, 0.1000000000000000056 ) ;
#227156=CARTESIAN_POINT ( 'NONE',  ( 20.94999999999999929, 71.14953271029261828, -148.5573748935260880 ) ) ;
#227192=DIRECTION ( 'NONE',  ( 1.000000000000000000, 0.000000000000000000, 0.000000000000000000 ) ) ;
#227218=VERTEX_POINT ( 'NONE', #255320 ) ;
#227238=DIRECTION ( 'NONE',  ( 0.000000000000000000, 1.000000000000000000, 0.000000000000000000 ) ) ;
#227240=FACE_OUTER_BOUND ( 'NONE', #120749, .T. ) ;
#227250=DIRECTION ( 'NONE',  ( 0.000000000000000000, 0.000000000000000000, 1.000000000000000000 ) ) ;
#227260=LINE ( 'NONE', #69503, #125189 ) ;
#227324=AXIS2_PLACEMENT_3D ( 'NONE', #41976, #250, #121522 ) ;
#227329=DIRECTION ( 'NONE',  ( 0.000000000000000000, -6.467318590049456648E-15, 1.000000000000000000 ) ) ;
#227362=VERTEX_POINT ( 'NONE', #240951 ) ;
#227403=EDGE_CURVE ( 'NONE', #29869, #128626, #93483, .T. ) ;
#227417=ORIENTED_EDGE ( 'NONE', *, *, #117301, .T. ) ;
#227430=ADVANCED_FACE ( 'NONE', ( #123568 ), #182266, .F. ) ;
#227532=EDGE_CURVE ( 'NONE', #10427, #72750, #218547, .T. ) ;
#227547=VECTOR ( 'NONE', #133375, 1000.000000000000000 ) ;
#227552=ORIENTED_EDGE ( 'NONE', *, *, #54532, .F. ) ;
#227556=TOROIDAL_SURFACE ( 'NONE', #115153, 3.899999999999999467, 0.1000000000000000056 ) ;
#227561=DIRECTION ( 'NONE',  ( 1.000000000000000000, 0.000000000000000000, 0.000000000000000000 ) ) ;
#227596=DIRECTION ( 'NONE',  ( 0.000000000000000000, 0.8660254037844420383, -0.4999999999999943379 ) ) ;
#227632=AXIS2_PLACEMENT_3D ( 'NONE', #182667, #4005, #6573 ) ;
#227642=EDGE_CURVE ( 'NONE', #183531, #174107, #176906, .T. ) ;
#227663=FACE_OUTER_BOUND ( 'NONE', #180102, .T. ) ;
#227694=CARTESIAN_POINT ( 'NONE',  ( 18.47688499308725341, 85.46485595029625415, -129.8217597313868623 ) ) ;
#227698=ORIENTED_EDGE ( 'NONE', *, *, #154407, .T. ) ;
#227713=FACE_OUTER_BOUND ( 'NONE', #214341, .T. ) ;
#227723=DIRECTION ( 'NONE',  ( -0.000000000000000000, 1.000000000000000000, 6.982962677686267499E-15 ) ) ;
#227726=EDGE_CURVE ( 'NONE', #5518, #51370, #241904, .T. ) ;
#227758=EDGE_LOOP ( 'NONE', ( #191780, #194014, #244884, #250408 ) ) ;
#227785=ORIENTED_EDGE ( 'NONE', *, *, #49668, .F. ) ;
#227788=DIRECTION ( 'NONE',  ( 1.000000000000000000, 0.000000000000000000, 0.000000000000000000 ) ) ;
#227846=CARTESIAN_POINT ( 'NONE',  ( 18.49999999999999645, 76.00000000001237765, -170.0231074845243597 ) ) ;
#227857=ORIENTED_EDGE ( 'NONE', *, *, #132173, .F. ) ;
#227873=CARTESIAN_POINT ( 'NONE',  ( -21.04999999999999716, 85.60000000001232934, -162.9910380878246201 ) ) ;
#227882=CARTESIAN_POINT ( 'NONE',  ( -20.94999999999999929, 68.97833521811203639, -132.8895420826271163 ) ) ;
#227885=CARTESIAN_POINT ( 'NONE',  ( 21.53551880898956838, 69.21520223859606347, -170.1220772190960702 ) ) ;
#227896=AXIS2_PLACEMENT_3D ( 'NONE', #233003, #76458, #13940 ) ;
#227931=ORIENTED_EDGE ( 'NONE', *, *, #75155, .T. ) ;
#227957=EDGE_CURVE ( 'NONE', #168984, #112163, #178782, .T. ) ;
#228004=DIRECTION ( 'NONE',  ( 1.000000000000000000, 0.000000000000000000, 0.000000000000000000 ) ) ;
#228006=DIRECTION ( 'NONE',  ( 1.000000000000000000, 0.000000000000000000, 0.000000000000000000 ) ) ;
#228007=FACE_OUTER_BOUND ( 'NONE', #112103, .T. ) ;
#228027=DIRECTION ( 'NONE',  ( 0.000000000000000000, -6.982962677686266711E-15, 1.000000000000000000 ) ) ;
#228029=CARTESIAN_POINT ( 'NONE',  ( -18.59999999999999787, 77.25000000001209344, -128.7226267301092548 ) ) ;
#228053=CYLINDRICAL_SURFACE ( 'NONE', #166600, 7.899999999999990585 ) ;
#228060=DIRECTION ( 'NONE',  ( 0.000000000000000000, 0.000000000000000000, 1.000000000000000000 ) ) ;
#228071=AXIS2_PLACEMENT_3D ( 'NONE', #193650, #211935, #251028 ) ;
#228112=ORIENTED_EDGE ( 'NONE', *, *, #105663, .T. ) ;
#228113=CARTESIAN_POINT ( 'NONE',  ( -20.54999999999999716, 85.00000000001222134, -146.0170766071767332 ) ) ;
#228128=ORIENTED_EDGE ( 'NONE', *, *, #111916, .T. ) ;
#228129=DIRECTION ( 'NONE',  ( 0.000000000000000000, 1.000000000000000000, 0.000000000000000000 ) ) ;
#228225=CYLINDRICAL_SURFACE ( 'NONE', #33200, 0.09999999999999939493 ) ;
#228232=ORIENTED_EDGE ( 'NONE', *, *, #126226, .T. ) ;
#228233=AXIS2_PLACEMENT_3D ( 'NONE', #52712, #215634, #76133 ) ;
#228247=EDGE_LOOP ( 'NONE', ( #17439, #11169, #19920, #105474 ) ) ;
#228249=ORIENTED_EDGE ( 'NONE', *, *, #195351, .F. ) ;
#228278=DIRECTION ( 'NONE',  ( 0.000000000000000000, -1.000000000000000000, -6.982962677686266711E-15 ) ) ;
#228287=AXIS2_PLACEMENT_3D ( 'NONE', #165764, #245287, #104452 ) ;
#228310=VERTEX_POINT ( 'NONE', #257924 ) ;
#228328=CARTESIAN_POINT ( 'NONE',  ( -21.11927991906891222, 75.99091632053855960, -176.4716006030158724 ) ) ;
#228334=CARTESIAN_POINT ( 'NONE',  ( 21.10320863425824811, 69.59972261355321166, -170.0481297357515302 ) ) ;
#228341=DIRECTION ( 'NONE',  ( 1.000000000000000000, 0.000000000000000000, 0.000000000000000000 ) ) ;
#228376=AXIS2_PLACEMENT_3D ( 'NONE', #203309, #3819, #145884 ) ;
#228402=AXIS2_PLACEMENT_3D ( 'NONE', #14432, #172240, #187917 ) ;
#228492=ORIENTED_EDGE ( 'NONE', *, *, #173760, .T. ) ;
#228498=FACE_OUTER_BOUND ( 'NONE', #6522, .T. ) ;
#228499=VERTEX_POINT ( 'NONE', #94737 ) ;
#228515=ORIENTED_EDGE ( 'NONE', *, *, #249904, .T. ) ;
#228531=CARTESIAN_POINT ( 'NONE',  ( -20.94999999999999929, 68.92903212821327941, -132.7765432626560766 ) ) ;
#228549=EDGE_LOOP ( 'NONE', ( #186752, #220239, #232012, #146942 ) ) ;
#228560=CARTESIAN_POINT ( 'NONE',  ( -21.14999999999999503, 64.25000000001233502, -163.1039602385656337 ) ) ;
#228564=CARTESIAN_POINT ( 'NONE',  ( -23.15000000000000213, 74.00000000001229239, -156.7984855617622770 ) ) ;
#228568=VERTEX_POINT ( 'NONE', #129998 ) ;
#228607=ORIENTED_EDGE ( 'NONE', *, *, #216633, .F. ) ;
#228610=EDGE_CURVE ( 'NONE', #25144, #218493, #115080, .T. ) ;
#228634=ORIENTED_EDGE ( 'NONE', *, *, #45645, .T. ) ;
#228636=CIRCLE ( 'NONE', #186948, 11.64999999999999325 ) ;
#228638=CARTESIAN_POINT ( 'NONE',  ( -20.94999999999999929, 77.16270174995034381, -162.0231074845243313 ) ) ;
#228643=DIRECTION ( 'NONE',  ( 0.000000000000000000, -1.000000000000000000, -6.982962677686266711E-15 ) ) ;
#228656=SPHERICAL_SURFACE ( 'NONE', #138884, 0.1000000000000000056 ) ;
#228663=DIRECTION ( 'NONE',  ( 0.000000000000000000, -0.9908441862701420355, -0.1350103645453197554 ) ) ;
#228729=CARTESIAN_POINT ( 'NONE',  ( 18.59999999999999076, 64.35000000001214460, -136.5231074845244166 ) ) ;
#228730=EDGE_CURVE ( 'NONE', #6455, #7639, #162443, .T. ) ;
#228737=DIRECTION ( 'NONE',  ( 0.000000000000000000, -1.000000000000000000, 0.000000000000000000 ) ) ;
#228771=ORIENTED_EDGE ( 'NONE', *, *, #234927, .F. ) ;
#228789=CARTESIAN_POINT ( 'NONE',  ( 22.39999999999999503, 75.90000000001242597, -177.8138870828977360 ) ) ;
#228793=SPHERICAL_SURFACE ( 'NONE', #220968, 0.1000000000000000056 ) ;
#228799=ORIENTED_EDGE ( 'NONE', *, *, #8767, .F. ) ;
#228802=EDGE_LOOP ( 'NONE', ( #78045, #41889, #115433, #59489, #61418, #73260, #196379, #48450, #195693, #74993, #49706 ) ) ;
#228810=VERTEX_POINT ( 'NONE', #204104 ) ;
#228857=DIRECTION ( 'NONE',  ( 0.000000000000000000, -6.467318590049456648E-15, 1.000000000000000000 ) ) ;
#228886=AXIS2_PLACEMENT_3D ( 'NONE', #256899, #159163, #40514 ) ;
#228912=ORIENTED_EDGE ( 'NONE', *, *, #159458, .T. ) ;
#228930=CARTESIAN_POINT ( 'NONE',  ( -22.59999999999999787, 64.25043287652299284, -170.1239658536231616 ) ) ;
#228975=EDGE_CURVE ( 'NONE', #10427, #186771, #123639, .T. ) ;
#228988=DIRECTION ( 'NONE',  ( -1.000000000000000000, -0.000000000000000000, -0.000000000000000000 ) ) ;
#229013=CARTESIAN_POINT ( 'NONE',  ( 22.50000000000000000, 75.90000000001242597, -177.8138870828977360 ) ) ;
#229016=ADVANCED_FACE ( 'NONE', ( #134820 ), #215651, .T. ) ;
#229041=DIRECTION ( 'NONE',  ( 0.000000000000000000, 0.3738317757009942399, -0.9274965247785252886 ) ) ;
#229054=ORIENTED_EDGE ( 'NONE', *, *, #24101, .F. ) ;
#229065=ADVANCED_FACE ( 'NONE', ( #78706 ), #46013, .F. ) ;
#229088=CARTESIAN_POINT ( 'NONE',  ( -23.25000000000000000, 87.75000000001246292, -181.7731074845242745 ) ) ;
#229147=ORIENTED_EDGE ( 'NONE', *, *, #142557, .F. ) ;
#229164=DIRECTION ( 'NONE',  ( 0.000000000000000000, -6.853228547068871147E-15, 1.000000000000000000 ) ) ;
#229167=DIRECTION ( 'NONE',  ( 1.000000000000000000, 0.000000000000000000, 0.000000000000000000 ) ) ;
#229169=DIRECTION ( 'NONE',  ( -0.000000000000000000, 1.000000000000000000, 6.982962677686267499E-15 ) ) ;
#229192=ADVANCED_FACE ( 'NONE', ( #6890 ), #121728, .T. ) ;
#229200=AXIS2_PLACEMENT_3D ( 'NONE', #16057, #133414, #233806 ) ;
#229230=EDGE_CURVE ( 'NONE', #90874, #164553, #63008, .T. ) ;
#229236=VERTEX_POINT ( 'NONE', #30329 ) ;
#229243=DIRECTION ( 'NONE',  ( 0.000000000000000000, -6.769652589177795712E-15, 1.000000000000000000 ) ) ;
#229266=CARTESIAN_POINT ( 'NONE',  ( 20.84451136049622377, 65.37985808520402031, -162.5291829250029991 ) ) ;
#229324=AXIS2_PLACEMENT_3D ( 'NONE', #38121, #118942, #197166 ) ;
#229347=DIRECTION ( 'NONE',  ( 0.000000000000000000, 6.982962677686266711E-15, -1.000000000000000000 ) ) ;
#229354=VERTEX_POINT ( 'NONE', #35485 ) ;
#229363=ADVANCED_FACE ( 'NONE', ( #95423 ), #178851, .T. ) ;
#229384=ORIENTED_EDGE ( 'NONE', *, *, #24625, .F. ) ;
#229397=CARTESIAN_POINT ( 'NONE',  ( 20.95392731769792150, 67.11693852082356671, -161.5008795049531329 ) ) ;
#229402=ORIENTED_EDGE ( 'NONE', *, *, #244689, .T. ) ;
#229477=DIRECTION ( 'NONE',  ( 0.000000000000000000, -0.1568667991644355497, -0.9876197685951332295 ) ) ;
#229478=ORIENTED_EDGE ( 'NONE', *, *, #98490, .F. ) ;
#229551=CARTESIAN_POINT ( 'NONE',  ( -23.15000000000000213, 64.35000000001228670, -157.8731074845244393 ) ) ;
#229564=EDGE_LOOP ( 'NONE', ( #95112, #131269, #205154 ) ) ;
#229586=CARTESIAN_POINT ( 'NONE',  ( -18.59999999999999787, 64.25000000001246292, -181.7731074845244450 ) ) ;
#229591=VECTOR ( 'NONE', #26413, 999.9999999999998863 ) ;
#229604=AXIS2_PLACEMENT_3D ( 'NONE', #111625, #232878, #192448 ) ;
#229607=DIRECTION ( 'NONE',  ( 0.000000000000000000, -6.982962677686266711E-15, 1.000000000000000000 ) ) ;
#229627=VECTOR ( 'NONE', #178312, 1000.000000000000000 ) ;
#229711=AXIS2_PLACEMENT_3D ( 'NONE', #40658, #181428, #82269 ) ;
#229718=CARTESIAN_POINT ( 'NONE',  ( -18.39999999999999858, 85.50000000001233502, -162.9910380878246201 ) ) ;
#229744=ORIENTED_EDGE ( 'NONE', *, *, #16448, .F. ) ;
#229777=TOROIDAL_SURFACE ( 'NONE', #175629, 0.4000000000000003553, 0.1000000000000000056 ) ;
#229786=CARTESIAN_POINT ( 'NONE',  ( -20.94999999999999929, 77.73625713160970463, -158.4544551555068495 ) ) ;
#229797=CARTESIAN_POINT ( 'NONE',  ( -21.14999999999999858, 64.25000000001237765, -170.0231074845244166 ) ) ;
#229813=ORIENTED_EDGE ( 'NONE', *, *, #114556, .T. ) ;
#229822=DIRECTION ( 'NONE',  ( -1.000000000000000000, -0.000000000000000000, -0.000000000000000000 ) ) ;
#229836=DIRECTION ( 'NONE',  ( -0.000000000000000000, -0.8660254037844377084, -0.5000000000000016653 ) ) ;
#229873=CIRCLE ( 'NONE', #117458, 0.09999999999999939493 ) ;
#229889=CARTESIAN_POINT ( 'NONE',  ( -22.39999999999999858, 64.35000000001238618, -170.1231074845244393 ) ) ;
#229903=DIRECTION ( 'NONE',  ( 0.000000000000000000, 0.000000000000000000, 1.000000000000000000 ) ) ;
#229926=CARTESIAN_POINT ( 'NONE',  ( -18.50000000000000711, 64.35000000001234355, -163.0083017138704236 ) ) ;
#229933=AXIS2_PLACEMENT_3D ( 'NONE', #104153, #125031, #3790 ) ;
#229954=ORIENTED_EDGE ( 'NONE', *, *, #224730, .T. ) ;
#229964=ADVANCED_FACE ( 'NONE', ( #117258 ), #157710, .F. ) ;
#229965=VERTEX_POINT ( 'NONE', #161530 ) ;
#229971=ADVANCED_FACE ( 'NONE', ( #220212 ), #140553, .T. ) ;
#229972=CYLINDRICAL_SURFACE ( 'NONE', #85704, 0.09999999999998898659 ) ;
#229982=DIRECTION ( 'NONE',  ( 0.000000000000000000, 0.9908441862701791170, -0.1350103645450472789 ) ) ;
#230096=CARTESIAN_POINT ( 'NONE',  ( 20.94999999999999929, 76.00000000001213607, -136.5231074845243313 ) ) ;
#230101=CARTESIAN_POINT ( 'NONE',  ( 21.05000000000000071, 76.00000000001215028, -138.5231074845243313 ) ) ;
#230104=CARTESIAN_POINT ( 'NONE',  ( 18.59999999999999076, 77.83585931145570669, -124.9186683157258244 ) ) ;
#230106=ORIENTED_EDGE ( 'NONE', *, *, #210180, .T. ) ;
#230138=CARTESIAN_POINT ( 'NONE',  ( 20.99780126800921209, 64.39461131213559497, -143.4357549128189646 ) ) ;
#230247=CARTESIAN_POINT ( 'NONE',  ( 20.95512820512820440, 67.12384868372411972, -148.7731074845244166 ) ) ;
#230256=LINE ( 'NONE', #35937, #191386 ) ;
#230279=ORIENTED_EDGE ( 'NONE', *, *, #98480, .T. ) ;
#230282=AXIS2_PLACEMENT_3D ( 'NONE', #52487, #206765, #152924 ) ;
#230293=CARTESIAN_POINT ( 'NONE',  ( -23.15000000000000213, 76.00000000001237765, -170.0231074845243597 ) ) ;
#230308=FACE_OUTER_BOUND ( 'NONE', #142190, .T. ) ;
#230316=CIRCLE ( 'NONE', #172114, 0.5999999999999894307 ) ;
#230324=ORIENTED_EDGE ( 'NONE', *, *, #129975, .F. ) ;
#230338=ORIENTED_EDGE ( 'NONE', *, *, #206818, .T. ) ;
#230362=ORIENTED_EDGE ( 'NONE', *, *, #211593, .F. ) ;
#230364=AXIS2_PLACEMENT_3D ( 'NONE', #41560, #248723, #229164 ) ;
#230411=FACE_OUTER_BOUND ( 'NONE', #33604, .T. ) ;
#230429=CARTESIAN_POINT ( 'NONE',  ( -21.05000000000000071, 76.00000000001213607, -136.5231074845243313 ) ) ;
#230442=ORIENTED_EDGE ( 'NONE', *, *, #125512, .F. ) ;
#230446=DIRECTION ( 'NONE',  ( -0.000000000000000000, -0.1350103645451835865, -0.9908441862701606873 ) ) ;
#230503=ORIENTED_EDGE ( 'NONE', *, *, #215719, .T. ) ;
#230504=VERTEX_POINT ( 'NONE', #150317 ) ;
#230506=DIRECTION ( 'NONE',  ( -1.000000000000000000, 0.000000000000000000, -0.000000000000000000 ) ) ;
#230525=CARTESIAN_POINT ( 'NONE',  ( 21.14999999999999858, 65.28660755661240955, -157.7731074845244166 ) ) ;
#230535=DIRECTION ( 'NONE',  ( 0.000000000000000000, 7.026728003956695223E-15, -1.000000000000000000 ) ) ;
#230537=CARTESIAN_POINT ( 'NONE',  ( -23.15000000000000213, 71.65000000001222702, -148.6731074845243938 ) ) ;
#230556=ORIENTED_EDGE ( 'NONE', *, *, #65839, .F. ) ;
#230557=ORIENTED_EDGE ( 'NONE', *, *, #30871, .F. ) ;
#230558=DIRECTION ( 'NONE',  ( -2.952720810173289112E-16, -1.000000000000000000, -6.982962677686266711E-15 ) ) ;
#230564=ORIENTED_EDGE ( 'NONE', *, *, #34909, .T. ) ;
#230568=FACE_OUTER_BOUND ( 'NONE', #104581, .T. ) ;
#230578=ORIENTED_EDGE ( 'NONE', *, *, #14106, .T. ) ;
#230599=CARTESIAN_POINT ( 'NONE',  ( -21.05000000000000071, 76.00000000001237765, -170.0231074845243597 ) ) ;
#230621=EDGE_CURVE ( 'NONE', #26287, #20561, #215407, .T. ) ;
#230630=CARTESIAN_POINT ( 'NONE',  ( -20.54999999999999716, 85.40000000001231228, -160.1291383618718385 ) ) ;
#230636=DIRECTION ( 'NONE',  ( 0.000000000000000000, -1.000000000000000000, -6.982962677686266711E-15 ) ) ;
#230717=EDGE_LOOP ( 'NONE', ( #20706, #125163, #196425, #73006 ) ) ;
#230733=VERTEX_POINT ( 'NONE', #224389 ) ;
#230745=AXIS2_PLACEMENT_3D ( 'NONE', #203196, #247458, #84484 ) ;
#230784=CARTESIAN_POINT ( 'NONE',  ( 23.14999999999999858, 76.00000000001213607, -136.5231074845243313 ) ) ;
#230785=EDGE_CURVE ( 'NONE', #76888, #94890, #22372, .T. ) ;
#230829=EDGE_LOOP ( 'NONE', ( #230557, #225437, #75707, #164884, #111147, #251960 ) ) ;
#230842=DIRECTION ( 'NONE',  ( 1.000000000000000000, -6.938893903907222067E-15, -4.845403715540888588E-29 ) ) ;
#230866=DIRECTION ( 'NONE',  ( -1.000000000000000000, 0.000000000000000000, 0.000000000000000000 ) ) ;
#230868=DIRECTION ( 'NONE',  ( -1.000000000000000000, 0.000000000000000000, 0.000000000000000000 ) ) ;
#230878=CARTESIAN_POINT ( 'NONE',  ( 23.14999999999999858, 69.35000000001228670, -157.6731074845243938 ) ) ;
#230911=DIRECTION ( 'NONE',  ( -3.469446951953515108E-14, -1.000000000000000000, 0.000000000000000000 ) ) ;
#230915=CARTESIAN_POINT ( 'NONE',  ( 21.14999999999999858, 69.45934304831114048, -170.0231074845243882 ) ) ;
#230927=EDGE_CURVE ( 'NONE', #188264, #251940, #131990, .T. ) ;
#230930=DIRECTION ( 'NONE',  ( 0.000000000000000000, 0.000000000000000000, 1.000000000000000000 ) ) ;
#230942=CARTESIAN_POINT ( 'NONE',  ( -20.64999999999999858, 73.60000000001230092, -156.7984855617622770 ) ) ;
#230986=CARTESIAN_POINT ( 'NONE',  ( -23.25000000000000000, 87.75000000001236344, -166.9231074845242802 ) ) ;
#231030=CARTESIAN_POINT ( 'NONE',  ( 23.15000000000000213, 87.48912529308822172, -139.5231074845243029 ) ) ;
#231039=DIRECTION ( 'NONE',  ( -0.000000000000000000, 6.982962677686266711E-15, -1.000000000000000000 ) ) ;
#231046=CARTESIAN_POINT ( 'NONE',  ( 18.59999999999999076, 64.25000000001232081, -161.9231074845244223 ) ) ;
#231062=CARTESIAN_POINT ( 'NONE',  ( -20.64999999999999858, 68.75000000001230660, -157.6731074845243938 ) ) ;
#231077=ORIENTED_EDGE ( 'NONE', *, *, #225652, .F. ) ;
#231125=DIRECTION ( 'NONE',  ( 0.000000000000000000, 0.000000000000000000, 1.000000000000000000 ) ) ;
#231130=FILL_AREA_STYLE ('',( #154186 ) ) ;
#231161=DIRECTION ( 'NONE',  ( 0.000000000000000000, 0.4930308989874980785, 0.8700118002898462599 ) ) ;
#231192=ORIENTED_EDGE ( 'NONE', *, *, #92786, .T. ) ;
#231222=CARTESIAN_POINT ( 'NONE',  ( 23.15000000000000213, 85.00000000001232081, -160.1291383618718385 ) ) ;
#231254=CARTESIAN_POINT ( 'NONE',  ( -20.00857864376270001, 66.65000000001222702, -148.7731074845244166 ) ) ;
#231258=CARTESIAN_POINT ( 'NONE',  ( -18.54260524012593692, 85.62421939008603999, -129.7823344387537361 ) ) ;
#231266=CARTESIAN_POINT ( 'NONE',  ( 23.25000000000000000, 87.48912529308822172, -139.6231074845242688 ) ) ;
#231269=ORIENTED_EDGE ( 'NONE', *, *, #246644, .F. ) ;
#231279=EDGE_CURVE ( 'NONE', #117495, #210038, #19769, .T. ) ;
#231285=DIRECTION ( 'NONE',  ( 0.000000000000000000, 6.938893903907222067E-15, -1.000000000000000000 ) ) ;
#231287=VECTOR ( 'NONE', #29577, 1000.000000000000000 ) ;
#231294=ADVANCED_FACE ( 'NONE', ( #38987 ), #95093, .F. ) ;
#231301=CARTESIAN_POINT ( 'NONE',  ( -23.25000000000000000, 76.00000000001229239, -157.2481074845243540 ) ) ;
#231309=CIRCLE ( 'NONE', #102079, 0.1000000000000046685 ) ;
#231343=VERTEX_POINT ( 'NONE', #178510 ) ;
#231350=EDGE_LOOP ( 'NONE', ( #222005, #127081 ) ) ;
#231429=CARTESIAN_POINT ( 'NONE',  ( 23.25000000000000000, 85.60000000001221565, -146.4170766071767389 ) ) ;
#231442=CARTESIAN_POINT ( 'NONE',  ( 20.99749315643149927, 64.25000000001219291, -143.5379132532823689 ) ) ;
#231457=ORIENTED_EDGE ( 'NONE', *, *, #242061, .T. ) ;
#231555=PRESENTATION_STYLE_ASSIGNMENT (( #13783 ) ) ;
#231586=ORIENTED_EDGE ( 'NONE', *, *, #69720, .T. ) ;
#231613=EDGE_CURVE ( 'NONE', #80723, #108723, #19949, .T. ) ;
#231616=VECTOR ( 'NONE', #18807, 999.9999999999998863 ) ;
#231632=VERTEX_POINT ( 'NONE', #53081 ) ;
#231658=EDGE_LOOP ( 'NONE', ( #93089, #111158, #198343, #233823 ) ) ;
#231677=EDGE_LOOP ( 'NONE', ( #252080, #93346, #208839, #80534, #60842 ) ) ;
#231689=EDGE_CURVE ( 'NONE', #241979, #173065, #244966, .T. ) ;
#231753=CARTESIAN_POINT ( 'NONE',  ( 21.05000000000000071, 74.83729825007431202, -161.9231074845243654 ) ) ;
#231775=EDGE_LOOP ( 'NONE', ( #166204, #115963, #235461, #120332, #73960, #153563, #238744, #192250, #118033, #22528 ) ) ;
#231792=ORIENTED_EDGE ( 'NONE', *, *, #46787, .F. ) ;
#231801=CARTESIAN_POINT ( 'NONE',  ( -21.37071067811865532, 67.92928932189357738, -148.8731074845244393 ) ) ;
#231805=ORIENTED_EDGE ( 'NONE', *, *, #250721, .T. ) ;
#231829=PLANE ( 'NONE',  #147272 ) ;
#231830=ADVANCED_FACE ( 'NONE', ( #227240 ), #95129, .T. ) ;
#231838=VERTEX_POINT ( 'NONE', #240712 ) ;
#231841=EDGE_CURVE ( 'NONE', #157707, #219341, #107294, .T. ) ;
#231851=DIRECTION ( 'NONE',  ( 0.000000000000000000, -6.982962677686266711E-15, 1.000000000000000000 ) ) ;
#231852=DIRECTION ( 'NONE',  ( -0.000000000000000000, -6.982962677686266711E-15, 1.000000000000000000 ) ) ;
#231855=CARTESIAN_POINT ( 'NONE',  ( -21.46681500593006930, 69.14248884062519096, -170.0231074845244166 ) ) ;
#231859=CARTESIAN_POINT ( 'NONE',  ( 18.59999999999999076, 74.16465844978787914, -158.4679561919613775 ) ) ;
#231874=EDGE_CURVE ( 'NONE', #245795, #84708, #53439, .T. ) ;
#231921=EDGE_CURVE ( 'NONE', #206325, #184497, #170189, .T. ) ;
#231928=AXIS2_PLACEMENT_3D ( 'NONE', #232707, #249688, #191018 ) ;
#231943=VERTEX_POINT ( 'NONE', #13344 ) ;
#231967=ADVANCED_FACE ( 'NONE', ( #94148 ), #190847, .F. ) ;
#231971=AXIS2_PLACEMENT_3D ( 'NONE', #147492, #112234, #247871 ) ;
#232008=CARTESIAN_POINT ( 'NONE',  ( -21.44999999999999929, 68.75000000001223555, -148.7731074845244166 ) ) ;
#232012=ORIENTED_EDGE ( 'NONE', *, *, #159458, .F. ) ;
#232019=AXIS2_PLACEMENT_3D ( 'NONE', #233702, #56316, #257050 ) ;
#232035=ORIENTED_EDGE ( 'NONE', *, *, #12656, .F. ) ;
#232077=VERTEX_POINT ( 'NONE', #181423 ) ;
#232091=VECTOR ( 'NONE', #135918, 1000.000000000000000 ) ;
#232092=ADVANCED_FACE ( 'NONE', ( #238813 ), #132747, .T. ) ;
#232110=PLANE ( 'NONE',  #47463 ) ;
#232186=DIRECTION ( 'NONE',  ( 1.000000000000000000, 0.000000000000000000, 0.000000000000000000 ) ) ;
#232231=FACE_OUTER_BOUND ( 'NONE', #116252, .T. ) ;
#232260=EDGE_CURVE ( 'NONE', #54460, #5643, #111896, .T. ) ;
#232290=ORIENTED_EDGE ( 'NONE', *, *, #134969, .T. ) ;
#232292=ORIENTED_EDGE ( 'NONE', *, *, #134290, .F. ) ;
#232307=EDGE_CURVE ( 'NONE', #101496, #99805, #194270, .T. ) ;
#232352=CARTESIAN_POINT ( 'NONE',  ( -21.05000000000000071, 64.25000000001219291, -143.5379132551784096 ) ) ;
#232377=ORIENTED_EDGE ( 'NONE', *, *, #3950, .F. ) ;
#232393=CARTESIAN_POINT ( 'NONE',  ( -21.14999999999999858, 64.35000000001238618, -170.0231074845244166 ) ) ;
#232427=EDGE_LOOP ( 'NONE', ( #195104, #144729, #3481, #40809 ) ) ;
#232488=ORIENTED_EDGE ( 'NONE', *, *, #96158, .T. ) ;
#232492=LINE ( 'NONE', #53833, #227547 ) ;
#232520=CARTESIAN_POINT ( 'NONE',  ( 21.05000000000000071, 65.51556651037061840, -162.5663016830325489 ) ) ;
#232535=DIRECTION ( 'NONE',  ( -0.000000000000000000, 1.000000000000000000, 6.982962677686266711E-15 ) ) ;
#232542=ADVANCED_FACE ( 'NONE', ( #244911 ), #241091, .T. ) ;
#232548=CARTESIAN_POINT ( 'NONE',  ( -18.48408745364679362, 85.66432225867526995, -129.8400289511960182 ) ) ;
#232583=AXIS2_PLACEMENT_3D ( 'NONE', #201250, #242945, #1759 ) ;
#232593=EDGE_LOOP ( 'NONE', ( #96770, #208648, #20601, #81668 ) ) ;
#232616=CARTESIAN_POINT ( 'NONE',  ( -20.64999999999999858, 76.00000000001213607, -136.5231074845243313 ) ) ;
#232662=ORIENTED_EDGE ( 'NONE', *, *, #127667, .F. ) ;
#232681=CARTESIAN_POINT ( 'NONE',  ( 20.85000000000000142, 77.83585931145570669, -125.0186683157258045 ) ) ;
#232694=CARTESIAN_POINT ( 'NONE',  ( -21.13422380239012810, 76.00000000001243450, -176.5164339993298483 ) ) ;
#232707=CARTESIAN_POINT ( 'NONE',  ( 21.05000000000000071, 76.00000000001212186, -134.6231074845243256 ) ) ;
#232715=DIRECTION ( 'NONE',  ( -0.000000000000000000, -6.982962677686266711E-15, 1.000000000000000000 ) ) ;
#232744=CARTESIAN_POINT ( 'NONE',  ( -22.50000000000000000, 76.00000000001246292, -181.6726782920691505 ) ) ;
#232775=DIRECTION ( 'NONE',  ( -1.000000000000000000, -0.000000000000000000, -0.000000000000000000 ) ) ;
#232794=CARTESIAN_POINT ( 'NONE',  ( -22.49999999999999645, 64.25043287652299284, -170.1239658536231616 ) ) ;
#232812=FACE_OUTER_BOUND ( 'NONE', #33045, .T. ) ;
#232818=ORIENTED_EDGE ( 'NONE', *, *, #79029, .F. ) ;
#232839=AXIS2_PLACEMENT_3D ( 'NONE', #101637, #220354, #76970 ) ;
#232859=CARTESIAN_POINT ( 'NONE',  ( -18.40000000000000213, 85.50000000001236344, -163.0237453873441780 ) ) ;
#232864=CIRCLE ( 'NONE', #95472, 0.09999999999998898659 ) ;
#232878=DIRECTION ( 'NONE',  ( -3.440080580676165868E-14, 0.1298341882520054891, 0.9915357197604850459 ) ) ;
#232884=AXIS2_PLACEMENT_3D ( 'NONE', #206429, #147748, #27829 ) ;
#232896=CARTESIAN_POINT ( 'NONE',  ( -20.87600722750343252, 65.66887361445355964, -130.9329845918269370 ) ) ;
#232922=ORIENTED_EDGE ( 'NONE', *, *, #4053, .T. ) ;
#232988=AXIS2_PLACEMENT_3D ( 'NONE', #189163, #211294, #32702 ) ;
#233003=CARTESIAN_POINT ( 'NONE',  ( 20.04142135623730070, 64.35000000001222986, -148.6731074845244507 ) ) ;
#233031=EDGE_LOOP ( 'NONE', ( #148332, #15490, #95082, #49192 ) ) ;
#233037=ORIENTED_EDGE ( 'NONE', *, *, #238619, .F. ) ;
#233039=ORIENTED_EDGE ( 'NONE', *, *, #4434, .T. ) ;
#233041=DIRECTION ( 'NONE',  ( 1.000000000000000000, 0.000000000000000000, 0.000000000000000000 ) ) ;
#233048=VECTOR ( 'NONE', #134344, 1000.000000000000000 ) ;
#233053=ORIENTED_EDGE ( 'NONE', *, *, #7172, .T. ) ;
#233078=ADVANCED_FACE ( 'NONE', ( #198745 ), #218288, .F. ) ;
#233095=FACE_OUTER_BOUND ( 'NONE', #184208, .T. ) ;
#233098=CARTESIAN_POINT ( 'NONE',  ( 18.59999999999999787, 77.85102823015316176, -158.3691942151018566 ) ) ;
#233104=DIRECTION ( 'NONE',  ( -2.342056488767301376E-15, 0.1350103645451974088, -0.9908441862701587999 ) ) ;
#233111=CARTESIAN_POINT ( 'NONE',  ( 20.95512840106816199, 65.37615130623896675, -157.8206282637254674 ) ) ;
#233135=EDGE_LOOP ( 'NONE', ( #145387, #94035, #32619, #9772 ) ) ;
#233151=EDGE_LOOP ( 'NONE', ( #148164, #235962, #129153, #169245 ) ) ;
#233152=DIRECTION ( 'NONE',  ( 0.000000000000000000, -6.853228547068871147E-15, 1.000000000000000000 ) ) ;
#233156=CIRCLE ( 'NONE', #29166, 0.09999999999998898659 ) ;
#233162=LINE ( 'NONE', #192736, #22431 ) ;
#233202=DIRECTION ( 'NONE',  ( 1.000000000000000000, -2.952720810173289112E-16, -2.061873921506763405E-30 ) ) ;
#233223=CARTESIAN_POINT ( 'NONE',  ( -23.15000000000000213, 76.00000000001237765, -170.0231074845243597 ) ) ;
#233258=EDGE_LOOP ( 'NONE', ( #137546, #26453, #168517, #11413 ) ) ;
#233269=TOROIDAL_SURFACE ( 'NONE', #162518, 6.258578643762712446, 0.1000000000000000056 ) ;
#233273=AXIS2_PLACEMENT_3D ( 'NONE', #174067, #157043, #99588 ) ;
#233311=DIRECTION ( 'NONE',  ( -0.7071067811865127117, -0.7071067811865821007, 0.000000000000000000 ) ) ;
#233346=EDGE_LOOP ( 'NONE', ( #27057, #41554, #119832, #190219 ) ) ;
#233369=ORIENTED_EDGE ( 'NONE', *, *, #245758, .T. ) ;
#233389=ADVANCED_FACE ( 'NONE', ( #126925 ), #175023, .F. ) ;
#233414=CARTESIAN_POINT ( 'NONE',  ( -20.94999999999999929, 76.00000000001213607, -136.5231074845243313 ) ) ;
#233426=AXIS2_PLACEMENT_3D ( 'NONE', #230293, #189895, #128650 ) ;
#233430=CARTESIAN_POINT ( 'NONE',  ( 23.14999999999999858, 64.35000000001218723, -143.5379132551783812 ) ) ;
#233439=AXIS2_PLACEMENT_3D ( 'NONE', #243677, #25925, #144561 ) ;
#233449=DIRECTION ( 'NONE',  ( 0.000000000000000000, 0.000000000000000000, -1.000000000000000000 ) ) ;
#233463=CARTESIAN_POINT ( 'NONE',  ( 18.49999999999999289, 64.25000000001220712, -145.1731074845244507 ) ) ;
#233490=CARTESIAN_POINT ( 'NONE',  ( 20.94999999999999574, 76.00000000001237765, -170.0231074845243597 ) ) ;
#233519=CARTESIAN_POINT ( 'NONE',  ( -21.05000000000000071, 76.00000000001213607, -136.5231074845243313 ) ) ;
#233543=CYLINDRICAL_SURFACE ( 'NONE', #2246, 0.1000000000000028644 ) ;
#233547=VECTOR ( 'NONE', #193038, 1000.000000000000000 ) ;
#233577=FACE_OUTER_BOUND ( 'NONE', #228247, .T. ) ;
#233612=CIRCLE ( 'NONE', #246264, 0.09999999999998898659 ) ;
#233618=ORIENTED_EDGE ( 'NONE', *, *, #4293, .F. ) ;
#233619=CARTESIAN_POINT ( 'NONE',  ( -21.14999999999999858, 87.65000000001238334, -170.0231074845242745 ) ) ;
#233630=EDGE_CURVE ( 'NONE', #165825, #59337, #166812, .T. ) ;
#233657=CARTESIAN_POINT ( 'NONE',  ( 18.51997666896864914, 85.39233213153103463, -162.8797012970400999 ) ) ;
#233660=LINE ( 'NONE', #158008, #180901 ) ;
#233672=ORIENTED_EDGE ( 'NONE', *, *, #143343, .T. ) ;
#233694=LINE ( 'NONE', #155472, #213254 ) ;
#233702=CARTESIAN_POINT ( 'NONE',  ( -23.15000000000000213, 87.65000000001215597, -139.6231074845242688 ) ) ;
#233713=CIRCLE ( 'NONE', #125544, 0.1000000000000070832 ) ;
#233738=DIRECTION ( 'NONE',  ( -0.000000000000000000, 6.982962677686266711E-15, -1.000000000000000000 ) ) ;
#233742=CARTESIAN_POINT ( 'NONE',  ( -20.94999999999999929, 87.48912529308842068, -167.1231074845242688 ) ) ;
#233757=AXIS2_PLACEMENT_3D ( 'NONE', #36530, #178607, #76897 ) ;
#233804=AXIS2_PLACEMENT_3D ( 'NONE', #96182, #37524, #135308 ) ;
#233806=DIRECTION ( 'NONE',  ( 0.000000000000000000, 0.000000000000000000, 1.000000000000000000 ) ) ;
#233807=FACE_OUTER_BOUND ( 'NONE', #167938, .T. ) ;
#233813=CARTESIAN_POINT ( 'NONE',  ( -23.24999999999999645, 85.60000000001210196, -129.8229180933022633 ) ) ;
#233823=ORIENTED_EDGE ( 'NONE', *, *, #16658, .F. ) ;
#233830=ADVANCED_FACE ( 'NONE', ( #160003 ), #116884, .T. ) ;
#233861=FACE_OUTER_BOUND ( 'NONE', #78245, .T. ) ;
#233863=DIRECTION ( 'NONE',  ( 0.000000000000000000, 0.000000000000000000, 1.000000000000000000 ) ) ;
#233872=EDGE_CURVE ( 'NONE', #116513, #242376, #79136, .T. ) ;
#233929=CARTESIAN_POINT ( 'NONE',  ( -23.15000000000000213, 64.25000000001229239, -157.8731074845244393 ) ) ;
#233957=CARTESIAN_POINT ( 'NONE',  ( -21.11833042828134666, 75.99289949095320651, -176.4687521783799298 ) ) ;
#233981=ADVANCED_FACE ( 'NONE', ( #204230 ), #24340, .F. ) ;
#233994=ORIENTED_EDGE ( 'NONE', *, *, #202512, .T. ) ;
#234068=CIRCLE ( 'NONE', #59241, 0.09999999999998898659 ) ;
#234069=EDGE_LOOP ( 'NONE', ( #127958, #128250, #26729, #17058 ) ) ;
#234102=CARTESIAN_POINT ( 'NONE',  ( -23.15000000000000213, 64.35000000001222986, -148.6731074845244507 ) ) ;
#234114=AXIS2_PLACEMENT_3D ( 'NONE', #191685, #132974, #213777 ) ;
#234138=ORIENTED_EDGE ( 'NONE', *, *, #123623, .F. ) ;
#234195=ADVANCED_FACE ( 'NONE', ( #52855 ), #89415, .F. ) ;
#234207=CARTESIAN_POINT ( 'NONE',  ( -20.54999999999999716, 76.00000000001213607, -136.5231074845243313 ) ) ;
#234214=CARTESIAN_POINT ( 'NONE',  ( -20.54999999999999716, 76.00000000001213607, -136.5231074845243313 ) ) ;
#234245=CARTESIAN_POINT ( 'NONE',  ( -22.50000000000000000, 75.90000000001245439, -181.6726782920691505 ) ) ;
#234314=EDGE_LOOP ( 'NONE', ( #178501, #202354, #2017, #168376 ) ) ;
#234315=CYLINDRICAL_SURFACE ( 'NONE', #81797, 0.09999999999999939493 ) ;
#234321=EDGE_CURVE ( 'NONE', #113005, #238125, #175411, .T. ) ;
#234324=DIRECTION ( 'NONE',  ( -0.000000000000000000, -6.982962677686266711E-15, 1.000000000000000000 ) ) ;
#234341=DIRECTION ( 'NONE',  ( 0.7071067811865475727, -0.7071067811865475727, -4.937700262164531476E-15 ) ) ;
#234355=CARTESIAN_POINT ( 'NONE',  ( 21.04999999999999716, 65.37127968600792371, -157.8731074845244393 ) ) ;
#234364=ORIENTED_EDGE ( 'NONE', *, *, #217362, .F. ) ;
#234373=DIRECTION ( 'NONE',  ( 0.000000000000000000, -6.938893903907229955E-15, 1.000000000000000000 ) ) ;
#234385=CIRCLE ( 'NONE', #230282, 0.09999999999998898659 ) ;
#234390=CARTESIAN_POINT ( 'NONE',  ( -21.55000000000000426, 68.29142135624952914, -148.7731074845244166 ) ) ;
#234402=ORIENTED_EDGE ( 'NONE', *, *, #56813, .T. ) ;
#234451=AXIS2_PLACEMENT_3D ( 'NONE', #229088, #209511, #30915 ) ;
#234485=VECTOR ( 'NONE', #289, 1000.000000000000000 ) ;
#234486=( BOUNDED_SURFACE ( )  B_SPLINE_SURFACE ( 3, 2, ( 
 ( #149004, #126850, #251930 ),
 ( #68159, #129417, #107282 ),
 ( #190709, #8201, #27784 ),
 ( #90269, #188111, #91578 ) ),
 .UNSPECIFIED., .F., .F., .F. ) 
 B_SPLINE_SURFACE_WITH_KNOTS ( ( 4, 4 ),
 ( 3, 3 ),
 ( -1.044899843732904898E-17, 0.0003124336600439518762 ),
 ( 0.000000000000000000, 1.000000000000000000 ),
 .UNSPECIFIED. ) 
 GEOMETRIC_REPRESENTATION_ITEM ( )  RATIONAL_B_SPLINE_SURFACE ( (
 ( 1.000000000000000000, 0.7071067811865475727, 1.000000000000000000),
 ( 1.000000000000000000, 0.7089187706050192883, 1.000000000000000000),
 ( 1.000000000000000000, 0.7039288185052067215, 1.000000000000000000),
 ( 1.000000000000000000, 0.7040654476015839602, 1.000000000000000000) ) ) 
 REPRESENTATION_ITEM ( '' )  SURFACE ( )  );
#234492=ORIENTED_EDGE ( 'NONE', *, *, #79273, .T. ) ;
#234503=VECTOR ( 'NONE', #246391, 1000.000000000000000 ) ;
#234514=ORIENTED_EDGE ( 'NONE', *, *, #33450, .T. ) ;
#234529=ORIENTED_EDGE ( 'NONE', *, *, #79470, .F. ) ;
#234533=EDGE_CURVE ( 'NONE', #168738, #133183, #220349, .T. ) ;
#234540=CARTESIAN_POINT ( 'NONE',  ( 20.94999999999997442, 77.26327546522934142, -128.6212428177779543 ) ) ;
#234588=ORIENTED_EDGE ( 'NONE', *, *, #152737, .T. ) ;
#234601=DIRECTION ( 'NONE',  ( 0.000000000000000000, 1.000000000000000000, 0.000000000000000000 ) ) ;
#234606=AXIS2_PLACEMENT_3D ( 'NONE', #24819, #27396, #67762 ) ;
#234613=EDGE_CURVE ( 'NONE', #33310, #5863, #44276, .T. ) ;
#234623=DIRECTION ( 'NONE',  ( 0.000000000000000000, 0.000000000000000000, 1.000000000000000000 ) ) ;
#234625=ORIENTED_EDGE ( 'NONE', *, *, #189420, .F. ) ;
#234642=ORIENTED_EDGE ( 'NONE', *, *, #204115, .T. ) ;
#234686=LINE ( 'NONE', #135567, #173842 ) ;
#234729=ORIENTED_EDGE ( 'NONE', *, *, #181262, .F. ) ;
#234735=CARTESIAN_POINT ( 'NONE',  ( -23.25000000000000000, 76.00000000001240608, -174.0731074845243711 ) ) ;
#234764=TOROIDAL_SURFACE ( 'NONE', #218164, 4.099999999999999645, 0.1000000000000000056 ) ;
#234781=FACE_OUTER_BOUND ( 'NONE', #47764, .T. ) ;
#234789=B_SPLINE_CURVE_WITH_KNOTS ( 'NONE', 3,
 ( #192907, #211179, #11711, #14288, #213741, #250303 ),
 .UNSPECIFIED., .F., .F.,
 ( 4, 2, 4 ),
 ( 0.000000000000000000, 0.0001891491689349668738, 0.0003782983378699337476 ),
 .UNSPECIFIED. ) ;
#234867=EDGE_CURVE ( 'NONE', #143593, #190389, #75756, .T. ) ;
#234927=EDGE_CURVE ( 'NONE', #49697, #994, #219478, .T. ) ;
#234937=CARTESIAN_POINT ( 'NONE',  ( 18.52165635395168053, 85.48115071129463161, -162.9982699016619847 ) ) ;
#234956=EDGE_LOOP ( 'NONE', ( #247916, #210202, #17387, #20876 ) ) ;
#234992=CARTESIAN_POINT ( 'NONE',  ( -22.39999999999999858, 64.25000000001237765, -169.9231074845244507 ) ) ;
#235004=DIRECTION ( 'NONE',  ( -1.000000000000000000, 0.000000000000000000, -0.000000000000000000 ) ) ;
#235017=CYLINDRICAL_SURFACE ( 'NONE', #95410, 0.09999999999999939493 ) ;
#235097=FACE_OUTER_BOUND ( 'NONE', #82137, .T. ) ;
#235106=EDGE_CURVE ( 'NONE', #70695, #214666, #134001, .T. ) ;
#235140=CARTESIAN_POINT ( 'NONE',  ( -20.54999999999999716, 66.65000000001222702, -148.8731074845244393 ) ) ;
#235144=DIRECTION ( 'NONE',  ( -3.265361837132813093E-16, -1.000000000000000000, 7.445645354460596589E-46 ) ) ;
#235175=CARTESIAN_POINT ( 'NONE',  ( -18.59999999999999787, 64.35000000001222986, -148.7731074845244450 ) ) ;
#235189=DIRECTION ( 'NONE',  ( -1.000000000000000000, 0.000000000000000000, 0.000000000000000000 ) ) ;
#235222=CARTESIAN_POINT ( 'NONE',  ( 20.02499999999999858, 66.25000000001223555, -148.7731074845244450 ) ) ;
#235228=EDGE_CURVE ( 'NONE', #194806, #248967, #83694, .T. ) ;
#235231=CARTESIAN_POINT ( 'NONE',  ( -20.54999999999999716, 76.00000000001222134, -149.3981074845243313 ) ) ;
#235232=DIRECTION ( 'NONE',  ( -1.000000000000000000, 0.000000000000000000, 0.000000000000000000 ) ) ;
#235289=EDGE_CURVE ( 'NONE', #49319, #180142, #202406, .T. ) ;
#235293=VERTEX_POINT ( 'NONE', #42071 ) ;
#235294=CIRCLE ( 'NONE', #252064, 12.97499999999998721 ) ;
#235308=FACE_OUTER_BOUND ( 'NONE', #164977, .T. ) ;
#235381=CARTESIAN_POINT ( 'NONE',  ( 21.10257677756355932, 75.97504925044442814, -176.4214892270570942 ) ) ;
#235382=CYLINDRICAL_SURFACE ( 'NONE', #218384, 0.1000000000000046685 ) ;
#235394=LINE ( 'NONE', #212005, #189834 ) ;
#235399=ORIENTED_EDGE ( 'NONE', *, *, #196070, .T. ) ;
#235404=CARTESIAN_POINT ( 'NONE',  ( -20.54999999999999716, 84.73084112150763758, -160.4250327655399531 ) ) ;
#235412=DIRECTION ( 'NONE',  ( 0.000000000000000000, -0.4999999999999088507, 0.8660254037844913322 ) ) ;
#235456=EDGE_CURVE ( 'NONE', #109498, #44088, #97488, .T. ) ;
#235461=ORIENTED_EDGE ( 'NONE', *, *, #211949, .T. ) ;
#235486=CONICAL_SURFACE ( 'NONE', #173203, 4.049999999999998046, 0.7853981633974604915 ) ;
#235493=FACE_OUTER_BOUND ( 'NONE', #231350, .T. ) ;
#235497=FACE_OUTER_BOUND ( 'NONE', #126488, .T. ) ;
#235517=ORIENTED_EDGE ( 'NONE', *, *, #218500, .T. ) ;
#235526=DIRECTION ( 'NONE',  ( 0.000000000000000000, 0.000000000000000000, 1.000000000000000000 ) ) ;
#235527=AXIS2_PLACEMENT_3D ( 'NONE', #176511, #215609, #214340 ) ;
#235530=CARTESIAN_POINT ( 'NONE',  ( -22.45372860728439690, 75.98507938046395793, -181.6729046192282340 ) ) ;
#235540=CARTESIAN_POINT ( 'NONE',  ( 18.42555734704286152, 85.49715836194906160, -162.9832769867893774 ) ) ;
#235572=EDGE_CURVE ( 'NONE', #219200, #79629, #13480, .T. ) ;
#235575=CARTESIAN_POINT ( 'NONE',  ( 21.14999999999999503, 76.10085836911117951, -181.7726746080137445 ) ) ;
#235577=DIRECTION ( 'NONE',  ( 0.000000000000000000, -6.769652589177795712E-15, 1.000000000000000000 ) ) ;
#235594=VERTEX_POINT ( 'NONE', #255600 ) ;
#235624=AXIS2_PLACEMENT_3D ( 'NONE', #49850, #210236, #53703 ) ;
#235651=DIRECTION ( 'NONE',  ( -1.000000000000000000, 0.000000000000000000, -0.000000000000000000 ) ) ;
#235676=CIRCLE ( 'NONE', #31716, 4.000000000000003553 ) ;
#235713=EDGE_CURVE ( 'NONE', #184497, #151457, #62596, .T. ) ;
#235735=EDGE_CURVE ( 'NONE', #26629, #23601, #213368, .T. ) ;
#235746=VERTEX_POINT ( 'NONE', #44322 ) ;
#235767=CARTESIAN_POINT ( 'NONE',  ( 18.59999999999999076, 77.83585931145570669, -125.0186683157258329 ) ) ;
#235776=CARTESIAN_POINT ( 'NONE',  ( 21.05000000000000071, 77.73625713160970463, -158.4544551555068495 ) ) ;
#235793=ADVANCED_FACE ( 'NONE', ( #186402 ), #164271, .F. ) ;
#235810=ORIENTED_EDGE ( 'NONE', *, *, #94417, .T. ) ;
#235823=DIRECTION ( 'NONE',  ( -1.000000000000000000, 0.000000000000000000, -0.000000000000000000 ) ) ;
#235878=DIRECTION ( 'NONE',  ( 0.000000000000000000, 0.000000000000000000, 1.000000000000000000 ) ) ;
#235892=CARTESIAN_POINT ( 'NONE',  ( 21.05000000000000071, 85.40000000001221281, -146.4170766071767389 ) ) ;
#235902=AXIS2_PLACEMENT_3D ( 'NONE', #122269, #92114, #12611 ) ;
#235908=VECTOR ( 'NONE', #60376, 1000.000000000000000 ) ;
#235920=CARTESIAN_POINT ( 'NONE',  ( -20.64999999999999858, 71.65000000001228386, -157.6731074845243938 ) ) ;
#235941=EDGE_LOOP ( 'NONE', ( #218092, #169424, #77433 ) ) ;
#235944=DIRECTION ( 'NONE',  ( -1.000000000000000000, -0.000000000000000000, -0.000000000000000000 ) ) ;
#235954=CARTESIAN_POINT ( 'NONE',  ( 18.59999999999998366, 76.00000000001213607, -136.5231074845243313 ) ) ;
#235958=ORIENTED_EDGE ( 'NONE', *, *, #31454, .T. ) ;
#235961=CARTESIAN_POINT ( 'NONE',  ( -20.64999999999999858, 74.07476635515247665, -157.2928639513982318 ) ) ;
#235962=ORIENTED_EDGE ( 'NONE', *, *, #117433, .T. ) ;
#235989=CARTESIAN_POINT ( 'NONE',  ( 23.14999999999999858, 76.00000000001213607, -136.5231074845243313 ) ) ;
#235991=ADVANCED_FACE ( 'NONE', ( #81800 ), #209831, .T. ) ;
#235994=DIRECTION ( 'NONE',  ( 1.000000000000000000, 0.000000000000000000, 0.000000000000000000 ) ) ;
#236013=CARTESIAN_POINT ( 'NONE',  ( -20.54999999999999716, 66.65000000001229807, -157.7731074845244166 ) ) ;
#236028=EDGE_CURVE ( 'NONE', #24875, #241247, #68355, .T. ) ;
#236059=CYLINDRICAL_SURFACE ( 'NONE', #5830, 0.09999999999998898659 ) ;
#236088=EDGE_CURVE ( 'NONE', #46365, #16105, #243124, .T. ) ;
#236105=VECTOR ( 'NONE', #146058, 999.9999999999998863 ) ;
#236131=EDGE_LOOP ( 'NONE', ( #224316, #134415, #100581, #88799 ) ) ;
#236135=ORIENTED_EDGE ( 'NONE', *, *, #118683, .F. ) ;
#236159=CIRCLE ( 'NONE', #127849, 0.5000000000000004441 ) ;
#236180=ORIENTED_EDGE ( 'NONE', *, *, #185330, .F. ) ;
#236181=EDGE_LOOP ( 'NONE', ( #125341, #45342, #121784, #248416 ) ) ;
#236193=VERTEX_POINT ( 'NONE', #206923 ) ;
#236212=DIRECTION ( 'NONE',  ( 0.7071067811865127117, 0.7071067811865821007, 0.000000000000000000 ) ) ;
#236234=DIRECTION ( 'NONE',  ( 1.000000000000000000, -3.265361837132813093E-16, -2.280189983783949500E-30 ) ) ;
#236286=FACE_OUTER_BOUND ( 'NONE', #226195, .T. ) ;
#236311=VERTEX_POINT ( 'NONE', #248614 ) ;
#236345=ADVANCED_FACE ( 'NONE', ( #180636 ), #116806, .F. ) ;
#236360=EDGE_CURVE ( 'NONE', #119183, #14612, #200199, .T. ) ;
#236361=CARTESIAN_POINT ( 'NONE',  ( 23.24999999999999645, 76.00000000001237765, -170.0231074845243597 ) ) ;
#236368=CARTESIAN_POINT ( 'NONE',  ( -18.48179518608921157, 85.51832530050738512, -129.6334019077617938 ) ) ;
#236372=EDGE_LOOP ( 'NONE', ( #34864, #193120 ) ) ;
#236389=CIRCLE ( 'NONE', #123976, 0.2000000000000057288 ) ;
#236392=EDGE_CURVE ( 'NONE', #144474, #6603, #56032, .T. ) ;
#236396=ORIENTED_EDGE ( 'NONE', *, *, #163463, .F. ) ;
#236447=CYLINDRICAL_SURFACE ( 'NONE', #168109, 0.1000000000000028644 ) ;
#236489=DIRECTION ( 'NONE',  ( 0.000000000000000000, -1.000000000000000000, 0.000000000000000000 ) ) ;
#236517=DIRECTION ( 'NONE',  ( 1.000000000000000000, 0.000000000000000000, 0.000000000000000000 ) ) ;
#236519=ORIENTED_EDGE ( 'NONE', *, *, #94992, .F. ) ;
#236590=ADVANCED_FACE ( 'NONE', ( #233577 ), #215283, .F. ) ;
#236596=DIRECTION ( 'NONE',  ( 1.000000000000000000, 0.000000000000000000, 0.000000000000000000 ) ) ;
#236610=CARTESIAN_POINT ( 'NONE',  ( -23.25000000000000000, 71.75000000001229239, -157.8731074845243825 ) ) ;
#236614=EDGE_CURVE ( 'NONE', #239159, #123863, #64255, .T. ) ;
#236628=CARTESIAN_POINT ( 'NONE',  ( 22.49436431346199683, 64.35004905235891215, -170.0900110142466986 ) ) ;
#236671=CARTESIAN_POINT ( 'NONE',  ( 18.49999999999999289, 65.79142135392905288, -145.3206006188949004 ) ) ;
#236692=ORIENTED_EDGE ( 'NONE', *, *, #115717, .F. ) ;
#236715=EDGE_LOOP ( 'NONE', ( #65362, #189662, #15069, #249295 ) ) ;
#236731=CIRCLE ( 'NONE', #28522, 0.09999999999999939493 ) ;
#236736=CIRCLE ( 'NONE', #182800, 0.1000000000000072220 ) ;
#236744=CIRCLE ( 'NONE', #66067, 0.2000000000000057288 ) ;
#236751=ADVANCED_FACE ( 'NONE', ( #58750 ), #82160, .F. ) ;
#236788=CARTESIAN_POINT ( 'NONE',  ( 21.05000000000000071, 76.00000000001227818, -157.0481074845243938 ) ) ;
#236814=AXIS2_PLACEMENT_3D ( 'NONE', #64259, #223312, #148948 ) ;
#236820=DIRECTION ( 'NONE',  ( 0.000000000000000000, 0.000000000000000000, 1.000000000000000000 ) ) ;
#236823=CARTESIAN_POINT ( 'NONE',  ( 18.45068634130098673, 85.48650607335510188, -162.9543290533561617 ) ) ;
#236857=ORIENTED_EDGE ( 'NONE', *, *, #100388, .F. ) ;
#236926=ORIENTED_EDGE ( 'NONE', *, *, #41741, .F. ) ;
#236927=VECTOR ( 'NONE', #103427, 1000.000000000000000 ) ;
#236932=EDGE_CURVE ( 'NONE', #21932, #70242, #226835, .T. ) ;
#236965=AXIS2_PLACEMENT_3D ( 'NONE', #181098, #41596, #80669 ) ;
#236980=ORIENTED_EDGE ( 'NONE', *, *, #64741, .F. ) ;
#236987=VERTEX_POINT ( 'NONE', #156322 ) ;
#236996=AXIS2_PLACEMENT_3D ( 'NONE', #230537, #34932, #132727 ) ;
#236997=CARTESIAN_POINT ( 'NONE',  ( 21.05000000000000071, 67.22371710471985295, -161.5351067629400461 ) ) ;
#237010=CIRCLE ( 'NONE', #166304, 0.1000000000000033362 ) ;
#237019=VECTOR ( 'NONE', #114942, 1000.000000000000000 ) ;
#237028=ORIENTED_EDGE ( 'NONE', *, *, #255942, .T. ) ;
#237060=AXIS2_PLACEMENT_3D ( 'NONE', #68500, #148036, #227561 ) ;
#237071=DIRECTION ( 'NONE',  ( 0.000000000000000000, 1.000000000000000000, 6.982962677686266711E-15 ) ) ;
#237093=CARTESIAN_POINT ( 'NONE',  ( 18.31572054635679336, 85.54847543579123226, -129.6725373197760689 ) ) ;
#237147=VECTOR ( 'NONE', #245984, 1000.000000000000000 ) ;
#237149=CIRCLE ( 'NONE', #232884, 0.09999999999998898659 ) ;
#237150=ORIENTED_EDGE ( 'NONE', *, *, #20114, .F. ) ;
#237165=ORIENTED_EDGE ( 'NONE', *, *, #147953, .F. ) ;
#237170=EDGE_LOOP ( 'NONE', ( #122457, #16534, #157531, #232292 ) ) ;
#237181=CARTESIAN_POINT ( 'NONE',  ( 23.14999999999999147, 71.85000000001237197, -170.0231074845243882 ) ) ;
#237195=LINE ( 'NONE', #161521, #100938 ) ;
#237205=CARTESIAN_POINT ( 'NONE',  ( -21.05000000000000071, 77.16270174995034381, -161.9231074845243370 ) ) ;
#237219=CARTESIAN_POINT ( 'NONE',  ( 20.94999999999999929, 69.45000000001230944, -160.0060803140843859 ) ) ;
#237221=CARTESIAN_POINT ( 'NONE',  ( 18.50000000000000000, 85.40000000001232650, -162.7258477248609836 ) ) ;
#237222=LINE ( 'NONE', #217622, #188412 ) ;
#237262=VECTOR ( 'NONE', #251700, 1000.000000000000000 ) ;
#237267=CARTESIAN_POINT ( 'NONE',  ( 18.49999999999999289, 69.35000000001222986, -148.6731074845243938 ) ) ;
#237273=CARTESIAN_POINT ( 'NONE',  ( -23.15000000000000213, 64.35000000001245724, -181.7731074845244450 ) ) ;
#237280=VERTEX_POINT ( 'NONE', #46582 ) ;
#237284=DIRECTION ( 'NONE',  ( 0.000000000000000000, 0.000000000000000000, 1.000000000000000000 ) ) ;
#237286=CARTESIAN_POINT ( 'NONE',  ( -22.47071067811865319, 68.27992525551432834, -170.1221999392270163 ) ) ;
#237296=EDGE_CURVE ( 'NONE', #84927, #113219, #185425, .T. ) ;
#237297=AXIS2_PLACEMENT_3D ( 'NONE', #75106, #35962, #239289 ) ;
#237322=AXIS2_PLACEMENT_3D ( 'NONE', #204195, #225029, #42558 ) ;
#237332=ORIENTED_EDGE ( 'NONE', *, *, #74173, .T. ) ;
#237350=CARTESIAN_POINT ( 'NONE',  ( 18.59999999999996945, 65.66751761918692409, -130.9282609406112670 ) ) ;
#237352=EDGE_LOOP ( 'NONE', ( #165411, #29441, #257442 ) ) ;
#237369=DIRECTION ( 'NONE',  ( 1.000000000000000000, 0.000000000000000000, 0.000000000000000000 ) ) ;
#237371=VECTOR ( 'NONE', #131601, 1000.000000000000000 ) ;
#237385=EDGE_CURVE ( 'NONE', #173680, #23601, #85419, .T. ) ;
#237391=ORIENTED_EDGE ( 'NONE', *, *, #8599, .F. ) ;
#237393=CARTESIAN_POINT ( 'NONE',  ( -22.14074124539699540, 75.90094710416836676, -177.4131853355681301 ) ) ;
#237412=ORIENTED_EDGE ( 'NONE', *, *, #53040, .F. ) ;
#237418=ORIENTED_EDGE ( 'NONE', *, *, #188315, .T. ) ;
#237473=EDGE_CURVE ( 'NONE', #218618, #243885, #198073, .T. ) ;
#237485=DIRECTION ( 'NONE',  ( 0.000000000000000000, 0.1455152366551700771, 0.9893560106964479628 ) ) ;
#237506=DIRECTION ( 'NONE',  ( -0.000000000000000000, -1.000000000000000000, -6.982962677686266711E-15 ) ) ;
#237511=CARTESIAN_POINT ( 'NONE',  ( 18.43709777086139923, 85.68240343348847432, -129.8662641071115331 ) ) ;
#237517=CARTESIAN_POINT ( 'NONE',  ( 21.09696443733127325, 65.27599011609382273, -157.7883299574762077 ) ) ;
#237537=LINE ( 'NONE', #77161, #99981 ) ;
#237541=LINE ( 'NONE', #219242, #26541 ) ;
#237557=AXIS2_PLACEMENT_3D ( 'NONE', #218825, #119767, #199290 ) ;
#237570=EDGE_LOOP ( 'NONE', ( #209574, #216231, #102070, #56593 ) ) ;
#237572=AXIS2_PLACEMENT_3D ( 'NONE', #104025, #167912, #246138 ) ;
#237597=AXIS2_PLACEMENT_3D ( 'NONE', #215269, #139560, #219101 ) ;
#237606=ORIENTED_EDGE ( 'NONE', *, *, #61654, .F. ) ;
#237607=ADVANCED_FACE ( 'NONE', ( #235497 ), #18994, .F. ) ;
#237638=ORIENTED_EDGE ( 'NONE', *, *, #11621, .T. ) ;
#237641=VECTOR ( 'NONE', #84896, 1000.000000000000000 ) ;
#237678=ADVANCED_FACE ( 'NONE', ( #138936 ), #39880, .F. ) ;
#237702=VECTOR ( 'NONE', #87139, 1000.000000000000000 ) ;
#237728=ADVANCED_FACE ( 'NONE', ( #184508 ), #26760, .T. ) ;
#237781=EDGE_LOOP ( 'NONE', ( #142087, #145086, #72998, #113493 ) ) ;
#237787=VERTEX_POINT ( 'NONE', #52703 ) ;
#237795=VERTEX_POINT ( 'NONE', #31899 ) ;
#237814=CYLINDRICAL_SURFACE ( 'NONE', #238754, 11.74999999999999645 ) ;
#237842=CARTESIAN_POINT ( 'NONE',  ( -23.25000000000000000, 85.60000000001220144, -146.4170766071767389 ) ) ;
#237866=ORIENTED_EDGE ( 'NONE', *, *, #227957, .T. ) ;
#237907=CARTESIAN_POINT ( 'NONE',  ( -18.50000000000000711, 85.41920341803901806, -162.7753216740956645 ) ) ;
#237920=CARTESIAN_POINT ( 'NONE',  ( 22.49806830649814060, 64.35011034517329165, -170.1005718008499343 ) ) ;
#237964=CARTESIAN_POINT ( 'NONE',  ( -18.52186455169013612, 85.48101848145468296, -162.9980910066095987 ) ) ;
#238024=CIRCLE ( 'NONE', #200441, 0.09999999999998986089 ) ;
#238025=DIRECTION ( 'NONE',  ( 0.000000000000000000, 7.056502275159890832E-15, -1.000000000000000000 ) ) ;
#238055=ADVANCED_FACE ( 'NONE', ( #177949 ), #257410, .T. ) ;
#238083=EDGE_CURVE ( 'NONE', #168523, #99277, #39740, .T. ) ;
#238125=VERTEX_POINT ( 'NONE', #243035 ) ;
#238148=FACE_OUTER_BOUND ( 'NONE', #4189, .T. ) ;
#238150=ORIENTED_EDGE ( 'NONE', *, *, #255409, .F. ) ;
#238157=CARTESIAN_POINT ( 'NONE',  ( -22.39999999999999503, 76.00000000001243450, -177.8138870828977360 ) ) ;
#238220=CIRCLE ( 'NONE', #9285, 0.09999999999999939493 ) ;
#238290=VERTEX_POINT ( 'NONE', #228638 ) ;
#238312=CYLINDRICAL_SURFACE ( 'NONE', #89422, 0.5000000000000004441 ) ;
#238318=CYLINDRICAL_SURFACE ( 'NONE', #217800, 0.09999999999999939493 ) ;
#238328=AXIS2_PLACEMENT_3D ( 'NONE', #82117, #182555, #61303 ) ;
#238348=FACE_OUTER_BOUND ( 'NONE', #156985, .T. ) ;
#238350=EDGE_CURVE ( 'NONE', #109724, #86120, #13431, .T. ) ;
#238389=CARTESIAN_POINT ( 'NONE',  ( 23.14999999999998437, 64.25000000001237765, -170.0231074845244166 ) ) ;
#238405=VECTOR ( 'NONE', #60560, 1000.000000000000000 ) ;
#238408=DIRECTION ( 'NONE',  ( 1.000000000000000000, 0.000000000000000000, 0.000000000000000000 ) ) ;
#238448=VERTEX_POINT ( 'NONE', #193358 ) ;
#238449=CARTESIAN_POINT ( 'NONE',  ( -18.59999999999999787, 68.75000000001223555, -148.6731074845244223 ) ) ;
#238485=CARTESIAN_POINT ( 'NONE',  ( 23.14999999999998437, 87.75000000001237765, -170.0231074845242745 ) ) ;
#238515=CARTESIAN_POINT ( 'NONE',  ( 21.05000000000000071, 77.16270174995034381, -161.9231074845243370 ) ) ;
#238524=CIRCLE ( 'NONE', #88465, 0.09999999999999459321 ) ;
#238550=EDGE_LOOP ( 'NONE', ( #49591, #78145, #251660, #225752, #124629 ) ) ;
#238580=DIRECTION ( 'NONE',  ( 0.000000000000000000, -6.982962677686266711E-15, 1.000000000000000000 ) ) ;
#238608=DIRECTION ( 'NONE',  ( 0.000000000000000000, 0.000000000000000000, 1.000000000000000000 ) ) ;
#238619=EDGE_CURVE ( 'NONE', #138157, #173065, #25000, .T. ) ;
#238627=DIRECTION ( 'NONE',  ( 3.469446951953728416E-14, 0.8660254037844343777, -0.5000000000000074385 ) ) ;
#238647=DIRECTION ( 'NONE',  ( 1.000000000000000000, 0.000000000000000000, 0.000000000000000000 ) ) ;
#238650=CARTESIAN_POINT ( 'NONE',  ( -20.94999999999999929, 74.16465844978787914, -158.4679561919613775 ) ) ;
#238669=CARTESIAN_POINT ( 'NONE',  ( -20.00857864376270001, 66.75000000001223555, -148.8731074845244393 ) ) ;
#238671=CARTESIAN_POINT ( 'NONE',  ( -21.95218792049438861, 75.90097156021251124, -177.2246150457710314 ) ) ;
#238689=ORIENTED_EDGE ( 'NONE', *, *, #120333, .F. ) ;
#238691=ADVANCED_FACE ( 'NONE', ( #26268 ), #157139, .F. ) ;
#238697=DIRECTION ( 'NONE',  ( 0.000000000000000000, -0.4999999999999608646, 0.8660254037844612451 ) ) ;
#238713=EDGE_CURVE ( 'NONE', #115527, #77194, #27972, .T. ) ;
#238728=AXIS2_PLACEMENT_3D ( 'NONE', #60464, #22665, #486 ) ;
#238744=ORIENTED_EDGE ( 'NONE', *, *, #186367, .T. ) ;
#238754=AXIS2_PLACEMENT_3D ( 'NONE', #174032, #236517, #136109 ) ;
#238758=ORIENTED_EDGE ( 'NONE', *, *, #219778, .F. ) ;
#238765=EDGE_CURVE ( 'NONE', #79629, #105518, #177805, .T. ) ;
#238771=ORIENTED_EDGE ( 'NONE', *, *, #88699, .T. ) ;
#238777=FACE_OUTER_BOUND ( 'NONE', #204461, .T. ) ;
#238813=FACE_OUTER_BOUND ( 'NONE', #192002, .T. ) ;
#238826=DIRECTION ( 'NONE',  ( 0.000000000000000000, -0.008583690987162452199, -0.9999631594459053030 ) ) ;
#238847=VERTEX_POINT ( 'NONE', #76933 ) ;
#238859=DIRECTION ( 'NONE',  ( 0.000000000000000000, -6.982962677686266711E-15, 1.000000000000000000 ) ) ;
#238883=DIRECTION ( 'NONE',  ( 1.000000000000000000, -2.952720810173289112E-16, -2.061873921506763405E-30 ) ) ;
#238906=FACE_OUTER_BOUND ( 'NONE', #195654, .T. ) ;
#238910=CARTESIAN_POINT ( 'NONE',  ( -23.15000000000000213, 64.25000000001222134, -148.6731074845244507 ) ) ;
#238928=ORIENTED_EDGE ( 'NONE', *, *, #160265, .T. ) ;
#238950=DIRECTION ( 'NONE',  ( 0.000000000000000000, 0.000000000000000000, 1.000000000000000000 ) ) ;
#238970=AXIS2_PLACEMENT_3D ( 'NONE', #141880, #183589, #184856 ) ;
#238977=CARTESIAN_POINT ( 'NONE',  ( -21.14999999999999858, 87.65000000001235492, -167.1231074845242688 ) ) ;
#239037=ORIENTED_EDGE ( 'NONE', *, *, #137848, .F. ) ;
#239083=ORIENTED_EDGE ( 'NONE', *, *, #186340, .F. ) ;
#239114=CIRCLE ( 'NONE', #1593, 0.5000000000000004441 ) ;
#239116=AXIS2_PLACEMENT_3D ( 'NONE', #191364, #68833, #212196 ) ;
#239150=ADVANCED_FACE ( 'NONE', ( #108063 ), #190173, .F. ) ;
#239152=ORIENTED_EDGE ( 'NONE', *, *, #141267, .T. ) ;
#239159=VERTEX_POINT ( 'NONE', #151043 ) ;
#239231=EDGE_CURVE ( 'NONE', #235594, #59416, #130303, .T. ) ;
#239234=CIRCLE ( 'NONE', #255761, 0.09999999999998898659 ) ;
#239275=CARTESIAN_POINT ( 'NONE',  ( 22.50497660315937765, 76.07871793023797125, -181.7729029894197481 ) ) ;
#239285=AXIS2_PLACEMENT_3D ( 'NONE', #245873, #106329, #146736 ) ;
#239289=DIRECTION ( 'NONE',  ( 0.000000000000000000, 0.000000000000000000, -1.000000000000000000 ) ) ;
#239322=DIRECTION ( 'NONE',  ( -0.000000000000000000, 6.982962677686266711E-15, -1.000000000000000000 ) ) ;
#239327=FACE_OUTER_BOUND ( 'NONE', #195437, .T. ) ;
#239343=ORIENTED_EDGE ( 'NONE', *, *, #67009, .F. ) ;
#239348=ORIENTED_EDGE ( 'NONE', *, *, #162189, .T. ) ;
#239377=EDGE_CURVE ( 'NONE', #168523, #149398, #74128, .T. ) ;
#239406=DIRECTION ( 'NONE',  ( 1.000000000000000000, 0.000000000000000000, 0.000000000000000000 ) ) ;
#239431=DIRECTION ( 'NONE',  ( 0.000000000000000000, 6.982962677686266711E-15, -1.000000000000000000 ) ) ;
#239557=CARTESIAN_POINT ( 'NONE',  ( 21.05000000000000071, 69.65564095796925415, -170.0379631194183503 ) ) ;
#239591=EDGE_CURVE ( 'NONE', #34506, #203324, #35636, .T. ) ;
#239596=CARTESIAN_POINT ( 'NONE',  ( -18.59999999999999787, 77.16412189325330928, -128.6082593989527254 ) ) ;
#239628=CARTESIAN_POINT ( 'NONE',  ( 18.59999999999999076, 77.14957036958777792, -128.7071950000224092 ) ) ;
#239636=ORIENTED_EDGE ( 'NONE', *, *, #5572, .T. ) ;
#239641=ORIENTED_EDGE ( 'NONE', *, *, #257669, .F. ) ;
#239684=EDGE_CURVE ( 'NONE', #79646, #101850, #157519, .T. ) ;
#239694=AXIS2_PLACEMENT_3D ( 'NONE', #133441, #78589, #218088 ) ;
#239697=EDGE_CURVE ( 'NONE', #160821, #235594, #244763, .T. ) ;
#239699=ORIENTED_EDGE ( 'NONE', *, *, #31476, .T. ) ;
#239735=ORIENTED_EDGE ( 'NONE', *, *, #238350, .F. ) ;
#239750=ORIENTED_EDGE ( 'NONE', *, *, #105516, .T. ) ;
#239765=CARTESIAN_POINT ( 'NONE',  ( 23.14999999999999858, 74.00000000001213607, -136.5231074845243597 ) ) ;
#239771=LINE ( 'NONE', #61120, #62269 ) ;
#239776=EDGE_CURVE ( 'NONE', #60057, #140162, #143673, .T. ) ;
#239812=ORIENTED_EDGE ( 'NONE', *, *, #118683, .T. ) ;
#239866=FACE_OUTER_BOUND ( 'NONE', #151989, .T. ) ;
#239884=DIRECTION ( 'NONE',  ( -1.000000000000000000, 0.000000000000000000, 0.000000000000000000 ) ) ;
#239885=CYLINDRICAL_SURFACE ( 'NONE', #72311, 0.09999999999999939493 ) ;
#239908=EDGE_CURVE ( 'NONE', #57514, #108723, #199173, .T. ) ;
#239917=DIRECTION ( 'NONE',  ( 2.952720810173289112E-16, 1.000000000000000000, 1.261617073437673512E-14 ) ) ;
#239924=CARTESIAN_POINT ( 'NONE',  ( 18.52643265882457868, 65.68026841930924320, -130.9725740131889893 ) ) ;
#239948=ORIENTED_EDGE ( 'NONE', *, *, #45645, .F. ) ;
#239950=AXIS2_PLACEMENT_3D ( 'NONE', #58818, #61416, #123973 ) ;
#240002=CARTESIAN_POINT ( 'NONE',  ( -21.05000000000000071, 76.00000000001237765, -170.0231074845243597 ) ) ;
#240010=DIRECTION ( 'NONE',  ( 0.000000000000000000, 6.982962677686266711E-15, -1.000000000000000000 ) ) ;
#240057=EDGE_CURVE ( 'NONE', #176291, #115527, #99383, .T. ) ;
#240117=CARTESIAN_POINT ( 'NONE',  ( -20.94999999999999929, 74.83729825007431202, -161.9231074845243654 ) ) ;
#240129=CARTESIAN_POINT ( 'NONE',  ( -21.05000000000000071, 76.00000000001234923, -165.7231074845244052 ) ) ;
#240147=ORIENTED_EDGE ( 'NONE', *, *, #52880, .T. ) ;
#240174=DIRECTION ( 'NONE',  ( 0.000000000000000000, 1.000000000000000000, -5.551115123125777653E-14 ) ) ;
#240179=FACE_OUTER_BOUND ( 'NONE', #4035, .T. ) ;
#240184=CYLINDRICAL_SURFACE ( 'NONE', #110857, 4.000000000000003553 ) ;
#240207=FACE_OUTER_BOUND ( 'NONE', #158741, .T. ) ;
#240220=DIRECTION ( 'NONE',  ( -3.265361837132813093E-16, -1.000000000000000000, 7.445645354460596589E-46 ) ) ;
#240241=VERTEX_POINT ( 'NONE', #8994 ) ;
#240243=ORIENTED_EDGE ( 'NONE', *, *, #7344, .F. ) ;
#240264=CARTESIAN_POINT ( 'NONE',  ( -21.55000000000000426, 68.29142135624960019, -157.6731074845243938 ) ) ;
#240269=DIRECTION ( 'NONE',  ( 1.000000000000000000, -3.265361837132813093E-16, -2.280189983783949500E-30 ) ) ;
#240286=DIRECTION ( 'NONE',  ( 0.000000000000000000, 0.9654727137038715545, -0.2605042016806676242 ) ) ;
#240310=DIRECTION ( 'NONE',  ( 0.000000000000000000, -6.454785026890406770E-15, 1.000000000000000000 ) ) ;
#240312=ORIENTED_EDGE ( 'NONE', *, *, #161270, .F. ) ;
#240335=EDGE_CURVE ( 'NONE', #138313, #217847, #31168, .T. ) ;
#240370=ORIENTED_EDGE ( 'NONE', *, *, #105663, .F. ) ;
#240374=CARTESIAN_POINT ( 'NONE',  ( -18.59999999999999787, 77.16270174995034381, -161.9231074845243370 ) ) ;
#240376=DIRECTION ( 'NONE',  ( -0.000000000000000000, -6.982962677686266711E-15, 1.000000000000000000 ) ) ;
#240379=AXIS2_PLACEMENT_3D ( 'NONE', #255992, #156975, #218179 ) ;
#240394=CARTESIAN_POINT ( 'NONE',  ( 20.94999999999999929, 65.61821452928816711, -131.0152621206402443 ) ) ;
#240426=CIRCLE ( 'NONE', #152978, 0.09999999999998898659 ) ;
#240428=VERTEX_POINT ( 'NONE', #57076 ) ;
#240435=EDGE_CURVE ( 'NONE', #11624, #75529, #82781, .T. ) ;
#240450=CARTESIAN_POINT ( 'NONE',  ( -20.54999999999999716, 76.00000000001212186, -134.6231074845243256 ) ) ;
#240476=EDGE_CURVE ( 'NONE', #115854, #99277, #16221, .T. ) ;
#240480=CARTESIAN_POINT ( 'NONE',  ( -18.49499033040906681, 85.43814877175698541, -162.8249542586008545 ) ) ;
#240507=EDGE_LOOP ( 'NONE', ( #215435, #136461, #172085, #233618 ) ) ;
#240541=ORIENTED_EDGE ( 'NONE', *, *, #139749, .F. ) ;
#240547=AXIS2_PLACEMENT_3D ( 'NONE', #46987, #126552, #246492 ) ;
#240571=VERTEX_POINT ( 'NONE', #143037 ) ;
#240575=CARTESIAN_POINT ( 'NONE',  ( 18.39999999999999858, 85.60000000001232934, -162.9910380878246201 ) ) ;
#240579=DIRECTION ( 'NONE',  ( 0.000000000000000000, 0.000000000000000000, 1.000000000000000000 ) ) ;
#240592=CARTESIAN_POINT ( 'NONE',  ( 18.49999999999999645, 70.05000000001236060, -159.7174051794895320 ) ) ;
#240601=CIRCLE ( 'NONE', #153165, 2.100000000000004530 ) ;
#240617=CARTESIAN_POINT ( 'NONE',  ( -21.05000000000000071, 76.00000000001237765, -170.0231074845243597 ) ) ;
#240642=AXIS2_PLACEMENT_3D ( 'NONE', #184191, #128090, #145067 ) ;
#240697=CARTESIAN_POINT ( 'NONE',  ( 20.84999999999998721, 65.66751761918692409, -130.9282609406112670 ) ) ;
#240712=CARTESIAN_POINT ( 'NONE',  ( 21.05000000000000071, 70.50000000001223555, -148.9283735034374843 ) ) ;
#240736=DIRECTION ( 'NONE',  ( 0.000000000000000000, -0.1350103645451807555, -0.9908441862701610203 ) ) ;
#240754=TOROIDAL_SURFACE ( 'NONE', #15927, 4.149999999999999467, 0.1000000000000000056 ) ;
#240759=EDGE_LOOP ( 'NONE', ( #32140, #15152, #121473, #232662 ) ) ;
#240763=CARTESIAN_POINT ( 'NONE',  ( 21.14999999999999858, 67.21339244341217523, -157.6731074845244223 ) ) ;
#240781=ORIENTED_EDGE ( 'NONE', *, *, #206946, .T. ) ;
#240871=EDGE_LOOP ( 'NONE', ( #153160, #54373, #160829, #228249 ) ) ;
#240876=AXIS2_PLACEMENT_3D ( 'NONE', #180743, #30348, #81594 ) ;
#240888=DIRECTION ( 'NONE',  ( 1.000000000000000000, 0.000000000000000000, 0.000000000000000000 ) ) ;
#240902=LINE ( 'NONE', #89505, #242756 ) ;
#240951=CARTESIAN_POINT ( 'NONE',  ( -18.50000000000000000, 68.87972903831453664, -132.8635444426850825 ) ) ;
#241003=ORIENTED_EDGE ( 'NONE', *, *, #19152, .T. ) ;
#241030=DIRECTION ( 'NONE',  ( 1.000000000000000000, -3.265361837132813093E-16, -2.280189983783949500E-30 ) ) ;
#241084=DIRECTION ( 'NONE',  ( 0.000000000000000000, -7.304098846218085561E-15, 1.000000000000000000 ) ) ;
#241091=CYLINDRICAL_SURFACE ( 'NONE', #16397, 0.1000000000000070832 ) ;
#241092=CARTESIAN_POINT ( 'NONE',  ( -20.54999999999999716, 71.65000000001222702, -148.7731074845243882 ) ) ;
#241115=DIRECTION ( 'NONE',  ( 1.000000000000000000, 0.000000000000000000, 0.000000000000000000 ) ) ;
#241125=ADVANCED_FACE ( 'NONE', ( #196025 ), #151774, .F. ) ;
#241143=LINE ( 'NONE', #117325, #223645 ) ;
#241161=FACE_OUTER_BOUND ( 'NONE', #228549, .T. ) ;
#241166=DIRECTION ( 'NONE',  ( -0.000000000000000000, 1.000000000000000000, 7.172728831056617961E-15 ) ) ;
#241170=CIRCLE ( 'NONE', #24704, 0.09999999999998898659 ) ;
#241171=AXIS2_PLACEMENT_3D ( 'NONE', #46012, #125556, #206386 ) ;
#241172=CARTESIAN_POINT ( 'NONE',  ( -23.15000000000000213, 85.50000000001222134, -146.4170766071767389 ) ) ;
#241229=FACE_BOUND ( 'NONE', #167524, .T. ) ;
#241247=VERTEX_POINT ( 'NONE', #231301 ) ;
#241251=ADVANCED_FACE ( 'NONE', ( #211738 ), #132185, .T. ) ;
#241312=ORIENTED_EDGE ( 'NONE', *, *, #54045, .T. ) ;
#241317=EDGE_LOOP ( 'NONE', ( #233039, #15727, #133409, #46146 ) ) ;
#241324=ORIENTED_EDGE ( 'NONE', *, *, #235735, .T. ) ;
#241329=EDGE_LOOP ( 'NONE', ( #180567, #64130, #61343, #40266 ) ) ;
#241336=ORIENTED_EDGE ( 'NONE', *, *, #43760, .F. ) ;
#241368=CARTESIAN_POINT ( 'NONE',  ( 20.85000000000000142, 76.00000000001207923, -128.6231074845243540 ) ) ;
#241379=ADVANCED_FACE ( 'NONE', ( #3909 ), #166053, .T. ) ;
#241383=EDGE_LOOP ( 'NONE', ( #30271, #183332, #29231, #10796, #130220 ) ) ;
#241405=CARTESIAN_POINT ( 'NONE',  ( -21.05000000000000071, 64.35000000001238618, -169.9231074845244507 ) ) ;
#241419=CIRCLE ( 'NONE', #75019, 0.2000000000000057288 ) ;
#241427=AXIS2_PLACEMENT_3D ( 'NONE', #98407, #37217, #5425 ) ;
#241446=CARTESIAN_POINT ( 'NONE',  ( 20.44999100639871514, 65.56028929680051931, -162.2640317585554044 ) ) ;
#241461=DIRECTION ( 'NONE',  ( 0.000000000000000000, -6.938893903907222067E-15, 1.000000000000000000 ) ) ;
#241463=DIRECTION ( 'NONE',  ( -1.000000000000000000, 0.000000000000000000, -0.000000000000000000 ) ) ;
#241521=EDGE_LOOP ( 'NONE', ( #81054, #155511, #4147 ) ) ;
#241527=AXIS2_PLACEMENT_3D ( 'NONE', #136501, #54417, #195246 ) ;
#241534=DIRECTION ( 'NONE',  ( 0.000000000000000000, -7.124650136758317602E-15, 1.000000000000000000 ) ) ;
#241539=CIRCLE ( 'NONE', #141569, 4.099999999999992539 ) ;
#241561=CARTESIAN_POINT ( 'NONE',  ( 21.04105312098497649, 67.12466737696867369, -157.6946007373123564 ) ) ;
#241610=CYLINDRICAL_SURFACE ( 'NONE', #236814, 0.1000000000000118433 ) ;
#241638=AXIS2_PLACEMENT_3D ( 'NONE', #48506, #185460, #204990 ) ;
#241641=VERTEX_POINT ( 'NONE', #187251 ) ;
#241654=DIRECTION ( 'NONE',  ( -0.000000000000000000, 6.982962677686266711E-15, -1.000000000000000000 ) ) ;
#241659=DIRECTION ( 'NONE',  ( -0.000000000000000000, -6.982962677686266711E-15, 1.000000000000000000 ) ) ;
#241691=DIRECTION ( 'NONE',  ( -2.840903330521632269E-16, -0.8700118002898356018, 0.4930308989875170078 ) ) ;
#241713=EDGE_CURVE ( 'NONE', #25616, #6721, #74673, .T. ) ;
#241727=DIRECTION ( 'NONE',  ( 0.000000000000000000, -6.982962677686266711E-15, 1.000000000000000000 ) ) ;
#241788=TOROIDAL_SURFACE ( 'NONE', #12862, 11.70000000000000462, 0.1000000000000000056 ) ;
#241815=B_SPLINE_CURVE_WITH_KNOTS ( 'NONE', 3,
 ( #208556, #29925, #91154, #170750, #131567, #109418, #229397, #50714, #190271, #11641 ),
 .UNSPECIFIED., .F., .F.,
 ( 4, 3, 3, 4 ),
 ( 0.000000000000000000, 3.394313611811463347E-05, 6.779740500699467213E-05, 0.0001049857339142579784 ),
 .UNSPECIFIED. ) ;
#241837=B_SPLINE_CURVE_WITH_KNOTS ( 'NONE', 3,
 ( #222733, #204454, #148347, #10126, #143201, #207042, #167942, #227885, #105326, #169231 ),
 .UNSPECIFIED., .F., .F.,
 ( 4, 3, 3, 4 ),
 ( 0.000000000000000000, 0.0002000000000002908468, 0.001000000000045115191, 0.001967863649472108723 ),
 .UNSPECIFIED. ) ;
#241863=ORIENTED_EDGE ( 'NONE', *, *, #87036, .F. ) ;
#241904=LINE ( 'NONE', #84069, #73063 ) ;
#241929=ADVANCED_FACE ( 'NONE', ( #92973 ), #211663, .T. ) ;
#241979=VERTEX_POINT ( 'NONE', #98078 ) ;
#241982=CARTESIAN_POINT ( 'NONE',  ( -20.00857864376270001, 66.65000000001222702, -148.8731074845244393 ) ) ;
#242012=ORIENTED_EDGE ( 'NONE', *, *, #236028, .T. ) ;
#242061=EDGE_CURVE ( 'NONE', #88568, #91302, #37409, .T. ) ;
#242070=ADVANCED_FACE ( 'NONE', ( #240207 ), #208101, .T. ) ;
#242088=EDGE_CURVE ( 'NONE', #71592, #104858, #19879, .T. ) ;
#242091=EDGE_CURVE ( 'NONE', #199740, #187756, #101934, .T. ) ;
#242096=SPHERICAL_SURFACE ( 'NONE', #59312, 0.1000000000000000056 ) ;
#242111=CARTESIAN_POINT ( 'NONE',  ( -23.15000000000000213, 64.35000000001228670, -157.8731074845244393 ) ) ;
#242121=AXIS2_PLACEMENT_3D ( 'NONE', #177418, #176128, #135673 ) ;
#242133=CARTESIAN_POINT ( 'NONE',  ( 21.07964655665547227, 67.22511038503374436, -157.8011909015603749 ) ) ;
#242152=CARTESIAN_POINT ( 'NONE',  ( 21.14999999999999858, 76.00000000001246292, -181.6726782920691505 ) ) ;
#242166=VERTEX_POINT ( 'NONE', #202349 ) ;
#242183=CARTESIAN_POINT ( 'NONE',  ( 23.15000000000000213, 87.65000000001215597, -139.5231074845243029 ) ) ;
#242209=ORIENTED_EDGE ( 'NONE', *, *, #95989, .T. ) ;
#242225=CARTESIAN_POINT ( 'NONE',  ( -20.94999999999999929, 76.00000000001213607, -136.5231074845243313 ) ) ;
#242231=DIRECTION ( 'NONE',  ( 0.000000000000000000, 0.000000000000000000, 1.000000000000000000 ) ) ;
#242247=PLANE ( 'NONE',  #68081 ) ;
#242249=ADVANCED_FACE ( 'NONE', ( #32742 ), #203981, .F. ) ;
#242257=DIRECTION ( 'NONE',  ( 0.000000000000000000, -1.000000000000000000, -6.982962677686266711E-15 ) ) ;
#242261=EDGE_CURVE ( 'NONE', #223637, #189423, #90087, .T. ) ;
#242282=ORIENTED_EDGE ( 'NONE', *, *, #198683, .F. ) ;
#242315=AXIS2_PLACEMENT_3D ( 'NONE', #216090, #37483, #218654 ) ;
#242323=CARTESIAN_POINT ( 'NONE',  ( 20.94999999999999929, 64.36312671090810511, -143.3448666978490849 ) ) ;
#242332=AXIS2_PLACEMENT_3D ( 'NONE', #152337, #256469, #94885 ) ;
#242338=ORIENTED_EDGE ( 'NONE', *, *, #42281, .T. ) ;
#242376=VERTEX_POINT ( 'NONE', #176091 ) ;
#242395=ORIENTED_EDGE ( 'NONE', *, *, #7344, .T. ) ;
#242456=EDGE_CURVE ( 'NONE', #53585, #3049, #241419, .T. ) ;
#242461=CARTESIAN_POINT ( 'NONE',  ( -23.15000000000000213, 64.35000000001218723, -143.5379132551784096 ) ) ;
#242474=EDGE_CURVE ( 'NONE', #121863, #138951, #20856, .T. ) ;
#242481=DIRECTION ( 'NONE',  ( 1.000000000000000000, 0.000000000000000000, 0.000000000000000000 ) ) ;
#242482=ORIENTED_EDGE ( 'NONE', *, *, #29356, .T. ) ;
#242483=FACE_OUTER_BOUND ( 'NONE', #227758, .T. ) ;
#242495=ORIENTED_EDGE ( 'NONE', *, *, #153670, .F. ) ;
#242532=FACE_OUTER_BOUND ( 'NONE', #253174, .T. ) ;
#242547=CARTESIAN_POINT ( 'NONE',  ( -22.49806830649814415, 64.35011034517329165, -170.1005718008499343 ) ) ;
#242548=CARTESIAN_POINT ( 'NONE',  ( 20.84999999999999787, 64.25000000001219291, -143.4422547304831710 ) ) ;
#242572=EDGE_CURVE ( 'NONE', #232077, #248304, #220732, .T. ) ;
#242626=CARTESIAN_POINT ( 'NONE',  ( 20.00000000000000355, 64.25000000001220712, -145.3731074845244393 ) ) ;
#242631=CARTESIAN_POINT ( 'NONE',  ( 21.12769345151713196, 65.28071232307172522, -157.7756271383269393 ) ) ;
#242637=ORIENTED_EDGE ( 'NONE', *, *, #203043, .T. ) ;
#242649=ORIENTED_EDGE ( 'NONE', *, *, #187026, .T. ) ;
#242674=CARTESIAN_POINT ( 'NONE',  ( 20.94999999999999929, 71.14953271029267512, -157.9888400755227167 ) ) ;
#242684=VECTOR ( 'NONE', #175140, 1000.000000000000000 ) ;
#242690=EDGE_CURVE ( 'NONE', #162856, #243905, #187429, .T. ) ;
#242693=CIRCLE ( 'NONE', #180351, 0.09999999999999939493 ) ;
#242747=FACE_OUTER_BOUND ( 'NONE', #71632, .T. ) ;
#242750=ADVANCED_FACE ( 'NONE', ( #171944 ), #53239, .F. ) ;
#242756=VECTOR ( 'NONE', #169099, 1000.000000000000000 ) ;
#242772=FACE_OUTER_BOUND ( 'NONE', #94492, .T. ) ;
#242774=CIRCLE ( 'NONE', #172091, 4.149999999999987033 ) ;
#242790=EDGE_LOOP ( 'NONE', ( #94101, #106219, #205057, #245854 ) ) ;
#242812=CARTESIAN_POINT ( 'NONE',  ( 18.59999999999997655, 76.00000000001213607, -136.5231074845243313 ) ) ;
#242814=EDGE_CURVE ( 'NONE', #11624, #219843, #40122, .T. ) ;
#242822=CARTESIAN_POINT ( 'NONE',  ( -21.05000000000000071, 69.45934304831114048, -170.0231074845243882 ) ) ;
#242844=CIRCLE ( 'NONE', #59643, 12.77499999999999503 ) ;
#242847=AXIS2_PLACEMENT_3D ( 'NONE', #198905, #99780, #195087 ) ;
#242893=ORIENTED_EDGE ( 'NONE', *, *, #142432, .F. ) ;
#242903=ORIENTED_EDGE ( 'NONE', *, *, #40593, .F. ) ;
#242925=DIRECTION ( 'NONE',  ( 1.836970198721029934E-16, 1.000000000000000000, 6.982962677686266711E-15 ) ) ;
#242934=SPHERICAL_SURFACE ( 'NONE', #132401, 0.1000000000000000056 ) ;
#242945=DIRECTION ( 'NONE',  ( -1.000000000000000000, 0.000000000000000000, -0.000000000000000000 ) ) ;
#242952=DIRECTION ( 'NONE',  ( -0.8660254037843277963, 0.000000000000000000, 0.5000000000001921796 ) ) ;
#242967=AXIS2_PLACEMENT_3D ( 'NONE', #28688, #7802, #62637 ) ;
#242987=CARTESIAN_POINT ( 'NONE',  ( -22.39999999999999858, 64.35000000001238618, -170.0231074845244166 ) ) ;
#242989=EDGE_CURVE ( 'NONE', #223292, #4792, #91910, .T. ) ;
#243024=CIRCLE ( 'NONE', #76424, 0.09999999999998898659 ) ;
#243026=DIRECTION ( 'NONE',  ( 2.915501640297156255E-16, 1.000000000000000000, 6.997203936713175802E-15 ) ) ;
#243035=CARTESIAN_POINT ( 'NONE',  ( 23.14999999999999858, 70.50000000001230660, -157.6178414656113205 ) ) ;
#243070=CIRCLE ( 'NONE', #68302, 11.80000000000000426 ) ;
#243071=ORIENTED_EDGE ( 'NONE', *, *, #216633, .T. ) ;
#243078=EDGE_CURVE ( 'NONE', #207248, #127786, #223838, .T. ) ;
#243090=AXIS2_PLACEMENT_3D ( 'NONE', #194409, #15780, #116144 ) ;
#243124=CIRCLE ( 'NONE', #176515, 0.09999999999998898659 ) ;
#243145=CARTESIAN_POINT ( 'NONE',  ( -23.15000000000000213, 64.25000000001219291, -143.3647081744214802 ) ) ;
#243167=DIRECTION ( 'NONE',  ( 0.000000000000000000, -6.938893903907222067E-15, 1.000000000000000000 ) ) ;
#243208=ORIENTED_EDGE ( 'NONE', *, *, #249338, .F. ) ;
#243248=DIRECTION ( 'NONE',  ( 0.000000000000000000, 0.000000000000000000, 1.000000000000000000 ) ) ;
#243249=ORIENTED_EDGE ( 'NONE', *, *, #180106, .T. ) ;
#243296=EDGE_CURVE ( 'NONE', #235293, #1901, #254389, .T. ) ;
#243299=ORIENTED_EDGE ( 'NONE', *, *, #125992, .T. ) ;
#243318=ORIENTED_EDGE ( 'NONE', *, *, #224744, .T. ) ;
#243348=CARTESIAN_POINT ( 'NONE',  ( 21.00000000000000000, 66.25000000001223555, -148.8731074845244393 ) ) ;
#243369=AXIS2_PLACEMENT_3D ( 'NONE', #136303, #213292, #152074 ) ;
#243375=AXIS2_PLACEMENT_3D ( 'NONE', #127075, #224872, #48814 ) ;
#243407=CARTESIAN_POINT ( 'NONE',  ( -20.64999999999999858, 71.65000000001222702, -148.7731074845243882 ) ) ;
#243463=ADVANCED_FACE ( 'NONE', ( #187025 ), #111322, .F. ) ;
#243465=VERTEX_POINT ( 'NONE', #50051 ) ;
#243496=ORIENTED_EDGE ( 'NONE', *, *, #120686, .F. ) ;
#243528=DIRECTION ( 'NONE',  ( 0.000000000000000000, -1.000000000000000000, -7.272083257015735086E-15 ) ) ;
#243537=EDGE_CURVE ( 'NONE', #218463, #38071, #46298, .T. ) ;
#243567=ORIENTED_EDGE ( 'NONE', *, *, #247298, .F. ) ;
#243585=EDGE_CURVE ( 'NONE', #216520, #145447, #104719, .T. ) ;
#243594=ORIENTED_EDGE ( 'NONE', *, *, #48001, .T. ) ;
#243601=DIRECTION ( 'NONE',  ( 0.000000000000000000, 0.4930308989874980785, 0.8700118002898462599 ) ) ;
#243604=ORIENTED_EDGE ( 'NONE', *, *, #45296, .T. ) ;
#243608=CARTESIAN_POINT ( 'NONE',  ( -20.07928932188135107, 66.77928932189357170, -148.8731074845244393 ) ) ;
#243633=ORIENTED_EDGE ( 'NONE', *, *, #116442, .F. ) ;
#243640=CARTESIAN_POINT ( 'NONE',  ( -21.05000000000000071, 64.40000000001219860, -143.4513107147999449 ) ) ;
#243677=CARTESIAN_POINT ( 'NONE',  ( 20.94999999999999929, 71.00000000001230660, -157.6178414656113205 ) ) ;
#243685=EDGE_CURVE ( 'NONE', #205324, #212994, #17292, .T. ) ;
#243735=ADVANCED_FACE ( 'NONE', ( #242483 ), #143388, .F. ) ;
#243769=ORIENTED_EDGE ( 'NONE', *, *, #246900, .T. ) ;
#243798=ORIENTED_EDGE ( 'NONE', *, *, #124110, .F. ) ;
#243841=ORIENTED_EDGE ( 'NONE', *, *, #65839, .T. ) ;
#243850=EDGE_CURVE ( 'NONE', #70242, #188351, #196327, .T. ) ;
#243869=ORIENTED_EDGE ( 'NONE', *, *, #136835, .F. ) ;
#243885=VERTEX_POINT ( 'NONE', #170711 ) ;
#243905=VERTEX_POINT ( 'NONE', #53283 ) ;
#243943=ORIENTED_EDGE ( 'NONE', *, *, #165335, .T. ) ;
#243959=DIRECTION ( 'NONE',  ( 0.000000000000000000, -0.1350103645451945777, 0.9908441862701590219 ) ) ;
#243968=DIRECTION ( 'NONE',  ( 1.000000000000000000, 0.000000000000000000, 0.000000000000000000 ) ) ;
#243977=CARTESIAN_POINT ( 'NONE',  ( -23.15000000000000213, 64.40000000001219860, -143.4513107147999449 ) ) ;
#243979=CIRCLE ( 'NONE', #89854, 0.1000000000000070832 ) ;
#244007=DIRECTION ( 'NONE',  ( 0.000000000000000000, -8.717686153663073805E-15, 1.000000000000000000 ) ) ;
#244061=ORIENTED_EDGE ( 'NONE', *, *, #114701, .F. ) ;
#244071=CARTESIAN_POINT ( 'NONE',  ( -20.94999999999999929, 77.36242903720540198, -128.6342262366031548 ) ) ;
#244088=DIRECTION ( 'NONE',  ( 1.000000000000000000, 0.000000000000000000, 0.000000000000000000 ) ) ;
#244104=DIRECTION ( 'NONE',  ( 0.000000000000000000, 6.982962677686266711E-15, -1.000000000000000000 ) ) ;
#244119=CARTESIAN_POINT ( 'NONE',  ( 21.14999999999999858, 67.21339244341217523, -157.7731074845244166 ) ) ;
#244166=ORIENTED_EDGE ( 'NONE', *, *, #216867, .F. ) ;
#244192=AXIS2_PLACEMENT_3D ( 'NONE', #181811, #60565, #196228 ) ;
#244200=FACE_OUTER_BOUND ( 'NONE', #32158, .T. ) ;
#244212=AXIS2_PLACEMENT_3D ( 'NONE', #84045, #144053, #223587 ) ;
#244219=SPHERICAL_SURFACE ( 'NONE', #44530, 0.1000000000000000056 ) ;
#244244=CYLINDRICAL_SURFACE ( 'NONE', #12680, 0.09999999999998898659 ) ;
#244253=CARTESIAN_POINT ( 'NONE',  ( -21.00219873199078435, 64.39461131213575129, -163.1104600562298401 ) ) ;
#244371=CARTESIAN_POINT ( 'NONE',  ( 18.59999999999999076, 74.16465844978787914, -158.3679561919613832 ) ) ;
#244372=CARTESIAN_POINT ( 'NONE',  ( -20.54999999999999716, 87.75000000001223555, -148.8731074845242972 ) ) ;
#244400=FACE_OUTER_BOUND ( 'NONE', #6265, .T. ) ;
#244419=AXIS2_PLACEMENT_3D ( 'NONE', #145330, #125768, #26705 ) ;
#244431=DIRECTION ( 'NONE',  ( -0.000000000000000000, -6.982962677686266711E-15, 1.000000000000000000 ) ) ;
#244480=DIRECTION ( 'NONE',  ( 0.000000000000000000, 0.000000000000000000, 1.000000000000000000 ) ) ;
#244485=ORIENTED_EDGE ( 'NONE', *, *, #148858, .F. ) ;
#244509=VERTEX_POINT ( 'NONE', #5804 ) ;
#244556=ORIENTED_EDGE ( 'NONE', *, *, #182156, .F. ) ;
#244569=EDGE_CURVE ( 'NONE', #76314, #111495, #142526, .T. ) ;
#244608=FACE_OUTER_BOUND ( 'NONE', #250078, .T. ) ;
#244612=CARTESIAN_POINT ( 'NONE',  ( -18.59999999999999787, 85.48068669529106955, -129.5819923157664562 ) ) ;
#244630=ADVANCED_FACE ( 'NONE', ( #209156 ), #146599, .T. ) ;
#244641=DIRECTION ( 'NONE',  ( 0.000000000000000000, 0.8660254037844424824, 0.4999999999999934497 ) ) ;
#244656=ORIENTED_EDGE ( 'NONE', *, *, #75087, .F. ) ;
#244688=DIRECTION ( 'NONE',  ( -1.000000000000000000, -0.000000000000000000, -0.000000000000000000 ) ) ;
#244689=EDGE_CURVE ( 'NONE', #45573, #228499, #64276, .T. ) ;
#244698=CARTESIAN_POINT ( 'NONE',  ( 23.14999999999999858, 72.00000000001213607, -136.5231074845243597 ) ) ;
#244760=EDGE_CURVE ( 'NONE', #128659, #209214, #76732, .T. ) ;
#244761=VERTEX_POINT ( 'NONE', #13545 ) ;
#244763=CIRCLE ( 'NONE', #132342, 6.329289321881370611 ) ;
#244808=VERTEX_POINT ( 'NONE', #57776 ) ;
#244821=VECTOR ( 'NONE', #257373, 1000.000000000000000 ) ;
#244825=DIRECTION ( 'NONE',  ( 1.000000000000000000, 0.000000000000000000, 0.000000000000000000 ) ) ;
#244844=VERTEX_POINT ( 'NONE', #38242 ) ;
#244853=EDGE_LOOP ( 'NONE', ( #108117, #112166, #251082 ) ) ;
#244857=CARTESIAN_POINT ( 'NONE',  ( -23.25000000000000000, 77.16412189325330928, -128.6082593989527254 ) ) ;
#244884=ORIENTED_EDGE ( 'NONE', *, *, #170637, .F. ) ;
#244886=CARTESIAN_POINT ( 'NONE',  ( -18.59999999999999787, 85.40000000001209912, -129.6410656363516125 ) ) ;
#244893=FACE_OUTER_BOUND ( 'NONE', #201519, .T. ) ;
#244911=FACE_OUTER_BOUND ( 'NONE', #108632, .T. ) ;
#244949=AXIS2_PLACEMENT_3D ( 'NONE', #130892, #33131, #192177 ) ;
#244957=ORIENTED_EDGE ( 'NONE', *, *, #254569, .F. ) ;
#244966=CIRCLE ( 'NONE', #99197, 0.09999999999999939493 ) ;
#244975=DIRECTION ( 'NONE',  ( 0.000000000000000000, 0.8660254037844281605, -0.5000000000000185407 ) ) ;
#245009=VERTEX_POINT ( 'NONE', #143741 ) ;
#245016=CARTESIAN_POINT ( 'NONE',  ( -20.64999999999999858, 85.00000000001222134, -146.4170766071767389 ) ) ;
#245032=EDGE_CURVE ( 'NONE', #157707, #64893, #201819, .T. ) ;
#245038=CARTESIAN_POINT ( 'NONE',  ( -18.59999999999999787, 85.32100840337361092, -162.7871692354464130 ) ) ;
#245105=( BOUNDED_CURVE ( )  B_SPLINE_CURVE ( 3, ( #141658, #221184, #201630, #197778 ),
 .UNSPECIFIED., .F., .F. ) 
 B_SPLINE_CURVE_WITH_KNOTS ( ( 4, 4 ),
 ( 3.192897208853993085, 4.712388980384689674 ),
 .UNSPECIFIED. ) 
 CURVE ( )  GEOMETRIC_REPRESENTATION_ITEM ( )  RATIONAL_B_SPLINE_CURVE ( ( 1.000000000000000000, 0.8166740347213228279, 0.8166740347213228279, 1.000000000000000000 ) ) 
 REPRESENTATION_ITEM ( '' )  );
#245113=EDGE_CURVE ( 'NONE', #23601, #237787, #150188, .T. ) ;
#245144=EDGE_LOOP ( 'NONE', ( #159591, #215282, #34191, #190663, #141328 ) ) ;
#245152=AXIS2_PLACEMENT_3D ( 'NONE', #255561, #213921, #76971 ) ;
#245175=LINE ( 'NONE', #66541, #236105 ) ;
#245216=CARTESIAN_POINT ( 'NONE',  ( 21.14999999999999858, 69.35000000001228670, -157.6731074845243938 ) ) ;
#245269=CIRCLE ( 'NONE', #132837, 0.5000000000000004441 ) ;
#245284=EDGE_LOOP ( 'NONE', ( #12946, #155157, #216408, #150292 ) ) ;
#245287=DIRECTION ( 'NONE',  ( -1.000000000000000000, 0.000000000000000000, -0.000000000000000000 ) ) ;
#245377=EDGE_CURVE ( 'NONE', #232077, #34228, #114337, .T. ) ;
#245421=PLANE ( 'NONE',  #114464 ) ;
#245423=DIRECTION ( 'NONE',  ( 9.044546369203337730E-15, 0.7397360091702647189, 0.6728971962616949742 ) ) ;
#245430=EDGE_CURVE ( 'NONE', #184336, #39426, #226764, .T. ) ;
#245456=ORIENTED_EDGE ( 'NONE', *, *, #242456, .F. ) ;
#245458=ORIENTED_EDGE ( 'NONE', *, *, #248808, .T. ) ;
#245496=ORIENTED_EDGE ( 'NONE', *, *, #214430, .F. ) ;
#245508=EDGE_CURVE ( 'NONE', #69713, #75413, #73376, .T. ) ;
#245514=ORIENTED_EDGE ( 'NONE', *, *, #21398, .T. ) ;
#245532=CIRCLE ( 'NONE', #203999, 0.09999999999998898659 ) ;
#245605=AXIS2_PLACEMENT_3D ( 'NONE', #163300, #15119, #35972 ) ;
#245622=CARTESIAN_POINT ( 'NONE',  ( 21.05000000000000071, 70.60000000001221565, -146.4170766071768526 ) ) ;
#245657=CARTESIAN_POINT ( 'NONE',  ( -23.15000000000000213, 76.00000000001216449, -140.4231074845243370 ) ) ;
#245665=ORIENTED_EDGE ( 'NONE', *, *, #243537, .F. ) ;
#245696=AXIS2_PLACEMENT_3D ( 'NONE', #70598, #247909, #147535 ) ;
#245708=DIRECTION ( 'NONE',  ( -1.000000000000000000, 0.000000000000000000, 0.000000000000000000 ) ) ;
#245730=DIRECTION ( 'NONE',  ( 0.000000000000000000, -0.6728971962617102953, -0.7397360091702507301 ) ) ;
#245758=EDGE_CURVE ( 'NONE', #116101, #16833, #224399, .T. ) ;
#245778=FACE_OUTER_BOUND ( 'NONE', #53071, .T. ) ;
#245795=VERTEX_POINT ( 'NONE', #28831 ) ;
#245807=VECTOR ( 'NONE', #230558, 1000.000000000000000 ) ;
#245815=EDGE_LOOP ( 'NONE', ( #246866, #167404, #219750, #193823 ) ) ;
#245818=CARTESIAN_POINT ( 'NONE',  ( -23.25000000000000000, 85.60000000001221565, -146.4170766071767389 ) ) ;
#245827=EDGE_CURVE ( 'NONE', #58185, #60353, #178857, .T. ) ;
#245854=ORIENTED_EDGE ( 'NONE', *, *, #8783, .F. ) ;
#245862=VECTOR ( 'NONE', #62223, 1000.000000000000000 ) ;
#245863=CARTESIAN_POINT ( 'NONE',  ( 21.08489834409762054, 65.37767610527676254, -157.6731074845243938 ) ) ;
#245873=CARTESIAN_POINT ( 'NONE',  ( -21.05000000000000071, 76.00000000001210765, -132.4231074845243370 ) ) ;
#245875=DIRECTION ( 'NONE',  ( 0.000000000000000000, -6.982962677686266711E-15, 1.000000000000000000 ) ) ;
#245893=AXIS2_PLACEMENT_3D ( 'NONE', #121484, #116332, #155484 ) ;
#245899=EDGE_CURVE ( 'NONE', #200182, #168523, #13088, .T. ) ;
#245936=( BOUNDED_SURFACE ( )  B_SPLINE_SURFACE ( 3, 2, ( 
 ( #17622, #94596, #132451 ),
 ( #153344, #97129, #236671 ),
 ( #112891, #55444, #58023 ),
 ( #176733, #37220, #253665 ),
 ( #213259, #114168, #256179 ),
 ( #115447, #134993, #215815 ) ),
 .UNSPECIFIED., .F., .F., .F. ) 
 B_SPLINE_SURFACE_WITH_KNOTS ( ( 4, 2, 4 ),
 ( 3, 3 ),
 ( 3.141592653589783346, 3.926990816987233845, 4.712388980384684345 ),
 ( 0.000000000000000000, 1.000000000000000000 ),
 .UNSPECIFIED. ) 
 GEOMETRIC_REPRESENTATION_ITEM ( )  RATIONAL_B_SPLINE_SURFACE ( (
 ( 1.000000000000000000, 0.9238795325112774126, 1.000000000000000000),
 ( 1.000000000000000000, 0.9240297172243894241, 1.000000000000000000),
 ( 1.000000000000000000, 0.9038128468038970631, 1.000000000000000000),
 ( 1.000000000000000000, 0.8282379607649767994, 1.000000000000000000),
 ( 1.000000000000000000, 0.7727932973491338231, 1.000000000000000000),
 ( 1.000000000000000000, 0.7071067811865475727, 1.000000000000000000) ) ) 
 REPRESENTATION_ITEM ( '' )  SURFACE ( )  );
#245943=EDGE_CURVE ( 'NONE', #77748, #252845, #162081, .T. ) ;
#245960=ORIENTED_EDGE ( 'NONE', *, *, #29547, .T. ) ;
#245984=DIRECTION ( 'NONE',  ( -1.000000000000000000, -0.000000000000000000, -0.000000000000000000 ) ) ;
#245992=CARTESIAN_POINT ( 'NONE',  ( -18.59999999999999787, 74.75000000001232081, -162.0231074845243597 ) ) ;
#245996=CARTESIAN_POINT ( 'NONE',  ( 18.50000000000000355, 85.41907808086162390, -129.6931821343160038 ) ) ;
#246000=CARTESIAN_POINT ( 'NONE',  ( 21.07199075132372101, 67.22505500089620512, -157.8095753229115701 ) ) ;
#246010=EDGE_LOOP ( 'NONE', ( #124224, #138504, #74208 ) ) ;
#246024=DIRECTION ( 'NONE',  ( 0.000000000000000000, -1.000000000000000000, -6.982962677686266711E-15 ) ) ;
#246026=ORIENTED_EDGE ( 'NONE', *, *, #257687, .T. ) ;
#246049=DIRECTION ( 'NONE',  ( 1.000000000000000000, 0.000000000000000000, 0.000000000000000000 ) ) ;
#246072=ORIENTED_EDGE ( 'NONE', *, *, #254906, .F. ) ;
#246092=CARTESIAN_POINT ( 'NONE',  ( -21.45000000000000284, 68.29142135624960019, -157.7731074845244166 ) ) ;
#246103=CARTESIAN_POINT ( 'NONE',  ( -22.50000000000088463, 75.95463834342467635, -181.6736163187343038 ) ) ;
#246110=EDGE_CURVE ( 'NONE', #20227, #149556, #80720, .T. ) ;
#246115=AXIS2_PLACEMENT_3D ( 'NONE', #104935, #85373, #244480 ) ;
#246138=DIRECTION ( 'NONE',  ( 0.000000000000000000, 0.000000000000000000, 1.000000000000000000 ) ) ;
#246189=CIRCLE ( 'NONE', #221036, 0.2000000000000057288 ) ;
#246217=CARTESIAN_POINT ( 'NONE',  ( -23.15000000000000213, 73.40000000001228386, -156.7984855617622770 ) ) ;
#246225=CIRCLE ( 'NONE', #33883, 11.75000000000001066 ) ;
#246245=AXIS2_PLACEMENT_3D ( 'NONE', #131122, #191131, #9890 ) ;
#246252=CARTESIAN_POINT ( 'NONE',  ( -20.94999999999999929, 76.00000000001237765, -170.0231074845243597 ) ) ;
#246264=AXIS2_PLACEMENT_3D ( 'NONE', #68961, #51912, #128918 ) ;
#246295=DIRECTION ( 'NONE',  ( 0.000000000000000000, 0.8777080977375655291, -0.4791956752370622463 ) ) ;
#246311=EDGE_LOOP ( 'NONE', ( #134765, #161603, #213459, #171998, #4535, #34964, #180364, #189141 ) ) ;
#246318=CIRCLE ( 'NONE', #121453, 0.4000000000000114575 ) ;
#246386=CARTESIAN_POINT ( 'NONE',  ( -21.59142135623730852, 68.15000000001222702, -148.7731074845244166 ) ) ;
#246391=DIRECTION ( 'NONE',  ( -0.000000000000000000, 6.982962677686266711E-15, -1.000000000000000000 ) ) ;
#246392=VECTOR ( 'NONE', #204124, 1000.000000000000114 ) ;
#246450=ORIENTED_EDGE ( 'NONE', *, *, #247196, .F. ) ;
#246492=DIRECTION ( 'NONE',  ( 1.000000000000000000, 0.000000000000000000, 0.000000000000000000 ) ) ;
#246493=LINE ( 'NONE', #249085, #61813 ) ;
#246540=AXIS2_PLACEMENT_3D ( 'NONE', #29515, #188549, #115426 ) ;
#246567=CIRCLE ( 'NONE', #125941, 0.09999999999998898659 ) ;
#246572=AXIS2_PLACEMENT_3D ( 'NONE', #80747, #198144, #42931 ) ;
#246627=ADVANCED_FACE ( 'NONE', ( #102518 ), #205497, .T. ) ;
#246644=EDGE_CURVE ( 'NONE', #237795, #80942, #241539, .T. ) ;
#246667=DIRECTION ( 'NONE',  ( 0.000000000000000000, -1.000000000000000000, -7.272083257015735086E-15 ) ) ;
#246672=DIRECTION ( 'NONE',  ( 0.000000000000000000, 1.000000000000000000, 6.982962677686266711E-15 ) ) ;
#246677=EDGE_CURVE ( 'NONE', #114980, #18391, #45907, .T. ) ;
#246686=EDGE_CURVE ( 'NONE', #128947, #44761, #195775, .T. ) ;
#246713=FACE_OUTER_BOUND ( 'NONE', #187883, .T. ) ;
#246718=DIRECTION ( 'NONE',  ( 1.000000000000000000, 0.000000000000000000, 0.000000000000000000 ) ) ;
#246733=FACE_OUTER_BOUND ( 'NONE', #32996, .T. ) ;
#246774=CARTESIAN_POINT ( 'NONE',  ( -21.33487959338958362, 69.27444184810119054, -170.0231074845243882 ) ) ;
#246799=ADVANCED_FACE ( 'NONE', ( #9871 ), #199866, .T. ) ;
#246807=ORIENTED_EDGE ( 'NONE', *, *, #59736, .F. ) ;
#246816=VERTEX_POINT ( 'NONE', #89402 ) ;
#246820=CARTESIAN_POINT ( 'NONE',  ( -20.54999999999999716, 68.85000000001228670, -157.7731074845244166 ) ) ;
#246845=LINE ( 'NONE', #223427, #16917 ) ;
#246854=DIRECTION ( 'NONE',  ( 0.000000000000000000, -7.429790795770644761E-15, 1.000000000000000000 ) ) ;
#246866=ORIENTED_EDGE ( 'NONE', *, *, #24740, .T. ) ;
#246872=EDGE_CURVE ( 'NONE', #91629, #92370, #219303, .T. ) ;
#246894=DIRECTION ( 'NONE',  ( 0.000000000000000000, -6.308085367188367561E-15, 1.000000000000000000 ) ) ;
#246900=EDGE_CURVE ( 'NONE', #218463, #236987, #21140, .T. ) ;
#246906=DIRECTION ( 'NONE',  ( 1.000000000000000000, 0.000000000000000000, 0.000000000000000000 ) ) ;
#246947=DIRECTION ( 'NONE',  ( 0.000000000000000000, 6.982962677686266711E-15, -1.000000000000000000 ) ) ;
#246957=EDGE_CURVE ( 'NONE', #158699, #157707, #87579, .T. ) ;
#247007=AXIS2_PLACEMENT_3D ( 'NONE', #134099, #196644, #216202 ) ;
#247051=AXIS2_PLACEMENT_3D ( 'NONE', #84164, #202884, #64656 ) ;
#247073=FACE_OUTER_BOUND ( 'NONE', #107984, .T. ) ;
#247080=DIRECTION ( 'NONE',  ( -1.000000000000000000, -7.304098846218134667E-16, -5.311601492717084346E-30 ) ) ;
#247085=CIRCLE ( 'NONE', #18156, 0.09999999999998898659 ) ;
#247093=CARTESIAN_POINT ( 'NONE',  ( -21.02374657821591342, 64.39999999919201912, -143.4513107143264108 ) ) ;
#247094=CARTESIAN_POINT ( 'NONE',  ( 20.95561247346651967, 65.40499263480876380, -162.4293247175427837 ) ) ;
#247116=AXIS2_PLACEMENT_3D ( 'NONE', #176336, #214160, #35551 ) ;
#247117=CARTESIAN_POINT ( 'NONE',  ( 20.94999999999999574, 74.75000000001232081, -162.0231074845243597 ) ) ;
#247125=DIRECTION ( 'NONE',  ( -0.000000000000000000, 1.000000000000000000, 6.982962677686266711E-15 ) ) ;
#247137=AXIS2_PLACEMENT_3D ( 'NONE', #96152, #214828, #160022 ) ;
#247196=EDGE_CURVE ( 'NONE', #194619, #91227, #133064, .T. ) ;
#247209=EDGE_CURVE ( 'NONE', #132867, #47267, #35278, .T. ) ;
#247229=VECTOR ( 'NONE', #61061, 1000.000000000000000 ) ;
#247235=VERTEX_POINT ( 'NONE', #96467 ) ;
#247254=CARTESIAN_POINT ( 'NONE',  ( 23.14999999999999858, 80.00000000001215028, -136.5231074845243029 ) ) ;
#247292=FACE_OUTER_BOUND ( 'NONE', #201956, .T. ) ;
#247297=ORIENTED_EDGE ( 'NONE', *, *, #157215, .T. ) ;
#247298=EDGE_CURVE ( 'NONE', #33088, #180036, #246189, .T. ) ;
#247303=DIRECTION ( 'NONE',  ( 0.000000000000000000, 1.000000000000000000, 6.938893903907222067E-15 ) ) ;
#247314=EDGE_CURVE ( 'NONE', #253610, #171646, #192044, .T. ) ;
#247321=VECTOR ( 'NONE', #6040, 1000.000000000000000 ) ;
#247340=AXIS2_PLACEMENT_3D ( 'NONE', #94333, #155643, #154368 ) ;
#247342=CARTESIAN_POINT ( 'NONE',  ( 21.05000000000000071, 76.10000000001245724, -181.6726782920691505 ) ) ;
#247362=TOROIDAL_SURFACE ( 'NONE', #172409, 0.2000000000000000111, 0.1000000000000000056 ) ;
#247364=CARTESIAN_POINT ( 'NONE',  ( -22.39999999999999858, 76.00000000001246292, -181.6726782920691505 ) ) ;
#247405=ORIENTED_EDGE ( 'NONE', *, *, #195659, .T. ) ;
#247406=ADVANCED_FACE ( 'NONE', ( #239866 ), #61217, .F. ) ;
#247434=VERTEX_POINT ( 'NONE', #203295 ) ;
#247458=DIRECTION ( 'NONE',  ( 0.000000000000000000, -1.000000000000000000, -6.982962677686265922E-15 ) ) ;
#247475=CARTESIAN_POINT ( 'NONE',  ( 23.15000000000000213, 84.66355140188136374, -146.0472086025916099 ) ) ;
#247495=DIRECTION ( 'NONE',  ( -1.000000000000000000, 0.000000000000000000, -0.000000000000000000 ) ) ;
#247505=DIRECTION ( 'NONE',  ( -1.000000000000000000, -0.000000000000000000, -0.000000000000000000 ) ) ;
#247526=ORIENTED_EDGE ( 'NONE', *, *, #130174, .T. ) ;
#247535=CARTESIAN_POINT ( 'NONE',  ( 20.22516295850462598, 66.10063570456208026, -162.1130417724336041 ) ) ;
#247587=DIRECTION ( 'NONE',  ( 0.000000000000000000, 0.000000000000000000, 1.000000000000000000 ) ) ;
#247606=AXIS2_PLACEMENT_3D ( 'NONE', #147874, #248247, #210420 ) ;
#247628=TOROIDAL_SURFACE ( 'NONE', #26902, 12.77499999999999858, 0.1000000000000000056 ) ;
#247630=CIRCLE ( 'NONE', #81015, 0.1000000000000028644 ) ;
#247642=CARTESIAN_POINT ( 'NONE',  ( 22.39999999999999858, 68.20922040163900135, -170.1231074845244109 ) ) ;
#247671=CARTESIAN_POINT ( 'NONE',  ( -23.15000000000000213, 71.75000000001229239, -157.7731074845243882 ) ) ;
#247690=ORIENTED_EDGE ( 'NONE', *, *, #135616, .T. ) ;
#247698=EDGE_CURVE ( 'NONE', #59420, #84927, #88112, .T. ) ;
#247717=DIRECTION ( 'NONE',  ( 1.000000000000000000, -0.000000000000000000, 0.000000000000000000 ) ) ;
#247719=ORIENTED_EDGE ( 'NONE', *, *, #74677, .T. ) ;
#247724=DIRECTION ( 'NONE',  ( 1.000000000000000000, 0.000000000000000000, 0.000000000000000000 ) ) ;
#247725=DIRECTION ( 'NONE',  ( -3.265361837132813093E-16, -1.000000000000000000, -6.938893903907229955E-15 ) ) ;
#247730=EDGE_CURVE ( 'NONE', #137060, #238125, #72801, .T. ) ;
#247740=ORIENTED_EDGE ( 'NONE', *, *, #85426, .T. ) ;
#247746=ADVANCED_FACE ( 'NONE', ( #253954 ), #36236, .T. ) ;
#247778=EDGE_CURVE ( 'NONE', #218857, #148346, #182145, .T. ) ;
#247799=DIRECTION ( 'NONE',  ( 0.000000000000000000, 0.000000000000000000, 1.000000000000000000 ) ) ;
#247833=CARTESIAN_POINT ( 'NONE',  ( 21.05000000000000071, 87.39257802171783851, -139.5970570643562212 ) ) ;
#247850=EDGE_LOOP ( 'NONE', ( #59005, #73991, #247862, #119008 ) ) ;
#247855=EDGE_CURVE ( 'NONE', #1798, #35577, #113096, .T. ) ;
#247862=ORIENTED_EDGE ( 'NONE', *, *, #48242, .F. ) ;
#247871=DIRECTION ( 'NONE',  ( 0.000000000000000000, 0.000000000000000000, 1.000000000000000000 ) ) ;
#247897=FACE_OUTER_BOUND ( 'NONE', #21228, .T. ) ;
#247907=FACE_OUTER_BOUND ( 'NONE', #159393, .T. ) ;
#247909=DIRECTION ( 'NONE',  ( 0.000000000000000000, 1.000000000000000000, 6.982962677686266711E-15 ) ) ;
#247916=ORIENTED_EDGE ( 'NONE', *, *, #57309, .F. ) ;
#247929=EDGE_LOOP ( 'NONE', ( #152672, #80420, #105070, #72526, #74134, #128575, #63425, #60305, #22346, #239343, #34557, #61508, #145753, #35750, #1579, #242395, #42893, #33913 ) ) ;
#247939=ORIENTED_EDGE ( 'NONE', *, *, #87723, .T. ) ;
#247941=ORIENTED_EDGE ( 'NONE', *, *, #129975, .T. ) ;
#247947=EDGE_CURVE ( 'NONE', #77802, #94999, #184691, .T. ) ;
#247993=ADVANCED_FACE ( 'NONE', ( #45186 ), #24367, .T. ) ;
#248001=B_SPLINE_CURVE_WITH_KNOTS ( 'NONE', 3,
 ( #136953, #80813, #19592, #216491, #99088, #37884, #160403, #196924, #159115, #239924, #61275, #97799, #140814, #220360, #78254, #41731, #121289, #181243, #237350 ),
 .UNSPECIFIED., .F., .F.,
 ( 4, 3, 3, 3, 3, 3, 4 ),
 ( -2.000416914662652606E-06, 0.000000000000000000, 4.714008503747417261E-05, 9.979203887777324331E-05, 0.0001372215519229504641, 0.0001635031576221021479, 0.0001900083748504133785 ),
 .UNSPECIFIED. ) ;
#248017=ORIENTED_EDGE ( 'NONE', *, *, #148904, .T. ) ;
#248045=ORIENTED_EDGE ( 'NONE', *, *, #89371, .T. ) ;
#248052=EDGE_CURVE ( 'NONE', #106358, #49789, #163177, .T. ) ;
#248088=CARTESIAN_POINT ( 'NONE',  ( -23.25000000000000000, 69.06610602788578035, -132.7374616501508342 ) ) ;
#248095=FACE_OUTER_BOUND ( 'NONE', #257132, .T. ) ;
#248173=DIRECTION ( 'NONE',  ( 0.000000000000000000, -1.000000000000000000, 0.000000000000000000 ) ) ;
#248191=DIRECTION ( 'NONE',  ( 0.000000000000000000, -7.116814260417668513E-15, 1.000000000000000000 ) ) ;
#248221=VERTEX_POINT ( 'NONE', #21492 ) ;
#248229=AXIS2_PLACEMENT_3D ( 'NONE', #212271, #113152, #192698 ) ;
#248247=DIRECTION ( 'NONE',  ( -0.000000000000000000, 1.000000000000000000, 6.982962677686266711E-15 ) ) ;
#248266=EDGE_CURVE ( 'NONE', #5558, #145447, #234068, .T. ) ;
#248268=CIRCLE ( 'NONE', #81629, 0.8750000000000007772 ) ;
#248304=VERTEX_POINT ( 'NONE', #186992 ) ;
#248307=FACE_OUTER_BOUND ( 'NONE', #48761, .T. ) ;
#248308=CARTESIAN_POINT ( 'NONE',  ( 18.59999999999999432, 74.83729825007431202, -161.9231074845243654 ) ) ;
#248315=ORIENTED_EDGE ( 'NONE', *, *, #3950, .T. ) ;
#248348=ORIENTED_EDGE ( 'NONE', *, *, #153312, .F. ) ;
#248354=DIRECTION ( 'NONE',  ( 1.000000000000000000, -1.836970198721029934E-16, -1.282749433769087582E-30 ) ) ;
#248356=EDGE_CURVE ( 'NONE', #244509, #94515, #183126, .T. ) ;
#248367=CARTESIAN_POINT ( 'NONE',  ( 20.94999999999999929, 84.66355140188147743, -160.4990063664569959 ) ) ;
#248369=CYLINDRICAL_SURFACE ( 'NONE', #49190, 0.09999999999999939493 ) ;
#248387=CIRCLE ( 'NONE', #135949, 0.1000000000000072220 ) ;
#248391=CARTESIAN_POINT ( 'NONE',  ( -21.05000000000000071, 76.09999996531196587, -176.5006596670181409 ) ) ;
#248410=DIRECTION ( 'NONE',  ( 1.000000000000000000, 0.000000000000000000, 0.000000000000000000 ) ) ;
#248416=ORIENTED_EDGE ( 'NONE', *, *, #198243, .F. ) ;
#248453=EDGE_CURVE ( 'NONE', #111495, #241979, #71214, .T. ) ;
#248460=CARTESIAN_POINT ( 'NONE',  ( -21.05000000000000071, 77.16270174995034381, -162.0231074845243313 ) ) ;
#248474=EDGE_CURVE ( 'NONE', #212171, #126961, #58703, .T. ) ;
#248490=DIRECTION ( 'NONE',  ( -0.000000000000000000, 0.1350103645451859180, 0.9908441862701603542 ) ) ;
#248492=CARTESIAN_POINT ( 'NONE',  ( 21.05000000000000071, 74.16465844978787914, -158.4679561919613775 ) ) ;
#248502=DIRECTION ( 'NONE',  ( 0.000000000000000000, -1.000000000000000000, -6.982962677686265922E-15 ) ) ;
#248528=CIRCLE ( 'NONE', #78023, 12.87499999999999822 ) ;
#248539=CARTESIAN_POINT ( 'NONE',  ( -23.15000000000000213, 85.00000000001222134, -146.4170766071767389 ) ) ;
#248540=ORIENTED_EDGE ( 'NONE', *, *, #4283, .F. ) ;
#248559=CARTESIAN_POINT ( 'NONE',  ( 20.94999999999999929, 77.83534155023671985, -158.4679561919613491 ) ) ;
#248569=DIRECTION ( 'NONE',  ( -1.000000000000000000, 1.836970198721029934E-16, 1.282749433769087757E-30 ) ) ;
#248573=ORIENTED_EDGE ( 'NONE', *, *, #27927, .F. ) ;
#248590=EDGE_CURVE ( 'NONE', #71080, #128626, #125411, .T. ) ;
#248595=CYLINDRICAL_SURFACE ( 'NONE', #118041, 0.1000000000000106914 ) ;
#248614=CARTESIAN_POINT ( 'NONE',  ( 23.15000000000000213, 87.75000000001216449, -139.6231074845242688 ) ) ;
#248618=DIRECTION ( 'NONE',  ( 0.000000000000000000, -0.1495327102803283015, 0.9887567792719397231 ) ) ;
#248657=CARTESIAN_POINT ( 'NONE',  ( -22.50875500270927532, 76.10085791378705267, -181.7726746119222696 ) ) ;
#248708=VERTEX_POINT ( 'NONE', #211042 ) ;
#248723=DIRECTION ( 'NONE',  ( 1.000000000000000000, 0.000000000000000000, 0.000000000000000000 ) ) ;
#248747=DIRECTION ( 'NONE',  ( 0.000000000000000000, 0.000000000000000000, 1.000000000000000000 ) ) ;
#248769=B_SPLINE_CURVE_WITH_KNOTS ( 'NONE', 3,
 ( #175483, #51628, #251124, #131191, #253701, #15115, #115479, #195047, #32126, #174222, #73825, #214576, #153378, #94631, #111636, #232896, #11259, #55471, #133760 ),
 .UNSPECIFIED., .F., .F.,
 ( 4, 3, 3, 3, 3, 3, 4 ),
 ( -2.000416914646550933E-06, 0.000000000000000000, 4.714008503745887181E-05, 9.979203887778609111E-05, 0.0001372215519229623361, 0.0001635031576221138302, 0.0001900083748504290723 ),
 .UNSPECIFIED. ) ;
#248778=CARTESIAN_POINT ( 'NONE',  ( 23.14999999999999503, 69.55000000001228955, -157.6731074845243938 ) ) ;
#248795=TOROIDAL_SURFACE ( 'NONE', #23783, 0.2000000000000000111, 0.1000000000000000056 ) ;
#248808=EDGE_CURVE ( 'NONE', #174607, #94890, #233713, .T. ) ;
#248809=VERTEX_POINT ( 'NONE', #102600 ) ;
#248826=CARTESIAN_POINT ( 'NONE',  ( 22.39999999999999503, 64.25000000001237765, -169.9231074845244507 ) ) ;
#248828=CARTESIAN_POINT ( 'NONE',  ( -23.15000000000000213, 76.00000000001213607, -136.5231074845243313 ) ) ;
#248836=FACE_OUTER_BOUND ( 'NONE', #237352, .T. ) ;
#248837=VECTOR ( 'NONE', #63205, 999.9999999999998863 ) ;
#248907=LINE ( 'NONE', #11587, #24956 ) ;
#248915=DIRECTION ( 'NONE',  ( 0.000000000000000000, 0.000000000000000000, -1.000000000000000000 ) ) ;
#248967=VERTEX_POINT ( 'NONE', #229013 ) ;
#248971=EDGE_CURVE ( 'NONE', #22950, #194825, #13129, .T. ) ;
#248977=CIRCLE ( 'NONE', #169899, 0.09999999999998900047 ) ;
#248991=ORIENTED_EDGE ( 'NONE', *, *, #125324, .F. ) ;
#249006=CARTESIAN_POINT ( 'NONE',  ( 23.24999999999999645, 70.40000000001222702, -148.9283735034374843 ) ) ;
#249011=EDGE_CURVE ( 'NONE', #176438, #212994, #196273, .T. ) ;
#249074=EDGE_CURVE ( 'NONE', #85130, #111529, #75678, .T. ) ;
#249081=DIRECTION ( 'NONE',  ( 0.000000000000000000, 0.000000000000000000, -1.000000000000000000 ) ) ;
#249085=CARTESIAN_POINT ( 'NONE',  ( 20.94999999999999929, 87.39257802171783851, -139.5970570643562212 ) ) ;
#249140=DIRECTION ( 'NONE',  ( 2.952720810173289112E-16, 1.000000000000000000, 6.530723674265620862E-15 ) ) ;
#249154=VERTEX_POINT ( 'NONE', #205123 ) ;
#249230=ORIENTED_EDGE ( 'NONE', *, *, #76117, .F. ) ;
#249289=EDGE_LOOP ( 'NONE', ( #198541, #50658, #200764, #190019 ) ) ;
#249295=ORIENTED_EDGE ( 'NONE', *, *, #242814, .F. ) ;
#249296=CYLINDRICAL_SURFACE ( 'NONE', #91795, 0.09999999999998898659 ) ;
#249332=ORIENTED_EDGE ( 'NONE', *, *, #170355, .F. ) ;
#249338=EDGE_CURVE ( 'NONE', #153611, #112125, #50685, .T. ) ;
#249358=ORIENTED_EDGE ( 'NONE', *, *, #142305, .T. ) ;
#249376=DIRECTION ( 'NONE',  ( 1.000000000000000000, 0.000000000000000000, 0.000000000000000000 ) ) ;
#249398=DIRECTION ( 'NONE',  ( 1.000000000000000000, 0.000000000000000000, 0.000000000000000000 ) ) ;
#249399=ORIENTED_EDGE ( 'NONE', *, *, #210333, .T. ) ;
#249444=ORIENTED_EDGE ( 'NONE', *, *, #184216, .F. ) ;
#249491=ORIENTED_EDGE ( 'NONE', *, *, #198635, .T. ) ;
#249492=CARTESIAN_POINT ( 'NONE',  ( 22.00356870141230914, 68.74575763752079638, -170.0231074845244450 ) ) ;
#249497=DIRECTION ( 'NONE',  ( 0.000000000000000000, -0.9654727137038715545, -0.2605042016806676242 ) ) ;
#249545=ORIENTED_EDGE ( 'NONE', *, *, #5572, .F. ) ;
#249549=DIRECTION ( 'NONE',  ( 1.000000000000000000, 0.000000000000000000, 0.000000000000000000 ) ) ;
#249552=AXIS2_PLACEMENT_3D ( 'NONE', #192411, #211985, #253643 ) ;
#249556=DIRECTION ( 'NONE',  ( 0.000000000000000000, -7.056502275159890832E-15, 1.000000000000000000 ) ) ;
#249583=DIRECTION ( 'NONE',  ( -0.000000000000000000, 7.272083257015735086E-15, -1.000000000000000000 ) ) ;
#249586=ORIENTED_EDGE ( 'NONE', *, *, #31839, .T. ) ;
#249588=AXIS2_PLACEMENT_3D ( 'NONE', #87537, #126685, #206224 ) ;
#249658=LINE ( 'NONE', #54010, #256101 ) ;
#249673=DIRECTION ( 'NONE',  ( -1.000000000000000000, 2.952720810173289112E-16, 2.061873921506763405E-30 ) ) ;
#249683=ORIENTED_EDGE ( 'NONE', *, *, #112252, .T. ) ;
#249688=DIRECTION ( 'NONE',  ( -0.000000000000000000, 1.000000000000000000, 6.982962677686266711E-15 ) ) ;
#249711=CARTESIAN_POINT ( 'NONE',  ( -23.25000000000000000, 64.25000000001222134, -148.6731074845244507 ) ) ;
#249774=DIRECTION ( 'NONE',  ( 0.000000000000000000, -0.9274965247785555977, 0.3738317757009190223 ) ) ;
#249777=AXIS2_PLACEMENT_3D ( 'NONE', #253046, #74456, #154010 ) ;
#249781=ORIENTED_EDGE ( 'NONE', *, *, #157193, .F. ) ;
#249783=FACE_OUTER_BOUND ( 'NONE', #27257, .T. ) ;
#249790=DIRECTION ( 'NONE',  ( -0.000000000000000000, -6.982962677686266711E-15, 1.000000000000000000 ) ) ;
#249829=SURFACE_STYLE_FILL_AREA ( #174187 ) ;
#249846=ORIENTED_EDGE ( 'NONE', *, *, #161784, .T. ) ;
#249857=CARTESIAN_POINT ( 'NONE',  ( -18.50000000000000000, 77.73625713160970463, -158.4544551555068495 ) ) ;
#249871=ORIENTED_EDGE ( 'NONE', *, *, #4987, .F. ) ;
#249904=EDGE_CURVE ( 'NONE', #167959, #220534, #95551, .T. ) ;
#249910=AXIS2_PLACEMENT_3D ( 'NONE', #124698, #142943, #43874 ) ;
#249946=CIRCLE ( 'NONE', #37581, 0.09999999999998898659 ) ;
#249951=ORIENTED_EDGE ( 'NONE', *, *, #1617, .T. ) ;
#249976=CARTESIAN_POINT ( 'NONE',  ( 23.15000000000000213, 87.75000000001229239, -157.8731074845242688 ) ) ;
#249996=CARTESIAN_POINT ( 'NONE',  ( 18.59999999999997655, 64.25000000001215028, -136.5231074845244166 ) ) ;
#250031=ORIENTED_EDGE ( 'NONE', *, *, #22430, .F. ) ;
#250039=CYLINDRICAL_SURFACE ( 'NONE', #19297, 0.5000000000000004441 ) ;
#250041=VECTOR ( 'NONE', #16294, 1000.000000000000000 ) ;
#250078=EDGE_LOOP ( 'NONE', ( #200498, #46375, #136166, #97379 ) ) ;
#250087=ADVANCED_FACE ( 'NONE', ( #5407 ), #203641, .T. ) ;
#250113=ORIENTED_EDGE ( 'NONE', *, *, #251983, .F. ) ;
#250114=CARTESIAN_POINT ( 'NONE',  ( 23.14999999999999503, 64.25000000001222134, -148.7731074845244450 ) ) ;
#250130=ADVANCED_FACE ( 'NONE', ( #247897 ), #131802, .F. ) ;
#250156=AXIS2_PLACEMENT_3D ( 'NONE', #4194, #199863, #241534 ) ;
#250198=LINE ( 'NONE', #71585, #79518 ) ;
#250223=CARTESIAN_POINT ( 'NONE',  ( 23.24999999999999645, 76.00000000001237765, -170.0231074845243597 ) ) ;
#250230=ORIENTED_EDGE ( 'NONE', *, *, #153312, .T. ) ;
#250235=CIRCLE ( 'NONE', #208738, 11.64999999999999325 ) ;
#250262=ORIENTED_EDGE ( 'NONE', *, *, #151131, .T. ) ;
#250271=ORIENTED_EDGE ( 'NONE', *, *, #155642, .T. ) ;
#250303=CARTESIAN_POINT ( 'NONE',  ( -21.05000000000000071, 76.10000000001241460, -176.5637644362255969 ) ) ;
#250312=CIRCLE ( 'NONE', #137861, 0.09999999999999939493 ) ;
#250325=AXIS2_PLACEMENT_3D ( 'NONE', #157869, #138236, #40484 ) ;
#250350=DIRECTION ( 'NONE',  ( 0.000000000000000000, 6.982962677686266711E-15, -1.000000000000000000 ) ) ;
#250377=EDGE_CURVE ( 'NONE', #181798, #96638, #212641, .T. ) ;
#250383=ORIENTED_EDGE ( 'NONE', *, *, #16673, .F. ) ;
#250406=EDGE_CURVE ( 'NONE', #235746, #24875, #230316, .T. ) ;
#250408=ORIENTED_EDGE ( 'NONE', *, *, #61952, .F. ) ;
#250411=VERTEX_POINT ( 'NONE', #59945 ) ;
#250425=ORIENTED_EDGE ( 'NONE', *, *, #60650, .F. ) ;
#250433=CARTESIAN_POINT ( 'NONE',  ( -21.05000000000000071, 76.00000000001237765, -170.0231074845243597 ) ) ;
#250440=VECTOR ( 'NONE', #136544, 1000.000000000000000 ) ;
#250451=DIRECTION ( 'NONE',  ( -1.000000000000000000, -0.000000000000000000, -0.000000000000000000 ) ) ;
#250519=DIRECTION ( 'NONE',  ( 0.000000000000000000, 1.000000000000000000, 6.982962677686266711E-15 ) ) ;
#250532=EDGE_CURVE ( 'NONE', #58292, #206737, #91090, .T. ) ;
#250536=ORIENTED_EDGE ( 'NONE', *, *, #36832, .F. ) ;
#250543=ADVANCED_FACE ( 'NONE', ( #71548 ), #59605, .F. ) ;
#250562=AXIS2_PLACEMENT_3D ( 'NONE', #213872, #255512, #211309 ) ;
#250568=ORIENTED_EDGE ( 'NONE', *, *, #85599, .F. ) ;
#250589=DIRECTION ( 'NONE',  ( 0.000000000000000000, 0.000000000000000000, -1.000000000000000000 ) ) ;
#250601=VERTEX_POINT ( 'NONE', #37544 ) ;
#250620=CARTESIAN_POINT ( 'NONE',  ( -21.14999999999999858, 76.10000000001245724, -181.6726782920691505 ) ) ;
#250646=DIRECTION ( 'NONE',  ( 0.000000000000000000, -7.034366652768095332E-15, 1.000000000000000000 ) ) ;
#250651=( NAMED_UNIT ( * ) PLANE_ANGLE_UNIT ( ) SI_UNIT ( $, .RADIAN. ) );
#250681=CARTESIAN_POINT ( 'NONE',  ( 19.99999999999998934, 64.25000000001222134, -148.6731074845244507 ) ) ;
#250704=ORIENTED_EDGE ( 'NONE', *, *, #111307, .F. ) ;
#250721=EDGE_CURVE ( 'NONE', #160806, #74964, #218013, .T. ) ;
#250739=EDGE_CURVE ( 'NONE', #222373, #125758, #93132, .T. ) ;
#250740=CARTESIAN_POINT ( 'NONE',  ( -20.54999999999999716, 71.65000000001228386, -157.6731074845243938 ) ) ;
#250753=CARTESIAN_POINT ( 'NONE',  ( 21.46681500593530956, 69.14248884063026424, -170.0231074845244166 ) ) ;
#250783=EDGE_CURVE ( 'NONE', #30238, #168004, #197874, .T. ) ;
#250788=CIRCLE ( 'NONE', #242967, 0.5000000000000004441 ) ;
#250792=CARTESIAN_POINT ( 'NONE',  ( -18.59999994787167310, 85.52363768977403424, -129.6406579497522387 ) ) ;
#250797=DIRECTION ( 'NONE',  ( -1.000000000000000000, 0.000000000000000000, -0.000000000000000000 ) ) ;
#250862=EDGE_CURVE ( 'NONE', #177752, #208786, #253385, .T. ) ;
#250913=LINE ( 'NONE', #190984, #214464 ) ;
#250934=CIRCLE ( 'NONE', #67610, 0.09999999999998898659 ) ;
#250936=CARTESIAN_POINT ( 'NONE',  ( -21.04999999999895977, 75.94867256767074082, -176.3232908207953074 ) ) ;
#250941=EDGE_CURVE ( 'NONE', #36614, #55132, #84727, .T. ) ;
#250954=EDGE_LOOP ( 'NONE', ( #182675, #88175, #3972, #74041 ) ) ;
#250957=ADVANCED_FACE ( 'NONE', ( #154339 ), #22249, .F. ) ;
#250968=CARTESIAN_POINT ( 'NONE',  ( 20.94560253601876809, 64.25000000001219291, -143.5130239720093641 ) ) ;
#250973=DIRECTION ( 'NONE',  ( 0.000000000000000000, 0.000000000000000000, -1.000000000000000000 ) ) ;
#251028=DIRECTION ( 'NONE',  ( 0.000000000000000000, -1.000000000000000000, 0.000000000000000000 ) ) ;
#251082=ORIENTED_EDGE ( 'NONE', *, *, #75459, .F. ) ;
#251094=FACE_OUTER_BOUND ( 'NONE', #190610, .T. ) ;
#251110=CIRCLE ( 'NONE', #13631, 7.800000000000001599 ) ;
#251124=CARTESIAN_POINT ( 'NONE',  ( -20.94999675878240808, 65.70692517833255408, -131.0644653378304270 ) ) ;
#251129=AXIS2_PLACEMENT_3D ( 'NONE', #144087, #180676, #64563 ) ;
#251148=VECTOR ( 'NONE', #195655, 1000.000000000000000 ) ;
#251161=EDGE_CURVE ( 'NONE', #25144, #226867, #26710, .T. ) ;
#251184=ORIENTED_EDGE ( 'NONE', *, *, #179433, .T. ) ;
#251206=CARTESIAN_POINT ( 'NONE',  ( 23.24999999999999289, 69.35000000001228670, -157.8731074845244109 ) ) ;
#251212=ADVANCED_FACE ( 'NONE', ( #45892 ), #130734, .T. ) ;
#251216=CIRCLE ( 'NONE', #1425, 0.09999999999999939493 ) ;
#251221=ORIENTED_EDGE ( 'NONE', *, *, #242091, .T. ) ;
#251235=CARTESIAN_POINT ( 'NONE',  ( -23.15000000000000213, 76.00000000001210765, -132.6231074845243540 ) ) ;
#251287=DIRECTION ( 'NONE',  ( 0.000000000000000000, 0.8777080977375655291, -0.4791956752370622463 ) ) ;
#251309=DIRECTION ( 'NONE',  ( 0.000000000000000000, 0.000000000000000000, 1.000000000000000000 ) ) ;
#251312=ORIENTED_EDGE ( 'NONE', *, *, #39375, .T. ) ;
#251330=DIRECTION ( 'NONE',  ( 0.000000000000000000, 1.000000000000000000, 1.387778780781444413E-14 ) ) ;
#251337=CARTESIAN_POINT ( 'NONE',  ( -21.05000000000000071, 77.25000000001232081, -162.0231074845243313 ) ) ;
#251380=DIRECTION ( 'NONE',  ( -1.000000000000000000, -0.000000000000000000, 0.000000000000000000 ) ) ;
#251381=CARTESIAN_POINT ( 'NONE',  ( 18.59999999999999076, 74.25000000001229239, -158.3535959266227451 ) ) ;
#251383=AXIS2_PLACEMENT_3D ( 'NONE', #242461, #238627, #22166 ) ;
#251397=AXIS2_PLACEMENT_3D ( 'NONE', #231859, #175742, #33689 ) ;
#251400=CARTESIAN_POINT ( 'NONE',  ( 21.05000000000000071, 76.00000000001213607, -136.5231074845243313 ) ) ;
#251405=PRODUCT_DEFINITION_SHAPE ( 'NONE', 'NONE',  #252419 ) ;
#251433=DIRECTION ( 'NONE',  ( 1.000000000000000000, 0.000000000000000000, 0.000000000000000000 ) ) ;
#251442=ORIENTED_EDGE ( 'NONE', *, *, #241713, .F. ) ;
#251523=DIRECTION ( 'NONE',  ( -3.265361837132813093E-16, -1.000000000000000000, -6.982962677686266711E-15 ) ) ;
#251542=VERTEX_POINT ( 'NONE', #26031 ) ;
#251552=CIRCLE ( 'NONE', #80852, 0.09999999999998898659 ) ;
#251573=CARTESIAN_POINT ( 'NONE',  ( 18.59999999999999787, 76.00000000001237765, -170.0231074845243597 ) ) ;
#251587=EDGE_CURVE ( 'NONE', #248221, #28696, #143397, .T. ) ;
#251618=CARTESIAN_POINT ( 'NONE',  ( -23.15000000000000213, 76.00000000001212186, -134.5231074845243313 ) ) ;
#251654=FACE_BOUND ( 'NONE', #43389, .T. ) ;
#251660=ORIENTED_EDGE ( 'NONE', *, *, #256017, .T. ) ;
#251665=DIRECTION ( 'NONE',  ( -1.000000000000000000, 0.000000000000000000, 0.000000000000000000 ) ) ;
#251678=VERTEX_POINT ( 'NONE', #147245 ) ;
#251700=DIRECTION ( 'NONE',  ( 0.000000000000000000, 6.982962677686266711E-15, -1.000000000000000000 ) ) ;
#251701=CARTESIAN_POINT ( 'NONE',  ( 22.16821283564876666, 68.44102665923161055, -170.0231074845243882 ) ) ;
#251721=EDGE_CURVE ( 'NONE', #251940, #48052, #247630, .T. ) ;
#251738=ORIENTED_EDGE ( 'NONE', *, *, #174213, .F. ) ;
#251747=CARTESIAN_POINT ( 'NONE',  ( -23.25000000000000000, 77.83585931145570669, -124.9186683157258244 ) ) ;
#251796=VECTOR ( 'NONE', #115929, 1000.000000000000000 ) ;
#251807=LINE ( 'NONE', #254353, #252908 ) ;
#251830=DIRECTION ( 'NONE',  ( 1.000000000000000000, 0.000000000000000000, 0.000000000000000000 ) ) ;
#251855=ORIENTED_EDGE ( 'NONE', *, *, #208146, .T. ) ;
#251857=CARTESIAN_POINT ( 'NONE',  ( -21.05000000000000071, 76.00000000001213607, -136.5231074845243313 ) ) ;
#251870=LINE ( 'NONE', #155384, #237019 ) ;
#251872=CARTESIAN_POINT ( 'NONE',  ( -23.15000000000000213, 74.00000000001229239, -156.7984855617622770 ) ) ;
#251930=CARTESIAN_POINT ( 'NONE',  ( 22.59999999999999432, 75.89914163091374633, -181.7726746080137445 ) ) ;
#251940=VERTEX_POINT ( 'NONE', #239628 ) ;
#251960=ORIENTED_EDGE ( 'NONE', *, *, #182057, .T. ) ;
#251974=DIRECTION ( 'NONE',  ( 4.239556034732057360E-17, 0.1298341882519953860, 0.9915357197604862671 ) ) ;
#251982=CARTESIAN_POINT ( 'NONE',  ( 23.14999999999998437, 71.95000000001238050, -170.0231074845243882 ) ) ;
#251983=EDGE_CURVE ( 'NONE', #231632, #91302, #89576, .T. ) ;
#252026=CARTESIAN_POINT ( 'NONE',  ( 23.14999999999999503, 64.25000000001219291, -143.5379132551784096 ) ) ;
#252039=CARTESIAN_POINT ( 'NONE',  ( -21.05000000000000071, 76.00000000001210765, -132.5231074845243313 ) ) ;
#252045=( BOUNDED_CURVE ( )  B_SPLINE_CURVE ( 3, ( #232352, #191953, #113659, #35450 ),
 .UNSPECIFIED., .F., .T. ) 
 B_SPLINE_CURVE_WITH_KNOTS ( ( 4, 4 ),
 ( 3.141592653589791784, 4.712388980384688786 ),
 .UNSPECIFIED. ) 
 CURVE ( )  GEOMETRIC_REPRESENTATION_ITEM ( )  RATIONAL_B_SPLINE_CURVE ( ( 1.000000000000000000, 0.8047378541243649375, 0.8047378541243649375, 1.000000000000000000 ) ) 
 REPRESENTATION_ITEM ( '' )  );
#252049=DIRECTION ( 'NONE',  ( 1.000000000000000000, 0.000000000000000000, 0.000000000000000000 ) ) ;
#252052=DIRECTION ( 'NONE',  ( 1.040834085586049673E-13, 0.7899159663865300551, 0.6132151058540831201 ) ) ;
#252064=AXIS2_PLACEMENT_3D ( 'NONE', #58496, #37702, #74268 ) ;
#252080=ORIENTED_EDGE ( 'NONE', *, *, #155746, .T. ) ;
#252112=ORIENTED_EDGE ( 'NONE', *, *, #220705, .T. ) ;
#252187=VECTOR ( 'NONE', #92303, 1000.000000000000000 ) ;
#252225=DIRECTION ( 'NONE',  ( 1.000000000000000000, 0.000000000000000000, 0.000000000000000000 ) ) ;
#252233=DIRECTION ( 'NONE',  ( -0.000000000000000000, -1.000000000000000000, -6.982962677686266711E-15 ) ) ;
#252235=AXIS2_PLACEMENT_3D ( 'NONE', #40500, #41769, #162995 ) ;
#252243=ORIENTED_EDGE ( 'NONE', *, *, #171338, .F. ) ;
#252279=CIRCLE ( 'NONE', #139856, 0.09999999999998898659 ) ;
#252304=LINE ( 'NONE', #88081, #91381 ) ;
#252382=AXIS2_PLACEMENT_3D ( 'NONE', #21950, #242257, #162751 ) ;
#252419=PRODUCT_DEFINITION ( 'UNKNOWN', '', #107198, #35018 ) ;
#252461=DIRECTION ( 'NONE',  ( 0.000000000000000000, -6.938893903907222067E-15, 1.000000000000000000 ) ) ;
#252513=LINE ( 'NONE', #115578, #254274 ) ;
#252528=CIRCLE ( 'NONE', #140098, 11.64999999999999325 ) ;
#252592=ADVANCED_FACE ( 'NONE', ( #43245 ), #219301, .T. ) ;
#252631=CARTESIAN_POINT ( 'NONE',  ( 21.09793522318408066, 65.27537548979951509, -157.7838166135473728 ) ) ;
#252640=DIRECTION ( 'NONE',  ( 0.000000000000000000, -5.956132106358139644E-15, -1.000000000000000000 ) ) ;
#252680=DIRECTION ( 'NONE',  ( -2.827886303505248766E-16, -0.8660254037844377084, -0.5000000000000015543 ) ) ;
#252720=CARTESIAN_POINT ( 'NONE',  ( 23.24999999999999645, 76.00000000001213607, -136.5231074845243313 ) ) ;
#252733=CARTESIAN_POINT ( 'NONE',  ( -20.64999999999999858, 76.00000000001213607, -136.5231074845243313 ) ) ;
#252742=B_SPLINE_CURVE_WITH_KNOTS ( 'NONE', 3,
 ( #240697, #163735, #82863, #84130, #205401, #162460, #101128, #4632, #26816, #21659, #64619, #63326, #184564, #182012, #124608, #106295, #145433, #180733, #41244 ),
 .UNSPECIFIED., .F., .F.,
 ( 4, 3, 3, 3, 3, 3, 4 ),
 ( 1.387778780781445676E-17, 2.646747978908693493E-05, 5.271166642129208971E-05, 9.008788829885705832E-05, 0.0001426648776561096276, 0.0001897378458660022580, 0.0001917382627806449270 ),
 .UNSPECIFIED. ) ;
#252765=EDGE_CURVE ( 'NONE', #91225, #43942, #214851, .T. ) ;
#252787=CARTESIAN_POINT ( 'NONE',  ( 20.85000000000000142, 76.00000000001207923, -128.7231074845243484 ) ) ;
#252790=CIRCLE ( 'NONE', #244419, 7.791421356237338003 ) ;
#252793=DIRECTION ( 'NONE',  ( 1.000000000000000000, 0.000000000000000000, 0.000000000000000000 ) ) ;
#252845=VERTEX_POINT ( 'NONE', #216428 ) ;
#252871=CARTESIAN_POINT ( 'NONE',  ( -21.05000000000000071, 76.00000000001232081, -162.1231074845243540 ) ) ;
#252877=CARTESIAN_POINT ( 'NONE',  ( 21.14999999999999503, 76.10000000001245724, -181.6726782920691505 ) ) ;
#252878=CARTESIAN_POINT ( 'NONE',  ( -21.05000000000000071, 76.00000000001216449, -140.6231074845243256 ) ) ;
#252897=EDGE_CURVE ( 'NONE', #225850, #215500, #44190, .T. ) ;
#252908=VECTOR ( 'NONE', #154048, 1000.000000000000000 ) ;
#252931=ORIENTED_EDGE ( 'NONE', *, *, #8783, .T. ) ;
#252940=CARTESIAN_POINT ( 'NONE',  ( 22.47071067811865319, 75.90090754530983475, -177.7431822290224090 ) ) ;
#252980=CARTESIAN_POINT ( 'NONE',  ( -21.17356465864818560, 69.57719687377066009, -170.1220187255382541 ) ) ;
#253007=CARTESIAN_POINT ( 'NONE',  ( -21.08884785362073089, 75.95021690494570521, -176.3803008519499826 ) ) ;
#253046=CARTESIAN_POINT ( 'NONE',  ( 20.85000000000000142, 76.00000000001213607, -136.5231074845243313 ) ) ;
#253106=AXIS2_PLACEMENT_3D ( 'NONE', #102073, #83775, #163368 ) ;
#253118=AXIS2_PLACEMENT_3D ( 'NONE', #155276, #13173, #74458 ) ;
#253149=EDGE_CURVE ( 'NONE', #168221, #9791, #206669, .T. ) ;
#253174=EDGE_LOOP ( 'NONE', ( #167298, #173859, #39221, #204392, #61493, #233994, #236857, #116855, #220669, #34679, #111108, #58119, #82530, #28997, #224238, #98455, #68847, #97578, #109171, #101261, #44413, #27474, #18992 ) ) ;
#253221=DIRECTION ( 'NONE',  ( -1.000000000000000000, 0.000000000000000000, 0.000000000000000000 ) ) ;
#253232=DIRECTION ( 'NONE',  ( -0.000000000000000000, 6.982962677686266711E-15, -1.000000000000000000 ) ) ;
#253254=AXIS2_PLACEMENT_3D ( 'NONE', #191109, #249774, #171554 ) ;
#253298=ORIENTED_EDGE ( 'NONE', *, *, #242091, .F. ) ;
#253315=ORIENTED_EDGE ( 'NONE', *, *, #254868, .T. ) ;
#253385=LINE ( 'NONE', #212978, #255401 ) ;
#253409=CARTESIAN_POINT ( 'NONE',  ( -23.25000000000000000, 76.00000000001210765, -132.6231074845243540 ) ) ;
#253410=PLANE ( 'NONE',  #105878 ) ;
#253422=EDGE_CURVE ( 'NONE', #138157, #140576, #249658, .T. ) ;
#253428=ORIENTED_EDGE ( 'NONE', *, *, #254569, .T. ) ;
#253435=EDGE_CURVE ( 'NONE', #205761, #245795, #250913, .T. ) ;
#253450=DIRECTION ( 'NONE',  ( 0.000000000000000000, 0.9908441862701420355, 0.1350103645453197554 ) ) ;
#253451=ORIENTED_EDGE ( 'NONE', *, *, #139976, .F. ) ;
#253460=CARTESIAN_POINT ( 'NONE',  ( -20.94999999999999929, 74.14897176987143723, -158.3691942151018850 ) ) ;
#253469=ORIENTED_EDGE ( 'NONE', *, *, #37533, .T. ) ;
#253473=CIRCLE ( 'NONE', #70362, 0.2000000000000057288 ) ;
#253483=ORIENTED_EDGE ( 'NONE', *, *, #130271, .F. ) ;
#253498=CARTESIAN_POINT ( 'NONE',  ( -20.94999999999999929, 76.00000000001237765, -170.0231074845243597 ) ) ;
#253510=CARTESIAN_POINT ( 'NONE',  ( -20.94999999999999929, 87.48912529308822172, -139.6231074845242688 ) ) ;
#253518=AXIS2_PLACEMENT_3D ( 'NONE', #31634, #12062, #126848 ) ;
#253545=FACE_OUTER_BOUND ( 'NONE', #221065, .T. ) ;
#253601=CARTESIAN_POINT ( 'NONE',  ( -22.57320508075686405, 64.25000000001236344, -170.0231074845243882 ) ) ;
#253610=VERTEX_POINT ( 'NONE', #235222 ) ;
#253626=CONICAL_SURFACE ( 'NONE', #161908, 7.750000000000034639, 0.7853981633974531640 ) ;
#253643=DIRECTION ( 'NONE',  ( 0.000000000000000000, 0.000000000000000000, 1.000000000000000000 ) ) ;
#253665=CARTESIAN_POINT ( 'NONE',  ( 18.49999999999999289, 65.65621891165909574, -145.1946622066474504 ) ) ;
#253701=CARTESIAN_POINT ( 'NONE',  ( -20.94983749550516450, 65.70233904877032671, -131.0487410911968880 ) ) ;
#253706=DIRECTION ( 'NONE',  ( -1.000000000000000000, 7.304098846218134667E-16, 5.100424963727256530E-30 ) ) ;
#253742=DIRECTION ( 'NONE',  ( -6.938893903907224433E-15, -1.000000000000000000, -6.982962677686266711E-15 ) ) ;
#253762=DIRECTION ( 'NONE',  ( 0.000000000000000000, -0.4999999999999608646, -0.8660254037844612451 ) ) ;
#253820=EDGE_CURVE ( 'NONE', #245009, #239159, #168906, .T. ) ;
#253840=DIRECTION ( 'NONE',  ( 1.000000000000000000, 0.000000000000000000, 0.000000000000000000 ) ) ;
#253886=DIRECTION ( 'NONE',  ( 0.000000000000000000, -6.938893903907222067E-15, 1.000000000000000000 ) ) ;
#253887=DIRECTION ( 'NONE',  ( 0.000000000000000000, -0.1350103645451945777, 0.9908441862701590219 ) ) ;
#253893=PLANE ( 'NONE',  #133382 ) ;
#253904=VERTEX_POINT ( 'NONE', #173707 ) ;
#253913=CARTESIAN_POINT ( 'NONE',  ( 18.59999999999999432, 74.26374286841490857, -158.4544551555068779 ) ) ;
#253922=AXIS2_PLACEMENT_3D ( 'NONE', #53477, #10510, #52176 ) ;
#253928=CARTESIAN_POINT ( 'NONE',  ( -21.14999999999999858, 76.00000000001242029, -176.2816861282870775 ) ) ;
#253951=ADVANCED_FACE ( 'NONE', ( #138351 ), #6548, .T. ) ;
#253954=FACE_OUTER_BOUND ( 'NONE', #19085, .T. ) ;
#253969=DIRECTION ( 'NONE',  ( 0.000000000000000000, -7.056502275159890043E-15, 1.000000000000000000 ) ) ;
#253971=CARTESIAN_POINT ( 'NONE',  ( 23.14999999999999858, 71.00000000001230660, -157.6178414656113205 ) ) ;
#254025=AXIS2_PLACEMENT_3D ( 'NONE', #221288, #223857, #46507 ) ;
#254063=CARTESIAN_POINT ( 'NONE',  ( -21.64999999999999858, 68.65000000001229807, -157.6731074845243938 ) ) ;
#254091=ADVANCED_FACE ( 'NONE', ( #3998 ), #106674, .F. ) ;
#254103=CARTESIAN_POINT ( 'NONE',  ( 19.58285714285715073, 66.98499851036373798, -161.6024546684427037 ) ) ;
#254157=CARTESIAN_POINT ( 'NONE',  ( 21.05000000000000071, 64.35000000001228670, -157.8731074845244393 ) ) ;
#254169=PLANE ( 'NONE',  #234114 ) ;
#254173=ORIENTED_EDGE ( 'NONE', *, *, #133045, .T. ) ;
#254202=CARTESIAN_POINT ( 'NONE',  ( -21.05000000000000071, 76.00000000001237765, -170.0231074845243597 ) ) ;
#254222=LINE ( 'NONE', #116033, #145918 ) ;
#254274=VECTOR ( 'NONE', #11354, 1000.000000000000000 ) ;
#254312=DIRECTION ( 'NONE',  ( 0.000000000000000000, -1.000000000000000000, 0.000000000000000000 ) ) ;
#254322=EDGE_LOOP ( 'NONE', ( #18804, #75535, #234588, #66525 ) ) ;
#254332=CARTESIAN_POINT ( 'NONE',  ( -21.05000000000000071, 76.00000000001237765, -170.0231074845243597 ) ) ;
#254353=CARTESIAN_POINT ( 'NONE',  ( 23.24999999999999289, 64.25000000001237765, -169.9231074845244507 ) ) ;
#254369=CARTESIAN_POINT ( 'NONE',  ( -22.39999999999999858, 64.35000000001238618, -170.1231074845244393 ) ) ;
#254389=CIRCLE ( 'NONE', #8717, 0.09999999999998802902 ) ;
#254424=DIRECTION ( 'NONE',  ( -1.000000000000000000, 0.000000000000000000, 0.000000000000000000 ) ) ;
#254452=ADVANCED_FACE ( 'NONE', ( #165005 ), #136606, .T. ) ;
#254457=CARTESIAN_POINT ( 'NONE',  ( -21.65000000000000213, 68.29142135624960019, -157.6731074845243938 ) ) ;
#254475=EDGE_CURVE ( 'NONE', #93776, #39887, #146697, .T. ) ;
#254487=ORIENTED_EDGE ( 'NONE', *, *, #96761, .F. ) ;
#254495=ORIENTED_EDGE ( 'NONE', *, *, #230621, .T. ) ;
#254568=DIRECTION ( 'NONE',  ( 0.000000000000000000, 0.000000000000000000, 1.000000000000000000 ) ) ;
#254569=EDGE_CURVE ( 'NONE', #101850, #68928, #52692, .T. ) ;
#254580=SPHERICAL_SURFACE ( 'NONE', #107247, 0.1000000000000000056 ) ;
#254610=( BOUNDED_SURFACE ( )  B_SPLINE_SURFACE ( 3, 2, ( 
 ( #50568, #234355, #91000 ),
 ( #233111, #175697, #114423 ),
 ( #55685, #214796, #72762 ),
 ( #255152, #15343, #252631 ),
 ( #71466, #76567, #92278 ),
 ( #74045, #150985, #230525 ) ),
 .UNSPECIFIED., .F., .F., .T. ) 
 B_SPLINE_SURFACE_WITH_KNOTS ( ( 4, 2, 4 ),
 ( 3, 3 ),
 ( 0.0001342700090130149982, 0.0002909192928057525150, 0.0004475685765984900046 ),
 ( 0.000000000000000000, 1.000000000000000000 ),
 .UNSPECIFIED. ) 
 GEOMETRIC_REPRESENTATION_ITEM ( )  RATIONAL_B_SPLINE_SURFACE ( (
 ( 1.000000000000000000, 0.7250110520819876836, 1.000000000000000000),
 ( 1.000000000000000000, 0.7257599279136385251, 1.000000000000000000),
 ( 1.000000000000000000, 0.7137594617280956788, 1.000000000000000000),
 ( 1.000000000000000000, 0.6959270178813491414, 1.000000000000000000),
 ( 1.000000000000000000, 0.6919879549336065416, 1.000000000000000000),
 ( 1.000000000000000000, 0.7071067811865494601, 1.000000000000000000) ) ) 
 REPRESENTATION_ITEM ( '' )  SURFACE ( )  );
#254612=CARTESIAN_POINT ( 'NONE',  ( 21.97500000000000497, 66.25000000001229239, -157.6731074845244223 ) ) ;
#254623=CARTESIAN_POINT ( 'NONE',  ( -18.36527282682031625, 85.50000060001103463, -129.6009585200223455 ) ) ;
#254651=CIRCLE ( 'NONE', #33981, 11.64999999999999325 ) ;
#254658=DIRECTION ( 'NONE',  ( 0.000000000000000000, 0.000000000000000000, 1.000000000000000000 ) ) ;
#254696=CARTESIAN_POINT ( 'NONE',  ( 23.14999999999999503, 64.35000000001245724, -181.7731074845244450 ) ) ;
#254709=CARTESIAN_POINT ( 'NONE',  ( 20.97239005616515328, 67.12515615866219321, -157.7729546823712496 ) ) ;
#254734=VECTOR ( 'NONE', #253232, 1000.000000000000000 ) ;
#254769=ADVANCED_FACE ( 'NONE', ( #166020 ), #244219, .F. ) ;
#254819=CARTESIAN_POINT ( 'NONE',  ( 23.14999999999999503, 64.35000000001218723, -143.5379132551784096 ) ) ;
#254820=EDGE_LOOP ( 'NONE', ( #91987, #187560, #27758, #228799 ) ) ;
#254836=DIRECTION ( 'NONE',  ( 1.000000000000000000, 0.000000000000000000, 0.000000000000000000 ) ) ;
#254854=CARTESIAN_POINT ( 'NONE',  ( 23.14999999999999858, 70.50000000001223555, -148.9283735034374843 ) ) ;
#254859=VECTOR ( 'NONE', #103244, 1000.000000000000114 ) ;
#254868=EDGE_CURVE ( 'NONE', #20227, #31671, #86182, .T. ) ;
#254885=AXIS2_PLACEMENT_3D ( 'NONE', #72793, #231852, #14086 ) ;
#254892=PLANE ( 'NONE',  #224747 ) ;
#254897=TOROIDAL_SURFACE ( 'NONE', #38488, 1.900000000000002576, 0.1000000000000000056 ) ;
#254906=EDGE_CURVE ( 'NONE', #99805, #61430, #152884, .T. ) ;
#254930=EDGE_LOOP ( 'NONE', ( #124816, #148026, #232488, #189333 ) ) ;
#254959=ORIENTED_EDGE ( 'NONE', *, *, #176133, .F. ) ;
#254968=EDGE_LOOP ( 'NONE', ( #173621, #133961, #110037, #230564 ) ) ;
#254980=EDGE_LOOP ( 'NONE', ( #153725, #38516, #105666, #241324 ) ) ;
#255005=DIRECTION ( 'NONE',  ( 1.000000000000000000, 0.000000000000000000, 0.000000000000000000 ) ) ;
#255008=DIRECTION ( 'NONE',  ( 0.000000000000000000, 1.000000000000000000, 7.272083257015735086E-15 ) ) ;
#255034=CARTESIAN_POINT ( 'NONE',  ( -22.46246831459151494, 75.97808783307303315, -181.6729720457343262 ) ) ;
#255044=CARTESIAN_POINT ( 'NONE',  ( 18.46858270002953972, 85.47420267472293176, -162.9210855498204182 ) ) ;
#255082=CARTESIAN_POINT ( 'NONE',  ( -18.59999999999999787, 74.65925378207876406, -180.2959699899455472 ) ) ;
#255111=DIRECTION ( 'NONE',  ( 0.000000000000000000, 6.853228547068871147E-15, -1.000000000000000000 ) ) ;
#255125=CARTESIAN_POINT ( 'NONE',  ( -18.50000000000000000, 64.25000000001237765, -169.9231074845244507 ) ) ;
#255143=ORIENTED_EDGE ( 'NONE', *, *, #183432, .T. ) ;
#255152=CARTESIAN_POINT ( 'NONE',  ( 21.04116576186320486, 65.37533692126093854, -157.6945257158966740 ) ) ;
#255161=DIRECTION ( 'NONE',  ( 1.000000000000000000, -0.000000000000000000, 0.000000000000000000 ) ) ;
#255165=CARTESIAN_POINT ( 'NONE',  ( 20.94999999999999929, 76.00000000001216449, -139.4231074845243654 ) ) ;
#255208=CARTESIAN_POINT ( 'NONE',  ( 21.12642695952774474, 75.90109671682306214, -176.3987674065595286 ) ) ;
#255234=DIRECTION ( 'NONE',  ( 0.000000000000000000, 0.000000000000000000, -1.000000000000000000 ) ) ;
#255236=ORIENTED_EDGE ( 'NONE', *, *, #139976, .T. ) ;
#255320=CARTESIAN_POINT ( 'NONE',  ( -20.54999999999999716, 74.05981308412442843, -157.1939882734710352 ) ) ;
#255352=DIRECTION ( 'NONE',  ( 0.000000000000000000, 0.000000000000000000, 1.000000000000000000 ) ) ;
#255354=CARTESIAN_POINT ( 'NONE',  ( 23.24999999999999645, 73.90000000001214175, -136.5231074845243882 ) ) ;
#255384=VERTEX_POINT ( 'NONE', #20755 ) ;
#255386=EDGE_CURVE ( 'NONE', #113546, #16833, #153556, .T. ) ;
#255393=ADVANCED_FACE ( 'NONE', ( #1146 ), #156434, .F. ) ;
#255401=VECTOR ( 'NONE', #74796, 1000.000000000000000 ) ;
#255405=CARTESIAN_POINT ( 'NONE',  ( 21.05000000000000071, 70.15000000001221281, -146.6556047088023149 ) ) ;
#255409=EDGE_CURVE ( 'NONE', #217454, #99384, #237222, .T. ) ;
#255424=DIRECTION ( 'NONE',  ( 1.000000000000000000, 0.000000000000000000, 0.000000000000000000 ) ) ;
#255435=EDGE_LOOP ( 'NONE', ( #76920, #164311, #157955, #165217 ) ) ;
#255458=CARTESIAN_POINT ( 'NONE',  ( -23.15000000000000213, 73.50000000001223555, -149.7477294072864709 ) ) ;
#255480=AXIS2_PLACEMENT_3D ( 'NONE', #107565, #142821, #223653 ) ;
#255512=DIRECTION ( 'NONE',  ( -1.000000000000000000, 3.265361837132813093E-16, 2.280189983783949500E-30 ) ) ;
#255561=CARTESIAN_POINT ( 'NONE',  ( 20.94999999999999929, 76.00000000001213607, -136.5231074845243313 ) ) ;
#255572=DIRECTION ( 'NONE',  ( 0.000000000000000000, 1.000000000000000000, 0.000000000000000000 ) ) ;
#255577=EDGE_LOOP ( 'NONE', ( #201888, #3579, #73338, #210989 ) ) ;
#255600=CARTESIAN_POINT ( 'NONE',  ( 21.07928932188134397, 75.90110485435802445, -176.3516241409176644 ) ) ;
#255601=CARTESIAN_POINT ( 'NONE',  ( -20.94999999999999929, 76.00000000001222134, -148.3231074845243427 ) ) ;
#255628=LINE ( 'NONE', #53633, #188537 ) ;
#255682=EDGE_CURVE ( 'NONE', #28076, #236193, #100886, .T. ) ;
#255728=DIRECTION ( 'NONE',  ( 0.000000000000000000, 0.000000000000000000, 1.000000000000000000 ) ) ;
#255737=CARTESIAN_POINT ( 'NONE',  ( -18.59999999999999787, 64.35000000001234355, -163.0083017138704236 ) ) ;
#255761=AXIS2_PLACEMENT_3D ( 'NONE', #123053, #184291, #202582 ) ;
#255810=LINE ( 'NONE', #214168, #80145 ) ;
#255835=EDGE_CURVE ( 'NONE', #46965, #132176, #159221, .T. ) ;
#255856=LINE ( 'NONE', #156838, #242684 ) ;
#255875=CARTESIAN_POINT ( 'NONE',  ( -20.64999999999999858, 68.85000000001222986, -148.8731074845244109 ) ) ;
#255880=CARTESIAN_POINT ( 'NONE',  ( -18.47130263965444996, 85.47115558597597840, -129.8397027190475512 ) ) ;
#255885=ORIENTED_EDGE ( 'NONE', *, *, #210239, .T. ) ;
#255891=VERTEX_POINT ( 'NONE', #99928 ) ;
#255897=VERTEX_POINT ( 'NONE', #25571 ) ;
#255898=CARTESIAN_POINT ( 'NONE',  ( 23.24999999999999289, 69.55000000001228955, -157.6731074845243938 ) ) ;
#255924=ORIENTED_EDGE ( 'NONE', *, *, #29301, .F. ) ;
#255940=VECTOR ( 'NONE', #206296, 999.9999999999998863 ) ;
#255942=EDGE_CURVE ( 'NONE', #209999, #198367, #102491, .T. ) ;
#255956=ORIENTED_EDGE ( 'NONE', *, *, #19152, .F. ) ;
#255961=CARTESIAN_POINT ( 'NONE',  ( -21.98333005346336932, 76.00000000001243450, -177.3971828135810256 ) ) ;
#255963=ORIENTED_EDGE ( 'NONE', *, *, #46683, .F. ) ;
#255978=CIRCLE ( 'NONE', #176960, 0.5000000000000004441 ) ;
#255992=CARTESIAN_POINT ( 'NONE',  ( -20.94999999999999929, 87.48912529308842068, -166.9231074845242802 ) ) ;
#256012=ORIENTED_EDGE ( 'NONE', *, *, #149128, .F. ) ;
#256017=EDGE_CURVE ( 'NONE', #39426, #101907, #234385, .T. ) ;
#256033=EDGE_CURVE ( 'NONE', #91448, #52101, #167781, .T. ) ;
#256083=VECTOR ( 'NONE', #191652, 1000.000000000000000 ) ;
#256096=CARTESIAN_POINT ( 'NONE',  ( -18.50000000000000000, 64.35000000001238618, -169.9231074845244507 ) ) ;
#256101=VECTOR ( 'NONE', #133548, 1000.000000000000000 ) ;
#256106=DIRECTION ( 'NONE',  ( 0.000000000000000000, -7.086529944415886769E-15, 1.000000000000000000 ) ) ;
#256121=CARTESIAN_POINT ( 'NONE',  ( -21.05000000000000071, 76.00000000001213607, -136.5231074845243313 ) ) ;
#256139=CARTESIAN_POINT ( 'NONE',  ( 21.14999999999999147, 76.00000000001242029, -176.5637644362255969 ) ) ;
#256153=ADVANCED_FACE ( 'NONE', ( #40690 ), #159334, .T. ) ;
#256163=CARTESIAN_POINT ( 'NONE',  ( -23.15000000000000213, 76.00000000001213607, -136.5231074845243313 ) ) ;
#256179=CARTESIAN_POINT ( 'NONE',  ( 18.49999999999999289, 65.58283456529579780, -145.1731074851066410 ) ) ;
#256198=ORIENTED_EDGE ( 'NONE', *, *, #189882, .F. ) ;
#256251=CYLINDRICAL_SURFACE ( 'NONE', #109024, 0.09999999999998898659 ) ;
#256253=ORIENTED_EDGE ( 'NONE', *, *, #90199, .T. ) ;
#256255=FACE_OUTER_BOUND ( 'NONE', #210390, .T. ) ;
#256271=AXIS2_PLACEMENT_3D ( 'NONE', #178826, #256986, #217888 ) ;
#256281=DIRECTION ( 'NONE',  ( 0.000000000000000000, -6.982962677686266711E-15, 1.000000000000000000 ) ) ;
#256346=ORIENTED_EDGE ( 'NONE', *, *, #197992, .F. ) ;
#256349=LINE ( 'NONE', #774, #71018 ) ;
#256357=DIRECTION ( 'NONE',  ( 0.000000000000000000, -0.9908441862701791170, 0.1350103645450472789 ) ) ;
#256431=AXIS2_PLACEMENT_3D ( 'NONE', #49330, #85857, #149746 ) ;
#256443=EDGE_CURVE ( 'NONE', #138337, #137060, #205525, .T. ) ;
#256456=DIRECTION ( 'NONE',  ( 0.000000000000000000, 0.000000000000000000, -1.000000000000000000 ) ) ;
#256459=CARTESIAN_POINT ( 'NONE',  ( 21.00000000000000000, 66.25000000001229239, -157.7731074845244166 ) ) ;
#256469=DIRECTION ( 'NONE',  ( 1.000000000000000000, 0.000000000000000000, 0.000000000000000000 ) ) ;
#256482=FACE_OUTER_BOUND ( 'NONE', #48157, .T. ) ;
#256495=CARTESIAN_POINT ( 'NONE',  ( -20.54999999999999716, 74.07476635515247665, -157.2928639513982318 ) ) ;
#256499=( BOUNDED_CURVE ( )  B_SPLINE_CURVE ( 3, ( #124665, #106350, #166387, #8567 ),
 .UNSPECIFIED., .F., .F. ) 
 B_SPLINE_CURVE_WITH_KNOTS ( ( 4, 4 ),
 ( 3.141592653589778461, 4.712388980384686121 ),
 .UNSPECIFIED. ) 
 CURVE ( )  GEOMETRIC_REPRESENTATION_ITEM ( )  RATIONAL_B_SPLINE_CURVE ( ( 1.000000000000000000, 0.8047378541243622729, 0.8047378541243622729, 1.000000000000000000 ) ) 
 REPRESENTATION_ITEM ( '' )  );
#256511=CIRCLE ( 'NONE', #223246, 0.09999999999999344136 ) ;
#256535=CARTESIAN_POINT ( 'NONE',  ( 23.14999999999999503, 69.35000000001222986, -148.7731074845244166 ) ) ;
#256563=AXIS2_PLACEMENT_3D ( 'NONE', #52806, #119227, #20128 ) ;
#256586=AXIS2_PLACEMENT_3D ( 'NONE', #7933, #130429, #151303 ) ;
#256596=CARTESIAN_POINT ( 'NONE',  ( 18.46932045258642674, 85.67068520027788736, -129.8492471115277169 ) ) ;
#256598=DIRECTION ( 'NONE',  ( 0.000000000000000000, -1.000000000000000000, -6.982962677686265922E-15 ) ) ;
#256649=ORIENTED_EDGE ( 'NONE', *, *, #252897, .T. ) ;
#256661=VECTOR ( 'NONE', #104984, 1000.000000000000000 ) ;
#256677=LINE ( 'NONE', #252871, #72770 ) ;
#256684=DIRECTION ( 'NONE',  ( 0.000000000000000000, 1.000000000000000000, 6.982962677686266711E-15 ) ) ;
#256686=VERTEX_POINT ( 'NONE', #192869 ) ;
#256795=ADVANCED_FACE ( 'NONE', ( #214979 ), #234764, .F. ) ;
#256812=CIRCLE ( 'NONE', #123594, 0.1000000000000028644 ) ;
#256824=ORIENTED_EDGE ( 'NONE', *, *, #126217, .F. ) ;
#256840=FACE_OUTER_BOUND ( 'NONE', #23277, .T. ) ;
#256841=EDGE_CURVE ( 'NONE', #207248, #35313, #130699, .T. ) ;
#256844=DIRECTION ( 'NONE',  ( 1.000000000000000000, 0.000000000000000000, 0.000000000000000000 ) ) ;
#256855=ORIENTED_EDGE ( 'NONE', *, *, #138757, .T. ) ;
#256899=CARTESIAN_POINT ( 'NONE',  ( -23.25000000000000000, 69.01799029515568407, -132.8269553662681233 ) ) ;
#256909=CARTESIAN_POINT ( 'NONE',  ( 18.59999999999999076, 64.35000000001245724, -181.7731074845244450 ) ) ;
#256936=CARTESIAN_POINT ( 'NONE',  ( 21.14999999999999858, 64.35000000001237197, -169.9231074845244507 ) ) ;
#256986=DIRECTION ( 'NONE',  ( -1.000000000000000000, 0.000000000000000000, -0.000000000000000000 ) ) ;
#256988=DIRECTION ( 'NONE',  ( 0.000000000000000000, 0.9893560106964510714, -0.1455152366551481502 ) ) ;
#256995=CIRCLE ( 'NONE', #148739, 0.09999999999999939493 ) ;
#257017=DIRECTION ( 'NONE',  ( 1.000000000000000000, 0.000000000000000000, 0.000000000000000000 ) ) ;
#257050=DIRECTION ( 'NONE',  ( 1.000000000000000000, 0.000000000000000000, 0.000000000000000000 ) ) ;
#257058=DIRECTION ( 'NONE',  ( -1.000000000000000000, 0.000000000000000000, 0.000000000000000000 ) ) ;
#257101=DIRECTION ( 'NONE',  ( -1.000000000000000000, -0.000000000000000000, -0.000000000000000000 ) ) ;
#257126=DIRECTION ( 'NONE',  ( 1.000000000000000000, 0.000000000000000000, 0.000000000000000000 ) ) ;
#257132=EDGE_LOOP ( 'NONE', ( #66306, #138836, #43695, #234402, #72466, #40446, #59800, #138641, #243299, #46939 ) ) ;
#257172=ORIENTED_EDGE ( 'NONE', *, *, #222878, .T. ) ;
#257176=ORIENTED_EDGE ( 'NONE', *, *, #33450, .F. ) ;
#257178=EDGE_LOOP ( 'NONE', ( #239152, #23472, #250031, #99682 ) ) ;
#257179=FACE_OUTER_BOUND ( 'NONE', #85591, .T. ) ;
#257185=CIRCLE ( 'NONE', #153216, 0.09999999999998898659 ) ;
#257188=DIRECTION ( 'NONE',  ( -1.000000000000000000, 0.000000000000000000, 0.000000000000000000 ) ) ;
#257245=DIRECTION ( 'NONE',  ( 0.000000000000000000, -7.086529944415894657E-15, 1.000000000000000000 ) ) ;
#257246=CARTESIAN_POINT ( 'NONE',  ( -23.25000000000000000, 77.83585931145570669, -125.0186683157258329 ) ) ;
#257286=CARTESIAN_POINT ( 'NONE',  ( 18.59999999999999787, 77.83534155023670564, -158.4679561919613491 ) ) ;
#257302=EDGE_CURVE ( 'NONE', #113635, #181798, #210199, .T. ) ;
#257337=AXIS2_PLACEMENT_3D ( 'NONE', #64128, #127955, #165817 ) ;
#257373=DIRECTION ( 'NONE',  ( -0.000000000000000000, -6.982962677686266711E-15, 1.000000000000000000 ) ) ;
#257384=VECTOR ( 'NONE', #247080, 1000.000000000000000 ) ;
#257386=ORIENTED_EDGE ( 'NONE', *, *, #247209, .F. ) ;
#257405=ORIENTED_EDGE ( 'NONE', *, *, #19582, .F. ) ;
#257408=CIRCLE ( 'NONE', #165918, 0.8750000000000007772 ) ;
#257410=CYLINDRICAL_SURFACE ( 'NONE', #60877, 7.899999999999990585 ) ;
#257413=CARTESIAN_POINT ( 'NONE',  ( -18.42554971533678199, 85.49715966945009882, -162.9832805709756371 ) ) ;
#257414=AXIS2_PLACEMENT_3D ( 'NONE', #222060, #205079, #128142 ) ;
#257434=TOROIDAL_SURFACE ( 'NONE', #228287, 11.65000000000000036, 0.1000000000000000056 ) ;
#257442=ORIENTED_EDGE ( 'NONE', *, *, #222094, .T. ) ;
#257453=EDGE_CURVE ( 'NONE', #228499, #113219, #168874, .T. ) ;
#257474=FACE_OUTER_BOUND ( 'NONE', #88624, .T. ) ;
#257511=ORIENTED_EDGE ( 'NONE', *, *, #103803, .T. ) ;
#257571=VERTEX_POINT ( 'NONE', #123950 ) ;
#257577=ORIENTED_EDGE ( 'NONE', *, *, #200506, .T. ) ;
#257581=EDGE_LOOP ( 'NONE', ( #249683, #21017, #97257, #230578 ) ) ;
#257592=AXIS2_PLACEMENT_3D ( 'NONE', #176086, #198181, #240310 ) ;
#257599=EDGE_CURVE ( 'NONE', #101496, #106082, #27056, .T. ) ;
#257650=CIRCLE ( 'NONE', #241171, 0.5000000000000004441 ) ;
#257669=EDGE_CURVE ( 'NONE', #171719, #251940, #21014, .T. ) ;
#257687=EDGE_CURVE ( 'NONE', #11381, #38071, #89933, .T. ) ;
#257693=DIRECTION ( 'NONE',  ( 0.000000000000000000, -6.352154140967427193E-15, 1.000000000000000000 ) ) ;
#257756=DIRECTION ( 'NONE',  ( 1.000000000000000000, 0.000000000000000000, 0.000000000000000000 ) ) ;
#257767=DIRECTION ( 'NONE',  ( 0.000000000000000000, -6.982962677686266711E-15, 1.000000000000000000 ) ) ;
#257774=CARTESIAN_POINT ( 'NONE',  ( 21.05000000000000071, 69.52244781751889491, -169.9231075192253115 ) ) ;
#257786=CARTESIAN_POINT ( 'NONE',  ( -21.05000000000000071, 76.00000000001237765, -170.0231074845243597 ) ) ;
#257819=EDGE_CURVE ( 'NONE', #121672, #70695, #235294, .T. ) ;
#257875=DIRECTION ( 'NONE',  ( 0.000000000000000000, -0.1495327102803283015, 0.9887567792719397231 ) ) ;
#257881=CARTESIAN_POINT ( 'NONE',  ( 18.43466021071410310, 85.49419069046865616, -129.9060459243966932 ) ) ;
#257889=CARTESIAN_POINT ( 'NONE',  ( -20.54999999999999716, 74.00000000001229239, -157.2984855617622770 ) ) ;
#257924=CARTESIAN_POINT ( 'NONE',  ( 18.49999999999999289, 65.79142135624951493, -145.3731074845244109 ) ) ;
#257963=CARTESIAN_POINT ( 'NONE',  ( 18.59999999999999076, 76.00000000001213607, -136.5231074845243313 ) ) ;
#257971=AXIS2_PLACEMENT_3D ( 'NONE', #37604, #237071, #77982 ) ;
#257995=AXIS2_PLACEMENT_3D ( 'NONE', #226870, #26122, #48235 ) ;
#258015=VERTEX_POINT ( 'NONE', #102751 ) ;
#258064=SPHERICAL_SURFACE ( 'NONE', #159041, 0.1000000000000000056 ) ;
ENDSEC;
END-ISO-10303-21;
